ISO-10303-21;
HEADER;
/* Generated by software containing ST-Developer
 * from STEP Tools, Inc. (www.steptools.com) 
 */

FILE_DESCRIPTION(
/* description */ (''),
/* implementation_level */ '2;1');

FILE_NAME(
/* name */ 'Screw_01.step',
/* time_stamp */ '2026-10-05T00:14:20-07:00',
/* author */ (''),
/* organization */ (''),
/* preprocessor_version */ 'ST-DEVELOPER v20.2',
/* originating_system */ 'Autodesk Translation Framework v15.15.0.0',
/* authorisation */ '');

FILE_SCHEMA (('AUTOMOTIVE_DESIGN { 1 0 10303 214 3 1 1 }'));
ENDSEC;

DATA;
#10=MECHANICAL_DESIGN_GEOMETRIC_PRESENTATION_REPRESENTATION('',(#3376),#75336);
#43=(
BOUNDED_SURFACE()
B_SPLINE_SURFACE(1,2,((#54054,#54055,#54056,#54057,#54058,#54059,#54060,
#54061,#54062,#54063,#54064,#54065,#54066,#54067,#54068,#54069,#54070,#54071,
#54072,#54073,#54074,#54075,#54076,#54077,#54078,#54079,#54080,#54081,#54082,
#54083,#54084,#54085,#54086,#54087,#54088,#54089,#54090,#54091,#54092,#54093,
#54094,#54095,#54096,#54097,#54098,#54099,#54100,#54101,#54102,#54103,#54104,
#54105,#54106,#54107,#54108,#54109,#54110,#54111,#54112,#54113,#54114,#54115,
#54116,#54117,#54118,#54119,#54120,#54121,#54122,#54123,#54124,#54125,#54126,
#54127,#54128,#54129,#54130,#54131,#54132,#54133,#54134,#54135,#54136,#54137,
#54138,#54139,#54140,#54141,#54142,#54143,#54144,#54145,#54146,#54147,#54148,
#54149,#54150,#54151,#54152,#54153,#54154,#54155,#54156,#54157,#54158,#54159,
#54160,#54161,#54162,#54163,#54164,#54165,#54166,#54167,#54168,#54169,#54170,
#54171,#54172,#54173,#54174,#54175,#54176,#54177,#54178,#54179,#54180,#54181,
#54182,#54183,#54184,#54185,#54186,#54187,#54188,#54189,#54190,#54191,#54192,
#54193,#54194,#54195,#54196,#54197,#54198,#54199,#54200,#54201,#54202,#54203,
#54204,#54205,#54206,#54207,#54208,#54209,#54210,#54211,#54212,#54213,#54214,
#54215,#54216,#54217,#54218,#54219,#54220,#54221,#54222,#54223,#54224,#54225,
#54226,#54227,#54228,#54229,#54230,#54231,#54232,#54233,#54234,#54235,#54236,
#54237,#54238,#54239,#54240,#54241,#54242,#54243,#54244,#54245,#54246,#54247,
#54248,#54249,#54250,#54251,#54252,#54253,#54254,#54255,#54256,#54257,#54258,
#54259,#54260,#54261,#54262,#54263,#54264,#54265,#54266,#54267,#54268,#54269,
#54270,#54271,#54272,#54273,#54274,#54275,#54276,#54277,#54278,#54279,#54280,
#54281,#54282,#54283,#54284,#54285,#54286,#54287,#54288,#54289,#54290,#54291,
#54292,#54293,#54294,#54295,#54296,#54297,#54298,#54299,#54300,#54301,#54302,
#54303,#54304,#54305,#54306,#54307,#54308,#54309,#54310,#54311,#54312,#54313,
#54314,#54315,#54316,#54317,#54318,#54319,#54320,#54321,#54322,#54323,#54324,
#54325,#54326,#54327,#54328,#54329,#54330,#54331,#54332,#54333,#54334,#54335,
#54336,#54337,#54338,#54339,#54340,#54341,#54342,#54343,#54344,#54345,#54346,
#54347,#54348,#54349,#54350,#54351,#54352,#54353,#54354,#54355,#54356,#54357,
#54358,#54359,#54360,#54361,#54362,#54363,#54364,#54365,#54366,#54367,#54368,
#54369,#54370,#54371,#54372,#54373,#54374,#54375,#54376,#54377,#54378,#54379,
#54380,#54381,#54382,#54383,#54384,#54385,#54386,#54387,#54388,#54389,#54390,
#54391,#54392,#54393,#54394,#54395,#54396,#54397,#54398,#54399,#54400,#54401,
#54402,#54403,#54404,#54405,#54406,#54407,#54408,#54409,#54410,#54411,#54412,
#54413,#54414,#54415,#54416,#54417,#54418,#54419,#54420,#54421,#54422,#54423,
#54424,#54425,#54426),(#54427,#54428,#54429,#54430,#54431,#54432,#54433,
#54434,#54435,#54436,#54437,#54438,#54439,#54440,#54441,#54442,#54443,#54444,
#54445,#54446,#54447,#54448,#54449,#54450,#54451,#54452,#54453,#54454,#54455,
#54456,#54457,#54458,#54459,#54460,#54461,#54462,#54463,#54464,#54465,#54466,
#54467,#54468,#54469,#54470,#54471,#54472,#54473,#54474,#54475,#54476,#54477,
#54478,#54479,#54480,#54481,#54482,#54483,#54484,#54485,#54486,#54487,#54488,
#54489,#54490,#54491,#54492,#54493,#54494,#54495,#54496,#54497,#54498,#54499,
#54500,#54501,#54502,#54503,#54504,#54505,#54506,#54507,#54508,#54509,#54510,
#54511,#54512,#54513,#54514,#54515,#54516,#54517,#54518,#54519,#54520,#54521,
#54522,#54523,#54524,#54525,#54526,#54527,#54528,#54529,#54530,#54531,#54532,
#54533,#54534,#54535,#54536,#54537,#54538,#54539,#54540,#54541,#54542,#54543,
#54544,#54545,#54546,#54547,#54548,#54549,#54550,#54551,#54552,#54553,#54554,
#54555,#54556,#54557,#54558,#54559,#54560,#54561,#54562,#54563,#54564,#54565,
#54566,#54567,#54568,#54569,#54570,#54571,#54572,#54573,#54574,#54575,#54576,
#54577,#54578,#54579,#54580,#54581,#54582,#54583,#54584,#54585,#54586,#54587,
#54588,#54589,#54590,#54591,#54592,#54593,#54594,#54595,#54596,#54597,#54598,
#54599,#54600,#54601,#54602,#54603,#54604,#54605,#54606,#54607,#54608,#54609,
#54610,#54611,#54612,#54613,#54614,#54615,#54616,#54617,#54618,#54619,#54620,
#54621,#54622,#54623,#54624,#54625,#54626,#54627,#54628,#54629,#54630,#54631,
#54632,#54633,#54634,#54635,#54636,#54637,#54638,#54639,#54640,#54641,#54642,
#54643,#54644,#54645,#54646,#54647,#54648,#54649,#54650,#54651,#54652,#54653,
#54654,#54655,#54656,#54657,#54658,#54659,#54660,#54661,#54662,#54663,#54664,
#54665,#54666,#54667,#54668,#54669,#54670,#54671,#54672,#54673,#54674,#54675,
#54676,#54677,#54678,#54679,#54680,#54681,#54682,#54683,#54684,#54685,#54686,
#54687,#54688,#54689,#54690,#54691,#54692,#54693,#54694,#54695,#54696,#54697,
#54698,#54699,#54700,#54701,#54702,#54703,#54704,#54705,#54706,#54707,#54708,
#54709,#54710,#54711,#54712,#54713,#54714,#54715,#54716,#54717,#54718,#54719,
#54720,#54721,#54722,#54723,#54724,#54725,#54726,#54727,#54728,#54729,#54730,
#54731,#54732,#54733,#54734,#54735,#54736,#54737,#54738,#54739,#54740,#54741,
#54742,#54743,#54744,#54745,#54746,#54747,#54748,#54749,#54750,#54751,#54752,
#54753,#54754,#54755,#54756,#54757,#54758,#54759,#54760,#54761,#54762,#54763,
#54764,#54765,#54766,#54767,#54768,#54769,#54770,#54771,#54772,#54773,#54774,
#54775,#54776,#54777,#54778,#54779,#54780,#54781,#54782,#54783,#54784,#54785,
#54786,#54787,#54788,#54789,#54790,#54791,#54792,#54793,#54794,#54795,#54796,
#54797,#54798,#54799)),.UNSPECIFIED.,.F.,.F.,.F.)
B_SPLINE_SURFACE_WITH_KNOTS((2,2),(3,2,2,2,2,2,2,2,2,2,2,2,2,2,2,2,2,2,
2,2,2,2,2,2,2,2,2,2,2,2,2,2,2,2,2,2,2,2,2,2,2,2,2,2,2,2,2,2,2,2,2,2,2,2,
2,2,2,2,2,2,2,2,2,2,2,2,2,2,2,2,2,2,2,2,2,2,2,2,2,2,2,2,2,2,2,2,2,2,2,2,
2,2,2,2,2,2,2,2,2,2,2,2,2,2,2,2,2,2,2,2,2,2,2,2,2,2,2,2,2,2,2,2,2,2,2,2,
2,2,2,2,2,2,2,2,2,2,2,2,2,2,2,2,2,2,2,2,2,2,2,2,2,2,2,2,2,2,2,2,2,2,2,2,
2,2,2,2,2,2,2,2,2,2,2,2,2,2,2,2,2,2,2,2,2,2,2,2,3),(-2.30253870309941E-5,
1.),(0.,0.00537634408602151,0.010752688172043,0.0161290322580645,0.021505376344086,
0.0268817204301075,0.032258064516129,0.0376344086021505,0.043010752688172,
0.0483870967741935,0.0537634408602151,0.0591397849462366,0.0645161290322581,
0.0698924731182796,0.0752688172043011,0.0806451612903226,0.0860215053763441,
0.0913978494623656,0.0967741935483871,0.102150537634409,0.10752688172043,
0.112903225806452,0.118279569892473,0.123655913978495,0.129032258064516,
0.134408602150538,0.139784946236559,0.145161290322581,0.150537634408602,
0.155913978494624,0.161290322580645,0.166666666666667,0.172043010752688,
0.17741935483871,0.182795698924731,0.188172043010753,0.193548387096774,
0.198924731182796,0.204301075268817,0.209677419354839,0.21505376344086,
0.220430107526882,0.225806451612903,0.231182795698925,0.236559139784946,
0.241935483870968,0.247311827956989,0.252688172043011,0.258064516129032,
0.263440860215054,0.268817204301075,0.274193548387097,0.279569892473118,
0.28494623655914,0.290322580645161,0.295698924731183,0.301075268817204,
0.306451612903226,0.311827956989247,0.317204301075269,0.32258064516129,
0.327956989247312,0.333333333333333,0.338709677419355,0.344086021505376,
0.349462365591398,0.354838709677419,0.360215053763441,0.365591397849462,
0.370967741935484,0.376344086021505,0.381720430107527,0.387096774193548,
0.39247311827957,0.397849462365591,0.403225806451613,0.408602150537634,
0.413978494623656,0.419354838709677,0.424731182795699,0.43010752688172,
0.435483870967742,0.440860215053763,0.446236559139785,0.451612903225806,
0.456989247311828,0.462365591397849,0.467741935483871,0.473118279569892,
0.478494623655914,0.483870967741935,0.489247311827957,0.494623655913978,
0.5,0.505376344086022,0.510752688172043,0.516129032258065,0.521505376344086,
0.526881720430108,0.532258064516129,0.537634408602151,0.543010752688172,
0.548387096774194,0.553763440860215,0.559139784946237,0.564516129032258,
0.56989247311828,0.575268817204301,0.580645161290323,0.586021505376344,
0.591397849462366,0.596774193548387,0.602150537634409,0.60752688172043,
0.612903225806452,0.618279569892473,0.623655913978495,0.629032258064516,
0.634408602150538,0.639784946236559,0.645161290322581,0.650537634408602,
0.655913978494624,0.661290322580645,0.666666666666667,0.672043010752688,
0.67741935483871,0.682795698924731,0.688172043010753,0.693548387096774,
0.698924731182796,0.704301075268817,0.709677419354839,0.71505376344086,
0.720430107526882,0.725806451612903,0.731182795698925,0.736559139784946,
0.741935483870968,0.747311827956989,0.752688172043011,0.758064516129032,
0.763440860215054,0.768817204301075,0.774193548387097,0.779569892473118,
0.78494623655914,0.790322580645161,0.795698924731183,0.801075268817204,
0.806451612903226,0.811827956989247,0.817204301075269,0.82258064516129,
0.827956989247312,0.833333333333333,0.838709677419355,0.844086021505376,
0.849462365591398,0.854838709677419,0.860215053763441,0.865591397849462,
0.870967741935484,0.876344086021505,0.881720430107527,0.887096774193548,
0.89247311827957,0.897849462365591,0.903225806451613,0.908602150537634,
0.913978494623656,0.919354838709677,0.924731182795699,0.93010752688172,
0.935483870967742,0.940860215053763,0.946236559139785,0.951612903225806,
0.956989247311828,0.962365591397849,0.967741935483871,0.973118279569892,
0.978494623655914,0.983870967741935,0.989247311827957,0.994623655913978,
1.),.UNSPECIFIED.)
GEOMETRIC_REPRESENTATION_ITEM()
RATIONAL_B_SPLINE_SURFACE(((1.,0.866025403784439,1.,0.866025403784439,1.,
0.866025403784439,1.,0.866025403784439,1.,0.866025403784439,1.,0.866025403784439,
1.,0.866025403784439,1.,0.866025403784439,1.,0.866025403784439,1.,0.866025403784439,
1.,0.866025403784439,1.,0.866025403784439,1.,0.866025403784439,1.,0.866025403784439,
1.,0.866025403784439,1.,0.866025403784439,1.,0.866025403784439,1.,0.866025403784439,
1.,0.866025403784439,1.,0.866025403784439,1.,0.866025403784439,1.,0.866025403784439,
1.,0.866025403784439,1.,0.866025403784439,1.,0.866025403784439,1.,0.866025403784439,
1.,0.866025403784439,1.,0.866025403784439,1.,0.866025403784439,1.,0.866025403784439,
1.,0.866025403784439,1.,0.866025403784439,1.,0.866025403784439,1.,0.866025403784439,
1.,0.866025403784439,1.,0.866025403784439,1.,0.866025403784439,1.,0.866025403784439,
1.,0.866025403784439,1.,0.866025403784439,1.,0.866025403784439,1.,0.866025403784439,
1.,0.866025403784439,1.,0.866025403784439,1.,0.866025403784439,1.,0.866025403784439,
1.,0.866025403784439,1.,0.866025403784439,1.,0.866025403784439,1.,0.866025403784439,
1.,0.866025403784439,1.,0.866025403784439,1.,0.866025403784439,1.,0.866025403784439,
1.,0.866025403784439,1.,0.866025403784439,1.,0.866025403784439,1.,0.866025403784439,
1.,0.866025403784439,1.,0.866025403784439,1.,0.866025403784439,1.,0.866025403784439,
1.,0.866025403784439,1.,0.866025403784439,1.,0.866025403784439,1.,0.866025403784439,
1.,0.866025403784439,1.,0.866025403784439,1.,0.866025403784439,1.,0.866025403784439,
1.,0.866025403784439,1.,0.866025403784439,1.,0.866025403784439,1.,0.866025403784439,
1.,0.866025403784439,1.,0.866025403784439,1.,0.866025403784439,1.,0.866025403784439,
1.,0.866025403784439,1.,0.866025403784439,1.,0.866025403784439,1.,0.866025403784439,
1.,0.866025403784439,1.,0.866025403784439,1.,0.866025403784439,1.,0.866025403784439,
1.,0.866025403784439,1.,0.866025403784439,1.,0.866025403784439,1.,0.866025403784439,
1.,0.866025403784439,1.,0.866025403784439,1.,0.866025403784439,1.,0.866025403784439,
1.,0.866025403784439,1.,0.866025403784439,1.,0.866025403784439,1.,0.866025403784439,
1.,0.866025403784439,1.,0.866025403784439,1.,0.866025403784439,1.,0.866025403784439,
1.,0.866025403784439,1.,0.866025403784439,1.,0.866025403784439,1.,0.866025403784439,
1.,0.866025403784439,1.,0.866025403784439,1.,0.866025403784439,1.,0.866025403784439,
1.,0.866025403784439,1.,0.866025403784439,1.,0.866025403784439,1.,0.866025403784439,
1.,0.866025403784439,1.,0.866025403784439,1.,0.866025403784439,1.,0.866025403784439,
1.,0.866025403784439,1.,0.866025403784439,1.,0.866025403784439,1.,0.866025403784439,
1.,0.866025403784439,1.,0.866025403784439,1.,0.866025403784439,1.,0.866025403784439,
1.,0.866025403784439,1.,0.866025403784439,1.,0.866025403784439,1.,0.866025403784439,
1.,0.866025403784439,1.,0.866025403784439,1.,0.866025403784439,1.,0.866025403784439,
1.,0.866025403784439,1.,0.866025403784439,1.,0.866025403784439,1.,0.866025403784439,
1.,0.866025403784439,1.,0.866025403784439,1.,0.866025403784439,1.,0.866025403784439,
1.,0.866025403784439,1.,0.866025403784439,1.,0.866025403784439,1.,0.866025403784439,
1.,0.866025403784439,1.,0.866025403784439,1.,0.866025403784439,1.,0.866025403784439,
1.,0.866025403784439,1.,0.866025403784439,1.,0.866025403784439,1.,0.866025403784439,
1.,0.866025403784439,1.,0.866025403784439,1.,0.866025403784439,1.,0.866025403784439,
1.,0.866025403784439,1.,0.866025403784439,1.,0.866025403784439,1.,0.866025403784439,
1.,0.866025403784439,1.,0.866025403784439,1.,0.866025403784439,1.,0.866025403784439,
1.,0.866025403784439,1.,0.866025403784439,1.,0.866025403784439,1.,0.866025403784439,
1.,0.866025403784439,1.,0.866025403784439,1.,0.866025403784439,1.,0.866025403784439,
1.,0.866025403784439,1.,0.866025403784439,1.,0.866025403784439,1.,0.866025403784439,
1.,0.866025403784439,1.,0.866025403784439,1.,0.866025403784439,1.,0.866025403784439,
1.,0.866025403784439,1.,0.866025403784439,1.,0.866025403784439,1.,0.866025403784439,
1.),(1.,0.866025403784439,1.,0.866025403784439,1.,0.866025403784439,1.,
0.866025403784439,1.,0.866025403784439,1.,0.866025403784439,1.,0.866025403784439,
1.,0.866025403784439,1.,0.866025403784439,1.,0.866025403784439,1.,0.866025403784439,
1.,0.866025403784439,1.,0.866025403784439,1.,0.866025403784439,1.,0.866025403784439,
1.,0.866025403784439,1.,0.866025403784439,1.,0.866025403784439,1.,0.866025403784439,
1.,0.866025403784439,1.,0.866025403784439,1.,0.866025403784439,1.,0.866025403784439,
1.,0.866025403784439,1.,0.866025403784439,1.,0.866025403784439,1.,0.866025403784439,
1.,0.866025403784439,1.,0.866025403784439,1.,0.866025403784439,1.,0.866025403784439,
1.,0.866025403784439,1.,0.866025403784439,1.,0.866025403784439,1.,0.866025403784439,
1.,0.866025403784439,1.,0.866025403784439,1.,0.866025403784439,1.,0.866025403784439,
1.,0.866025403784439,1.,0.866025403784439,1.,0.866025403784439,1.,0.866025403784439,
1.,0.866025403784439,1.,0.866025403784439,1.,0.866025403784439,1.,0.866025403784439,
1.,0.866025403784439,1.,0.866025403784439,1.,0.866025403784439,1.,0.866025403784439,
1.,0.866025403784439,1.,0.866025403784439,1.,0.866025403784439,1.,0.866025403784439,
1.,0.866025403784439,1.,0.866025403784439,1.,0.866025403784439,1.,0.866025403784439,
1.,0.866025403784439,1.,0.866025403784439,1.,0.866025403784439,1.,0.866025403784439,
1.,0.866025403784439,1.,0.866025403784439,1.,0.866025403784439,1.,0.866025403784439,
1.,0.866025403784439,1.,0.866025403784439,1.,0.866025403784439,1.,0.866025403784439,
1.,0.866025403784439,1.,0.866025403784439,1.,0.866025403784439,1.,0.866025403784439,
1.,0.866025403784439,1.,0.866025403784439,1.,0.866025403784439,1.,0.866025403784439,
1.,0.866025403784439,1.,0.866025403784439,1.,0.866025403784439,1.,0.866025403784439,
1.,0.866025403784439,1.,0.866025403784439,1.,0.866025403784439,1.,0.866025403784439,
1.,0.866025403784439,1.,0.866025403784439,1.,0.866025403784439,1.,0.866025403784439,
1.,0.866025403784439,1.,0.866025403784439,1.,0.866025403784439,1.,0.866025403784439,
1.,0.866025403784439,1.,0.866025403784439,1.,0.866025403784439,1.,0.866025403784439,
1.,0.866025403784439,1.,0.866025403784439,1.,0.866025403784439,1.,0.866025403784439,
1.,0.866025403784439,1.,0.866025403784439,1.,0.866025403784439,1.,0.866025403784439,
1.,0.866025403784439,1.,0.866025403784439,1.,0.866025403784439,1.,0.866025403784439,
1.,0.866025403784439,1.,0.866025403784439,1.,0.866025403784439,1.,0.866025403784439,
1.,0.866025403784439,1.,0.866025403784439,1.,0.866025403784439,1.,0.866025403784439,
1.,0.866025403784439,1.,0.866025403784439,1.,0.866025403784439,1.,0.866025403784439,
1.,0.866025403784439,1.,0.866025403784439,1.,0.866025403784439,1.,0.866025403784439,
1.,0.866025403784439,1.,0.866025403784439,1.,0.866025403784439,1.,0.866025403784439,
1.,0.866025403784439,1.,0.866025403784439,1.,0.866025403784439,1.,0.866025403784439,
1.,0.866025403784439,1.,0.866025403784439,1.,0.866025403784439,1.,0.866025403784439,
1.,0.866025403784439,1.,0.866025403784439,1.,0.866025403784439,1.,0.866025403784439,
1.,0.866025403784439,1.,0.866025403784439,1.,0.866025403784439,1.,0.866025403784439,
1.,0.866025403784439,1.,0.866025403784439,1.,0.866025403784439,1.,0.866025403784439,
1.,0.866025403784439,1.,0.866025403784439,1.,0.866025403784439,1.,0.866025403784439,
1.,0.866025403784439,1.,0.866025403784439,1.,0.866025403784439,1.,0.866025403784439,
1.,0.866025403784439,1.,0.866025403784439,1.,0.866025403784439,1.,0.866025403784439,
1.,0.866025403784439,1.,0.866025403784439,1.,0.866025403784439,1.,0.866025403784439,
1.,0.866025403784439,1.,0.866025403784439,1.,0.866025403784439,1.,0.866025403784439,
1.,0.866025403784439,1.,0.866025403784439,1.,0.866025403784439,1.,0.866025403784439,
1.,0.866025403784439,1.,0.866025403784439,1.,0.866025403784439,1.,0.866025403784439,
1.,0.866025403784439,1.,0.866025403784439,1.,0.866025403784439,1.,0.866025403784439,
1.,0.866025403784439,1.,0.866025403784439,1.,0.866025403784439,1.)))
REPRESENTATION_ITEM('')
SURFACE()
);
#44=(
BOUNDED_SURFACE()
B_SPLINE_SURFACE(1,2,((#54828,#54829,#54830,#54831,#54832,#54833,#54834,
#54835,#54836,#54837,#54838,#54839,#54840,#54841,#54842,#54843,#54844,#54845,
#54846,#54847,#54848,#54849,#54850,#54851,#54852,#54853,#54854,#54855,#54856,
#54857,#54858,#54859,#54860,#54861,#54862,#54863,#54864,#54865,#54866,#54867,
#54868,#54869,#54870,#54871,#54872,#54873,#54874,#54875,#54876,#54877,#54878,
#54879,#54880,#54881,#54882,#54883,#54884,#54885,#54886,#54887,#54888,#54889,
#54890,#54891,#54892,#54893,#54894,#54895,#54896,#54897,#54898,#54899,#54900,
#54901,#54902,#54903,#54904,#54905,#54906,#54907,#54908,#54909,#54910,#54911,
#54912,#54913,#54914,#54915,#54916,#54917,#54918,#54919,#54920,#54921,#54922,
#54923,#54924,#54925,#54926,#54927,#54928,#54929,#54930,#54931,#54932,#54933,
#54934,#54935,#54936,#54937,#54938,#54939,#54940,#54941,#54942,#54943,#54944,
#54945,#54946,#54947,#54948,#54949,#54950,#54951,#54952,#54953,#54954,#54955,
#54956,#54957,#54958,#54959,#54960,#54961,#54962,#54963,#54964,#54965,#54966,
#54967,#54968,#54969,#54970,#54971,#54972,#54973,#54974,#54975,#54976,#54977,
#54978,#54979,#54980,#54981,#54982,#54983,#54984,#54985,#54986,#54987,#54988,
#54989,#54990,#54991,#54992,#54993,#54994,#54995,#54996,#54997,#54998,#54999,
#55000,#55001,#55002,#55003,#55004,#55005,#55006,#55007,#55008,#55009,#55010,
#55011,#55012,#55013,#55014,#55015,#55016,#55017,#55018,#55019,#55020,#55021,
#55022,#55023,#55024,#55025,#55026,#55027,#55028,#55029,#55030,#55031,#55032,
#55033,#55034,#55035,#55036,#55037,#55038,#55039,#55040,#55041,#55042,#55043,
#55044,#55045,#55046,#55047,#55048,#55049,#55050,#55051,#55052,#55053,#55054,
#55055,#55056,#55057,#55058,#55059,#55060,#55061,#55062,#55063,#55064,#55065,
#55066,#55067,#55068,#55069,#55070,#55071,#55072,#55073,#55074,#55075,#55076,
#55077,#55078,#55079,#55080,#55081,#55082,#55083,#55084,#55085,#55086,#55087,
#55088,#55089,#55090,#55091,#55092,#55093,#55094,#55095,#55096,#55097,#55098,
#55099,#55100,#55101,#55102,#55103,#55104,#55105,#55106,#55107,#55108,#55109,
#55110,#55111,#55112,#55113,#55114,#55115,#55116,#55117,#55118,#55119,#55120,
#55121,#55122,#55123,#55124,#55125,#55126,#55127,#55128,#55129,#55130,#55131,
#55132,#55133,#55134,#55135,#55136,#55137,#55138,#55139,#55140,#55141,#55142,
#55143,#55144,#55145,#55146,#55147,#55148,#55149,#55150,#55151,#55152,#55153,
#55154,#55155,#55156,#55157,#55158,#55159,#55160,#55161,#55162,#55163,#55164,
#55165,#55166,#55167,#55168,#55169,#55170,#55171,#55172,#55173,#55174,#55175,
#55176,#55177,#55178,#55179,#55180,#55181,#55182,#55183,#55184,#55185,#55186,
#55187,#55188,#55189,#55190,#55191,#55192,#55193,#55194,#55195,#55196,#55197,
#55198,#55199,#55200),(#55201,#55202,#55203,#55204,#55205,#55206,#55207,
#55208,#55209,#55210,#55211,#55212,#55213,#55214,#55215,#55216,#55217,#55218,
#55219,#55220,#55221,#55222,#55223,#55224,#55225,#55226,#55227,#55228,#55229,
#55230,#55231,#55232,#55233,#55234,#55235,#55236,#55237,#55238,#55239,#55240,
#55241,#55242,#55243,#55244,#55245,#55246,#55247,#55248,#55249,#55250,#55251,
#55252,#55253,#55254,#55255,#55256,#55257,#55258,#55259,#55260,#55261,#55262,
#55263,#55264,#55265,#55266,#55267,#55268,#55269,#55270,#55271,#55272,#55273,
#55274,#55275,#55276,#55277,#55278,#55279,#55280,#55281,#55282,#55283,#55284,
#55285,#55286,#55287,#55288,#55289,#55290,#55291,#55292,#55293,#55294,#55295,
#55296,#55297,#55298,#55299,#55300,#55301,#55302,#55303,#55304,#55305,#55306,
#55307,#55308,#55309,#55310,#55311,#55312,#55313,#55314,#55315,#55316,#55317,
#55318,#55319,#55320,#55321,#55322,#55323,#55324,#55325,#55326,#55327,#55328,
#55329,#55330,#55331,#55332,#55333,#55334,#55335,#55336,#55337,#55338,#55339,
#55340,#55341,#55342,#55343,#55344,#55345,#55346,#55347,#55348,#55349,#55350,
#55351,#55352,#55353,#55354,#55355,#55356,#55357,#55358,#55359,#55360,#55361,
#55362,#55363,#55364,#55365,#55366,#55367,#55368,#55369,#55370,#55371,#55372,
#55373,#55374,#55375,#55376,#55377,#55378,#55379,#55380,#55381,#55382,#55383,
#55384,#55385,#55386,#55387,#55388,#55389,#55390,#55391,#55392,#55393,#55394,
#55395,#55396,#55397,#55398,#55399,#55400,#55401,#55402,#55403,#55404,#55405,
#55406,#55407,#55408,#55409,#55410,#55411,#55412,#55413,#55414,#55415,#55416,
#55417,#55418,#55419,#55420,#55421,#55422,#55423,#55424,#55425,#55426,#55427,
#55428,#55429,#55430,#55431,#55432,#55433,#55434,#55435,#55436,#55437,#55438,
#55439,#55440,#55441,#55442,#55443,#55444,#55445,#55446,#55447,#55448,#55449,
#55450,#55451,#55452,#55453,#55454,#55455,#55456,#55457,#55458,#55459,#55460,
#55461,#55462,#55463,#55464,#55465,#55466,#55467,#55468,#55469,#55470,#55471,
#55472,#55473,#55474,#55475,#55476,#55477,#55478,#55479,#55480,#55481,#55482,
#55483,#55484,#55485,#55486,#55487,#55488,#55489,#55490,#55491,#55492,#55493,
#55494,#55495,#55496,#55497,#55498,#55499,#55500,#55501,#55502,#55503,#55504,
#55505,#55506,#55507,#55508,#55509,#55510,#55511,#55512,#55513,#55514,#55515,
#55516,#55517,#55518,#55519,#55520,#55521,#55522,#55523,#55524,#55525,#55526,
#55527,#55528,#55529,#55530,#55531,#55532,#55533,#55534,#55535,#55536,#55537,
#55538,#55539,#55540,#55541,#55542,#55543,#55544,#55545,#55546,#55547,#55548,
#55549,#55550,#55551,#55552,#55553,#55554,#55555,#55556,#55557,#55558,#55559,
#55560,#55561,#55562,#55563,#55564,#55565,#55566,#55567,#55568,#55569,#55570,
#55571,#55572,#55573)),.UNSPECIFIED.,.F.,.F.,.F.)
B_SPLINE_SURFACE_WITH_KNOTS((2,2),(3,2,2,2,2,2,2,2,2,2,2,2,2,2,2,2,2,2,
2,2,2,2,2,2,2,2,2,2,2,2,2,2,2,2,2,2,2,2,2,2,2,2,2,2,2,2,2,2,2,2,2,2,2,2,
2,2,2,2,2,2,2,2,2,2,2,2,2,2,2,2,2,2,2,2,2,2,2,2,2,2,2,2,2,2,2,2,2,2,2,2,
2,2,2,2,2,2,2,2,2,2,2,2,2,2,2,2,2,2,2,2,2,2,2,2,2,2,2,2,2,2,2,2,2,2,2,2,
2,2,2,2,2,2,2,2,2,2,2,2,2,2,2,2,2,2,2,2,2,2,2,2,2,2,2,2,2,2,2,2,2,2,2,2,
2,2,2,2,2,2,2,2,2,2,2,2,2,2,2,2,2,2,2,2,2,2,2,2,3),(0.,1.00001535537392),
(0.,0.00537634408602151,0.010752688172043,0.0161290322580645,0.021505376344086,
0.0268817204301075,0.032258064516129,0.0376344086021505,0.043010752688172,
0.0483870967741935,0.0537634408602151,0.0591397849462366,0.0645161290322581,
0.0698924731182796,0.0752688172043011,0.0806451612903226,0.0860215053763441,
0.0913978494623656,0.0967741935483871,0.102150537634409,0.10752688172043,
0.112903225806452,0.118279569892473,0.123655913978495,0.129032258064516,
0.134408602150538,0.139784946236559,0.145161290322581,0.150537634408602,
0.155913978494624,0.161290322580645,0.166666666666667,0.172043010752688,
0.17741935483871,0.182795698924731,0.188172043010753,0.193548387096774,
0.198924731182796,0.204301075268817,0.209677419354839,0.21505376344086,
0.220430107526882,0.225806451612903,0.231182795698925,0.236559139784946,
0.241935483870968,0.247311827956989,0.252688172043011,0.258064516129032,
0.263440860215054,0.268817204301075,0.274193548387097,0.279569892473118,
0.28494623655914,0.290322580645161,0.295698924731183,0.301075268817204,
0.306451612903226,0.311827956989247,0.317204301075269,0.32258064516129,
0.327956989247312,0.333333333333333,0.338709677419355,0.344086021505376,
0.349462365591398,0.354838709677419,0.360215053763441,0.365591397849462,
0.370967741935484,0.376344086021505,0.381720430107527,0.387096774193548,
0.39247311827957,0.397849462365591,0.403225806451613,0.408602150537634,
0.413978494623656,0.419354838709677,0.424731182795699,0.43010752688172,
0.435483870967742,0.440860215053763,0.446236559139785,0.451612903225806,
0.456989247311828,0.462365591397849,0.467741935483871,0.473118279569892,
0.478494623655914,0.483870967741935,0.489247311827957,0.494623655913978,
0.5,0.505376344086022,0.510752688172043,0.516129032258065,0.521505376344086,
0.526881720430108,0.532258064516129,0.537634408602151,0.543010752688172,
0.548387096774194,0.553763440860215,0.559139784946237,0.564516129032258,
0.56989247311828,0.575268817204301,0.580645161290323,0.586021505376344,
0.591397849462366,0.596774193548387,0.602150537634409,0.60752688172043,
0.612903225806452,0.618279569892473,0.623655913978495,0.629032258064516,
0.634408602150538,0.639784946236559,0.645161290322581,0.650537634408602,
0.655913978494624,0.661290322580645,0.666666666666667,0.672043010752688,
0.67741935483871,0.682795698924731,0.688172043010753,0.693548387096774,
0.698924731182796,0.704301075268817,0.709677419354839,0.71505376344086,
0.720430107526882,0.725806451612903,0.731182795698925,0.736559139784946,
0.741935483870968,0.747311827956989,0.752688172043011,0.758064516129032,
0.763440860215054,0.768817204301075,0.774193548387097,0.779569892473118,
0.78494623655914,0.790322580645161,0.795698924731183,0.801075268817204,
0.806451612903226,0.811827956989247,0.817204301075269,0.82258064516129,
0.827956989247312,0.833333333333333,0.838709677419355,0.844086021505376,
0.849462365591398,0.854838709677419,0.860215053763441,0.865591397849462,
0.870967741935484,0.876344086021505,0.881720430107527,0.887096774193548,
0.89247311827957,0.897849462365591,0.903225806451613,0.908602150537634,
0.913978494623656,0.919354838709677,0.924731182795699,0.93010752688172,
0.935483870967742,0.940860215053763,0.946236559139785,0.951612903225806,
0.956989247311828,0.962365591397849,0.967741935483871,0.973118279569892,
0.978494623655914,0.983870967741935,0.989247311827957,0.994623655913978,
1.),.UNSPECIFIED.)
GEOMETRIC_REPRESENTATION_ITEM()
RATIONAL_B_SPLINE_SURFACE(((1.,0.866025403784439,1.,0.866025403784439,1.,
0.866025403784439,1.,0.866025403784439,1.,0.866025403784439,1.,0.866025403784439,
1.,0.866025403784439,1.,0.866025403784439,1.,0.866025403784439,1.,0.866025403784439,
1.,0.866025403784439,1.,0.866025403784439,1.,0.866025403784439,1.,0.866025403784439,
1.,0.866025403784439,1.,0.866025403784439,1.,0.866025403784439,1.,0.866025403784439,
1.,0.866025403784439,1.,0.866025403784439,1.,0.866025403784439,1.,0.866025403784439,
1.,0.866025403784439,1.,0.866025403784439,1.,0.866025403784439,1.,0.866025403784439,
1.,0.866025403784439,1.,0.866025403784439,1.,0.866025403784439,1.,0.866025403784439,
1.,0.866025403784439,1.,0.866025403784439,1.,0.866025403784439,1.,0.866025403784439,
1.,0.866025403784439,1.,0.866025403784439,1.,0.866025403784439,1.,0.866025403784439,
1.,0.866025403784439,1.,0.866025403784439,1.,0.866025403784439,1.,0.866025403784439,
1.,0.866025403784439,1.,0.866025403784439,1.,0.866025403784439,1.,0.866025403784439,
1.,0.866025403784439,1.,0.866025403784439,1.,0.866025403784439,1.,0.866025403784439,
1.,0.866025403784439,1.,0.866025403784439,1.,0.866025403784439,1.,0.866025403784439,
1.,0.866025403784439,1.,0.866025403784439,1.,0.866025403784439,1.,0.866025403784439,
1.,0.866025403784439,1.,0.866025403784439,1.,0.866025403784439,1.,0.866025403784439,
1.,0.866025403784439,1.,0.866025403784439,1.,0.866025403784439,1.,0.866025403784439,
1.,0.866025403784439,1.,0.866025403784439,1.,0.866025403784439,1.,0.866025403784439,
1.,0.866025403784439,1.,0.866025403784439,1.,0.866025403784439,1.,0.866025403784439,
1.,0.866025403784439,1.,0.866025403784439,1.,0.866025403784439,1.,0.866025403784439,
1.,0.866025403784439,1.,0.866025403784439,1.,0.866025403784439,1.,0.866025403784439,
1.,0.866025403784439,1.,0.866025403784439,1.,0.866025403784439,1.,0.866025403784439,
1.,0.866025403784439,1.,0.866025403784439,1.,0.866025403784439,1.,0.866025403784439,
1.,0.866025403784439,1.,0.866025403784439,1.,0.866025403784439,1.,0.866025403784439,
1.,0.866025403784439,1.,0.866025403784439,1.,0.866025403784439,1.,0.866025403784439,
1.,0.866025403784439,1.,0.866025403784439,1.,0.866025403784439,1.,0.866025403784439,
1.,0.866025403784439,1.,0.866025403784439,1.,0.866025403784439,1.,0.866025403784439,
1.,0.866025403784439,1.,0.866025403784439,1.,0.866025403784439,1.,0.866025403784439,
1.,0.866025403784439,1.,0.866025403784439,1.,0.866025403784439,1.,0.866025403784439,
1.,0.866025403784439,1.,0.866025403784439,1.,0.866025403784439,1.,0.866025403784439,
1.,0.866025403784439,1.,0.866025403784439,1.,0.866025403784439,1.,0.866025403784439,
1.,0.866025403784439,1.,0.866025403784439,1.,0.866025403784439,1.,0.866025403784439,
1.,0.866025403784439,1.,0.866025403784439,1.,0.866025403784439,1.,0.866025403784439,
1.,0.866025403784439,1.,0.866025403784439,1.,0.866025403784439,1.,0.866025403784439,
1.,0.866025403784439,1.,0.866025403784439,1.,0.866025403784439,1.,0.866025403784439,
1.,0.866025403784439,1.,0.866025403784439,1.,0.866025403784439,1.,0.866025403784439,
1.,0.866025403784439,1.,0.866025403784439,1.,0.866025403784439,1.,0.866025403784439,
1.,0.866025403784439,1.,0.866025403784439,1.,0.866025403784439,1.,0.866025403784439,
1.,0.866025403784439,1.,0.866025403784439,1.,0.866025403784439,1.,0.866025403784439,
1.,0.866025403784439,1.,0.866025403784439,1.,0.866025403784439,1.,0.866025403784439,
1.,0.866025403784439,1.,0.866025403784439,1.,0.866025403784439,1.,0.866025403784439,
1.,0.866025403784439,1.,0.866025403784439,1.,0.866025403784439,1.,0.866025403784439,
1.,0.866025403784439,1.,0.866025403784439,1.,0.866025403784439,1.,0.866025403784439,
1.,0.866025403784439,1.,0.866025403784439,1.,0.866025403784439,1.,0.866025403784439,
1.,0.866025403784439,1.,0.866025403784439,1.,0.866025403784439,1.,0.866025403784439,
1.,0.866025403784439,1.,0.866025403784439,1.,0.866025403784439,1.,0.866025403784439,
1.,0.866025403784439,1.,0.866025403784439,1.,0.866025403784439,1.,0.866025403784439,
1.),(1.,0.866025403784439,1.,0.866025403784439,1.,0.866025403784439,1.,
0.866025403784439,1.,0.866025403784439,1.,0.866025403784439,1.,0.866025403784439,
1.,0.866025403784439,1.,0.866025403784439,1.,0.866025403784439,1.,0.866025403784439,
1.,0.866025403784439,1.,0.866025403784439,1.,0.866025403784439,1.,0.866025403784439,
1.,0.866025403784439,1.,0.866025403784439,1.,0.866025403784439,1.,0.866025403784439,
1.,0.866025403784439,1.,0.866025403784439,1.,0.866025403784439,1.,0.866025403784439,
1.,0.866025403784439,1.,0.866025403784439,1.,0.866025403784439,1.,0.866025403784439,
1.,0.866025403784439,1.,0.866025403784439,1.,0.866025403784439,1.,0.866025403784439,
1.,0.866025403784439,1.,0.866025403784439,1.,0.866025403784439,1.,0.866025403784439,
1.,0.866025403784439,1.,0.866025403784439,1.,0.866025403784439,1.,0.866025403784439,
1.,0.866025403784439,1.,0.866025403784439,1.,0.866025403784439,1.,0.866025403784439,
1.,0.866025403784439,1.,0.866025403784439,1.,0.866025403784439,1.,0.866025403784439,
1.,0.866025403784439,1.,0.866025403784439,1.,0.866025403784439,1.,0.866025403784439,
1.,0.866025403784439,1.,0.866025403784439,1.,0.866025403784439,1.,0.866025403784439,
1.,0.866025403784439,1.,0.866025403784439,1.,0.866025403784439,1.,0.866025403784439,
1.,0.866025403784439,1.,0.866025403784439,1.,0.866025403784439,1.,0.866025403784439,
1.,0.866025403784439,1.,0.866025403784439,1.,0.866025403784439,1.,0.866025403784439,
1.,0.866025403784439,1.,0.866025403784439,1.,0.866025403784439,1.,0.866025403784439,
1.,0.866025403784439,1.,0.866025403784439,1.,0.866025403784439,1.,0.866025403784439,
1.,0.866025403784439,1.,0.866025403784439,1.,0.866025403784439,1.,0.866025403784439,
1.,0.866025403784439,1.,0.866025403784439,1.,0.866025403784439,1.,0.866025403784439,
1.,0.866025403784439,1.,0.866025403784439,1.,0.866025403784439,1.,0.866025403784439,
1.,0.866025403784439,1.,0.866025403784439,1.,0.866025403784439,1.,0.866025403784439,
1.,0.866025403784439,1.,0.866025403784439,1.,0.866025403784439,1.,0.866025403784439,
1.,0.866025403784439,1.,0.866025403784439,1.,0.866025403784439,1.,0.866025403784439,
1.,0.866025403784439,1.,0.866025403784439,1.,0.866025403784439,1.,0.866025403784439,
1.,0.866025403784439,1.,0.866025403784439,1.,0.866025403784439,1.,0.866025403784439,
1.,0.866025403784439,1.,0.866025403784439,1.,0.866025403784439,1.,0.866025403784439,
1.,0.866025403784439,1.,0.866025403784439,1.,0.866025403784439,1.,0.866025403784439,
1.,0.866025403784439,1.,0.866025403784439,1.,0.866025403784439,1.,0.866025403784439,
1.,0.866025403784439,1.,0.866025403784439,1.,0.866025403784439,1.,0.866025403784439,
1.,0.866025403784439,1.,0.866025403784439,1.,0.866025403784439,1.,0.866025403784439,
1.,0.866025403784439,1.,0.866025403784439,1.,0.866025403784439,1.,0.866025403784439,
1.,0.866025403784439,1.,0.866025403784439,1.,0.866025403784439,1.,0.866025403784439,
1.,0.866025403784439,1.,0.866025403784439,1.,0.866025403784439,1.,0.866025403784439,
1.,0.866025403784439,1.,0.866025403784439,1.,0.866025403784439,1.,0.866025403784439,
1.,0.866025403784439,1.,0.866025403784439,1.,0.866025403784439,1.,0.866025403784439,
1.,0.866025403784439,1.,0.866025403784439,1.,0.866025403784439,1.,0.866025403784439,
1.,0.866025403784439,1.,0.866025403784439,1.,0.866025403784439,1.,0.866025403784439,
1.,0.866025403784439,1.,0.866025403784439,1.,0.866025403784439,1.,0.866025403784439,
1.,0.866025403784439,1.,0.866025403784439,1.,0.866025403784439,1.,0.866025403784439,
1.,0.866025403784439,1.,0.866025403784439,1.,0.866025403784439,1.,0.866025403784439,
1.,0.866025403784439,1.,0.866025403784439,1.,0.866025403784439,1.,0.866025403784439,
1.,0.866025403784439,1.,0.866025403784439,1.,0.866025403784439,1.,0.866025403784439,
1.,0.866025403784439,1.,0.866025403784439,1.,0.866025403784439,1.,0.866025403784439,
1.,0.866025403784439,1.,0.866025403784439,1.,0.866025403784439,1.,0.866025403784439,
1.,0.866025403784439,1.,0.866025403784439,1.,0.866025403784439,1.)))
REPRESENTATION_ITEM('')
SURFACE()
);
#49=TOROIDAL_SURFACE('',#32314,2.58058373926377,0.0468749999999982);
#50=TOROIDAL_SURFACE('',#32610,2.721875,0.0468749999999996);
#51=TOROIDAL_SURFACE('',#32615,2.60625,0.0687500000000002);
#52=TOROIDAL_SURFACE('',#32618,1.65,0.15);
#53=TOROIDAL_SURFACE('',#32621,2.703125,0.0468750000000018);
#54=TOROIDAL_SURFACE('',#32625,2.703125,0.0468750000000018);
#55=TOROIDAL_SURFACE('',#32629,2.703125,0.0468750000000018);
#56=TOROIDAL_SURFACE('',#32633,2.703125,0.0468750000000018);
#57=TOROIDAL_SURFACE('',#32637,2.703125,0.0468750000000018);
#58=TOROIDAL_SURFACE('',#32641,2.703125,0.0468750000000018);
#59=TOROIDAL_SURFACE('',#32645,2.703125,0.0468750000000018);
#60=TOROIDAL_SURFACE('',#32649,2.703125,0.0468750000000018);
#61=TOROIDAL_SURFACE('',#32653,2.703125,0.0468750000000018);
#62=TOROIDAL_SURFACE('',#32657,2.703125,0.0468750000000018);
#63=TOROIDAL_SURFACE('',#32661,2.703125,0.0468750000000018);
#64=TOROIDAL_SURFACE('',#32665,2.703125,0.0468750000000018);
#65=TOROIDAL_SURFACE('',#32669,2.703125,0.0468750000000018);
#66=TOROIDAL_SURFACE('',#32673,2.703125,0.0468750000000018);
#67=TOROIDAL_SURFACE('',#32677,2.703125,0.0468750000000018);
#68=TOROIDAL_SURFACE('',#32681,2.703125,0.0468750000000018);
#69=TOROIDAL_SURFACE('',#32685,2.703125,0.0468750000000018);
#70=TOROIDAL_SURFACE('',#32689,2.703125,0.0468750000000018);
#71=TOROIDAL_SURFACE('',#32693,2.703125,0.0468750000000018);
#72=TOROIDAL_SURFACE('',#32697,2.703125,0.0468750000000018);
#73=TOROIDAL_SURFACE('',#32701,2.703125,0.0468750000000018);
#74=TOROIDAL_SURFACE('',#32705,2.703125,0.0468750000000018);
#75=TOROIDAL_SURFACE('',#32709,2.703125,0.0468750000000018);
#76=TOROIDAL_SURFACE('',#32713,2.703125,0.0468750000000018);
#77=TOROIDAL_SURFACE('',#32717,2.703125,0.0468750000000018);
#78=TOROIDAL_SURFACE('',#32721,2.703125,0.0468750000000018);
#79=TOROIDAL_SURFACE('',#32725,2.703125,0.0468750000000018);
#80=TOROIDAL_SURFACE('',#32729,2.703125,0.0468750000000018);
#81=TOROIDAL_SURFACE('',#32733,2.703125,0.0468750000000018);
#82=TOROIDAL_SURFACE('',#32737,2.703125,0.0468750000000018);
#83=TOROIDAL_SURFACE('',#32741,2.703125,0.0468750000000018);
#84=TOROIDAL_SURFACE('',#32745,2.703125,0.0468750000000018);
#85=TOROIDAL_SURFACE('',#32749,2.703125,0.0468750000000018);
#86=TOROIDAL_SURFACE('',#32753,2.703125,0.0468750000000018);
#87=TOROIDAL_SURFACE('',#32757,2.703125,0.0468750000000018);
#88=TOROIDAL_SURFACE('',#32761,2.703125,0.0468750000000018);
#89=TOROIDAL_SURFACE('',#32765,2.703125,0.0468750000000018);
#90=TOROIDAL_SURFACE('',#32769,2.703125,0.0468750000000018);
#91=TOROIDAL_SURFACE('',#32773,2.703125,0.0468750000000018);
#92=TOROIDAL_SURFACE('',#32777,2.703125,0.0468750000000018);
#93=TOROIDAL_SURFACE('',#32781,2.703125,0.0468750000000018);
#94=TOROIDAL_SURFACE('',#32785,2.703125,0.0468750000000018);
#95=TOROIDAL_SURFACE('',#32789,2.703125,0.0468750000000018);
#96=TOROIDAL_SURFACE('',#32793,2.703125,0.0468750000000018);
#97=TOROIDAL_SURFACE('',#32797,2.703125,0.0468750000000018);
#98=TOROIDAL_SURFACE('',#32801,2.703125,0.0468750000000018);
#99=TOROIDAL_SURFACE('',#32805,2.703125,0.0468750000000018);
#100=TOROIDAL_SURFACE('',#32809,2.703125,0.0468750000000018);
#101=TOROIDAL_SURFACE('',#32813,2.703125,0.0468750000000018);
#102=TOROIDAL_SURFACE('',#32817,2.703125,0.0468750000000018);
#103=TOROIDAL_SURFACE('',#32821,2.703125,0.0468750000000018);
#104=TOROIDAL_SURFACE('',#32825,2.703125,0.0468750000000018);
#105=TOROIDAL_SURFACE('',#32829,2.703125,0.0468750000000018);
#106=TOROIDAL_SURFACE('',#32833,2.703125,0.0468750000000018);
#107=TOROIDAL_SURFACE('',#32837,2.703125,0.0468750000000018);
#108=TOROIDAL_SURFACE('',#32841,2.703125,0.0468750000000018);
#109=TOROIDAL_SURFACE('',#32845,2.703125,0.0468750000000018);
#110=TOROIDAL_SURFACE('',#32849,2.703125,0.0468750000000018);
#111=TOROIDAL_SURFACE('',#32853,2.703125,0.0468750000000018);
#112=TOROIDAL_SURFACE('',#32857,2.703125,0.0468750000000018);
#113=TOROIDAL_SURFACE('',#32861,2.703125,0.0468750000000018);
#114=TOROIDAL_SURFACE('',#32865,2.703125,0.0468750000000018);
#115=TOROIDAL_SURFACE('',#32869,2.703125,0.0468750000000018);
#116=TOROIDAL_SURFACE('',#32873,2.703125,0.0468750000000018);
#117=TOROIDAL_SURFACE('',#32877,2.703125,0.0468750000000018);
#118=TOROIDAL_SURFACE('',#32881,2.703125,0.0468750000000018);
#119=TOROIDAL_SURFACE('',#32885,2.703125,0.0468750000000018);
#120=TOROIDAL_SURFACE('',#32889,2.703125,0.0468750000000018);
#121=TOROIDAL_SURFACE('',#32893,2.703125,0.0468750000000018);
#122=TOROIDAL_SURFACE('',#32897,2.703125,0.0468750000000018);
#123=TOROIDAL_SURFACE('',#32901,2.703125,0.0468750000000018);
#124=TOROIDAL_SURFACE('',#32905,2.703125,0.0468750000000018);
#125=TOROIDAL_SURFACE('',#32909,2.703125,0.0468750000000018);
#126=TOROIDAL_SURFACE('',#32913,2.703125,0.0468750000000018);
#127=TOROIDAL_SURFACE('',#32917,2.703125,0.0468750000000018);
#128=TOROIDAL_SURFACE('',#32921,2.703125,0.0468750000000018);
#129=TOROIDAL_SURFACE('',#32925,2.703125,0.0468750000000018);
#130=TOROIDAL_SURFACE('',#32929,2.703125,0.0468750000000018);
#131=TOROIDAL_SURFACE('',#32933,2.703125,0.0468750000000018);
#132=TOROIDAL_SURFACE('',#33095,2.703125,0.046874999999999);
#133=TOROIDAL_SURFACE('',#33098,2.703125,0.046874999999999);
#134=TOROIDAL_SURFACE('',#33101,2.703125,0.046874999999999);
#135=TOROIDAL_SURFACE('',#33104,2.703125,0.046874999999999);
#136=TOROIDAL_SURFACE('',#33107,2.703125,0.046874999999999);
#137=TOROIDAL_SURFACE('',#33110,2.703125,0.046874999999999);
#138=TOROIDAL_SURFACE('',#33113,2.703125,0.046874999999999);
#139=TOROIDAL_SURFACE('',#33116,2.703125,0.046874999999999);
#140=TOROIDAL_SURFACE('',#33119,2.703125,0.046874999999999);
#141=TOROIDAL_SURFACE('',#33122,2.703125,0.046874999999999);
#142=TOROIDAL_SURFACE('',#33125,2.703125,0.046874999999999);
#143=TOROIDAL_SURFACE('',#33128,2.703125,0.046874999999999);
#144=TOROIDAL_SURFACE('',#33131,2.703125,0.046874999999999);
#145=TOROIDAL_SURFACE('',#33134,2.703125,0.046874999999999);
#146=TOROIDAL_SURFACE('',#33137,2.703125,0.046874999999999);
#147=TOROIDAL_SURFACE('',#33140,2.703125,0.046874999999999);
#148=TOROIDAL_SURFACE('',#33143,2.703125,0.046874999999999);
#149=TOROIDAL_SURFACE('',#33146,2.703125,0.046874999999999);
#150=TOROIDAL_SURFACE('',#33149,2.703125,0.046874999999999);
#151=TOROIDAL_SURFACE('',#33152,2.703125,0.046874999999999);
#152=TOROIDAL_SURFACE('',#33155,2.703125,0.046874999999999);
#153=TOROIDAL_SURFACE('',#33158,2.703125,0.046874999999999);
#154=TOROIDAL_SURFACE('',#33161,2.703125,0.046874999999999);
#155=TOROIDAL_SURFACE('',#33164,2.703125,0.046874999999999);
#156=TOROIDAL_SURFACE('',#33167,2.703125,0.046874999999999);
#157=TOROIDAL_SURFACE('',#33170,2.703125,0.046874999999999);
#158=TOROIDAL_SURFACE('',#33173,2.703125,0.046874999999999);
#159=TOROIDAL_SURFACE('',#33176,2.703125,0.046874999999999);
#160=TOROIDAL_SURFACE('',#33179,2.703125,0.046874999999999);
#161=TOROIDAL_SURFACE('',#33182,2.703125,0.046874999999999);
#162=TOROIDAL_SURFACE('',#33185,2.703125,0.046874999999999);
#163=TOROIDAL_SURFACE('',#33188,2.703125,0.046874999999999);
#164=TOROIDAL_SURFACE('',#33191,2.703125,0.046874999999999);
#165=TOROIDAL_SURFACE('',#33194,2.703125,0.046874999999999);
#166=TOROIDAL_SURFACE('',#33197,2.703125,0.046874999999999);
#167=TOROIDAL_SURFACE('',#33200,2.703125,0.046874999999999);
#168=TOROIDAL_SURFACE('',#33203,2.703125,0.046874999999999);
#169=TOROIDAL_SURFACE('',#33206,2.703125,0.046874999999999);
#170=TOROIDAL_SURFACE('',#33209,2.703125,0.046874999999999);
#171=TOROIDAL_SURFACE('',#33212,2.703125,0.046874999999999);
#172=TOROIDAL_SURFACE('',#33215,2.703125,0.046874999999999);
#173=TOROIDAL_SURFACE('',#33218,2.703125,0.046874999999999);
#174=TOROIDAL_SURFACE('',#33221,2.703125,0.046874999999999);
#175=TOROIDAL_SURFACE('',#33224,2.703125,0.046874999999999);
#176=TOROIDAL_SURFACE('',#33227,2.703125,0.046874999999999);
#177=TOROIDAL_SURFACE('',#33230,2.703125,0.046874999999999);
#178=TOROIDAL_SURFACE('',#33233,2.703125,0.046874999999999);
#179=TOROIDAL_SURFACE('',#33236,2.703125,0.046874999999999);
#180=TOROIDAL_SURFACE('',#33239,2.703125,0.046874999999999);
#181=TOROIDAL_SURFACE('',#33242,2.703125,0.046874999999999);
#182=TOROIDAL_SURFACE('',#33245,2.703125,0.046874999999999);
#183=TOROIDAL_SURFACE('',#33248,2.703125,0.046874999999999);
#184=TOROIDAL_SURFACE('',#33251,2.703125,0.046874999999999);
#185=TOROIDAL_SURFACE('',#33254,2.703125,0.046874999999999);
#186=TOROIDAL_SURFACE('',#33257,2.703125,0.046874999999999);
#187=TOROIDAL_SURFACE('',#33260,2.703125,0.046874999999999);
#188=TOROIDAL_SURFACE('',#33263,2.703125,0.046874999999999);
#189=TOROIDAL_SURFACE('',#33266,2.703125,0.046874999999999);
#190=TOROIDAL_SURFACE('',#33269,2.703125,0.046874999999999);
#191=TOROIDAL_SURFACE('',#33272,2.703125,0.046874999999999);
#192=TOROIDAL_SURFACE('',#33275,2.703125,0.046874999999999);
#193=TOROIDAL_SURFACE('',#33278,2.703125,0.046874999999999);
#194=TOROIDAL_SURFACE('',#33281,2.703125,0.046874999999999);
#195=TOROIDAL_SURFACE('',#33284,2.703125,0.046874999999999);
#196=TOROIDAL_SURFACE('',#33287,2.703125,0.046874999999999);
#197=TOROIDAL_SURFACE('',#33290,2.703125,0.046874999999999);
#198=TOROIDAL_SURFACE('',#33293,2.703125,0.046874999999999);
#199=TOROIDAL_SURFACE('',#33296,2.703125,0.046874999999999);
#200=TOROIDAL_SURFACE('',#33299,2.703125,0.046874999999999);
#201=TOROIDAL_SURFACE('',#33302,2.703125,0.046874999999999);
#202=TOROIDAL_SURFACE('',#33305,2.703125,0.046874999999999);
#203=TOROIDAL_SURFACE('',#33308,2.703125,0.046874999999999);
#204=TOROIDAL_SURFACE('',#33311,2.703125,0.046874999999999);
#205=TOROIDAL_SURFACE('',#33314,2.703125,0.046874999999999);
#206=TOROIDAL_SURFACE('',#33317,2.703125,0.046874999999999);
#207=TOROIDAL_SURFACE('',#33320,2.703125,0.046874999999999);
#208=TOROIDAL_SURFACE('',#33323,2.703125,0.046874999999999);
#209=TOROIDAL_SURFACE('',#33326,2.703125,0.046874999999999);
#210=TOROIDAL_SURFACE('',#33329,2.703125,0.046874999999999);
#211=TOROIDAL_SURFACE('',#33334,2.703125,0.0468750000000018);
#212=TOROIDAL_SURFACE('',#33340,2.703125,0.046874999999999);
#541=(
BOUNDED_CURVE()
B_SPLINE_CURVE(2,(#50905,#50906,#50907),.UNSPECIFIED.,.F.,.F.)
B_SPLINE_CURVE_WITH_KNOTS((3,3),(-0.375752880509706,-0.25773139970398),
 .UNSPECIFIED.)
CURVE()
GEOMETRIC_REPRESENTATION_ITEM()
RATIONAL_B_SPLINE_CURVE((1.41147367097488,1.52065153937885,1.52065153937885))
REPRESENTATION_ITEM('')
);
#542=(
BOUNDED_CURVE()
B_SPLINE_CURVE(2,(#50909,#50910,#50911),.UNSPECIFIED.,.F.,.F.)
B_SPLINE_CURVE_WITH_KNOTS((3,3),(-0.375752880509709,-0.139709918898254),
 .UNSPECIFIED.)
CURVE()
GEOMETRIC_REPRESENTATION_ITEM()
RATIONAL_B_SPLINE_CURVE((1.41147367097488,1.62982940778282,1.41147367097488))
REPRESENTATION_ITEM('')
);
#543=(
BOUNDED_CURVE()
B_SPLINE_CURVE(2,(#50913,#50914,#50915),.UNSPECIFIED.,.F.,.F.)
B_SPLINE_CURVE_WITH_KNOTS((3,3),(-0.375752880509709,-0.139709918898254),
 .UNSPECIFIED.)
CURVE()
GEOMETRIC_REPRESENTATION_ITEM()
RATIONAL_B_SPLINE_CURVE((1.41147367097488,1.62982940778282,1.41147367097488))
REPRESENTATION_ITEM('')
);
#544=(
BOUNDED_CURVE()
B_SPLINE_CURVE(2,(#50917,#50918,#50919),.UNSPECIFIED.,.F.,.F.)
B_SPLINE_CURVE_WITH_KNOTS((3,3),(-0.375752880509708,-0.139709918898254),
 .UNSPECIFIED.)
CURVE()
GEOMETRIC_REPRESENTATION_ITEM()
RATIONAL_B_SPLINE_CURVE((1.41147367097487,1.62982940778281,1.41147367097487))
REPRESENTATION_ITEM('')
);
#545=(
BOUNDED_CURVE()
B_SPLINE_CURVE(2,(#50921,#50922,#50923),.UNSPECIFIED.,.F.,.F.)
B_SPLINE_CURVE_WITH_KNOTS((3,3),(-0.375752880509709,-0.139709918898253),
 .UNSPECIFIED.)
CURVE()
GEOMETRIC_REPRESENTATION_ITEM()
RATIONAL_B_SPLINE_CURVE((1.41147367097488,1.62982940778282,1.41147367097488))
REPRESENTATION_ITEM('')
);
#546=(
BOUNDED_CURVE()
B_SPLINE_CURVE(2,(#50925,#50926,#50927),.UNSPECIFIED.,.F.,.F.)
B_SPLINE_CURVE_WITH_KNOTS((3,3),(-0.375752880509709,-0.139709918898254),
 .UNSPECIFIED.)
CURVE()
GEOMETRIC_REPRESENTATION_ITEM()
RATIONAL_B_SPLINE_CURVE((1.41147367097488,1.62982940778282,1.41147367097488))
REPRESENTATION_ITEM('')
);
#547=(
BOUNDED_CURVE()
B_SPLINE_CURVE(2,(#50928,#50929,#50930),.UNSPECIFIED.,.F.,.F.)
B_SPLINE_CURVE_WITH_KNOTS((3,3),(-0.25773139970398,-0.139709918898256),
 .UNSPECIFIED.)
CURVE()
GEOMETRIC_REPRESENTATION_ITEM()
RATIONAL_B_SPLINE_CURVE((1.52065153937885,1.52065153937885,1.41147367097488))
REPRESENTATION_ITEM('')
);
#548=(
BOUNDED_CURVE()
B_SPLINE_CURVE(2,(#50952,#50953,#50954),.UNSPECIFIED.,.F.,.F.)
B_SPLINE_CURVE_WITH_KNOTS((3,3),(0.367644516946548,0.373830527582523),
 .UNSPECIFIED.)
CURVE()
GEOMETRIC_REPRESENTATION_ITEM()
RATIONAL_B_SPLINE_CURVE((1.13426390111316,1.13389822901309,1.13348223894575))
REPRESENTATION_ITEM('')
);
#549=(
BOUNDED_CURVE()
B_SPLINE_CURVE(2,(#50958,#50959,#50960),.UNSPECIFIED.,.F.,.F.)
B_SPLINE_CURVE_WITH_KNOTS((3,3),(0.271548216895916,0.277734227531904),
 .UNSPECIFIED.)
CURVE()
GEOMETRIC_REPRESENTATION_ITEM()
RATIONAL_B_SPLINE_CURVE((1.13348223894615,1.1338982290135,1.13426390111357))
REPRESENTATION_ITEM('')
);
#550=(
BOUNDED_CURVE()
B_SPLINE_CURVE(2,(#50964,#50965,#50966),.UNSPECIFIED.,.F.,.F.)
B_SPLINE_CURVE_WITH_KNOTS((3,3),(0.36764451694656,0.373830527582529),
 .UNSPECIFIED.)
CURVE()
GEOMETRIC_REPRESENTATION_ITEM()
RATIONAL_B_SPLINE_CURVE((1.13426390111306,1.13389822901299,1.13348223894565))
REPRESENTATION_ITEM('')
);
#551=(
BOUNDED_CURVE()
B_SPLINE_CURVE(2,(#50970,#50971,#50972),.UNSPECIFIED.,.F.,.F.)
B_SPLINE_CURVE_WITH_KNOTS((3,3),(0.271548216895914,0.277734227531901),
 .UNSPECIFIED.)
CURVE()
GEOMETRIC_REPRESENTATION_ITEM()
RATIONAL_B_SPLINE_CURVE((1.13348223894612,1.13389822901347,1.13426390111354))
REPRESENTATION_ITEM('')
);
#552=(
BOUNDED_CURVE()
B_SPLINE_CURVE(2,(#50976,#50977,#50978),.UNSPECIFIED.,.F.,.F.)
B_SPLINE_CURVE_WITH_KNOTS((3,3),(0.367644516946562,0.373830527582532),
 .UNSPECIFIED.)
CURVE()
GEOMETRIC_REPRESENTATION_ITEM()
RATIONAL_B_SPLINE_CURVE((1.13426390111304,1.13389822901297,1.13348223894563))
REPRESENTATION_ITEM('')
);
#553=(
BOUNDED_CURVE()
B_SPLINE_CURVE(2,(#50982,#50983,#50984),.UNSPECIFIED.,.F.,.F.)
B_SPLINE_CURVE_WITH_KNOTS((3,3),(0.27154821689591,0.277734227531895),
 .UNSPECIFIED.)
CURVE()
GEOMETRIC_REPRESENTATION_ITEM()
RATIONAL_B_SPLINE_CURVE((1.13348223894613,1.13389822901348,1.13426390111355))
REPRESENTATION_ITEM('')
);
#554=(
BOUNDED_CURVE()
B_SPLINE_CURVE(2,(#50988,#50989,#50990),.UNSPECIFIED.,.F.,.F.)
B_SPLINE_CURVE_WITH_KNOTS((3,3),(0.367644516946554,0.373830527582529),
 .UNSPECIFIED.)
CURVE()
GEOMETRIC_REPRESENTATION_ITEM()
RATIONAL_B_SPLINE_CURVE((1.13426390111305,1.13389822901299,1.13348223894564))
REPRESENTATION_ITEM('')
);
#555=(
BOUNDED_CURVE()
B_SPLINE_CURVE(2,(#50994,#50995,#50996),.UNSPECIFIED.,.F.,.F.)
B_SPLINE_CURVE_WITH_KNOTS((3,3),(0.271548216895907,0.277734227531893),
 .UNSPECIFIED.)
CURVE()
GEOMETRIC_REPRESENTATION_ITEM()
RATIONAL_B_SPLINE_CURVE((1.13348223894611,1.13389822901346,1.13426390111353))
REPRESENTATION_ITEM('')
);
#556=(
BOUNDED_CURVE()
B_SPLINE_CURVE(2,(#51000,#51001,#51002),.UNSPECIFIED.,.F.,.F.)
B_SPLINE_CURVE_WITH_KNOTS((3,3),(0.367644516946562,0.373830527582532),
 .UNSPECIFIED.)
CURVE()
GEOMETRIC_REPRESENTATION_ITEM()
RATIONAL_B_SPLINE_CURVE((1.13426390111302,1.13389822901296,1.13348223894561))
REPRESENTATION_ITEM('')
);
#557=(
BOUNDED_CURVE()
B_SPLINE_CURVE(2,(#51006,#51007,#51008),.UNSPECIFIED.,.F.,.F.)
B_SPLINE_CURVE_WITH_KNOTS((3,3),(0.271548216895914,0.277734227531899),
 .UNSPECIFIED.)
CURVE()
GEOMETRIC_REPRESENTATION_ITEM()
RATIONAL_B_SPLINE_CURVE((1.13348223894609,1.13389822901344,1.13426390111351))
REPRESENTATION_ITEM('')
);
#558=(
BOUNDED_CURVE()
B_SPLINE_CURVE(2,(#51012,#51013,#51014),.UNSPECIFIED.,.F.,.F.)
B_SPLINE_CURVE_WITH_KNOTS((3,3),(0.36764451694656,0.373830527582535),
 .UNSPECIFIED.)
CURVE()
GEOMETRIC_REPRESENTATION_ITEM()
RATIONAL_B_SPLINE_CURVE((1.13426390111302,1.13389822901295,1.1334822389456))
REPRESENTATION_ITEM('')
);
#559=(
BOUNDED_CURVE()
B_SPLINE_CURVE(2,(#51018,#51019,#51020),.UNSPECIFIED.,.F.,.F.)
B_SPLINE_CURVE_WITH_KNOTS((3,3),(0.271548216895908,0.277734227531894),
 .UNSPECIFIED.)
CURVE()
GEOMETRIC_REPRESENTATION_ITEM()
RATIONAL_B_SPLINE_CURVE((1.1334822389461,1.13389822901345,1.13426390111352))
REPRESENTATION_ITEM('')
);
#560=(
BOUNDED_CURVE()
B_SPLINE_CURVE(2,(#51024,#51025,#51026),.UNSPECIFIED.,.F.,.F.)
B_SPLINE_CURVE_WITH_KNOTS((3,3),(0.367644516946558,0.373830527582536),
 .UNSPECIFIED.)
CURVE()
GEOMETRIC_REPRESENTATION_ITEM()
RATIONAL_B_SPLINE_CURVE((1.13426390111302,1.13389822901295,1.13348223894561))
REPRESENTATION_ITEM('')
);
#561=(
BOUNDED_CURVE()
B_SPLINE_CURVE(2,(#51030,#51031,#51032),.UNSPECIFIED.,.F.,.F.)
B_SPLINE_CURVE_WITH_KNOTS((3,3),(0.271548216895914,0.277734227531899),
 .UNSPECIFIED.)
CURVE()
GEOMETRIC_REPRESENTATION_ITEM()
RATIONAL_B_SPLINE_CURVE((1.13348223894613,1.13389822901348,1.13426390111355))
REPRESENTATION_ITEM('')
);
#562=(
BOUNDED_CURVE()
B_SPLINE_CURVE(2,(#51036,#51037,#51038),.UNSPECIFIED.,.F.,.F.)
B_SPLINE_CURVE_WITH_KNOTS((3,3),(0.367644516946564,0.373830527582534),
 .UNSPECIFIED.)
CURVE()
GEOMETRIC_REPRESENTATION_ITEM()
RATIONAL_B_SPLINE_CURVE((1.13426390111303,1.13389822901296,1.13348223894561))
REPRESENTATION_ITEM('')
);
#563=(
BOUNDED_CURVE()
B_SPLINE_CURVE(2,(#51042,#51043,#51044),.UNSPECIFIED.,.F.,.F.)
B_SPLINE_CURVE_WITH_KNOTS((3,3),(0.271548216895916,0.277734227531901),
 .UNSPECIFIED.)
CURVE()
GEOMETRIC_REPRESENTATION_ITEM()
RATIONAL_B_SPLINE_CURVE((1.13348223894614,1.13389822901349,1.13426390111357))
REPRESENTATION_ITEM('')
);
#564=(
BOUNDED_CURVE()
B_SPLINE_CURVE(2,(#51048,#51049,#51050),.UNSPECIFIED.,.F.,.F.)
B_SPLINE_CURVE_WITH_KNOTS((3,3),(0.367644516946554,0.373830527582527),
 .UNSPECIFIED.)
CURVE()
GEOMETRIC_REPRESENTATION_ITEM()
RATIONAL_B_SPLINE_CURVE((1.13426390111312,1.13389822901305,1.13348223894571))
REPRESENTATION_ITEM('')
);
#565=(
BOUNDED_CURVE()
B_SPLINE_CURVE(2,(#51054,#51055,#51056),.UNSPECIFIED.,.F.,.F.)
B_SPLINE_CURVE_WITH_KNOTS((3,3),(0.271548216895913,0.2777342275319),
 .UNSPECIFIED.)
CURVE()
GEOMETRIC_REPRESENTATION_ITEM()
RATIONAL_B_SPLINE_CURVE((1.13348223894615,1.1338982290135,1.13426390111358))
REPRESENTATION_ITEM('')
);
#566=(
BOUNDED_CURVE()
B_SPLINE_CURVE(2,(#51060,#51061,#51062),.UNSPECIFIED.,.F.,.F.)
B_SPLINE_CURVE_WITH_KNOTS((3,3),(0.367644516946564,0.373830527582538),
 .UNSPECIFIED.)
CURVE()
GEOMETRIC_REPRESENTATION_ITEM()
RATIONAL_B_SPLINE_CURVE((1.134263901113,1.13389822901293,1.13348223894559))
REPRESENTATION_ITEM('')
);
#567=(
BOUNDED_CURVE()
B_SPLINE_CURVE(2,(#51066,#51067,#51068),.UNSPECIFIED.,.F.,.F.)
B_SPLINE_CURVE_WITH_KNOTS((3,3),(0.271548216895908,0.277734227531895),
 .UNSPECIFIED.)
CURVE()
GEOMETRIC_REPRESENTATION_ITEM()
RATIONAL_B_SPLINE_CURVE((1.13348223894615,1.1338982290135,1.13426390111358))
REPRESENTATION_ITEM('')
);
#568=(
BOUNDED_CURVE()
B_SPLINE_CURVE(2,(#51072,#51073,#51074),.UNSPECIFIED.,.F.,.F.)
B_SPLINE_CURVE_WITH_KNOTS((3,3),(0.367644516946561,0.373830527582532),
 .UNSPECIFIED.)
CURVE()
GEOMETRIC_REPRESENTATION_ITEM()
RATIONAL_B_SPLINE_CURVE((1.13426390111309,1.13389822901302,1.13348223894568))
REPRESENTATION_ITEM('')
);
#569=(
BOUNDED_CURVE()
B_SPLINE_CURVE(2,(#51078,#51079,#51080),.UNSPECIFIED.,.F.,.F.)
B_SPLINE_CURVE_WITH_KNOTS((3,3),(0.271548216895921,0.277734227531907),
 .UNSPECIFIED.)
CURVE()
GEOMETRIC_REPRESENTATION_ITEM()
RATIONAL_B_SPLINE_CURVE((1.13348223894616,1.13389822901351,1.13426390111358))
REPRESENTATION_ITEM('')
);
#570=(
BOUNDED_CURVE()
B_SPLINE_CURVE(2,(#51084,#51085,#51086),.UNSPECIFIED.,.F.,.F.)
B_SPLINE_CURVE_WITH_KNOTS((3,3),(0.367644516946558,0.373830527582535),
 .UNSPECIFIED.)
CURVE()
GEOMETRIC_REPRESENTATION_ITEM()
RATIONAL_B_SPLINE_CURVE((1.13426390111305,1.13389822901298,1.13348223894564))
REPRESENTATION_ITEM('')
);
#571=(
BOUNDED_CURVE()
B_SPLINE_CURVE(2,(#51090,#51091,#51092),.UNSPECIFIED.,.F.,.F.)
B_SPLINE_CURVE_WITH_KNOTS((3,3),(0.271548216895908,0.27773422753189),
 .UNSPECIFIED.)
CURVE()
GEOMETRIC_REPRESENTATION_ITEM()
RATIONAL_B_SPLINE_CURVE((1.13348223894616,1.13389822901351,1.13426390111359))
REPRESENTATION_ITEM('')
);
#572=(
BOUNDED_CURVE()
B_SPLINE_CURVE(2,(#51096,#51097,#51098),.UNSPECIFIED.,.F.,.F.)
B_SPLINE_CURVE_WITH_KNOTS((3,3),(0.367644516946548,0.373830527582523),
 .UNSPECIFIED.)
CURVE()
GEOMETRIC_REPRESENTATION_ITEM()
RATIONAL_B_SPLINE_CURVE((1.13426390111314,1.13389822901308,1.13348223894573))
REPRESENTATION_ITEM('')
);
#573=(
BOUNDED_CURVE()
B_SPLINE_CURVE(2,(#51102,#51103,#51104),.UNSPECIFIED.,.F.,.F.)
B_SPLINE_CURVE_WITH_KNOTS((3,3),(0.271548216895905,0.277734227531892),
 .UNSPECIFIED.)
CURVE()
GEOMETRIC_REPRESENTATION_ITEM()
RATIONAL_B_SPLINE_CURVE((1.13348223894608,1.13389822901343,1.1342639011135))
REPRESENTATION_ITEM('')
);
#574=(
BOUNDED_CURVE()
B_SPLINE_CURVE(2,(#51108,#51109,#51110),.UNSPECIFIED.,.F.,.F.)
B_SPLINE_CURVE_WITH_KNOTS((3,3),(0.36764451694655,0.373830527582528),
 .UNSPECIFIED.)
CURVE()
GEOMETRIC_REPRESENTATION_ITEM()
RATIONAL_B_SPLINE_CURVE((1.1342639011131,1.13389822901304,1.13348223894569))
REPRESENTATION_ITEM('')
);
#575=(
BOUNDED_CURVE()
B_SPLINE_CURVE(2,(#51114,#51115,#51116),.UNSPECIFIED.,.F.,.F.)
B_SPLINE_CURVE_WITH_KNOTS((3,3),(0.27154821689591,0.277734227531895),
 .UNSPECIFIED.)
CURVE()
GEOMETRIC_REPRESENTATION_ITEM()
RATIONAL_B_SPLINE_CURVE((1.13348223894612,1.13389822901347,1.13426390111354))
REPRESENTATION_ITEM('')
);
#576=(
BOUNDED_CURVE()
B_SPLINE_CURVE(2,(#51120,#51121,#51122),.UNSPECIFIED.,.F.,.F.)
B_SPLINE_CURVE_WITH_KNOTS((3,3),(0.367644516946551,0.373830527582525),
 .UNSPECIFIED.)
CURVE()
GEOMETRIC_REPRESENTATION_ITEM()
RATIONAL_B_SPLINE_CURVE((1.13426390111313,1.13389822901307,1.13348223894572))
REPRESENTATION_ITEM('')
);
#577=(
BOUNDED_CURVE()
B_SPLINE_CURVE(2,(#51126,#51127,#51128),.UNSPECIFIED.,.F.,.F.)
B_SPLINE_CURVE_WITH_KNOTS((3,3),(0.271548216895914,0.277734227531894),
 .UNSPECIFIED.)
CURVE()
GEOMETRIC_REPRESENTATION_ITEM()
RATIONAL_B_SPLINE_CURVE((1.13348223894619,1.13389822901354,1.13426390111361))
REPRESENTATION_ITEM('')
);
#578=(
BOUNDED_CURVE()
B_SPLINE_CURVE(2,(#51132,#51133,#51134),.UNSPECIFIED.,.F.,.F.)
B_SPLINE_CURVE_WITH_KNOTS((3,3),(0.367644516946565,0.373830527582531),
 .UNSPECIFIED.)
CURVE()
GEOMETRIC_REPRESENTATION_ITEM()
RATIONAL_B_SPLINE_CURVE((1.134263901113,1.13389822901293,1.13348223894559))
REPRESENTATION_ITEM('')
);
#579=(
BOUNDED_CURVE()
B_SPLINE_CURVE(2,(#51138,#51139,#51140),.UNSPECIFIED.,.F.,.F.)
B_SPLINE_CURVE_WITH_KNOTS((3,3),(0.271548216895912,0.277734227531896),
 .UNSPECIFIED.)
CURVE()
GEOMETRIC_REPRESENTATION_ITEM()
RATIONAL_B_SPLINE_CURVE((1.13348223894612,1.13389822901347,1.13426390111354))
REPRESENTATION_ITEM('')
);
#580=(
BOUNDED_CURVE()
B_SPLINE_CURVE(2,(#51144,#51145,#51146),.UNSPECIFIED.,.F.,.F.)
B_SPLINE_CURVE_WITH_KNOTS((3,3),(0.367644516946563,0.373830527582537),
 .UNSPECIFIED.)
CURVE()
GEOMETRIC_REPRESENTATION_ITEM()
RATIONAL_B_SPLINE_CURVE((1.13426390111305,1.13389822901298,1.13348223894564))
REPRESENTATION_ITEM('')
);
#581=(
BOUNDED_CURVE()
B_SPLINE_CURVE(2,(#51150,#51151,#51152),.UNSPECIFIED.,.F.,.F.)
B_SPLINE_CURVE_WITH_KNOTS((3,3),(0.271548216895909,0.277734227531891),
 .UNSPECIFIED.)
CURVE()
GEOMETRIC_REPRESENTATION_ITEM()
RATIONAL_B_SPLINE_CURVE((1.13348223894604,1.13389822901339,1.13426390111346))
REPRESENTATION_ITEM('')
);
#582=(
BOUNDED_CURVE()
B_SPLINE_CURVE(2,(#51156,#51157,#51158),.UNSPECIFIED.,.F.,.F.)
B_SPLINE_CURVE_WITH_KNOTS((3,3),(0.367644516946552,0.373830527582532),
 .UNSPECIFIED.)
CURVE()
GEOMETRIC_REPRESENTATION_ITEM()
RATIONAL_B_SPLINE_CURVE((1.13426390111305,1.13389822901299,1.13348223894564))
REPRESENTATION_ITEM('')
);
#583=(
BOUNDED_CURVE()
B_SPLINE_CURVE(2,(#51162,#51163,#51164),.UNSPECIFIED.,.F.,.F.)
B_SPLINE_CURVE_WITH_KNOTS((3,3),(0.271548216895916,0.277734227531902),
 .UNSPECIFIED.)
CURVE()
GEOMETRIC_REPRESENTATION_ITEM()
RATIONAL_B_SPLINE_CURVE((1.13348223894616,1.13389822901351,1.13426390111359))
REPRESENTATION_ITEM('')
);
#584=(
BOUNDED_CURVE()
B_SPLINE_CURVE(2,(#51168,#51169,#51170),.UNSPECIFIED.,.F.,.F.)
B_SPLINE_CURVE_WITH_KNOTS((3,3),(0.367644516946562,0.373830527582535),
 .UNSPECIFIED.)
CURVE()
GEOMETRIC_REPRESENTATION_ITEM()
RATIONAL_B_SPLINE_CURVE((1.13426390111309,1.13389822901302,1.13348223894568))
REPRESENTATION_ITEM('')
);
#585=(
BOUNDED_CURVE()
B_SPLINE_CURVE(2,(#51174,#51175,#51176),.UNSPECIFIED.,.F.,.F.)
B_SPLINE_CURVE_WITH_KNOTS((3,3),(0.271548216895913,0.277734227531904),
 .UNSPECIFIED.)
CURVE()
GEOMETRIC_REPRESENTATION_ITEM()
RATIONAL_B_SPLINE_CURVE((1.13348223894619,1.13389822901354,1.13426390111362))
REPRESENTATION_ITEM('')
);
#586=(
BOUNDED_CURVE()
B_SPLINE_CURVE(2,(#51180,#51181,#51182),.UNSPECIFIED.,.F.,.F.)
B_SPLINE_CURVE_WITH_KNOTS((3,3),(0.36764451694655,0.373830527582524),
 .UNSPECIFIED.)
CURVE()
GEOMETRIC_REPRESENTATION_ITEM()
RATIONAL_B_SPLINE_CURVE((1.13426390111312,1.13389822901305,1.13348223894571))
REPRESENTATION_ITEM('')
);
#587=(
BOUNDED_CURVE()
B_SPLINE_CURVE(2,(#51186,#51187,#51188),.UNSPECIFIED.,.F.,.F.)
B_SPLINE_CURVE_WITH_KNOTS((3,3),(0.271548216895921,0.277734227531899),
 .UNSPECIFIED.)
CURVE()
GEOMETRIC_REPRESENTATION_ITEM()
RATIONAL_B_SPLINE_CURVE((1.13348223894619,1.13389822901354,1.13426390111361))
REPRESENTATION_ITEM('')
);
#588=(
BOUNDED_CURVE()
B_SPLINE_CURVE(2,(#51192,#51193,#51194),.UNSPECIFIED.,.F.,.F.)
B_SPLINE_CURVE_WITH_KNOTS((3,3),(0.367644516946559,0.373830527582526),
 .UNSPECIFIED.)
CURVE()
GEOMETRIC_REPRESENTATION_ITEM()
RATIONAL_B_SPLINE_CURVE((1.1342639011131,1.13389822901303,1.13348223894569))
REPRESENTATION_ITEM('')
);
#589=(
BOUNDED_CURVE()
B_SPLINE_CURVE(2,(#51198,#51199,#51200),.UNSPECIFIED.,.F.,.F.)
B_SPLINE_CURVE_WITH_KNOTS((3,3),(0.271548216895914,0.2777342275319),
 .UNSPECIFIED.)
CURVE()
GEOMETRIC_REPRESENTATION_ITEM()
RATIONAL_B_SPLINE_CURVE((1.13348223894616,1.13389822901351,1.13426390111358))
REPRESENTATION_ITEM('')
);
#590=(
BOUNDED_CURVE()
B_SPLINE_CURVE(2,(#51204,#51205,#51206),.UNSPECIFIED.,.F.,.F.)
B_SPLINE_CURVE_WITH_KNOTS((3,3),(0.367644516946557,0.373830527582536),
 .UNSPECIFIED.)
CURVE()
GEOMETRIC_REPRESENTATION_ITEM()
RATIONAL_B_SPLINE_CURVE((1.13426390111309,1.13389822901303,1.13348223894568))
REPRESENTATION_ITEM('')
);
#591=(
BOUNDED_CURVE()
B_SPLINE_CURVE(2,(#51210,#51211,#51212),.UNSPECIFIED.,.F.,.F.)
B_SPLINE_CURVE_WITH_KNOTS((3,3),(0.271548216895912,0.277734227531897),
 .UNSPECIFIED.)
CURVE()
GEOMETRIC_REPRESENTATION_ITEM()
RATIONAL_B_SPLINE_CURVE((1.13348223894616,1.13389822901351,1.13426390111358))
REPRESENTATION_ITEM('')
);
#592=(
BOUNDED_CURVE()
B_SPLINE_CURVE(2,(#51216,#51217,#51218),.UNSPECIFIED.,.F.,.F.)
B_SPLINE_CURVE_WITH_KNOTS((3,3),(0.367644516946558,0.373830527582532),
 .UNSPECIFIED.)
CURVE()
GEOMETRIC_REPRESENTATION_ITEM()
RATIONAL_B_SPLINE_CURVE((1.13426390111307,1.13389822901301,1.13348223894566))
REPRESENTATION_ITEM('')
);
#593=(
BOUNDED_CURVE()
B_SPLINE_CURVE(2,(#51222,#51223,#51224),.UNSPECIFIED.,.F.,.F.)
B_SPLINE_CURVE_WITH_KNOTS((3,3),(0.271548216895914,0.277734227531905),
 .UNSPECIFIED.)
CURVE()
GEOMETRIC_REPRESENTATION_ITEM()
RATIONAL_B_SPLINE_CURVE((1.13348223894616,1.13389822901351,1.13426390111358))
REPRESENTATION_ITEM('')
);
#594=(
BOUNDED_CURVE()
B_SPLINE_CURVE(2,(#51228,#51229,#51230),.UNSPECIFIED.,.F.,.F.)
B_SPLINE_CURVE_WITH_KNOTS((3,3),(0.367644516946569,0.373830527582539),
 .UNSPECIFIED.)
CURVE()
GEOMETRIC_REPRESENTATION_ITEM()
RATIONAL_B_SPLINE_CURVE((1.13426390111301,1.13389822901295,1.1334822389456))
REPRESENTATION_ITEM('')
);
#595=(
BOUNDED_CURVE()
B_SPLINE_CURVE(2,(#51234,#51235,#51236),.UNSPECIFIED.,.F.,.F.)
B_SPLINE_CURVE_WITH_KNOTS((3,3),(0.271548216895913,0.2777342275319),
 .UNSPECIFIED.)
CURVE()
GEOMETRIC_REPRESENTATION_ITEM()
RATIONAL_B_SPLINE_CURVE((1.13348223894614,1.13389822901349,1.13426390111356))
REPRESENTATION_ITEM('')
);
#596=(
BOUNDED_CURVE()
B_SPLINE_CURVE(2,(#51240,#51241,#51242),.UNSPECIFIED.,.F.,.F.)
B_SPLINE_CURVE_WITH_KNOTS((3,3),(0.367644516946566,0.373830527582539),
 .UNSPECIFIED.)
CURVE()
GEOMETRIC_REPRESENTATION_ITEM()
RATIONAL_B_SPLINE_CURVE((1.13426390111297,1.1338982290129,1.13348223894556))
REPRESENTATION_ITEM('')
);
#597=(
BOUNDED_CURVE()
B_SPLINE_CURVE(2,(#51246,#51247,#51248),.UNSPECIFIED.,.F.,.F.)
B_SPLINE_CURVE_WITH_KNOTS((3,3),(0.271548216895926,0.277734227531904),
 .UNSPECIFIED.)
CURVE()
GEOMETRIC_REPRESENTATION_ITEM()
RATIONAL_B_SPLINE_CURVE((1.13348223894627,1.13389822901362,1.1342639011137))
REPRESENTATION_ITEM('')
);
#598=(
BOUNDED_CURVE()
B_SPLINE_CURVE(2,(#51252,#51253,#51254),.UNSPECIFIED.,.F.,.F.)
B_SPLINE_CURVE_WITH_KNOTS((3,3),(0.367644516946557,0.373830527582532),
 .UNSPECIFIED.)
CURVE()
GEOMETRIC_REPRESENTATION_ITEM()
RATIONAL_B_SPLINE_CURVE((1.13426390111306,1.13389822901299,1.13348223894565))
REPRESENTATION_ITEM('')
);
#599=(
BOUNDED_CURVE()
B_SPLINE_CURVE(2,(#51258,#51259,#51260),.UNSPECIFIED.,.F.,.F.)
B_SPLINE_CURVE_WITH_KNOTS((3,3),(0.271548216895913,0.277734227531899),
 .UNSPECIFIED.)
CURVE()
GEOMETRIC_REPRESENTATION_ITEM()
RATIONAL_B_SPLINE_CURVE((1.13348223894618,1.13389822901353,1.13426390111361))
REPRESENTATION_ITEM('')
);
#600=(
BOUNDED_CURVE()
B_SPLINE_CURVE(2,(#51264,#51265,#51266),.UNSPECIFIED.,.F.,.F.)
B_SPLINE_CURVE_WITH_KNOTS((3,3),(0.367644516946561,0.373830527582535),
 .UNSPECIFIED.)
CURVE()
GEOMETRIC_REPRESENTATION_ITEM()
RATIONAL_B_SPLINE_CURVE((1.13426390111305,1.13389822901298,1.13348223894564))
REPRESENTATION_ITEM('')
);
#601=(
BOUNDED_CURVE()
B_SPLINE_CURVE(2,(#51270,#51271,#51272),.UNSPECIFIED.,.F.,.F.)
B_SPLINE_CURVE_WITH_KNOTS((3,3),(0.271548216895915,0.277734227531905),
 .UNSPECIFIED.)
CURVE()
GEOMETRIC_REPRESENTATION_ITEM()
RATIONAL_B_SPLINE_CURVE((1.13348223894613,1.13389822901348,1.13426390111356))
REPRESENTATION_ITEM('')
);
#602=(
BOUNDED_CURVE()
B_SPLINE_CURVE(2,(#51276,#51277,#51278),.UNSPECIFIED.,.F.,.F.)
B_SPLINE_CURVE_WITH_KNOTS((3,3),(0.367644516946559,0.373830527582528),
 .UNSPECIFIED.)
CURVE()
GEOMETRIC_REPRESENTATION_ITEM()
RATIONAL_B_SPLINE_CURVE((1.13426390111303,1.13389822901297,1.13348223894562))
REPRESENTATION_ITEM('')
);
#603=(
BOUNDED_CURVE()
B_SPLINE_CURVE(2,(#51282,#51283,#51284),.UNSPECIFIED.,.F.,.F.)
B_SPLINE_CURVE_WITH_KNOTS((3,3),(0.271548216895913,0.277734227531899),
 .UNSPECIFIED.)
CURVE()
GEOMETRIC_REPRESENTATION_ITEM()
RATIONAL_B_SPLINE_CURVE((1.13348223894613,1.13389822901348,1.13426390111356))
REPRESENTATION_ITEM('')
);
#604=(
BOUNDED_CURVE()
B_SPLINE_CURVE(2,(#51288,#51289,#51290),.UNSPECIFIED.,.F.,.F.)
B_SPLINE_CURVE_WITH_KNOTS((3,3),(0.367644516946557,0.373830527582533),
 .UNSPECIFIED.)
CURVE()
GEOMETRIC_REPRESENTATION_ITEM()
RATIONAL_B_SPLINE_CURVE((1.13426390111302,1.13389822901296,1.13348223894561))
REPRESENTATION_ITEM('')
);
#605=(
BOUNDED_CURVE()
B_SPLINE_CURVE(2,(#51294,#51295,#51296),.UNSPECIFIED.,.F.,.F.)
B_SPLINE_CURVE_WITH_KNOTS((3,3),(0.271548216895926,0.277734227531906),
 .UNSPECIFIED.)
CURVE()
GEOMETRIC_REPRESENTATION_ITEM()
RATIONAL_B_SPLINE_CURVE((1.13348223894624,1.13389822901359,1.13426390111366))
REPRESENTATION_ITEM('')
);
#606=(
BOUNDED_CURVE()
B_SPLINE_CURVE(2,(#51300,#51301,#51302),.UNSPECIFIED.,.F.,.F.)
B_SPLINE_CURVE_WITH_KNOTS((3,3),(0.367644516946561,0.373830527582536),
 .UNSPECIFIED.)
CURVE()
GEOMETRIC_REPRESENTATION_ITEM()
RATIONAL_B_SPLINE_CURVE((1.13426390111306,1.13389822901299,1.13348223894564))
REPRESENTATION_ITEM('')
);
#607=(
BOUNDED_CURVE()
B_SPLINE_CURVE(2,(#51306,#51307,#51308),.UNSPECIFIED.,.F.,.F.)
B_SPLINE_CURVE_WITH_KNOTS((3,3),(0.271548216895911,0.277734227531901),
 .UNSPECIFIED.)
CURVE()
GEOMETRIC_REPRESENTATION_ITEM()
RATIONAL_B_SPLINE_CURVE((1.13348223894609,1.13389822901344,1.13426390111352))
REPRESENTATION_ITEM('')
);
#608=(
BOUNDED_CURVE()
B_SPLINE_CURVE(2,(#51312,#51313,#51314),.UNSPECIFIED.,.F.,.F.)
B_SPLINE_CURVE_WITH_KNOTS((3,3),(0.367644516946558,0.373830527582533),
 .UNSPECIFIED.)
CURVE()
GEOMETRIC_REPRESENTATION_ITEM()
RATIONAL_B_SPLINE_CURVE((1.1342639011131,1.13389822901303,1.13348223894569))
REPRESENTATION_ITEM('')
);
#609=(
BOUNDED_CURVE()
B_SPLINE_CURVE(2,(#51318,#51319,#51320),.UNSPECIFIED.,.F.,.F.)
B_SPLINE_CURVE_WITH_KNOTS((3,3),(0.271548216895922,0.277734227531909),
 .UNSPECIFIED.)
CURVE()
GEOMETRIC_REPRESENTATION_ITEM()
RATIONAL_B_SPLINE_CURVE((1.13348223894623,1.13389822901358,1.13426390111366))
REPRESENTATION_ITEM('')
);
#610=(
BOUNDED_CURVE()
B_SPLINE_CURVE(2,(#51324,#51325,#51326),.UNSPECIFIED.,.F.,.F.)
B_SPLINE_CURVE_WITH_KNOTS((3,3),(0.367644516946562,0.373830527582538),
 .UNSPECIFIED.)
CURVE()
GEOMETRIC_REPRESENTATION_ITEM()
RATIONAL_B_SPLINE_CURVE((1.13426390111305,1.13389822901298,1.13348223894563))
REPRESENTATION_ITEM('')
);
#611=(
BOUNDED_CURVE()
B_SPLINE_CURVE(2,(#51330,#51331,#51332),.UNSPECIFIED.,.F.,.F.)
B_SPLINE_CURVE_WITH_KNOTS((3,3),(0.271548216895906,0.277734227531898),
 .UNSPECIFIED.)
CURVE()
GEOMETRIC_REPRESENTATION_ITEM()
RATIONAL_B_SPLINE_CURVE((1.13348223894604,1.13389822901339,1.13426390111346))
REPRESENTATION_ITEM('')
);
#612=(
BOUNDED_CURVE()
B_SPLINE_CURVE(2,(#51336,#51337,#51338),.UNSPECIFIED.,.F.,.F.)
B_SPLINE_CURVE_WITH_KNOTS((3,3),(0.367644516946563,0.373830527582537),
 .UNSPECIFIED.)
CURVE()
GEOMETRIC_REPRESENTATION_ITEM()
RATIONAL_B_SPLINE_CURVE((1.134263901113,1.13389822901294,1.13348223894559))
REPRESENTATION_ITEM('')
);
#613=(
BOUNDED_CURVE()
B_SPLINE_CURVE(2,(#51342,#51343,#51344),.UNSPECIFIED.,.F.,.F.)
B_SPLINE_CURVE_WITH_KNOTS((3,3),(0.271548216895914,0.277734227531897),
 .UNSPECIFIED.)
CURVE()
GEOMETRIC_REPRESENTATION_ITEM()
RATIONAL_B_SPLINE_CURVE((1.13348223894613,1.13389822901348,1.13426390111355))
REPRESENTATION_ITEM('')
);
#614=(
BOUNDED_CURVE()
B_SPLINE_CURVE(2,(#51348,#51349,#51350),.UNSPECIFIED.,.F.,.F.)
B_SPLINE_CURVE_WITH_KNOTS((3,3),(0.367644516946558,0.373830527582532),
 .UNSPECIFIED.)
CURVE()
GEOMETRIC_REPRESENTATION_ITEM()
RATIONAL_B_SPLINE_CURVE((1.13426390111307,1.133898229013,1.13348223894566))
REPRESENTATION_ITEM('')
);
#615=(
BOUNDED_CURVE()
B_SPLINE_CURVE(2,(#51354,#51355,#51356),.UNSPECIFIED.,.F.,.F.)
B_SPLINE_CURVE_WITH_KNOTS((3,3),(0.271548216895917,0.277734227531901),
 .UNSPECIFIED.)
CURVE()
GEOMETRIC_REPRESENTATION_ITEM()
RATIONAL_B_SPLINE_CURVE((1.13348223894616,1.1338982290135,1.13426390111358))
REPRESENTATION_ITEM('')
);
#616=(
BOUNDED_CURVE()
B_SPLINE_CURVE(2,(#51360,#51361,#51362),.UNSPECIFIED.,.F.,.F.)
B_SPLINE_CURVE_WITH_KNOTS((3,3),(0.367644516946556,0.37383052758253),
 .UNSPECIFIED.)
CURVE()
GEOMETRIC_REPRESENTATION_ITEM()
RATIONAL_B_SPLINE_CURVE((1.13426390111304,1.13389822901297,1.13348223894563))
REPRESENTATION_ITEM('')
);
#617=(
BOUNDED_CURVE()
B_SPLINE_CURVE(2,(#51366,#51367,#51368),.UNSPECIFIED.,.F.,.F.)
B_SPLINE_CURVE_WITH_KNOTS((3,3),(0.271548216895911,0.277734227531893),
 .UNSPECIFIED.)
CURVE()
GEOMETRIC_REPRESENTATION_ITEM()
RATIONAL_B_SPLINE_CURVE((1.13348223894607,1.13389822901342,1.13426390111349))
REPRESENTATION_ITEM('')
);
#618=(
BOUNDED_CURVE()
B_SPLINE_CURVE(2,(#51372,#51373,#51374),.UNSPECIFIED.,.F.,.F.)
B_SPLINE_CURVE_WITH_KNOTS((3,3),(0.367644516946565,0.373830527582539),
 .UNSPECIFIED.)
CURVE()
GEOMETRIC_REPRESENTATION_ITEM()
RATIONAL_B_SPLINE_CURVE((1.13426390111301,1.13389822901295,1.1334822389456))
REPRESENTATION_ITEM('')
);
#619=(
BOUNDED_CURVE()
B_SPLINE_CURVE(2,(#51378,#51379,#51380),.UNSPECIFIED.,.F.,.F.)
B_SPLINE_CURVE_WITH_KNOTS((3,3),(0.271548216895916,0.277734227531897),
 .UNSPECIFIED.)
CURVE()
GEOMETRIC_REPRESENTATION_ITEM()
RATIONAL_B_SPLINE_CURVE((1.13348223894613,1.13389822901348,1.13426390111355))
REPRESENTATION_ITEM('')
);
#620=(
BOUNDED_CURVE()
B_SPLINE_CURVE(2,(#51384,#51385,#51386),.UNSPECIFIED.,.F.,.F.)
B_SPLINE_CURVE_WITH_KNOTS((3,3),(0.36764451694656,0.373830527582534),
 .UNSPECIFIED.)
CURVE()
GEOMETRIC_REPRESENTATION_ITEM()
RATIONAL_B_SPLINE_CURVE((1.13426390111306,1.13389822901299,1.13348223894564))
REPRESENTATION_ITEM('')
);
#621=(
BOUNDED_CURVE()
B_SPLINE_CURVE(2,(#51390,#51391,#51392),.UNSPECIFIED.,.F.,.F.)
B_SPLINE_CURVE_WITH_KNOTS((3,3),(0.271548216895918,0.277734227531904),
 .UNSPECIFIED.)
CURVE()
GEOMETRIC_REPRESENTATION_ITEM()
RATIONAL_B_SPLINE_CURVE((1.13348223894613,1.13389822901348,1.13426390111355))
REPRESENTATION_ITEM('')
);
#622=(
BOUNDED_CURVE()
B_SPLINE_CURVE(2,(#51396,#51397,#51398),.UNSPECIFIED.,.F.,.F.)
B_SPLINE_CURVE_WITH_KNOTS((3,3),(0.367644516946555,0.373830527582533),
 .UNSPECIFIED.)
CURVE()
GEOMETRIC_REPRESENTATION_ITEM()
RATIONAL_B_SPLINE_CURVE((1.13426390111305,1.13389822901298,1.13348223894564))
REPRESENTATION_ITEM('')
);
#623=(
BOUNDED_CURVE()
B_SPLINE_CURVE(2,(#51402,#51403,#51404),.UNSPECIFIED.,.F.,.F.)
B_SPLINE_CURVE_WITH_KNOTS((3,3),(0.271548216895928,0.277734227531916),
 .UNSPECIFIED.)
CURVE()
GEOMETRIC_REPRESENTATION_ITEM()
RATIONAL_B_SPLINE_CURVE((1.13348223894621,1.13389822901356,1.13426390111363))
REPRESENTATION_ITEM('')
);
#624=(
BOUNDED_CURVE()
B_SPLINE_CURVE(2,(#51408,#51409,#51410),.UNSPECIFIED.,.F.,.F.)
B_SPLINE_CURVE_WITH_KNOTS((3,3),(0.367644516946548,0.373830527582523),
 .UNSPECIFIED.)
CURVE()
GEOMETRIC_REPRESENTATION_ITEM()
RATIONAL_B_SPLINE_CURVE((1.13426390111312,1.13389822901305,1.13348223894571))
REPRESENTATION_ITEM('')
);
#625=(
BOUNDED_CURVE()
B_SPLINE_CURVE(2,(#51414,#51415,#51416),.UNSPECIFIED.,.F.,.F.)
B_SPLINE_CURVE_WITH_KNOTS((3,3),(0.271548216895918,0.277734227531905),
 .UNSPECIFIED.)
CURVE()
GEOMETRIC_REPRESENTATION_ITEM()
RATIONAL_B_SPLINE_CURVE((1.13348223894611,1.13389822901346,1.13426390111354))
REPRESENTATION_ITEM('')
);
#626=(
BOUNDED_CURVE()
B_SPLINE_CURVE(2,(#51420,#51421,#51422),.UNSPECIFIED.,.F.,.F.)
B_SPLINE_CURVE_WITH_KNOTS((3,3),(0.367644516946559,0.373830527582532),
 .UNSPECIFIED.)
CURVE()
GEOMETRIC_REPRESENTATION_ITEM()
RATIONAL_B_SPLINE_CURVE((1.13426390111305,1.13389822901298,1.13348223894564))
REPRESENTATION_ITEM('')
);
#627=(
BOUNDED_CURVE()
B_SPLINE_CURVE(2,(#51426,#51427,#51428),.UNSPECIFIED.,.F.,.F.)
B_SPLINE_CURVE_WITH_KNOTS((3,3),(0.271548216895915,0.277734227531901),
 .UNSPECIFIED.)
CURVE()
GEOMETRIC_REPRESENTATION_ITEM()
RATIONAL_B_SPLINE_CURVE((1.13348223894615,1.1338982290135,1.13426390111357))
REPRESENTATION_ITEM('')
);
#628=(
BOUNDED_CURVE()
B_SPLINE_CURVE(2,(#51432,#51433,#51434),.UNSPECIFIED.,.F.,.F.)
B_SPLINE_CURVE_WITH_KNOTS((3,3),(0.367644516946548,0.373830527582526),
 .UNSPECIFIED.)
CURVE()
GEOMETRIC_REPRESENTATION_ITEM()
RATIONAL_B_SPLINE_CURVE((1.13426390111308,1.13389822901302,1.13348223894567))
REPRESENTATION_ITEM('')
);
#629=(
BOUNDED_CURVE()
B_SPLINE_CURVE(2,(#51438,#51439,#51440),.UNSPECIFIED.,.F.,.F.)
B_SPLINE_CURVE_WITH_KNOTS((3,3),(0.271548216895917,0.277734227531902),
 .UNSPECIFIED.)
CURVE()
GEOMETRIC_REPRESENTATION_ITEM()
RATIONAL_B_SPLINE_CURVE((1.13348223894615,1.1338982290135,1.13426390111358))
REPRESENTATION_ITEM('')
);
#630=(
BOUNDED_CURVE()
B_SPLINE_CURVE(2,(#51444,#51445,#51446),.UNSPECIFIED.,.F.,.F.)
B_SPLINE_CURVE_WITH_KNOTS((3,3),(0.367644516946561,0.373830527582534),
 .UNSPECIFIED.)
CURVE()
GEOMETRIC_REPRESENTATION_ITEM()
RATIONAL_B_SPLINE_CURVE((1.13426390111303,1.13389822901296,1.13348223894562))
REPRESENTATION_ITEM('')
);
#631=(
BOUNDED_CURVE()
B_SPLINE_CURVE(2,(#51450,#51451,#51452),.UNSPECIFIED.,.F.,.F.)
B_SPLINE_CURVE_WITH_KNOTS((3,3),(0.271548216895922,0.277734227531908),
 .UNSPECIFIED.)
CURVE()
GEOMETRIC_REPRESENTATION_ITEM()
RATIONAL_B_SPLINE_CURVE((1.13348223894617,1.13389822901352,1.1342639011136))
REPRESENTATION_ITEM('')
);
#632=(
BOUNDED_CURVE()
B_SPLINE_CURVE(2,(#51456,#51457,#51458),.UNSPECIFIED.,.F.,.F.)
B_SPLINE_CURVE_WITH_KNOTS((3,3),(0.367644516946555,0.373830527582532),
 .UNSPECIFIED.)
CURVE()
GEOMETRIC_REPRESENTATION_ITEM()
RATIONAL_B_SPLINE_CURVE((1.13426390111307,1.133898229013,1.13348223894566))
REPRESENTATION_ITEM('')
);
#633=(
BOUNDED_CURVE()
B_SPLINE_CURVE(2,(#51462,#51463,#51464),.UNSPECIFIED.,.F.,.F.)
B_SPLINE_CURVE_WITH_KNOTS((3,3),(0.27154821689592,0.277734227531907),
 .UNSPECIFIED.)
CURVE()
GEOMETRIC_REPRESENTATION_ITEM()
RATIONAL_B_SPLINE_CURVE((1.13348223894614,1.13389822901349,1.13426390111356))
REPRESENTATION_ITEM('')
);
#634=(
BOUNDED_CURVE()
B_SPLINE_CURVE(2,(#51468,#51469,#51470),.UNSPECIFIED.,.F.,.F.)
B_SPLINE_CURVE_WITH_KNOTS((3,3),(0.367644516946564,0.373830527582538),
 .UNSPECIFIED.)
CURVE()
GEOMETRIC_REPRESENTATION_ITEM()
RATIONAL_B_SPLINE_CURVE((1.13426390111299,1.13389822901292,1.13348223894557))
REPRESENTATION_ITEM('')
);
#635=(
BOUNDED_CURVE()
B_SPLINE_CURVE(2,(#51474,#51475,#51476),.UNSPECIFIED.,.F.,.F.)
B_SPLINE_CURVE_WITH_KNOTS((3,3),(0.271548216895926,0.277734227531912),
 .UNSPECIFIED.)
CURVE()
GEOMETRIC_REPRESENTATION_ITEM()
RATIONAL_B_SPLINE_CURVE((1.13348223894617,1.13389822901352,1.13426390111359))
REPRESENTATION_ITEM('')
);
#636=(
BOUNDED_CURVE()
B_SPLINE_CURVE(2,(#51480,#51481,#51482),.UNSPECIFIED.,.F.,.F.)
B_SPLINE_CURVE_WITH_KNOTS((3,3),(0.367644516946548,0.373830527582525),
 .UNSPECIFIED.)
CURVE()
GEOMETRIC_REPRESENTATION_ITEM()
RATIONAL_B_SPLINE_CURVE((1.13426390111308,1.13389822901301,1.13348223894567))
REPRESENTATION_ITEM('')
);
#637=(
BOUNDED_CURVE()
B_SPLINE_CURVE(2,(#51486,#51487,#51488),.UNSPECIFIED.,.F.,.F.)
B_SPLINE_CURVE_WITH_KNOTS((3,3),(0.271548216895921,0.277734227531907),
 .UNSPECIFIED.)
CURVE()
GEOMETRIC_REPRESENTATION_ITEM()
RATIONAL_B_SPLINE_CURVE((1.13348223894617,1.13389822901352,1.13426390111359))
REPRESENTATION_ITEM('')
);
#638=(
BOUNDED_CURVE()
B_SPLINE_CURVE(2,(#51492,#51493,#51494),.UNSPECIFIED.,.F.,.F.)
B_SPLINE_CURVE_WITH_KNOTS((3,3),(0.367644516946557,0.373830527582527),
 .UNSPECIFIED.)
CURVE()
GEOMETRIC_REPRESENTATION_ITEM()
RATIONAL_B_SPLINE_CURVE((1.1342639011131,1.13389822901303,1.13348223894569))
REPRESENTATION_ITEM('')
);
#639=(
BOUNDED_CURVE()
B_SPLINE_CURVE(2,(#51497,#51498,#51499),.UNSPECIFIED.,.F.,.F.)
B_SPLINE_CURVE_WITH_KNOTS((3,3),(0.271548216895922,0.277734227531908),
 .UNSPECIFIED.)
CURVE()
GEOMETRIC_REPRESENTATION_ITEM()
RATIONAL_B_SPLINE_CURVE((1.13348223894615,1.1338982290135,1.13426390111358))
REPRESENTATION_ITEM('')
);
#640=(
BOUNDED_CURVE()
B_SPLINE_CURVE(2,(#51501,#51502,#51503),.UNSPECIFIED.,.F.,.F.)
B_SPLINE_CURVE_WITH_KNOTS((3,3),(0.367644516946556,0.373830527582529),
 .UNSPECIFIED.)
CURVE()
GEOMETRIC_REPRESENTATION_ITEM()
RATIONAL_B_SPLINE_CURVE((1.13426390111308,1.13389822901301,1.13348223894567))
REPRESENTATION_ITEM('')
);
#641=(
BOUNDED_CURVE()
B_SPLINE_CURVE(2,(#51506,#51507,#51508),.UNSPECIFIED.,.F.,.F.)
B_SPLINE_CURVE_WITH_KNOTS((3,3),(0.271548216895921,0.277734227531909),
 .UNSPECIFIED.)
CURVE()
GEOMETRIC_REPRESENTATION_ITEM()
RATIONAL_B_SPLINE_CURVE((1.13348223894619,1.13389822901354,1.13426390111361))
REPRESENTATION_ITEM('')
);
#642=(
BOUNDED_CURVE()
B_SPLINE_CURVE(2,(#51510,#51511,#51512),.UNSPECIFIED.,.F.,.F.)
B_SPLINE_CURVE_WITH_KNOTS((3,3),(0.36764451694656,0.37383052758253),
 .UNSPECIFIED.)
CURVE()
GEOMETRIC_REPRESENTATION_ITEM()
RATIONAL_B_SPLINE_CURVE((1.13426390111303,1.13389822901296,1.13348223894562))
REPRESENTATION_ITEM('')
);
#643=(
BOUNDED_CURVE()
B_SPLINE_CURVE(2,(#51515,#51516,#51517),.UNSPECIFIED.,.F.,.F.)
B_SPLINE_CURVE_WITH_KNOTS((3,3),(0.271548216895921,0.277734227531907),
 .UNSPECIFIED.)
CURVE()
GEOMETRIC_REPRESENTATION_ITEM()
RATIONAL_B_SPLINE_CURVE((1.13348223894618,1.13389822901353,1.1342639011136))
REPRESENTATION_ITEM('')
);
#644=(
BOUNDED_CURVE()
B_SPLINE_CURVE(2,(#51519,#51520,#51521),.UNSPECIFIED.,.F.,.F.)
B_SPLINE_CURVE_WITH_KNOTS((3,3),(0.367644516946553,0.373830527582534),
 .UNSPECIFIED.)
CURVE()
GEOMETRIC_REPRESENTATION_ITEM()
RATIONAL_B_SPLINE_CURVE((1.13426390111306,1.13389822901299,1.13348223894565))
REPRESENTATION_ITEM('')
);
#645=(
BOUNDED_CURVE()
B_SPLINE_CURVE(2,(#51524,#51525,#51526),.UNSPECIFIED.,.F.,.F.)
B_SPLINE_CURVE_WITH_KNOTS((3,3),(0.271548216895916,0.277734227531903),
 .UNSPECIFIED.)
CURVE()
GEOMETRIC_REPRESENTATION_ITEM()
RATIONAL_B_SPLINE_CURVE((1.13348223894615,1.1338982290135,1.13426390111357))
REPRESENTATION_ITEM('')
);
#646=(
BOUNDED_CURVE()
B_SPLINE_CURVE(2,(#51528,#51529,#51530),.UNSPECIFIED.,.F.,.F.)
B_SPLINE_CURVE_WITH_KNOTS((3,3),(0.367644516946558,0.373830527582532),
 .UNSPECIFIED.)
CURVE()
GEOMETRIC_REPRESENTATION_ITEM()
RATIONAL_B_SPLINE_CURVE((1.13426390111307,1.13389822901301,1.13348223894566))
REPRESENTATION_ITEM('')
);
#647=(
BOUNDED_CURVE()
B_SPLINE_CURVE(2,(#51533,#51534,#51535),.UNSPECIFIED.,.F.,.F.)
B_SPLINE_CURVE_WITH_KNOTS((3,3),(0.271548216895911,0.277734227531895),
 .UNSPECIFIED.)
CURVE()
GEOMETRIC_REPRESENTATION_ITEM()
RATIONAL_B_SPLINE_CURVE((1.13348223894606,1.13389822901341,1.13426390111348))
REPRESENTATION_ITEM('')
);
#648=(
BOUNDED_CURVE()
B_SPLINE_CURVE(2,(#51537,#51538,#51539),.UNSPECIFIED.,.F.,.F.)
B_SPLINE_CURVE_WITH_KNOTS((3,3),(0.367644516946553,0.373830527582531),
 .UNSPECIFIED.)
CURVE()
GEOMETRIC_REPRESENTATION_ITEM()
RATIONAL_B_SPLINE_CURVE((1.13426390111307,1.133898229013,1.13348223894566))
REPRESENTATION_ITEM('')
);
#649=(
BOUNDED_CURVE()
B_SPLINE_CURVE(2,(#51542,#51543,#51544),.UNSPECIFIED.,.F.,.F.)
B_SPLINE_CURVE_WITH_KNOTS((3,3),(0.271548216895918,0.277734227531903),
 .UNSPECIFIED.)
CURVE()
GEOMETRIC_REPRESENTATION_ITEM()
RATIONAL_B_SPLINE_CURVE((1.13348223894611,1.13389822901346,1.13426390111353))
REPRESENTATION_ITEM('')
);
#650=(
BOUNDED_CURVE()
B_SPLINE_CURVE(2,(#51546,#51547,#51548),.UNSPECIFIED.,.F.,.F.)
B_SPLINE_CURVE_WITH_KNOTS((3,3),(0.367644516946551,0.373830527582526),
 .UNSPECIFIED.)
CURVE()
GEOMETRIC_REPRESENTATION_ITEM()
RATIONAL_B_SPLINE_CURVE((1.1342639011131,1.13389822901304,1.13348223894569))
REPRESENTATION_ITEM('')
);
#651=(
BOUNDED_CURVE()
B_SPLINE_CURVE(2,(#51551,#51552,#51553),.UNSPECIFIED.,.F.,.F.)
B_SPLINE_CURVE_WITH_KNOTS((3,3),(0.271548216895922,0.277734227531909),
 .UNSPECIFIED.)
CURVE()
GEOMETRIC_REPRESENTATION_ITEM()
RATIONAL_B_SPLINE_CURVE((1.13348223894615,1.1338982290135,1.13426390111357))
REPRESENTATION_ITEM('')
);
#652=(
BOUNDED_CURVE()
B_SPLINE_CURVE(2,(#51555,#51556,#51557),.UNSPECIFIED.,.F.,.F.)
B_SPLINE_CURVE_WITH_KNOTS((3,3),(0.36764451694656,0.373830527582534),
 .UNSPECIFIED.)
CURVE()
GEOMETRIC_REPRESENTATION_ITEM()
RATIONAL_B_SPLINE_CURVE((1.13426390111304,1.13389822901297,1.13348223894563))
REPRESENTATION_ITEM('')
);
#653=(
BOUNDED_CURVE()
B_SPLINE_CURVE(2,(#51560,#51561,#51562),.UNSPECIFIED.,.F.,.F.)
B_SPLINE_CURVE_WITH_KNOTS((3,3),(0.271548216895917,0.277734227531904),
 .UNSPECIFIED.)
CURVE()
GEOMETRIC_REPRESENTATION_ITEM()
RATIONAL_B_SPLINE_CURVE((1.13348223894616,1.13389822901351,1.13426390111359))
REPRESENTATION_ITEM('')
);
#654=(
BOUNDED_CURVE()
B_SPLINE_CURVE(2,(#51564,#51565,#51566),.UNSPECIFIED.,.F.,.F.)
B_SPLINE_CURVE_WITH_KNOTS((3,3),(0.367644516946562,0.373830527582537),
 .UNSPECIFIED.)
CURVE()
GEOMETRIC_REPRESENTATION_ITEM()
RATIONAL_B_SPLINE_CURVE((1.13426390111298,1.13389822901291,1.13348223894556))
REPRESENTATION_ITEM('')
);
#655=(
BOUNDED_CURVE()
B_SPLINE_CURVE(2,(#51569,#51570,#51571),.UNSPECIFIED.,.F.,.F.)
B_SPLINE_CURVE_WITH_KNOTS((3,3),(0.271548216895925,0.277734227531911),
 .UNSPECIFIED.)
CURVE()
GEOMETRIC_REPRESENTATION_ITEM()
RATIONAL_B_SPLINE_CURVE((1.13348223894616,1.13389822901351,1.13426390111359))
REPRESENTATION_ITEM('')
);
#656=(
BOUNDED_CURVE()
B_SPLINE_CURVE(2,(#51573,#51574,#51575),.UNSPECIFIED.,.F.,.F.)
B_SPLINE_CURVE_WITH_KNOTS((3,3),(0.367644516946555,0.373830527582529),
 .UNSPECIFIED.)
CURVE()
GEOMETRIC_REPRESENTATION_ITEM()
RATIONAL_B_SPLINE_CURVE((1.13426390111312,1.13389822901305,1.13348223894571))
REPRESENTATION_ITEM('')
);
#657=(
BOUNDED_CURVE()
B_SPLINE_CURVE(2,(#51578,#51579,#51580),.UNSPECIFIED.,.F.,.F.)
B_SPLINE_CURVE_WITH_KNOTS((3,3),(0.271548216895925,0.277734227531912),
 .UNSPECIFIED.)
CURVE()
GEOMETRIC_REPRESENTATION_ITEM()
RATIONAL_B_SPLINE_CURVE((1.13348223894618,1.13389822901353,1.1342639011136))
REPRESENTATION_ITEM('')
);
#658=(
BOUNDED_CURVE()
B_SPLINE_CURVE(2,(#51582,#51583,#51584),.UNSPECIFIED.,.F.,.F.)
B_SPLINE_CURVE_WITH_KNOTS((3,3),(0.367644516946557,0.373830527582532),
 .UNSPECIFIED.)
CURVE()
GEOMETRIC_REPRESENTATION_ITEM()
RATIONAL_B_SPLINE_CURVE((1.13426390111306,1.13389822901299,1.13348223894564))
REPRESENTATION_ITEM('')
);
#659=(
BOUNDED_CURVE()
B_SPLINE_CURVE(2,(#51587,#51588,#51589),.UNSPECIFIED.,.F.,.F.)
B_SPLINE_CURVE_WITH_KNOTS((3,3),(0.271548216895908,0.277734227531892),
 .UNSPECIFIED.)
CURVE()
GEOMETRIC_REPRESENTATION_ITEM()
RATIONAL_B_SPLINE_CURVE((1.13348223894609,1.13389822901344,1.13426390111352))
REPRESENTATION_ITEM('')
);
#660=(
BOUNDED_CURVE()
B_SPLINE_CURVE(2,(#51591,#51592,#51593),.UNSPECIFIED.,.F.,.F.)
B_SPLINE_CURVE_WITH_KNOTS((3,3),(0.367644516946557,0.373830527582522),
 .UNSPECIFIED.)
CURVE()
GEOMETRIC_REPRESENTATION_ITEM()
RATIONAL_B_SPLINE_CURVE((1.13426390111309,1.13389822901302,1.13348223894568))
REPRESENTATION_ITEM('')
);
#661=(
BOUNDED_CURVE()
B_SPLINE_CURVE(2,(#51596,#51597,#51598),.UNSPECIFIED.,.F.,.F.)
B_SPLINE_CURVE_WITH_KNOTS((3,3),(0.271548216895913,0.277734227531902),
 .UNSPECIFIED.)
CURVE()
GEOMETRIC_REPRESENTATION_ITEM()
RATIONAL_B_SPLINE_CURVE((1.1334822389461,1.13389822901345,1.13426390111352))
REPRESENTATION_ITEM('')
);
#662=(
BOUNDED_CURVE()
B_SPLINE_CURVE(2,(#51600,#51601,#51602),.UNSPECIFIED.,.F.,.F.)
B_SPLINE_CURVE_WITH_KNOTS((3,3),(0.367644516946559,0.373830527582539),
 .UNSPECIFIED.)
CURVE()
GEOMETRIC_REPRESENTATION_ITEM()
RATIONAL_B_SPLINE_CURVE((1.13426390111296,1.13389822901289,1.13348223894555))
REPRESENTATION_ITEM('')
);
#663=(
BOUNDED_CURVE()
B_SPLINE_CURVE(2,(#51605,#51606,#51607),.UNSPECIFIED.,.F.,.F.)
B_SPLINE_CURVE_WITH_KNOTS((3,3),(0.271548216895926,0.277734227531913),
 .UNSPECIFIED.)
CURVE()
GEOMETRIC_REPRESENTATION_ITEM()
RATIONAL_B_SPLINE_CURVE((1.13348223894622,1.13389822901357,1.13426390111365))
REPRESENTATION_ITEM('')
);
#664=(
BOUNDED_CURVE()
B_SPLINE_CURVE(2,(#51609,#51610,#51611),.UNSPECIFIED.,.F.,.F.)
B_SPLINE_CURVE_WITH_KNOTS((3,3),(0.36764451694656,0.373830527582534),
 .UNSPECIFIED.)
CURVE()
GEOMETRIC_REPRESENTATION_ITEM()
RATIONAL_B_SPLINE_CURVE((1.13426390111298,1.13389822901291,1.13348223894557))
REPRESENTATION_ITEM('')
);
#665=(
BOUNDED_CURVE()
B_SPLINE_CURVE(2,(#51614,#51615,#51616),.UNSPECIFIED.,.F.,.F.)
B_SPLINE_CURVE_WITH_KNOTS((3,3),(0.271548216895926,0.277734227531909),
 .UNSPECIFIED.)
CURVE()
GEOMETRIC_REPRESENTATION_ITEM()
RATIONAL_B_SPLINE_CURVE((1.13348223894617,1.13389822901352,1.13426390111359))
REPRESENTATION_ITEM('')
);
#666=(
BOUNDED_CURVE()
B_SPLINE_CURVE(2,(#51618,#51619,#51620),.UNSPECIFIED.,.F.,.F.)
B_SPLINE_CURVE_WITH_KNOTS((3,3),(0.367644516946566,0.373830527582539),
 .UNSPECIFIED.)
CURVE()
GEOMETRIC_REPRESENTATION_ITEM()
RATIONAL_B_SPLINE_CURVE((1.13426390111296,1.13389822901289,1.13348223894555))
REPRESENTATION_ITEM('')
);
#667=(
BOUNDED_CURVE()
B_SPLINE_CURVE(2,(#51623,#51624,#51625),.UNSPECIFIED.,.F.,.F.)
B_SPLINE_CURVE_WITH_KNOTS((3,3),(0.271548216895918,0.277734227531904),
 .UNSPECIFIED.)
CURVE()
GEOMETRIC_REPRESENTATION_ITEM()
RATIONAL_B_SPLINE_CURVE((1.13348223894611,1.13389822901346,1.13426390111353))
REPRESENTATION_ITEM('')
);
#668=(
BOUNDED_CURVE()
B_SPLINE_CURVE(2,(#51627,#51628,#51629),.UNSPECIFIED.,.F.,.F.)
B_SPLINE_CURVE_WITH_KNOTS((3,3),(0.367644516946555,0.373830527582529),
 .UNSPECIFIED.)
CURVE()
GEOMETRIC_REPRESENTATION_ITEM()
RATIONAL_B_SPLINE_CURVE((1.13426390111303,1.13389822901296,1.13348223894562))
REPRESENTATION_ITEM('')
);
#669=(
BOUNDED_CURVE()
B_SPLINE_CURVE(2,(#51633,#51634,#51635),.UNSPECIFIED.,.F.,.F.)
B_SPLINE_CURVE_WITH_KNOTS((3,3),(0.271548216895927,0.277734227531913),
 .UNSPECIFIED.)
CURVE()
GEOMETRIC_REPRESENTATION_ITEM()
RATIONAL_B_SPLINE_CURVE((1.13348223894624,1.13389822901359,1.13426390111366))
REPRESENTATION_ITEM('')
);
#670=(
BOUNDED_CURVE()
B_SPLINE_CURVE(2,(#51639,#51640,#51641),.UNSPECIFIED.,.F.,.F.)
B_SPLINE_CURVE_WITH_KNOTS((3,3),(0.367644516946557,0.373830527582527),
 .UNSPECIFIED.)
CURVE()
GEOMETRIC_REPRESENTATION_ITEM()
RATIONAL_B_SPLINE_CURVE((1.1342639011131,1.13389822901303,1.13348223894569))
REPRESENTATION_ITEM('')
);
#671=(
BOUNDED_CURVE()
B_SPLINE_CURVE(2,(#51645,#51646,#51647),.UNSPECIFIED.,.F.,.F.)
B_SPLINE_CURVE_WITH_KNOTS((3,3),(0.27154821689592,0.277734227531904),
 .UNSPECIFIED.)
CURVE()
GEOMETRIC_REPRESENTATION_ITEM()
RATIONAL_B_SPLINE_CURVE((1.13348223894613,1.13389822901348,1.13426390111355))
REPRESENTATION_ITEM('')
);
#672=(
BOUNDED_CURVE()
B_SPLINE_CURVE(2,(#51651,#51652,#51653),.UNSPECIFIED.,.F.,.F.)
B_SPLINE_CURVE_WITH_KNOTS((3,3),(0.367644516946566,0.373830527582538),
 .UNSPECIFIED.)
CURVE()
GEOMETRIC_REPRESENTATION_ITEM()
RATIONAL_B_SPLINE_CURVE((1.13426390111301,1.13389822901294,1.1334822389456))
REPRESENTATION_ITEM('')
);
#673=(
BOUNDED_CURVE()
B_SPLINE_CURVE(2,(#51657,#51658,#51659),.UNSPECIFIED.,.F.,.F.)
B_SPLINE_CURVE_WITH_KNOTS((3,3),(0.27154821689592,0.277734227531902),
 .UNSPECIFIED.)
CURVE()
GEOMETRIC_REPRESENTATION_ITEM()
RATIONAL_B_SPLINE_CURVE((1.1334822389461,1.13389822901344,1.13426390111352))
REPRESENTATION_ITEM('')
);
#674=(
BOUNDED_CURVE()
B_SPLINE_CURVE(2,(#51663,#51664,#51665),.UNSPECIFIED.,.F.,.F.)
B_SPLINE_CURVE_WITH_KNOTS((3,3),(0.367644516946558,0.373830527582536),
 .UNSPECIFIED.)
CURVE()
GEOMETRIC_REPRESENTATION_ITEM()
RATIONAL_B_SPLINE_CURVE((1.13426390111303,1.13389822901296,1.13348223894562))
REPRESENTATION_ITEM('')
);
#675=(
BOUNDED_CURVE()
B_SPLINE_CURVE(2,(#51669,#51670,#51671),.UNSPECIFIED.,.F.,.F.)
B_SPLINE_CURVE_WITH_KNOTS((3,3),(0.271548216895916,0.277734227531903),
 .UNSPECIFIED.)
CURVE()
GEOMETRIC_REPRESENTATION_ITEM()
RATIONAL_B_SPLINE_CURVE((1.13348223894608,1.13389822901343,1.1342639011135))
REPRESENTATION_ITEM('')
);
#676=(
BOUNDED_CURVE()
B_SPLINE_CURVE(2,(#51675,#51676,#51677),.UNSPECIFIED.,.F.,.F.)
B_SPLINE_CURVE_WITH_KNOTS((3,3),(0.367644516946558,0.373830527582538),
 .UNSPECIFIED.)
CURVE()
GEOMETRIC_REPRESENTATION_ITEM()
RATIONAL_B_SPLINE_CURVE((1.13426390111299,1.13389822901292,1.13348223894558))
REPRESENTATION_ITEM('')
);
#677=(
BOUNDED_CURVE()
B_SPLINE_CURVE(2,(#51681,#51682,#51683),.UNSPECIFIED.,.F.,.F.)
B_SPLINE_CURVE_WITH_KNOTS((3,3),(0.271548216895918,0.277734227531905),
 .UNSPECIFIED.)
CURVE()
GEOMETRIC_REPRESENTATION_ITEM()
RATIONAL_B_SPLINE_CURVE((1.13348223894618,1.13389822901353,1.1342639011136))
REPRESENTATION_ITEM('')
);
#678=(
BOUNDED_CURVE()
B_SPLINE_CURVE(2,(#51687,#51688,#51689),.UNSPECIFIED.,.F.,.F.)
B_SPLINE_CURVE_WITH_KNOTS((3,3),(0.367644516946549,0.373830527582523),
 .UNSPECIFIED.)
CURVE()
GEOMETRIC_REPRESENTATION_ITEM()
RATIONAL_B_SPLINE_CURVE((1.13426390111313,1.13389822901306,1.13348223894572))
REPRESENTATION_ITEM('')
);
#679=(
BOUNDED_CURVE()
B_SPLINE_CURVE(2,(#51693,#51694,#51695),.UNSPECIFIED.,.F.,.F.)
B_SPLINE_CURVE_WITH_KNOTS((3,3),(0.271548216895918,0.277734227531904),
 .UNSPECIFIED.)
CURVE()
GEOMETRIC_REPRESENTATION_ITEM()
RATIONAL_B_SPLINE_CURVE((1.13348223894607,1.13389822901342,1.1342639011135))
REPRESENTATION_ITEM('')
);
#680=(
BOUNDED_CURVE()
B_SPLINE_CURVE(2,(#51699,#51700,#51701),.UNSPECIFIED.,.F.,.F.)
B_SPLINE_CURVE_WITH_KNOTS((3,3),(0.367644516946553,0.373830527582525),
 .UNSPECIFIED.)
CURVE()
GEOMETRIC_REPRESENTATION_ITEM()
RATIONAL_B_SPLINE_CURVE((1.13426390111306,1.133898229013,1.13348223894565))
REPRESENTATION_ITEM('')
);
#681=(
BOUNDED_CURVE()
B_SPLINE_CURVE(2,(#51705,#51706,#51707),.UNSPECIFIED.,.F.,.F.)
B_SPLINE_CURVE_WITH_KNOTS((3,3),(0.271548216895918,0.277734227531897),
 .UNSPECIFIED.)
CURVE()
GEOMETRIC_REPRESENTATION_ITEM()
RATIONAL_B_SPLINE_CURVE((1.13348223894613,1.13389822901348,1.13426390111355))
REPRESENTATION_ITEM('')
);
#682=(
BOUNDED_CURVE()
B_SPLINE_CURVE(2,(#51711,#51712,#51713),.UNSPECIFIED.,.F.,.F.)
B_SPLINE_CURVE_WITH_KNOTS((3,3),(0.367644516946551,0.373830527582524),
 .UNSPECIFIED.)
CURVE()
GEOMETRIC_REPRESENTATION_ITEM()
RATIONAL_B_SPLINE_CURVE((1.13426390111309,1.13389822901302,1.13348223894568))
REPRESENTATION_ITEM('')
);
#683=(
BOUNDED_CURVE()
B_SPLINE_CURVE(2,(#51717,#51718,#51719),.UNSPECIFIED.,.F.,.F.)
B_SPLINE_CURVE_WITH_KNOTS((3,3),(0.271548216895914,0.2777342275319),
 .UNSPECIFIED.)
CURVE()
GEOMETRIC_REPRESENTATION_ITEM()
RATIONAL_B_SPLINE_CURVE((1.13348223894608,1.13389822901343,1.13426390111351))
REPRESENTATION_ITEM('')
);
#684=(
BOUNDED_CURVE()
B_SPLINE_CURVE(2,(#51723,#51724,#51725),.UNSPECIFIED.,.F.,.F.)
B_SPLINE_CURVE_WITH_KNOTS((3,3),(0.367644516946559,0.373830527582536),
 .UNSPECIFIED.)
CURVE()
GEOMETRIC_REPRESENTATION_ITEM()
RATIONAL_B_SPLINE_CURVE((1.13426390111305,1.13389822901298,1.13348223894564))
REPRESENTATION_ITEM('')
);
#685=(
BOUNDED_CURVE()
B_SPLINE_CURVE(2,(#51729,#51730,#51731),.UNSPECIFIED.,.F.,.F.)
B_SPLINE_CURVE_WITH_KNOTS((3,3),(0.27154821689591,0.277734227531898),
 .UNSPECIFIED.)
CURVE()
GEOMETRIC_REPRESENTATION_ITEM()
RATIONAL_B_SPLINE_CURVE((1.13348223894607,1.13389822901342,1.1342639011135))
REPRESENTATION_ITEM('')
);
#686=(
BOUNDED_CURVE()
B_SPLINE_CURVE(2,(#51735,#51736,#51737),.UNSPECIFIED.,.F.,.F.)
B_SPLINE_CURVE_WITH_KNOTS((3,3),(0.367644516946559,0.373830527582532),
 .UNSPECIFIED.)
CURVE()
GEOMETRIC_REPRESENTATION_ITEM()
RATIONAL_B_SPLINE_CURVE((1.13426390111307,1.133898229013,1.13348223894566))
REPRESENTATION_ITEM('')
);
#687=(
BOUNDED_CURVE()
B_SPLINE_CURVE(2,(#51741,#51742,#51743),.UNSPECIFIED.,.F.,.F.)
B_SPLINE_CURVE_WITH_KNOTS((3,3),(0.271548216895924,0.277734227531905),
 .UNSPECIFIED.)
CURVE()
GEOMETRIC_REPRESENTATION_ITEM()
RATIONAL_B_SPLINE_CURVE((1.13348223894618,1.13389822901353,1.1342639011136))
REPRESENTATION_ITEM('')
);
#688=(
BOUNDED_CURVE()
B_SPLINE_CURVE(2,(#51747,#51748,#51749),.UNSPECIFIED.,.F.,.F.)
B_SPLINE_CURVE_WITH_KNOTS((3,3),(0.367644516946555,0.373830527582531),
 .UNSPECIFIED.)
CURVE()
GEOMETRIC_REPRESENTATION_ITEM()
RATIONAL_B_SPLINE_CURVE((1.134263901113,1.13389822901293,1.13348223894559))
REPRESENTATION_ITEM('')
);
#689=(
BOUNDED_CURVE()
B_SPLINE_CURVE(2,(#51753,#51754,#51755),.UNSPECIFIED.,.F.,.F.)
B_SPLINE_CURVE_WITH_KNOTS((3,3),(0.271548216895916,0.277734227531902),
 .UNSPECIFIED.)
CURVE()
GEOMETRIC_REPRESENTATION_ITEM()
RATIONAL_B_SPLINE_CURVE((1.13348223894612,1.13389822901347,1.13426390111355))
REPRESENTATION_ITEM('')
);
#690=(
BOUNDED_CURVE()
B_SPLINE_CURVE(2,(#51759,#51760,#51761),.UNSPECIFIED.,.F.,.F.)
B_SPLINE_CURVE_WITH_KNOTS((3,3),(0.36764451694656,0.373830527582534),
 .UNSPECIFIED.)
CURVE()
GEOMETRIC_REPRESENTATION_ITEM()
RATIONAL_B_SPLINE_CURVE((1.13426390111302,1.13389822901296,1.13348223894561))
REPRESENTATION_ITEM('')
);
#691=(
BOUNDED_CURVE()
B_SPLINE_CURVE(2,(#51765,#51766,#51767),.UNSPECIFIED.,.F.,.F.)
B_SPLINE_CURVE_WITH_KNOTS((3,3),(0.271548216895913,0.277734227531896),
 .UNSPECIFIED.)
CURVE()
GEOMETRIC_REPRESENTATION_ITEM()
RATIONAL_B_SPLINE_CURVE((1.13348223894608,1.13389822901343,1.1342639011135))
REPRESENTATION_ITEM('')
);
#692=(
BOUNDED_CURVE()
B_SPLINE_CURVE(2,(#51771,#51772,#51773),.UNSPECIFIED.,.F.,.F.)
B_SPLINE_CURVE_WITH_KNOTS((3,3),(0.367644516946558,0.373830527582535),
 .UNSPECIFIED.)
CURVE()
GEOMETRIC_REPRESENTATION_ITEM()
RATIONAL_B_SPLINE_CURVE((1.13426390111305,1.13389822901298,1.13348223894563))
REPRESENTATION_ITEM('')
);
#693=(
BOUNDED_CURVE()
B_SPLINE_CURVE(2,(#51777,#51778,#51779),.UNSPECIFIED.,.F.,.F.)
B_SPLINE_CURVE_WITH_KNOTS((3,3),(0.271548216895911,0.277734227531902),
 .UNSPECIFIED.)
CURVE()
GEOMETRIC_REPRESENTATION_ITEM()
RATIONAL_B_SPLINE_CURVE((1.13348223894613,1.13389822901348,1.13426390111355))
REPRESENTATION_ITEM('')
);
#694=(
BOUNDED_CURVE()
B_SPLINE_CURVE(2,(#51783,#51784,#51785),.UNSPECIFIED.,.F.,.F.)
B_SPLINE_CURVE_WITH_KNOTS((3,3),(0.367644516946552,0.373830527582527),
 .UNSPECIFIED.)
CURVE()
GEOMETRIC_REPRESENTATION_ITEM()
RATIONAL_B_SPLINE_CURVE((1.13426390111308,1.13389822901301,1.13348223894567))
REPRESENTATION_ITEM('')
);
#695=(
BOUNDED_CURVE()
B_SPLINE_CURVE(2,(#51789,#51790,#51791),.UNSPECIFIED.,.F.,.F.)
B_SPLINE_CURVE_WITH_KNOTS((3,3),(0.271548216895913,0.277734227531896),
 .UNSPECIFIED.)
CURVE()
GEOMETRIC_REPRESENTATION_ITEM()
RATIONAL_B_SPLINE_CURVE((1.13348223894609,1.13389822901344,1.13426390111351))
REPRESENTATION_ITEM('')
);
#696=(
BOUNDED_CURVE()
B_SPLINE_CURVE(2,(#51795,#51796,#51797),.UNSPECIFIED.,.F.,.F.)
B_SPLINE_CURVE_WITH_KNOTS((3,3),(0.367644516946554,0.373830527582527),
 .UNSPECIFIED.)
CURVE()
GEOMETRIC_REPRESENTATION_ITEM()
RATIONAL_B_SPLINE_CURVE((1.13426390111307,1.13389822901301,1.13348223894566))
REPRESENTATION_ITEM('')
);
#697=(
BOUNDED_CURVE()
B_SPLINE_CURVE(2,(#51801,#51802,#51803),.UNSPECIFIED.,.F.,.F.)
B_SPLINE_CURVE_WITH_KNOTS((3,3),(0.271548216895912,0.277734227531901),
 .UNSPECIFIED.)
CURVE()
GEOMETRIC_REPRESENTATION_ITEM()
RATIONAL_B_SPLINE_CURVE((1.13348223894619,1.13389822901354,1.13426390111361))
REPRESENTATION_ITEM('')
);
#698=(
BOUNDED_CURVE()
B_SPLINE_CURVE(2,(#51807,#51808,#51809),.UNSPECIFIED.,.F.,.F.)
B_SPLINE_CURVE_WITH_KNOTS((3,3),(0.367644516946552,0.373830527582526),
 .UNSPECIFIED.)
CURVE()
GEOMETRIC_REPRESENTATION_ITEM()
RATIONAL_B_SPLINE_CURVE((1.13426390111306,1.13389822901299,1.13348223894565))
REPRESENTATION_ITEM('')
);
#699=(
BOUNDED_CURVE()
B_SPLINE_CURVE(2,(#51813,#51814,#51815),.UNSPECIFIED.,.F.,.F.)
B_SPLINE_CURVE_WITH_KNOTS((3,3),(0.271548216895908,0.277734227531896),
 .UNSPECIFIED.)
CURVE()
GEOMETRIC_REPRESENTATION_ITEM()
RATIONAL_B_SPLINE_CURVE((1.13348223894609,1.13389822901344,1.13426390111351))
REPRESENTATION_ITEM('')
);
#700=(
BOUNDED_CURVE()
B_SPLINE_CURVE(2,(#51819,#51820,#51821),.UNSPECIFIED.,.F.,.F.)
B_SPLINE_CURVE_WITH_KNOTS((3,3),(0.367644516946558,0.373830527582532),
 .UNSPECIFIED.)
CURVE()
GEOMETRIC_REPRESENTATION_ITEM()
RATIONAL_B_SPLINE_CURVE((1.13426390111305,1.13389822901298,1.13348223894564))
REPRESENTATION_ITEM('')
);
#701=(
BOUNDED_CURVE()
B_SPLINE_CURVE(2,(#51825,#51826,#51827),.UNSPECIFIED.,.F.,.F.)
B_SPLINE_CURVE_WITH_KNOTS((3,3),(0.271548216895918,0.27773422753191),
 .UNSPECIFIED.)
CURVE()
GEOMETRIC_REPRESENTATION_ITEM()
RATIONAL_B_SPLINE_CURVE((1.1334822389462,1.13389822901355,1.13426390111362))
REPRESENTATION_ITEM('')
);
#702=(
BOUNDED_CURVE()
B_SPLINE_CURVE(2,(#51831,#51832,#51833),.UNSPECIFIED.,.F.,.F.)
B_SPLINE_CURVE_WITH_KNOTS((3,3),(0.367644516946559,0.373830527582532),
 .UNSPECIFIED.)
CURVE()
GEOMETRIC_REPRESENTATION_ITEM()
RATIONAL_B_SPLINE_CURVE((1.13426390111305,1.13389822901299,1.13348223894564))
REPRESENTATION_ITEM('')
);
#703=(
BOUNDED_CURVE()
B_SPLINE_CURVE(2,(#51837,#51838,#51839),.UNSPECIFIED.,.F.,.F.)
B_SPLINE_CURVE_WITH_KNOTS((3,3),(0.271548216895917,0.277734227531899),
 .UNSPECIFIED.)
CURVE()
GEOMETRIC_REPRESENTATION_ITEM()
RATIONAL_B_SPLINE_CURVE((1.13348223894612,1.13389822901347,1.13426390111355))
REPRESENTATION_ITEM('')
);
#704=(
BOUNDED_CURVE()
B_SPLINE_CURVE(2,(#51843,#51844,#51845),.UNSPECIFIED.,.F.,.F.)
B_SPLINE_CURVE_WITH_KNOTS((3,3),(0.367644516946562,0.373830527582533),
 .UNSPECIFIED.)
CURVE()
GEOMETRIC_REPRESENTATION_ITEM()
RATIONAL_B_SPLINE_CURVE((1.13426390111306,1.13389822901299,1.13348223894564))
REPRESENTATION_ITEM('')
);
#705=(
BOUNDED_CURVE()
B_SPLINE_CURVE(2,(#51849,#51850,#51851),.UNSPECIFIED.,.F.,.F.)
B_SPLINE_CURVE_WITH_KNOTS((3,3),(0.271548216895905,0.277734227531891),
 .UNSPECIFIED.)
CURVE()
GEOMETRIC_REPRESENTATION_ITEM()
RATIONAL_B_SPLINE_CURVE((1.13348223894609,1.13389822901344,1.13426390111351))
REPRESENTATION_ITEM('')
);
#706=(
BOUNDED_CURVE()
B_SPLINE_CURVE(2,(#51855,#51856,#51857),.UNSPECIFIED.,.F.,.F.)
B_SPLINE_CURVE_WITH_KNOTS((3,3),(0.367644516946557,0.373830527582533),
 .UNSPECIFIED.)
CURVE()
GEOMETRIC_REPRESENTATION_ITEM()
RATIONAL_B_SPLINE_CURVE((1.13426390111305,1.13389822901299,1.13348223894564))
REPRESENTATION_ITEM('')
);
#707=(
BOUNDED_CURVE()
B_SPLINE_CURVE(2,(#51861,#51862,#51863),.UNSPECIFIED.,.F.,.F.)
B_SPLINE_CURVE_WITH_KNOTS((3,3),(0.271548216895918,0.277734227531906),
 .UNSPECIFIED.)
CURVE()
GEOMETRIC_REPRESENTATION_ITEM()
RATIONAL_B_SPLINE_CURVE((1.13348223894616,1.13389822901351,1.13426390111358))
REPRESENTATION_ITEM('')
);
#708=(
BOUNDED_CURVE()
B_SPLINE_CURVE(2,(#51885,#51886,#51887),.UNSPECIFIED.,.F.,.F.)
B_SPLINE_CURVE_WITH_KNOTS((3,3),(0.376641898803529,0.382940702095941),
 .UNSPECIFIED.)
CURVE()
GEOMETRIC_REPRESENTATION_ITEM()
RATIONAL_B_SPLINE_CURVE((1.12071541658433,1.1202411994692,1.11971735964528))
REPRESENTATION_ITEM('')
);
#709=(
BOUNDED_CURVE()
B_SPLINE_CURVE(2,(#51891,#51892,#51893),.UNSPECIFIED.,.F.,.F.)
B_SPLINE_CURVE_WITH_KNOTS((3,3),(0.249954652430657,0.25625345571807),
 .UNSPECIFIED.)
CURVE()
GEOMETRIC_REPRESENTATION_ITEM()
RATIONAL_B_SPLINE_CURVE((1.1197173596462,1.12024119946966,1.12071541658442))
REPRESENTATION_ITEM('')
);
#710=(
BOUNDED_CURVE()
B_SPLINE_CURVE(2,(#51897,#51898,#51899),.UNSPECIFIED.,.F.,.F.)
B_SPLINE_CURVE_WITH_KNOTS((3,3),(0.376641898803524,0.382940702095934),
 .UNSPECIFIED.)
CURVE()
GEOMETRIC_REPRESENTATION_ITEM()
RATIONAL_B_SPLINE_CURVE((1.12071541658448,1.12024119946934,1.11971735964542))
REPRESENTATION_ITEM('')
);
#711=(
BOUNDED_CURVE()
B_SPLINE_CURVE(2,(#51903,#51904,#51905),.UNSPECIFIED.,.F.,.F.)
B_SPLINE_CURVE_WITH_KNOTS((3,3),(0.249954652430655,0.256253455718069),
 .UNSPECIFIED.)
CURVE()
GEOMETRIC_REPRESENTATION_ITEM()
RATIONAL_B_SPLINE_CURVE((1.11971735964613,1.1202411994696,1.12071541658435))
REPRESENTATION_ITEM('')
);
#712=(
BOUNDED_CURVE()
B_SPLINE_CURVE(2,(#51909,#51910,#51911),.UNSPECIFIED.,.F.,.F.)
B_SPLINE_CURVE_WITH_KNOTS((3,3),(0.376641898803532,0.382940702095944),
 .UNSPECIFIED.)
CURVE()
GEOMETRIC_REPRESENTATION_ITEM()
RATIONAL_B_SPLINE_CURVE((1.12071541658434,1.12024119946921,1.11971735964529))
REPRESENTATION_ITEM('')
);
#713=(
BOUNDED_CURVE()
B_SPLINE_CURVE(2,(#51915,#51916,#51917),.UNSPECIFIED.,.F.,.F.)
B_SPLINE_CURVE_WITH_KNOTS((3,3),(0.249954652430645,0.256253455718059),
 .UNSPECIFIED.)
CURVE()
GEOMETRIC_REPRESENTATION_ITEM()
RATIONAL_B_SPLINE_CURVE((1.11971735964598,1.12024119946945,1.1207154165842))
REPRESENTATION_ITEM('')
);
#714=(
BOUNDED_CURVE()
B_SPLINE_CURVE(2,(#51921,#51922,#51923),.UNSPECIFIED.,.F.,.F.)
B_SPLINE_CURVE_WITH_KNOTS((3,3),(0.376641898803521,0.382940702095933),
 .UNSPECIFIED.)
CURVE()
GEOMETRIC_REPRESENTATION_ITEM()
RATIONAL_B_SPLINE_CURVE((1.1207154165845,1.12024119946936,1.11971735964544))
REPRESENTATION_ITEM('')
);
#715=(
BOUNDED_CURVE()
B_SPLINE_CURVE(2,(#51927,#51928,#51929),.UNSPECIFIED.,.F.,.F.)
B_SPLINE_CURVE_WITH_KNOTS((3,3),(0.249954652430661,0.256253455718076),
 .UNSPECIFIED.)
CURVE()
GEOMETRIC_REPRESENTATION_ITEM()
RATIONAL_B_SPLINE_CURVE((1.1197173596463,1.12024119946977,1.12071541658453))
REPRESENTATION_ITEM('')
);
#716=(
BOUNDED_CURVE()
B_SPLINE_CURVE(2,(#51933,#51934,#51935),.UNSPECIFIED.,.F.,.F.)
B_SPLINE_CURVE_WITH_KNOTS((3,3),(0.376641898803535,0.382940702095943),
 .UNSPECIFIED.)
CURVE()
GEOMETRIC_REPRESENTATION_ITEM()
RATIONAL_B_SPLINE_CURVE((1.12071541658437,1.12024119946923,1.11971735964532))
REPRESENTATION_ITEM('')
);
#717=(
BOUNDED_CURVE()
B_SPLINE_CURVE(2,(#51939,#51940,#51941),.UNSPECIFIED.,.F.,.F.)
B_SPLINE_CURVE_WITH_KNOTS((3,3),(0.249954652430645,0.256253455718058),
 .UNSPECIFIED.)
CURVE()
GEOMETRIC_REPRESENTATION_ITEM()
RATIONAL_B_SPLINE_CURVE((1.11971735964609,1.12024119946955,1.12071541658431))
REPRESENTATION_ITEM('')
);
#718=(
BOUNDED_CURVE()
B_SPLINE_CURVE(2,(#51945,#51946,#51947),.UNSPECIFIED.,.F.,.F.)
B_SPLINE_CURVE_WITH_KNOTS((3,3),(0.376641898803531,0.382940702095942),
 .UNSPECIFIED.)
CURVE()
GEOMETRIC_REPRESENTATION_ITEM()
RATIONAL_B_SPLINE_CURVE((1.12071541658437,1.12024119946923,1.11971735964532))
REPRESENTATION_ITEM('')
);
#719=(
BOUNDED_CURVE()
B_SPLINE_CURVE(2,(#51951,#51952,#51953),.UNSPECIFIED.,.F.,.F.)
B_SPLINE_CURVE_WITH_KNOTS((3,3),(0.249954652430646,0.256253455718059),
 .UNSPECIFIED.)
CURVE()
GEOMETRIC_REPRESENTATION_ITEM()
RATIONAL_B_SPLINE_CURVE((1.11971735964605,1.12024119946951,1.12071541658427))
REPRESENTATION_ITEM('')
);
#720=(
BOUNDED_CURVE()
B_SPLINE_CURVE(2,(#51957,#51958,#51959),.UNSPECIFIED.,.F.,.F.)
B_SPLINE_CURVE_WITH_KNOTS((3,3),(0.376641898803521,0.382940702095931),
 .UNSPECIFIED.)
CURVE()
GEOMETRIC_REPRESENTATION_ITEM()
RATIONAL_B_SPLINE_CURVE((1.12071541658451,1.12024119946938,1.11971735964546))
REPRESENTATION_ITEM('')
);
#721=(
BOUNDED_CURVE()
B_SPLINE_CURVE(2,(#51963,#51964,#51965),.UNSPECIFIED.,.F.,.F.)
B_SPLINE_CURVE_WITH_KNOTS((3,3),(0.249954652430639,0.256253455718052),
 .UNSPECIFIED.)
CURVE()
GEOMETRIC_REPRESENTATION_ITEM()
RATIONAL_B_SPLINE_CURVE((1.11971735964601,1.12024119946948,1.12071541658424))
REPRESENTATION_ITEM('')
);
#722=(
BOUNDED_CURVE()
B_SPLINE_CURVE(2,(#51969,#51970,#51971),.UNSPECIFIED.,.F.,.F.)
B_SPLINE_CURVE_WITH_KNOTS((3,3),(0.376641898803533,0.382940702095945),
 .UNSPECIFIED.)
CURVE()
GEOMETRIC_REPRESENTATION_ITEM()
RATIONAL_B_SPLINE_CURVE((1.12071541658434,1.1202411994692,1.11971735964528))
REPRESENTATION_ITEM('')
);
#723=(
BOUNDED_CURVE()
B_SPLINE_CURVE(2,(#51975,#51976,#51977),.UNSPECIFIED.,.F.,.F.)
B_SPLINE_CURVE_WITH_KNOTS((3,3),(0.249954652430659,0.256253455718072),
 .UNSPECIFIED.)
CURVE()
GEOMETRIC_REPRESENTATION_ITEM()
RATIONAL_B_SPLINE_CURVE((1.11971735964624,1.12024119946971,1.12071541658447))
REPRESENTATION_ITEM('')
);
#724=(
BOUNDED_CURVE()
B_SPLINE_CURVE(2,(#51981,#51982,#51983),.UNSPECIFIED.,.F.,.F.)
B_SPLINE_CURVE_WITH_KNOTS((3,3),(0.376641898803529,0.382940702095948),
 .UNSPECIFIED.)
CURVE()
GEOMETRIC_REPRESENTATION_ITEM()
RATIONAL_B_SPLINE_CURVE((1.12071541658446,1.12024119946932,1.1197173596454))
REPRESENTATION_ITEM('')
);
#725=(
BOUNDED_CURVE()
B_SPLINE_CURVE(2,(#51987,#51988,#51989),.UNSPECIFIED.,.F.,.F.)
B_SPLINE_CURVE_WITH_KNOTS((3,3),(0.249954652430643,0.256253455718057),
 .UNSPECIFIED.)
CURVE()
GEOMETRIC_REPRESENTATION_ITEM()
RATIONAL_B_SPLINE_CURVE((1.11971735964609,1.12024119946956,1.12071541658432))
REPRESENTATION_ITEM('')
);
#726=(
BOUNDED_CURVE()
B_SPLINE_CURVE(2,(#51993,#51994,#51995),.UNSPECIFIED.,.F.,.F.)
B_SPLINE_CURVE_WITH_KNOTS((3,3),(0.376641898803523,0.382940702095941),
 .UNSPECIFIED.)
CURVE()
GEOMETRIC_REPRESENTATION_ITEM()
RATIONAL_B_SPLINE_CURVE((1.12071541658451,1.12024119946937,1.11971735964545))
REPRESENTATION_ITEM('')
);
#727=(
BOUNDED_CURVE()
B_SPLINE_CURVE(2,(#51999,#52000,#52001),.UNSPECIFIED.,.F.,.F.)
B_SPLINE_CURVE_WITH_KNOTS((3,3),(0.249954652430644,0.256253455718058),
 .UNSPECIFIED.)
CURVE()
GEOMETRIC_REPRESENTATION_ITEM()
RATIONAL_B_SPLINE_CURVE((1.11971735964615,1.12024119946961,1.12071541658437))
REPRESENTATION_ITEM('')
);
#728=(
BOUNDED_CURVE()
B_SPLINE_CURVE(2,(#52005,#52006,#52007),.UNSPECIFIED.,.F.,.F.)
B_SPLINE_CURVE_WITH_KNOTS((3,3),(0.376641898803536,0.382940702095946),
 .UNSPECIFIED.)
CURVE()
GEOMETRIC_REPRESENTATION_ITEM()
RATIONAL_B_SPLINE_CURVE((1.12071541658451,1.12024119946938,1.11971735964546))
REPRESENTATION_ITEM('')
);
#729=(
BOUNDED_CURVE()
B_SPLINE_CURVE(2,(#52011,#52012,#52013),.UNSPECIFIED.,.F.,.F.)
B_SPLINE_CURVE_WITH_KNOTS((3,3),(0.24995465243065,0.256253455718062),
 .UNSPECIFIED.)
CURVE()
GEOMETRIC_REPRESENTATION_ITEM()
RATIONAL_B_SPLINE_CURVE((1.11971735964599,1.12024119946946,1.12071541658421))
REPRESENTATION_ITEM('')
);
#730=(
BOUNDED_CURVE()
B_SPLINE_CURVE(2,(#52017,#52018,#52019),.UNSPECIFIED.,.F.,.F.)
B_SPLINE_CURVE_WITH_KNOTS((3,3),(0.376641898803523,0.38294070209593),
 .UNSPECIFIED.)
CURVE()
GEOMETRIC_REPRESENTATION_ITEM()
RATIONAL_B_SPLINE_CURVE((1.1207154165845,1.12024119946936,1.11971735964544))
REPRESENTATION_ITEM('')
);
#731=(
BOUNDED_CURVE()
B_SPLINE_CURVE(2,(#52023,#52024,#52025),.UNSPECIFIED.,.F.,.F.)
B_SPLINE_CURVE_WITH_KNOTS((3,3),(0.249954652430653,0.256253455718064),
 .UNSPECIFIED.)
CURVE()
GEOMETRIC_REPRESENTATION_ITEM()
RATIONAL_B_SPLINE_CURVE((1.11971735964611,1.12024119946957,1.12071541658433))
REPRESENTATION_ITEM('')
);
#732=(
BOUNDED_CURVE()
B_SPLINE_CURVE(2,(#52029,#52030,#52031),.UNSPECIFIED.,.F.,.F.)
B_SPLINE_CURVE_WITH_KNOTS((3,3),(0.376641898803521,0.382940702095931),
 .UNSPECIFIED.)
CURVE()
GEOMETRIC_REPRESENTATION_ITEM()
RATIONAL_B_SPLINE_CURVE((1.12071541658461,1.12024119946947,1.11971735964555))
REPRESENTATION_ITEM('')
);
#733=(
BOUNDED_CURVE()
B_SPLINE_CURVE(2,(#52035,#52036,#52037),.UNSPECIFIED.,.F.,.F.)
B_SPLINE_CURVE_WITH_KNOTS((3,3),(0.249954652430661,0.256253455718072),
 .UNSPECIFIED.)
CURVE()
GEOMETRIC_REPRESENTATION_ITEM()
RATIONAL_B_SPLINE_CURVE((1.11971735964623,1.1202411994697,1.12071541658446))
REPRESENTATION_ITEM('')
);
#734=(
BOUNDED_CURVE()
B_SPLINE_CURVE(2,(#52041,#52042,#52043),.UNSPECIFIED.,.F.,.F.)
B_SPLINE_CURVE_WITH_KNOTS((3,3),(0.376641898803537,0.382940702095947),
 .UNSPECIFIED.)
CURVE()
GEOMETRIC_REPRESENTATION_ITEM()
RATIONAL_B_SPLINE_CURVE((1.1207154165845,1.12024119946936,1.11971735964544))
REPRESENTATION_ITEM('')
);
#735=(
BOUNDED_CURVE()
B_SPLINE_CURVE(2,(#52047,#52048,#52049),.UNSPECIFIED.,.F.,.F.)
B_SPLINE_CURVE_WITH_KNOTS((3,3),(0.249954652430645,0.256253455718056),
 .UNSPECIFIED.)
CURVE()
GEOMETRIC_REPRESENTATION_ITEM()
RATIONAL_B_SPLINE_CURVE((1.11971735964613,1.1202411994696,1.12071541658435))
REPRESENTATION_ITEM('')
);
#736=(
BOUNDED_CURVE()
B_SPLINE_CURVE(2,(#52053,#52054,#52055),.UNSPECIFIED.,.F.,.F.)
B_SPLINE_CURVE_WITH_KNOTS((3,3),(0.376641898803536,0.382940702095954),
 .UNSPECIFIED.)
CURVE()
GEOMETRIC_REPRESENTATION_ITEM()
RATIONAL_B_SPLINE_CURVE((1.12071541658435,1.12024119946922,1.1197173596453))
REPRESENTATION_ITEM('')
);
#737=(
BOUNDED_CURVE()
B_SPLINE_CURVE(2,(#52059,#52060,#52061),.UNSPECIFIED.,.F.,.F.)
B_SPLINE_CURVE_WITH_KNOTS((3,3),(0.249954652430663,0.256253455718072),
 .UNSPECIFIED.)
CURVE()
GEOMETRIC_REPRESENTATION_ITEM()
RATIONAL_B_SPLINE_CURVE((1.11971735964633,1.1202411994698,1.12071541658456))
REPRESENTATION_ITEM('')
);
#738=(
BOUNDED_CURVE()
B_SPLINE_CURVE(2,(#52065,#52066,#52067),.UNSPECIFIED.,.F.,.F.)
B_SPLINE_CURVE_WITH_KNOTS((3,3),(0.376641898803512,0.382940702095922),
 .UNSPECIFIED.)
CURVE()
GEOMETRIC_REPRESENTATION_ITEM()
RATIONAL_B_SPLINE_CURVE((1.12071541658461,1.12024119946947,1.11971735964555))
REPRESENTATION_ITEM('')
);
#739=(
BOUNDED_CURVE()
B_SPLINE_CURVE(2,(#52071,#52072,#52073),.UNSPECIFIED.,.F.,.F.)
B_SPLINE_CURVE_WITH_KNOTS((3,3),(0.249954652430648,0.256253455718062),
 .UNSPECIFIED.)
CURVE()
GEOMETRIC_REPRESENTATION_ITEM()
RATIONAL_B_SPLINE_CURVE((1.11971735964605,1.12024119946951,1.12071541658427))
REPRESENTATION_ITEM('')
);
#740=(
BOUNDED_CURVE()
B_SPLINE_CURVE(2,(#52077,#52078,#52079),.UNSPECIFIED.,.F.,.F.)
B_SPLINE_CURVE_WITH_KNOTS((3,3),(0.376641898803527,0.382940702095944),
 .UNSPECIFIED.)
CURVE()
GEOMETRIC_REPRESENTATION_ITEM()
RATIONAL_B_SPLINE_CURVE((1.12071541658444,1.12024119946931,1.11971735964539))
REPRESENTATION_ITEM('')
);
#741=(
BOUNDED_CURVE()
B_SPLINE_CURVE(2,(#52083,#52084,#52085),.UNSPECIFIED.,.F.,.F.)
B_SPLINE_CURVE_WITH_KNOTS((3,3),(0.24995465243065,0.256253455718066),
 .UNSPECIFIED.)
CURVE()
GEOMETRIC_REPRESENTATION_ITEM()
RATIONAL_B_SPLINE_CURVE((1.11971735964612,1.12024119946958,1.12071541658434))
REPRESENTATION_ITEM('')
);
#742=(
BOUNDED_CURVE()
B_SPLINE_CURVE(2,(#52089,#52090,#52091),.UNSPECIFIED.,.F.,.F.)
B_SPLINE_CURVE_WITH_KNOTS((3,3),(0.37664189880352,0.382940702095936),
 .UNSPECIFIED.)
CURVE()
GEOMETRIC_REPRESENTATION_ITEM()
RATIONAL_B_SPLINE_CURVE((1.12071541658452,1.12024119946938,1.11971735964546))
REPRESENTATION_ITEM('')
);
#743=(
BOUNDED_CURVE()
B_SPLINE_CURVE(2,(#52095,#52096,#52097),.UNSPECIFIED.,.F.,.F.)
B_SPLINE_CURVE_WITH_KNOTS((3,3),(0.249954652430664,0.25625345571808),
 .UNSPECIFIED.)
CURVE()
GEOMETRIC_REPRESENTATION_ITEM()
RATIONAL_B_SPLINE_CURVE((1.11971735964628,1.12024119946975,1.12071541658451))
REPRESENTATION_ITEM('')
);
#744=(
BOUNDED_CURVE()
B_SPLINE_CURVE(2,(#52101,#52102,#52103),.UNSPECIFIED.,.F.,.F.)
B_SPLINE_CURVE_WITH_KNOTS((3,3),(0.376641898803518,0.382940702095937),
 .UNSPECIFIED.)
CURVE()
GEOMETRIC_REPRESENTATION_ITEM()
RATIONAL_B_SPLINE_CURVE((1.12071541658454,1.12024119946941,1.11971735964549))
REPRESENTATION_ITEM('')
);
#745=(
BOUNDED_CURVE()
B_SPLINE_CURVE(2,(#52107,#52108,#52109),.UNSPECIFIED.,.F.,.F.)
B_SPLINE_CURVE_WITH_KNOTS((3,3),(0.249954652430639,0.256253455718056),
 .UNSPECIFIED.)
CURVE()
GEOMETRIC_REPRESENTATION_ITEM()
RATIONAL_B_SPLINE_CURVE((1.11971735964609,1.12024119946956,1.12071541658432))
REPRESENTATION_ITEM('')
);
#746=(
BOUNDED_CURVE()
B_SPLINE_CURVE(2,(#52113,#52114,#52115),.UNSPECIFIED.,.F.,.F.)
B_SPLINE_CURVE_WITH_KNOTS((3,3),(0.376641898803522,0.382940702095936),
 .UNSPECIFIED.)
CURVE()
GEOMETRIC_REPRESENTATION_ITEM()
RATIONAL_B_SPLINE_CURVE((1.12071541658447,1.12024119946934,1.11971735964542))
REPRESENTATION_ITEM('')
);
#747=(
BOUNDED_CURVE()
B_SPLINE_CURVE(2,(#52119,#52120,#52121),.UNSPECIFIED.,.F.,.F.)
B_SPLINE_CURVE_WITH_KNOTS((3,3),(0.249954652430657,0.256253455718066),
 .UNSPECIFIED.)
CURVE()
GEOMETRIC_REPRESENTATION_ITEM()
RATIONAL_B_SPLINE_CURVE((1.11971735964622,1.12024119946968,1.12071541658444))
REPRESENTATION_ITEM('')
);
#748=(
BOUNDED_CURVE()
B_SPLINE_CURVE(2,(#52125,#52126,#52127),.UNSPECIFIED.,.F.,.F.)
B_SPLINE_CURVE_WITH_KNOTS((3,3),(0.376641898803533,0.38294070209594),
 .UNSPECIFIED.)
CURVE()
GEOMETRIC_REPRESENTATION_ITEM()
RATIONAL_B_SPLINE_CURVE((1.12071541658433,1.1202411994692,1.11971735964528))
REPRESENTATION_ITEM('')
);
#749=(
BOUNDED_CURVE()
B_SPLINE_CURVE(2,(#52131,#52132,#52133),.UNSPECIFIED.,.F.,.F.)
B_SPLINE_CURVE_WITH_KNOTS((3,3),(0.249954652430642,0.256253455718055),
 .UNSPECIFIED.)
CURVE()
GEOMETRIC_REPRESENTATION_ITEM()
RATIONAL_B_SPLINE_CURVE((1.11971735964602,1.12024119946948,1.12071541658424))
REPRESENTATION_ITEM('')
);
#750=(
BOUNDED_CURVE()
B_SPLINE_CURVE(2,(#52137,#52138,#52139),.UNSPECIFIED.,.F.,.F.)
B_SPLINE_CURVE_WITH_KNOTS((3,3),(0.376641898803547,0.382940702095962),
 .UNSPECIFIED.)
CURVE()
GEOMETRIC_REPRESENTATION_ITEM()
RATIONAL_B_SPLINE_CURVE((1.12071541658418,1.12024119946904,1.11971735964512))
REPRESENTATION_ITEM('')
);
#751=(
BOUNDED_CURVE()
B_SPLINE_CURVE(2,(#52143,#52144,#52145),.UNSPECIFIED.,.F.,.F.)
B_SPLINE_CURVE_WITH_KNOTS((3,3),(0.249954652430658,0.256253455718078),
 .UNSPECIFIED.)
CURVE()
GEOMETRIC_REPRESENTATION_ITEM()
RATIONAL_B_SPLINE_CURVE((1.1197173596463,1.12024119946977,1.12071541658453))
REPRESENTATION_ITEM('')
);
#752=(
BOUNDED_CURVE()
B_SPLINE_CURVE(2,(#52149,#52150,#52151),.UNSPECIFIED.,.F.,.F.)
B_SPLINE_CURVE_WITH_KNOTS((3,3),(0.376641898803522,0.382940702095938),
 .UNSPECIFIED.)
CURVE()
GEOMETRIC_REPRESENTATION_ITEM()
RATIONAL_B_SPLINE_CURVE((1.12071541658451,1.12024119946937,1.11971735964545))
REPRESENTATION_ITEM('')
);
#753=(
BOUNDED_CURVE()
B_SPLINE_CURVE(2,(#52155,#52156,#52157),.UNSPECIFIED.,.F.,.F.)
B_SPLINE_CURVE_WITH_KNOTS((3,3),(0.249954652430655,0.25625345571807),
 .UNSPECIFIED.)
CURVE()
GEOMETRIC_REPRESENTATION_ITEM()
RATIONAL_B_SPLINE_CURVE((1.11971735964625,1.12024119946971,1.12071541658447))
REPRESENTATION_ITEM('')
);
#754=(
BOUNDED_CURVE()
B_SPLINE_CURVE(2,(#52161,#52162,#52163),.UNSPECIFIED.,.F.,.F.)
B_SPLINE_CURVE_WITH_KNOTS((3,3),(0.376641898803531,0.382940702095945),
 .UNSPECIFIED.)
CURVE()
GEOMETRIC_REPRESENTATION_ITEM()
RATIONAL_B_SPLINE_CURVE((1.12071541658432,1.12024119946919,1.11971735964527))
REPRESENTATION_ITEM('')
);
#755=(
BOUNDED_CURVE()
B_SPLINE_CURVE(2,(#52167,#52168,#52169),.UNSPECIFIED.,.F.,.F.)
B_SPLINE_CURVE_WITH_KNOTS((3,3),(0.249954652430637,0.256253455718055),
 .UNSPECIFIED.)
CURVE()
GEOMETRIC_REPRESENTATION_ITEM()
RATIONAL_B_SPLINE_CURVE((1.11971735964599,1.12024119946945,1.12071541658421))
REPRESENTATION_ITEM('')
);
#756=(
BOUNDED_CURVE()
B_SPLINE_CURVE(2,(#52173,#52174,#52175),.UNSPECIFIED.,.F.,.F.)
B_SPLINE_CURVE_WITH_KNOTS((3,3),(0.376641898803544,0.382940702095957),
 .UNSPECIFIED.)
CURVE()
GEOMETRIC_REPRESENTATION_ITEM()
RATIONAL_B_SPLINE_CURVE((1.12071541658422,1.12024119946908,1.11971735964516))
REPRESENTATION_ITEM('')
);
#757=(
BOUNDED_CURVE()
B_SPLINE_CURVE(2,(#52179,#52180,#52181),.UNSPECIFIED.,.F.,.F.)
B_SPLINE_CURVE_WITH_KNOTS((3,3),(0.249954652430653,0.256253455718062),
 .UNSPECIFIED.)
CURVE()
GEOMETRIC_REPRESENTATION_ITEM()
RATIONAL_B_SPLINE_CURVE((1.11971735964616,1.12024119946962,1.12071541658438))
REPRESENTATION_ITEM('')
);
#758=(
BOUNDED_CURVE()
B_SPLINE_CURVE(2,(#52185,#52186,#52187),.UNSPECIFIED.,.F.,.F.)
B_SPLINE_CURVE_WITH_KNOTS((3,3),(0.376641898803539,0.38294070209595),
 .UNSPECIFIED.)
CURVE()
GEOMETRIC_REPRESENTATION_ITEM()
RATIONAL_B_SPLINE_CURVE((1.12071541658449,1.12024119946935,1.11971735964543))
REPRESENTATION_ITEM('')
);
#759=(
BOUNDED_CURVE()
B_SPLINE_CURVE(2,(#52191,#52192,#52193),.UNSPECIFIED.,.F.,.F.)
B_SPLINE_CURVE_WITH_KNOTS((3,3),(0.249954652430653,0.256253455718071),
 .UNSPECIFIED.)
CURVE()
GEOMETRIC_REPRESENTATION_ITEM()
RATIONAL_B_SPLINE_CURVE((1.11971735964627,1.12024119946973,1.12071541658449))
REPRESENTATION_ITEM('')
);
#760=(
BOUNDED_CURVE()
B_SPLINE_CURVE(2,(#52197,#52198,#52199),.UNSPECIFIED.,.F.,.F.)
B_SPLINE_CURVE_WITH_KNOTS((3,3),(0.376641898803533,0.382940702095944),
 .UNSPECIFIED.)
CURVE()
GEOMETRIC_REPRESENTATION_ITEM()
RATIONAL_B_SPLINE_CURVE((1.12071541658435,1.12024119946922,1.1197173596453))
REPRESENTATION_ITEM('')
);
#761=(
BOUNDED_CURVE()
B_SPLINE_CURVE(2,(#52203,#52204,#52205),.UNSPECIFIED.,.F.,.F.)
B_SPLINE_CURVE_WITH_KNOTS((3,3),(0.249954652430647,0.256253455718059),
 .UNSPECIFIED.)
CURVE()
GEOMETRIC_REPRESENTATION_ITEM()
RATIONAL_B_SPLINE_CURVE((1.11971735964614,1.12024119946961,1.12071541658437))
REPRESENTATION_ITEM('')
);
#762=(
BOUNDED_CURVE()
B_SPLINE_CURVE(2,(#52209,#52210,#52211),.UNSPECIFIED.,.F.,.F.)
B_SPLINE_CURVE_WITH_KNOTS((3,3),(0.376641898803539,0.382940702095955),
 .UNSPECIFIED.)
CURVE()
GEOMETRIC_REPRESENTATION_ITEM()
RATIONAL_B_SPLINE_CURVE((1.12071541658434,1.1202411994692,1.11971735964528))
REPRESENTATION_ITEM('')
);
#763=(
BOUNDED_CURVE()
B_SPLINE_CURVE(2,(#52215,#52216,#52217),.UNSPECIFIED.,.F.,.F.)
B_SPLINE_CURVE_WITH_KNOTS((3,3),(0.249954652430656,0.256253455718067),
 .UNSPECIFIED.)
CURVE()
GEOMETRIC_REPRESENTATION_ITEM()
RATIONAL_B_SPLINE_CURVE((1.11971735964622,1.12024119946969,1.12071541658444))
REPRESENTATION_ITEM('')
);
#764=(
BOUNDED_CURVE()
B_SPLINE_CURVE(2,(#52221,#52222,#52223),.UNSPECIFIED.,.F.,.F.)
B_SPLINE_CURVE_WITH_KNOTS((3,3),(0.376641898803524,0.382940702095936),
 .UNSPECIFIED.)
CURVE()
GEOMETRIC_REPRESENTATION_ITEM()
RATIONAL_B_SPLINE_CURVE((1.12071541658457,1.12024119946943,1.11971735964551))
REPRESENTATION_ITEM('')
);
#765=(
BOUNDED_CURVE()
B_SPLINE_CURVE(2,(#52227,#52228,#52229),.UNSPECIFIED.,.F.,.F.)
B_SPLINE_CURVE_WITH_KNOTS((3,3),(0.249954652430651,0.256253455718065),
 .UNSPECIFIED.)
CURVE()
GEOMETRIC_REPRESENTATION_ITEM()
RATIONAL_B_SPLINE_CURVE((1.11971735964615,1.12024119946961,1.12071541658437))
REPRESENTATION_ITEM('')
);
#766=(
BOUNDED_CURVE()
B_SPLINE_CURVE(2,(#52233,#52234,#52235),.UNSPECIFIED.,.F.,.F.)
B_SPLINE_CURVE_WITH_KNOTS((3,3),(0.376641898803518,0.382940702095931),
 .UNSPECIFIED.)
CURVE()
GEOMETRIC_REPRESENTATION_ITEM()
RATIONAL_B_SPLINE_CURVE((1.12071541658449,1.12024119946936,1.11971735964544))
REPRESENTATION_ITEM('')
);
#767=(
BOUNDED_CURVE()
B_SPLINE_CURVE(2,(#52239,#52240,#52241),.UNSPECIFIED.,.F.,.F.)
B_SPLINE_CURVE_WITH_KNOTS((3,3),(0.249954652430648,0.256253455718058),
 .UNSPECIFIED.)
CURVE()
GEOMETRIC_REPRESENTATION_ITEM()
RATIONAL_B_SPLINE_CURVE((1.11971735964614,1.1202411994696,1.12071541658436))
REPRESENTATION_ITEM('')
);
#768=(
BOUNDED_CURVE()
B_SPLINE_CURVE(2,(#52245,#52246,#52247),.UNSPECIFIED.,.F.,.F.)
B_SPLINE_CURVE_WITH_KNOTS((3,3),(0.376641898803531,0.382940702095945),
 .UNSPECIFIED.)
CURVE()
GEOMETRIC_REPRESENTATION_ITEM()
RATIONAL_B_SPLINE_CURVE((1.12071541658451,1.12024119946937,1.11971735964545))
REPRESENTATION_ITEM('')
);
#769=(
BOUNDED_CURVE()
B_SPLINE_CURVE(2,(#52251,#52252,#52253),.UNSPECIFIED.,.F.,.F.)
B_SPLINE_CURVE_WITH_KNOTS((3,3),(0.249954652430648,0.256253455718067),
 .UNSPECIFIED.)
CURVE()
GEOMETRIC_REPRESENTATION_ITEM()
RATIONAL_B_SPLINE_CURVE((1.11971735964618,1.12024119946964,1.1207154165844))
REPRESENTATION_ITEM('')
);
#770=(
BOUNDED_CURVE()
B_SPLINE_CURVE(2,(#52257,#52258,#52259),.UNSPECIFIED.,.F.,.F.)
B_SPLINE_CURVE_WITH_KNOTS((3,3),(0.376641898803536,0.382940702095949),
 .UNSPECIFIED.)
CURVE()
GEOMETRIC_REPRESENTATION_ITEM()
RATIONAL_B_SPLINE_CURVE((1.12071541658431,1.12024119946918,1.11971735964526))
REPRESENTATION_ITEM('')
);
#771=(
BOUNDED_CURVE()
B_SPLINE_CURVE(2,(#52263,#52264,#52265),.UNSPECIFIED.,.F.,.F.)
B_SPLINE_CURVE_WITH_KNOTS((3,3),(0.249954652430665,0.256253455718077),
 .UNSPECIFIED.)
CURVE()
GEOMETRIC_REPRESENTATION_ITEM()
RATIONAL_B_SPLINE_CURVE((1.11971735964631,1.12024119946977,1.12071541658453))
REPRESENTATION_ITEM('')
);
#772=(
BOUNDED_CURVE()
B_SPLINE_CURVE(2,(#52269,#52270,#52271),.UNSPECIFIED.,.F.,.F.)
B_SPLINE_CURVE_WITH_KNOTS((3,3),(0.376641898803534,0.382940702095945),
 .UNSPECIFIED.)
CURVE()
GEOMETRIC_REPRESENTATION_ITEM()
RATIONAL_B_SPLINE_CURVE((1.12071541658427,1.12024119946914,1.11971735964522))
REPRESENTATION_ITEM('')
);
#773=(
BOUNDED_CURVE()
B_SPLINE_CURVE(2,(#52275,#52276,#52277),.UNSPECIFIED.,.F.,.F.)
B_SPLINE_CURVE_WITH_KNOTS((3,3),(0.249954652430654,0.256253455718069),
 .UNSPECIFIED.)
CURVE()
GEOMETRIC_REPRESENTATION_ITEM()
RATIONAL_B_SPLINE_CURVE((1.11971735964621,1.12024119946968,1.12071541658444))
REPRESENTATION_ITEM('')
);
#774=(
BOUNDED_CURVE()
B_SPLINE_CURVE(2,(#52281,#52282,#52283),.UNSPECIFIED.,.F.,.F.)
B_SPLINE_CURVE_WITH_KNOTS((3,3),(0.376641898803532,0.382940702095944),
 .UNSPECIFIED.)
CURVE()
GEOMETRIC_REPRESENTATION_ITEM()
RATIONAL_B_SPLINE_CURVE((1.12071541658432,1.12024119946919,1.11971735964527))
REPRESENTATION_ITEM('')
);
#775=(
BOUNDED_CURVE()
B_SPLINE_CURVE(2,(#52287,#52288,#52289),.UNSPECIFIED.,.F.,.F.)
B_SPLINE_CURVE_WITH_KNOTS((3,3),(0.249954652430654,0.256253455718072),
 .UNSPECIFIED.)
CURVE()
GEOMETRIC_REPRESENTATION_ITEM()
RATIONAL_B_SPLINE_CURVE((1.11971735964625,1.12024119946971,1.12071541658447))
REPRESENTATION_ITEM('')
);
#776=(
BOUNDED_CURVE()
B_SPLINE_CURVE(2,(#52293,#52294,#52295),.UNSPECIFIED.,.F.,.F.)
B_SPLINE_CURVE_WITH_KNOTS((3,3),(0.376641898803539,0.382940702095952),
 .UNSPECIFIED.)
CURVE()
GEOMETRIC_REPRESENTATION_ITEM()
RATIONAL_B_SPLINE_CURVE((1.1207154165844,1.12024119946926,1.11971735964534))
REPRESENTATION_ITEM('')
);
#777=(
BOUNDED_CURVE()
B_SPLINE_CURVE(2,(#52299,#52300,#52301),.UNSPECIFIED.,.F.,.F.)
B_SPLINE_CURVE_WITH_KNOTS((3,3),(0.249954652430648,0.256253455718062),
 .UNSPECIFIED.)
CURVE()
GEOMETRIC_REPRESENTATION_ITEM()
RATIONAL_B_SPLINE_CURVE((1.11971735964618,1.12024119946965,1.12071541658441))
REPRESENTATION_ITEM('')
);
#778=(
BOUNDED_CURVE()
B_SPLINE_CURVE(2,(#52305,#52306,#52307),.UNSPECIFIED.,.F.,.F.)
B_SPLINE_CURVE_WITH_KNOTS((3,3),(0.376641898803519,0.382940702095932),
 .UNSPECIFIED.)
CURVE()
GEOMETRIC_REPRESENTATION_ITEM()
RATIONAL_B_SPLINE_CURVE((1.12071541658452,1.12024119946938,1.11971735964546))
REPRESENTATION_ITEM('')
);
#779=(
BOUNDED_CURVE()
B_SPLINE_CURVE(2,(#52311,#52312,#52313),.UNSPECIFIED.,.F.,.F.)
B_SPLINE_CURVE_WITH_KNOTS((3,3),(0.249954652430659,0.256253455718071),
 .UNSPECIFIED.)
CURVE()
GEOMETRIC_REPRESENTATION_ITEM()
RATIONAL_B_SPLINE_CURVE((1.11971735964627,1.12024119946974,1.1207154165845))
REPRESENTATION_ITEM('')
);
#780=(
BOUNDED_CURVE()
B_SPLINE_CURVE(2,(#52317,#52318,#52319),.UNSPECIFIED.,.F.,.F.)
B_SPLINE_CURVE_WITH_KNOTS((3,3),(0.376641898803527,0.382940702095942),
 .UNSPECIFIED.)
CURVE()
GEOMETRIC_REPRESENTATION_ITEM()
RATIONAL_B_SPLINE_CURVE((1.12071541658453,1.1202411994694,1.11971735964547))
REPRESENTATION_ITEM('')
);
#781=(
BOUNDED_CURVE()
B_SPLINE_CURVE(2,(#52323,#52324,#52325),.UNSPECIFIED.,.F.,.F.)
B_SPLINE_CURVE_WITH_KNOTS((3,3),(0.249954652430662,0.256253455718075),
 .UNSPECIFIED.)
CURVE()
GEOMETRIC_REPRESENTATION_ITEM()
RATIONAL_B_SPLINE_CURVE((1.11971735964629,1.12024119946976,1.12071541658452))
REPRESENTATION_ITEM('')
);
#782=(
BOUNDED_CURVE()
B_SPLINE_CURVE(2,(#52329,#52330,#52331),.UNSPECIFIED.,.F.,.F.)
B_SPLINE_CURVE_WITH_KNOTS((3,3),(0.376641898803543,0.382940702095954),
 .UNSPECIFIED.)
CURVE()
GEOMETRIC_REPRESENTATION_ITEM()
RATIONAL_B_SPLINE_CURVE((1.12071541658423,1.1202411994691,1.11971735964518))
REPRESENTATION_ITEM('')
);
#783=(
BOUNDED_CURVE()
B_SPLINE_CURVE(2,(#52335,#52336,#52337),.UNSPECIFIED.,.F.,.F.)
B_SPLINE_CURVE_WITH_KNOTS((3,3),(0.249954652430648,0.256253455718061),
 .UNSPECIFIED.)
CURVE()
GEOMETRIC_REPRESENTATION_ITEM()
RATIONAL_B_SPLINE_CURVE((1.11971735964609,1.12024119946956,1.12071541658431))
REPRESENTATION_ITEM('')
);
#784=(
BOUNDED_CURVE()
B_SPLINE_CURVE(2,(#52341,#52342,#52343),.UNSPECIFIED.,.F.,.F.)
B_SPLINE_CURVE_WITH_KNOTS((3,3),(0.376641898803529,0.382940702095943),
 .UNSPECIFIED.)
CURVE()
GEOMETRIC_REPRESENTATION_ITEM()
RATIONAL_B_SPLINE_CURVE((1.12071541658438,1.12024119946925,1.11971735964533))
REPRESENTATION_ITEM('')
);
#785=(
BOUNDED_CURVE()
B_SPLINE_CURVE(2,(#52347,#52348,#52349),.UNSPECIFIED.,.F.,.F.)
B_SPLINE_CURVE_WITH_KNOTS((3,3),(0.249954652430657,0.256253455718069),
 .UNSPECIFIED.)
CURVE()
GEOMETRIC_REPRESENTATION_ITEM()
RATIONAL_B_SPLINE_CURVE((1.11971735964625,1.12024119946971,1.12071541658447))
REPRESENTATION_ITEM('')
);
#786=(
BOUNDED_CURVE()
B_SPLINE_CURVE(2,(#52353,#52354,#52355),.UNSPECIFIED.,.F.,.F.)
B_SPLINE_CURVE_WITH_KNOTS((3,3),(0.376641898803529,0.382940702095941),
 .UNSPECIFIED.)
CURVE()
GEOMETRIC_REPRESENTATION_ITEM()
RATIONAL_B_SPLINE_CURVE((1.12071541658439,1.12024119946925,1.11971735964533))
REPRESENTATION_ITEM('')
);
#787=(
BOUNDED_CURVE()
B_SPLINE_CURVE(2,(#52359,#52360,#52361),.UNSPECIFIED.,.F.,.F.)
B_SPLINE_CURVE_WITH_KNOTS((3,3),(0.24995465243065,0.256253455718062),
 .UNSPECIFIED.)
CURVE()
GEOMETRIC_REPRESENTATION_ITEM()
RATIONAL_B_SPLINE_CURVE((1.11971735964607,1.12024119946954,1.12071541658429))
REPRESENTATION_ITEM('')
);
#788=(
BOUNDED_CURVE()
B_SPLINE_CURVE(2,(#52365,#52366,#52367),.UNSPECIFIED.,.F.,.F.)
B_SPLINE_CURVE_WITH_KNOTS((3,3),(0.376641898803544,0.382940702095955),
 .UNSPECIFIED.)
CURVE()
GEOMETRIC_REPRESENTATION_ITEM()
RATIONAL_B_SPLINE_CURVE((1.12071541658421,1.12024119946907,1.11971735964515))
REPRESENTATION_ITEM('')
);
#789=(
BOUNDED_CURVE()
B_SPLINE_CURVE(2,(#52371,#52372,#52373),.UNSPECIFIED.,.F.,.F.)
B_SPLINE_CURVE_WITH_KNOTS((3,3),(0.249954652430658,0.256253455718075),
 .UNSPECIFIED.)
CURVE()
GEOMETRIC_REPRESENTATION_ITEM()
RATIONAL_B_SPLINE_CURVE((1.11971735964629,1.12024119946976,1.12071541658452))
REPRESENTATION_ITEM('')
);
#790=(
BOUNDED_CURVE()
B_SPLINE_CURVE(2,(#52377,#52378,#52379),.UNSPECIFIED.,.F.,.F.)
B_SPLINE_CURVE_WITH_KNOTS((3,3),(0.376641898803543,0.382940702095958),
 .UNSPECIFIED.)
CURVE()
GEOMETRIC_REPRESENTATION_ITEM()
RATIONAL_B_SPLINE_CURVE((1.12071541658432,1.12024119946919,1.11971735964527))
REPRESENTATION_ITEM('')
);
#791=(
BOUNDED_CURVE()
B_SPLINE_CURVE(2,(#52383,#52384,#52385),.UNSPECIFIED.,.F.,.F.)
B_SPLINE_CURVE_WITH_KNOTS((3,3),(0.249954652430663,0.256253455718076),
 .UNSPECIFIED.)
CURVE()
GEOMETRIC_REPRESENTATION_ITEM()
RATIONAL_B_SPLINE_CURVE((1.11971735964633,1.12024119946979,1.12071541658455))
REPRESENTATION_ITEM('')
);
#792=(
BOUNDED_CURVE()
B_SPLINE_CURVE(2,(#52389,#52390,#52391),.UNSPECIFIED.,.F.,.F.)
B_SPLINE_CURVE_WITH_KNOTS((3,3),(0.37664189880352,0.382940702095933),
 .UNSPECIFIED.)
CURVE()
GEOMETRIC_REPRESENTATION_ITEM()
RATIONAL_B_SPLINE_CURVE((1.1207154165845,1.12024119946936,1.11971735964544))
REPRESENTATION_ITEM('')
);
#793=(
BOUNDED_CURVE()
B_SPLINE_CURVE(2,(#52395,#52396,#52397),.UNSPECIFIED.,.F.,.F.)
B_SPLINE_CURVE_WITH_KNOTS((3,3),(0.249954652430661,0.256253455718074),
 .UNSPECIFIED.)
CURVE()
GEOMETRIC_REPRESENTATION_ITEM()
RATIONAL_B_SPLINE_CURVE((1.11971735964627,1.12024119946973,1.12071541658449))
REPRESENTATION_ITEM('')
);
#794=(
BOUNDED_CURVE()
B_SPLINE_CURVE(2,(#52401,#52402,#52403),.UNSPECIFIED.,.F.,.F.)
B_SPLINE_CURVE_WITH_KNOTS((3,3),(0.376641898803524,0.382940702095942),
 .UNSPECIFIED.)
CURVE()
GEOMETRIC_REPRESENTATION_ITEM()
RATIONAL_B_SPLINE_CURVE((1.12071541658449,1.12024119946935,1.11971735964543))
REPRESENTATION_ITEM('')
);
#795=(
BOUNDED_CURVE()
B_SPLINE_CURVE(2,(#52407,#52408,#52409),.UNSPECIFIED.,.F.,.F.)
B_SPLINE_CURVE_WITH_KNOTS((3,3),(0.249954652430645,0.256253455718058),
 .UNSPECIFIED.)
CURVE()
GEOMETRIC_REPRESENTATION_ITEM()
RATIONAL_B_SPLINE_CURVE((1.11971735964602,1.12024119946949,1.12071541658425))
REPRESENTATION_ITEM('')
);
#796=(
BOUNDED_CURVE()
B_SPLINE_CURVE(2,(#52413,#52414,#52415),.UNSPECIFIED.,.F.,.F.)
B_SPLINE_CURVE_WITH_KNOTS((3,3),(0.376641898803526,0.382940702095943),
 .UNSPECIFIED.)
CURVE()
GEOMETRIC_REPRESENTATION_ITEM()
RATIONAL_B_SPLINE_CURVE((1.12071541658447,1.12024119946934,1.11971735964542))
REPRESENTATION_ITEM('')
);
#797=(
BOUNDED_CURVE()
B_SPLINE_CURVE(2,(#52419,#52420,#52421),.UNSPECIFIED.,.F.,.F.)
B_SPLINE_CURVE_WITH_KNOTS((3,3),(0.249954652430656,0.25625345571807),
 .UNSPECIFIED.)
CURVE()
GEOMETRIC_REPRESENTATION_ITEM()
RATIONAL_B_SPLINE_CURVE((1.11971735964623,1.12024119946969,1.12071541658445))
REPRESENTATION_ITEM('')
);
#798=(
BOUNDED_CURVE()
B_SPLINE_CURVE(2,(#52425,#52426,#52427),.UNSPECIFIED.,.F.,.F.)
B_SPLINE_CURVE_WITH_KNOTS((3,3),(0.376641898803539,0.382940702095953),
 .UNSPECIFIED.)
CURVE()
GEOMETRIC_REPRESENTATION_ITEM()
RATIONAL_B_SPLINE_CURVE((1.12071541658437,1.12024119946923,1.11971735964531))
REPRESENTATION_ITEM('')
);
#799=(
BOUNDED_CURVE()
B_SPLINE_CURVE(2,(#52431,#52432,#52433),.UNSPECIFIED.,.F.,.F.)
B_SPLINE_CURVE_WITH_KNOTS((3,3),(0.249954652430661,0.256253455718075),
 .UNSPECIFIED.)
CURVE()
GEOMETRIC_REPRESENTATION_ITEM()
RATIONAL_B_SPLINE_CURVE((1.11971735964628,1.12024119946974,1.1207154165845))
REPRESENTATION_ITEM('')
);
#800=(
BOUNDED_CURVE()
B_SPLINE_CURVE(2,(#52437,#52438,#52439),.UNSPECIFIED.,.F.,.F.)
B_SPLINE_CURVE_WITH_KNOTS((3,3),(0.376641898803538,0.382940702095948),
 .UNSPECIFIED.)
CURVE()
GEOMETRIC_REPRESENTATION_ITEM()
RATIONAL_B_SPLINE_CURVE((1.12071541658433,1.1202411994692,1.11971735964528))
REPRESENTATION_ITEM('')
);
#801=(
BOUNDED_CURVE()
B_SPLINE_CURVE(2,(#52443,#52444,#52445),.UNSPECIFIED.,.F.,.F.)
B_SPLINE_CURVE_WITH_KNOTS((3,3),(0.249954652430662,0.256253455718076),
 .UNSPECIFIED.)
CURVE()
GEOMETRIC_REPRESENTATION_ITEM()
RATIONAL_B_SPLINE_CURVE((1.11971735964622,1.12024119946968,1.12071541658444))
REPRESENTATION_ITEM('')
);
#802=(
BOUNDED_CURVE()
B_SPLINE_CURVE(2,(#52449,#52450,#52451),.UNSPECIFIED.,.F.,.F.)
B_SPLINE_CURVE_WITH_KNOTS((3,3),(0.37664189880352,0.382940702095935),
 .UNSPECIFIED.)
CURVE()
GEOMETRIC_REPRESENTATION_ITEM()
RATIONAL_B_SPLINE_CURVE((1.12071541658454,1.12024119946941,1.11971735964549))
REPRESENTATION_ITEM('')
);
#803=(
BOUNDED_CURVE()
B_SPLINE_CURVE(2,(#52455,#52456,#52457),.UNSPECIFIED.,.F.,.F.)
B_SPLINE_CURVE_WITH_KNOTS((3,3),(0.24995465243066,0.256253455718075),
 .UNSPECIFIED.)
CURVE()
GEOMETRIC_REPRESENTATION_ITEM()
RATIONAL_B_SPLINE_CURVE((1.1197173596463,1.12024119946976,1.12071541658452))
REPRESENTATION_ITEM('')
);
#804=(
BOUNDED_CURVE()
B_SPLINE_CURVE(2,(#52461,#52462,#52463),.UNSPECIFIED.,.F.,.F.)
B_SPLINE_CURVE_WITH_KNOTS((3,3),(0.376641898803523,0.382940702095934),
 .UNSPECIFIED.)
CURVE()
GEOMETRIC_REPRESENTATION_ITEM()
RATIONAL_B_SPLINE_CURVE((1.12071541658448,1.12024119946934,1.11971735964542))
REPRESENTATION_ITEM('')
);
#805=(
BOUNDED_CURVE()
B_SPLINE_CURVE(2,(#52467,#52468,#52469),.UNSPECIFIED.,.F.,.F.)
B_SPLINE_CURVE_WITH_KNOTS((3,3),(0.249954652430663,0.256253455718077),
 .UNSPECIFIED.)
CURVE()
GEOMETRIC_REPRESENTATION_ITEM()
RATIONAL_B_SPLINE_CURVE((1.11971735964627,1.12024119946973,1.12071541658449))
REPRESENTATION_ITEM('')
);
#806=(
BOUNDED_CURVE()
B_SPLINE_CURVE(2,(#52473,#52474,#52475),.UNSPECIFIED.,.F.,.F.)
B_SPLINE_CURVE_WITH_KNOTS((3,3),(0.376641898803548,0.382940702095957),
 .UNSPECIFIED.)
CURVE()
GEOMETRIC_REPRESENTATION_ITEM()
RATIONAL_B_SPLINE_CURVE((1.12071541658418,1.12024119946905,1.11971735964513))
REPRESENTATION_ITEM('')
);
#807=(
BOUNDED_CURVE()
B_SPLINE_CURVE(2,(#52479,#52480,#52481),.UNSPECIFIED.,.F.,.F.)
B_SPLINE_CURVE_WITH_KNOTS((3,3),(0.249954652430651,0.256253455718065),
 .UNSPECIFIED.)
CURVE()
GEOMETRIC_REPRESENTATION_ITEM()
RATIONAL_B_SPLINE_CURVE((1.1197173596461,1.12024119946956,1.12071541658432))
REPRESENTATION_ITEM('')
);
#808=(
BOUNDED_CURVE()
B_SPLINE_CURVE(2,(#52485,#52486,#52487),.UNSPECIFIED.,.F.,.F.)
B_SPLINE_CURVE_WITH_KNOTS((3,3),(0.376641898803522,0.382940702095932),
 .UNSPECIFIED.)
CURVE()
GEOMETRIC_REPRESENTATION_ITEM()
RATIONAL_B_SPLINE_CURVE((1.12071541658448,1.12024119946934,1.11971735964542))
REPRESENTATION_ITEM('')
);
#809=(
BOUNDED_CURVE()
B_SPLINE_CURVE(2,(#52491,#52492,#52493),.UNSPECIFIED.,.F.,.F.)
B_SPLINE_CURVE_WITH_KNOTS((3,3),(0.249954652430654,0.256253455718068),
 .UNSPECIFIED.)
CURVE()
GEOMETRIC_REPRESENTATION_ITEM()
RATIONAL_B_SPLINE_CURVE((1.11971735964629,1.12024119946976,1.12071541658452))
REPRESENTATION_ITEM('')
);
#810=(
BOUNDED_CURVE()
B_SPLINE_CURVE(2,(#52497,#52498,#52499),.UNSPECIFIED.,.F.,.F.)
B_SPLINE_CURVE_WITH_KNOTS((3,3),(0.376641898803521,0.382940702095935),
 .UNSPECIFIED.)
CURVE()
GEOMETRIC_REPRESENTATION_ITEM()
RATIONAL_B_SPLINE_CURVE((1.12071541658442,1.12024119946928,1.11971735964536))
REPRESENTATION_ITEM('')
);
#811=(
BOUNDED_CURVE()
B_SPLINE_CURVE(2,(#52503,#52504,#52505),.UNSPECIFIED.,.F.,.F.)
B_SPLINE_CURVE_WITH_KNOTS((3,3),(0.24995465243066,0.256253455718076),
 .UNSPECIFIED.)
CURVE()
GEOMETRIC_REPRESENTATION_ITEM()
RATIONAL_B_SPLINE_CURVE((1.11971735964628,1.12024119946975,1.12071541658451))
REPRESENTATION_ITEM('')
);
#812=(
BOUNDED_CURVE()
B_SPLINE_CURVE(2,(#52509,#52510,#52511),.UNSPECIFIED.,.F.,.F.)
B_SPLINE_CURVE_WITH_KNOTS((3,3),(0.37664189880352,0.382940702095931),
 .UNSPECIFIED.)
CURVE()
GEOMETRIC_REPRESENTATION_ITEM()
RATIONAL_B_SPLINE_CURVE((1.12071541658452,1.12024119946938,1.11971735964546))
REPRESENTATION_ITEM('')
);
#813=(
BOUNDED_CURVE()
B_SPLINE_CURVE(2,(#52515,#52516,#52517),.UNSPECIFIED.,.F.,.F.)
B_SPLINE_CURVE_WITH_KNOTS((3,3),(0.249954652430663,0.25625345571808),
 .UNSPECIFIED.)
CURVE()
GEOMETRIC_REPRESENTATION_ITEM()
RATIONAL_B_SPLINE_CURVE((1.11971735964629,1.12024119946975,1.12071541658451))
REPRESENTATION_ITEM('')
);
#814=(
BOUNDED_CURVE()
B_SPLINE_CURVE(2,(#52521,#52522,#52523),.UNSPECIFIED.,.F.,.F.)
B_SPLINE_CURVE_WITH_KNOTS((3,3),(0.376641898803514,0.382940702095925),
 .UNSPECIFIED.)
CURVE()
GEOMETRIC_REPRESENTATION_ITEM()
RATIONAL_B_SPLINE_CURVE((1.12071541658449,1.12024119946936,1.11971735964544))
REPRESENTATION_ITEM('')
);
#815=(
BOUNDED_CURVE()
B_SPLINE_CURVE(2,(#52527,#52528,#52529),.UNSPECIFIED.,.F.,.F.)
B_SPLINE_CURVE_WITH_KNOTS((3,3),(0.249954652430668,0.25625345571808),
 .UNSPECIFIED.)
CURVE()
GEOMETRIC_REPRESENTATION_ITEM()
RATIONAL_B_SPLINE_CURVE((1.11971735964628,1.12024119946974,1.1207154165845))
REPRESENTATION_ITEM('')
);
#816=(
BOUNDED_CURVE()
B_SPLINE_CURVE(2,(#52533,#52534,#52535),.UNSPECIFIED.,.F.,.F.)
B_SPLINE_CURVE_WITH_KNOTS((3,3),(0.376641898803516,0.382940702095925),
 .UNSPECIFIED.)
CURVE()
GEOMETRIC_REPRESENTATION_ITEM()
RATIONAL_B_SPLINE_CURVE((1.1207154165845,1.12024119946936,1.11971735964544))
REPRESENTATION_ITEM('')
);
#817=(
BOUNDED_CURVE()
B_SPLINE_CURVE(2,(#52539,#52540,#52541),.UNSPECIFIED.,.F.,.F.)
B_SPLINE_CURVE_WITH_KNOTS((3,3),(0.24995465243065,0.256253455718064),
 .UNSPECIFIED.)
CURVE()
GEOMETRIC_REPRESENTATION_ITEM()
RATIONAL_B_SPLINE_CURVE((1.11971735964608,1.12024119946955,1.1207154165843))
REPRESENTATION_ITEM('')
);
#818=(
BOUNDED_CURVE()
B_SPLINE_CURVE(2,(#52545,#52546,#52547),.UNSPECIFIED.,.F.,.F.)
B_SPLINE_CURVE_WITH_KNOTS((3,3),(0.376641898803537,0.382940702095953),
 .UNSPECIFIED.)
CURVE()
GEOMETRIC_REPRESENTATION_ITEM()
RATIONAL_B_SPLINE_CURVE((1.12071541658421,1.12024119946908,1.11971735964516))
REPRESENTATION_ITEM('')
);
#819=(
BOUNDED_CURVE()
B_SPLINE_CURVE(2,(#52551,#52552,#52553),.UNSPECIFIED.,.F.,.F.)
B_SPLINE_CURVE_WITH_KNOTS((3,3),(0.249954652430652,0.256253455718068),
 .UNSPECIFIED.)
CURVE()
GEOMETRIC_REPRESENTATION_ITEM()
RATIONAL_B_SPLINE_CURVE((1.11971735964626,1.12024119946972,1.12071541658448))
REPRESENTATION_ITEM('')
);
#820=(
BOUNDED_CURVE()
B_SPLINE_CURVE(2,(#52557,#52558,#52559),.UNSPECIFIED.,.F.,.F.)
B_SPLINE_CURVE_WITH_KNOTS((3,3),(0.376641898803534,0.382940702095941),
 .UNSPECIFIED.)
CURVE()
GEOMETRIC_REPRESENTATION_ITEM()
RATIONAL_B_SPLINE_CURVE((1.12071541658423,1.1202411994691,1.11971735964518))
REPRESENTATION_ITEM('')
);
#821=(
BOUNDED_CURVE()
B_SPLINE_CURVE(2,(#52563,#52564,#52565),.UNSPECIFIED.,.F.,.F.)
B_SPLINE_CURVE_WITH_KNOTS((3,3),(0.249954652430639,0.256253455718054),
 .UNSPECIFIED.)
CURVE()
GEOMETRIC_REPRESENTATION_ITEM()
RATIONAL_B_SPLINE_CURVE((1.11971735964598,1.12024119946944,1.1207154165842))
REPRESENTATION_ITEM('')
);
#822=(
BOUNDED_CURVE()
B_SPLINE_CURVE(2,(#52569,#52570,#52571),.UNSPECIFIED.,.F.,.F.)
B_SPLINE_CURVE_WITH_KNOTS((3,3),(0.376641898803521,0.382940702095926),
 .UNSPECIFIED.)
CURVE()
GEOMETRIC_REPRESENTATION_ITEM()
RATIONAL_B_SPLINE_CURVE((1.12071541658441,1.12024119946928,1.11971735964536))
REPRESENTATION_ITEM('')
);
#823=(
BOUNDED_CURVE()
B_SPLINE_CURVE(2,(#52575,#52576,#52577),.UNSPECIFIED.,.F.,.F.)
B_SPLINE_CURVE_WITH_KNOTS((3,3),(0.249954652430644,0.256253455718059),
 .UNSPECIFIED.)
CURVE()
GEOMETRIC_REPRESENTATION_ITEM()
RATIONAL_B_SPLINE_CURVE((1.11971735964605,1.12024119946951,1.12071541658427))
REPRESENTATION_ITEM('')
);
#824=(
BOUNDED_CURVE()
B_SPLINE_CURVE(2,(#52581,#52582,#52583),.UNSPECIFIED.,.F.,.F.)
B_SPLINE_CURVE_WITH_KNOTS((3,3),(0.376641898803522,0.382940702095933),
 .UNSPECIFIED.)
CURVE()
GEOMETRIC_REPRESENTATION_ITEM()
RATIONAL_B_SPLINE_CURVE((1.12071541658452,1.12024119946939,1.11971735964547))
REPRESENTATION_ITEM('')
);
#825=(
BOUNDED_CURVE()
B_SPLINE_CURVE(2,(#52587,#52588,#52589),.UNSPECIFIED.,.F.,.F.)
B_SPLINE_CURVE_WITH_KNOTS((3,3),(0.249954652430652,0.256253455718069),
 .UNSPECIFIED.)
CURVE()
GEOMETRIC_REPRESENTATION_ITEM()
RATIONAL_B_SPLINE_CURVE((1.11971735964616,1.12024119946962,1.12071541658438))
REPRESENTATION_ITEM('')
);
#826=(
BOUNDED_CURVE()
B_SPLINE_CURVE(2,(#52593,#52594,#52595),.UNSPECIFIED.,.F.,.F.)
B_SPLINE_CURVE_WITH_KNOTS((3,3),(0.376641898803538,0.38294070209595),
 .UNSPECIFIED.)
CURVE()
GEOMETRIC_REPRESENTATION_ITEM()
RATIONAL_B_SPLINE_CURVE((1.12071541658426,1.12024119946913,1.11971735964521))
REPRESENTATION_ITEM('')
);
#827=(
BOUNDED_CURVE()
B_SPLINE_CURVE(2,(#52598,#52599,#52600),.UNSPECIFIED.,.F.,.F.)
B_SPLINE_CURVE_WITH_KNOTS((3,3),(0.249954652430655,0.256253455718073),
 .UNSPECIFIED.)
CURVE()
GEOMETRIC_REPRESENTATION_ITEM()
RATIONAL_B_SPLINE_CURVE((1.11971735964623,1.1202411994697,1.12071541658446))
REPRESENTATION_ITEM('')
);
#828=(
BOUNDED_CURVE()
B_SPLINE_CURVE(2,(#52602,#52603,#52604),.UNSPECIFIED.,.F.,.F.)
B_SPLINE_CURVE_WITH_KNOTS((3,3),(0.376641898803523,0.38294070209594),
 .UNSPECIFIED.)
CURVE()
GEOMETRIC_REPRESENTATION_ITEM()
RATIONAL_B_SPLINE_CURVE((1.12071541658441,1.12024119946928,1.11971735964536))
REPRESENTATION_ITEM('')
);
#829=(
BOUNDED_CURVE()
B_SPLINE_CURVE(2,(#52607,#52608,#52609),.UNSPECIFIED.,.F.,.F.)
B_SPLINE_CURVE_WITH_KNOTS((3,3),(0.249954652430659,0.256253455718073),
 .UNSPECIFIED.)
CURVE()
GEOMETRIC_REPRESENTATION_ITEM()
RATIONAL_B_SPLINE_CURVE((1.11971735964623,1.12024119946969,1.12071541658445))
REPRESENTATION_ITEM('')
);
#830=(
BOUNDED_CURVE()
B_SPLINE_CURVE(2,(#52611,#52612,#52613),.UNSPECIFIED.,.F.,.F.)
B_SPLINE_CURVE_WITH_KNOTS((3,3),(0.376641898803521,0.382940702095929),
 .UNSPECIFIED.)
CURVE()
GEOMETRIC_REPRESENTATION_ITEM()
RATIONAL_B_SPLINE_CURVE((1.12071541658454,1.1202411994694,1.11971735964548))
REPRESENTATION_ITEM('')
);
#831=(
BOUNDED_CURVE()
B_SPLINE_CURVE(2,(#52616,#52617,#52618),.UNSPECIFIED.,.F.,.F.)
B_SPLINE_CURVE_WITH_KNOTS((3,3),(0.249954652430646,0.256253455718056),
 .UNSPECIFIED.)
CURVE()
GEOMETRIC_REPRESENTATION_ITEM()
RATIONAL_B_SPLINE_CURVE((1.11971735964596,1.12024119946942,1.12071541658418))
REPRESENTATION_ITEM('')
);
#832=(
BOUNDED_CURVE()
B_SPLINE_CURVE(2,(#52620,#52621,#52622),.UNSPECIFIED.,.F.,.F.)
B_SPLINE_CURVE_WITH_KNOTS((3,3),(0.376641898803528,0.382940702095943),
 .UNSPECIFIED.)
CURVE()
GEOMETRIC_REPRESENTATION_ITEM()
RATIONAL_B_SPLINE_CURVE((1.12071541658433,1.1202411994692,1.11971735964528))
REPRESENTATION_ITEM('')
);
#833=(
BOUNDED_CURVE()
B_SPLINE_CURVE(2,(#52625,#52626,#52627),.UNSPECIFIED.,.F.,.F.)
B_SPLINE_CURVE_WITH_KNOTS((3,3),(0.24995465243066,0.256253455718077),
 .UNSPECIFIED.)
CURVE()
GEOMETRIC_REPRESENTATION_ITEM()
RATIONAL_B_SPLINE_CURVE((1.11971735964636,1.12024119946983,1.12071541658459))
REPRESENTATION_ITEM('')
);
#834=(
BOUNDED_CURVE()
B_SPLINE_CURVE(2,(#52629,#52630,#52631),.UNSPECIFIED.,.F.,.F.)
B_SPLINE_CURVE_WITH_KNOTS((3,3),(0.376641898803527,0.382940702095942),
 .UNSPECIFIED.)
CURVE()
GEOMETRIC_REPRESENTATION_ITEM()
RATIONAL_B_SPLINE_CURVE((1.12071541658443,1.12024119946929,1.11971735964537))
REPRESENTATION_ITEM('')
);
#835=(
BOUNDED_CURVE()
B_SPLINE_CURVE(2,(#52634,#52635,#52636),.UNSPECIFIED.,.F.,.F.)
B_SPLINE_CURVE_WITH_KNOTS((3,3),(0.249954652430663,0.256253455718073),
 .UNSPECIFIED.)
CURVE()
GEOMETRIC_REPRESENTATION_ITEM()
RATIONAL_B_SPLINE_CURVE((1.11971735964622,1.12024119946969,1.12071541658445))
REPRESENTATION_ITEM('')
);
#836=(
BOUNDED_CURVE()
B_SPLINE_CURVE(2,(#52638,#52639,#52640),.UNSPECIFIED.,.F.,.F.)
B_SPLINE_CURVE_WITH_KNOTS((3,3),(0.376641898803534,0.382940702095947),
 .UNSPECIFIED.)
CURVE()
GEOMETRIC_REPRESENTATION_ITEM()
RATIONAL_B_SPLINE_CURVE((1.12071541658425,1.12024119946912,1.1197173596452))
REPRESENTATION_ITEM('')
);
#837=(
BOUNDED_CURVE()
B_SPLINE_CURVE(2,(#52643,#52644,#52645),.UNSPECIFIED.,.F.,.F.)
B_SPLINE_CURVE_WITH_KNOTS((3,3),(0.249954652430658,0.256253455718067),
 .UNSPECIFIED.)
CURVE()
GEOMETRIC_REPRESENTATION_ITEM()
RATIONAL_B_SPLINE_CURVE((1.1197173596462,1.12024119946966,1.12071541658442))
REPRESENTATION_ITEM('')
);
#838=(
BOUNDED_CURVE()
B_SPLINE_CURVE(2,(#52647,#52648,#52649),.UNSPECIFIED.,.F.,.F.)
B_SPLINE_CURVE_WITH_KNOTS((3,3),(0.376641898803512,0.382940702095926),
 .UNSPECIFIED.)
CURVE()
GEOMETRIC_REPRESENTATION_ITEM()
RATIONAL_B_SPLINE_CURVE((1.12071541658454,1.12024119946941,1.11971735964549))
REPRESENTATION_ITEM('')
);
#839=(
BOUNDED_CURVE()
B_SPLINE_CURVE(2,(#52652,#52653,#52654),.UNSPECIFIED.,.F.,.F.)
B_SPLINE_CURVE_WITH_KNOTS((3,3),(0.249954652430648,0.256253455718064),
 .UNSPECIFIED.)
CURVE()
GEOMETRIC_REPRESENTATION_ITEM()
RATIONAL_B_SPLINE_CURVE((1.11971735964605,1.12024119946951,1.12071541658427))
REPRESENTATION_ITEM('')
);
#840=(
BOUNDED_CURVE()
B_SPLINE_CURVE(2,(#52656,#52657,#52658),.UNSPECIFIED.,.F.,.F.)
B_SPLINE_CURVE_WITH_KNOTS((3,3),(0.37664189880353,0.382940702095945),
 .UNSPECIFIED.)
CURVE()
GEOMETRIC_REPRESENTATION_ITEM()
RATIONAL_B_SPLINE_CURVE((1.12071541658432,1.12024119946919,1.11971735964527))
REPRESENTATION_ITEM('')
);
#841=(
BOUNDED_CURVE()
B_SPLINE_CURVE(2,(#52661,#52662,#52663),.UNSPECIFIED.,.F.,.F.)
B_SPLINE_CURVE_WITH_KNOTS((3,3),(0.24995465243065,0.256253455718062),
 .UNSPECIFIED.)
CURVE()
GEOMETRIC_REPRESENTATION_ITEM()
RATIONAL_B_SPLINE_CURVE((1.1197173596462,1.12024119946966,1.12071541658442))
REPRESENTATION_ITEM('')
);
#842=(
BOUNDED_CURVE()
B_SPLINE_CURVE(2,(#52665,#52666,#52667),.UNSPECIFIED.,.F.,.F.)
B_SPLINE_CURVE_WITH_KNOTS((3,3),(0.376641898803514,0.382940702095926),
 .UNSPECIFIED.)
CURVE()
GEOMETRIC_REPRESENTATION_ITEM()
RATIONAL_B_SPLINE_CURVE((1.12071541658458,1.12024119946944,1.11971735964552))
REPRESENTATION_ITEM('')
);
#843=(
BOUNDED_CURVE()
B_SPLINE_CURVE(2,(#52670,#52671,#52672),.UNSPECIFIED.,.F.,.F.)
B_SPLINE_CURVE_WITH_KNOTS((3,3),(0.249954652430654,0.256253455718075),
 .UNSPECIFIED.)
CURVE()
GEOMETRIC_REPRESENTATION_ITEM()
RATIONAL_B_SPLINE_CURVE((1.11971735964632,1.12024119946978,1.12071541658454))
REPRESENTATION_ITEM('')
);
#844=(
BOUNDED_CURVE()
B_SPLINE_CURVE(2,(#52674,#52675,#52676),.UNSPECIFIED.,.F.,.F.)
B_SPLINE_CURVE_WITH_KNOTS((3,3),(0.376641898803524,0.382940702095939),
 .UNSPECIFIED.)
CURVE()
GEOMETRIC_REPRESENTATION_ITEM()
RATIONAL_B_SPLINE_CURVE((1.12071541658443,1.1202411994693,1.11971735964538))
REPRESENTATION_ITEM('')
);
#845=(
BOUNDED_CURVE()
B_SPLINE_CURVE(2,(#52679,#52680,#52681),.UNSPECIFIED.,.F.,.F.)
B_SPLINE_CURVE_WITH_KNOTS((3,3),(0.249954652430651,0.256253455718065),
 .UNSPECIFIED.)
CURVE()
GEOMETRIC_REPRESENTATION_ITEM()
RATIONAL_B_SPLINE_CURVE((1.11971735964614,1.12024119946961,1.12071541658437))
REPRESENTATION_ITEM('')
);
#846=(
BOUNDED_CURVE()
B_SPLINE_CURVE(2,(#52683,#52684,#52685),.UNSPECIFIED.,.F.,.F.)
B_SPLINE_CURVE_WITH_KNOTS((3,3),(0.376641898803524,0.382940702095937),
 .UNSPECIFIED.)
CURVE()
GEOMETRIC_REPRESENTATION_ITEM()
RATIONAL_B_SPLINE_CURVE((1.12071541658443,1.1202411994693,1.11971735964538))
REPRESENTATION_ITEM('')
);
#847=(
BOUNDED_CURVE()
B_SPLINE_CURVE(2,(#52688,#52689,#52690),.UNSPECIFIED.,.F.,.F.)
B_SPLINE_CURVE_WITH_KNOTS((3,3),(0.24995465243066,0.256253455718078),
 .UNSPECIFIED.)
CURVE()
GEOMETRIC_REPRESENTATION_ITEM()
RATIONAL_B_SPLINE_CURVE((1.11971735964625,1.12024119946971,1.12071541658447))
REPRESENTATION_ITEM('')
);
#848=(
BOUNDED_CURVE()
B_SPLINE_CURVE(2,(#52692,#52693,#52694),.UNSPECIFIED.,.F.,.F.)
B_SPLINE_CURVE_WITH_KNOTS((3,3),(0.376641898803522,0.382940702095931),
 .UNSPECIFIED.)
CURVE()
GEOMETRIC_REPRESENTATION_ITEM()
RATIONAL_B_SPLINE_CURVE((1.1207154165845,1.12024119946936,1.11971735964544))
REPRESENTATION_ITEM('')
);
#849=(
BOUNDED_CURVE()
B_SPLINE_CURVE(2,(#52697,#52698,#52699),.UNSPECIFIED.,.F.,.F.)
B_SPLINE_CURVE_WITH_KNOTS((3,3),(0.249954652430652,0.256253455718071),
 .UNSPECIFIED.)
CURVE()
GEOMETRIC_REPRESENTATION_ITEM()
RATIONAL_B_SPLINE_CURVE((1.11971735964614,1.12024119946961,1.12071541658437))
REPRESENTATION_ITEM('')
);
#850=(
BOUNDED_CURVE()
B_SPLINE_CURVE(2,(#52701,#52702,#52703),.UNSPECIFIED.,.F.,.F.)
B_SPLINE_CURVE_WITH_KNOTS((3,3),(0.376641898803528,0.382940702095942),
 .UNSPECIFIED.)
CURVE()
GEOMETRIC_REPRESENTATION_ITEM()
RATIONAL_B_SPLINE_CURVE((1.12071541658436,1.12024119946922,1.1197173596453))
REPRESENTATION_ITEM('')
);
#851=(
BOUNDED_CURVE()
B_SPLINE_CURVE(2,(#52706,#52707,#52708),.UNSPECIFIED.,.F.,.F.)
B_SPLINE_CURVE_WITH_KNOTS((3,3),(0.249954652430651,0.256253455718071),
 .UNSPECIFIED.)
CURVE()
GEOMETRIC_REPRESENTATION_ITEM()
RATIONAL_B_SPLINE_CURVE((1.11971735964609,1.12024119946955,1.12071541658431))
REPRESENTATION_ITEM('')
);
#852=(
BOUNDED_CURVE()
B_SPLINE_CURVE(2,(#52710,#52711,#52712),.UNSPECIFIED.,.F.,.F.)
B_SPLINE_CURVE_WITH_KNOTS((3,3),(0.376641898803537,0.382940702095949),
 .UNSPECIFIED.)
CURVE()
GEOMETRIC_REPRESENTATION_ITEM()
RATIONAL_B_SPLINE_CURVE((1.12071541658424,1.1202411994691,1.11971735964519))
REPRESENTATION_ITEM('')
);
#853=(
BOUNDED_CURVE()
B_SPLINE_CURVE(2,(#52715,#52716,#52717),.UNSPECIFIED.,.F.,.F.)
B_SPLINE_CURVE_WITH_KNOTS((3,3),(0.249954652430663,0.256253455718077),
 .UNSPECIFIED.)
CURVE()
GEOMETRIC_REPRESENTATION_ITEM()
RATIONAL_B_SPLINE_CURVE((1.11971735964627,1.12024119946974,1.1207154165845))
REPRESENTATION_ITEM('')
);
#854=(
BOUNDED_CURVE()
B_SPLINE_CURVE(2,(#52719,#52720,#52721),.UNSPECIFIED.,.F.,.F.)
B_SPLINE_CURVE_WITH_KNOTS((3,3),(0.376641898803535,0.382940702095948),
 .UNSPECIFIED.)
CURVE()
GEOMETRIC_REPRESENTATION_ITEM()
RATIONAL_B_SPLINE_CURVE((1.12071541658433,1.1202411994692,1.11971735964528))
REPRESENTATION_ITEM('')
);
#855=(
BOUNDED_CURVE()
B_SPLINE_CURVE(2,(#52724,#52725,#52726),.UNSPECIFIED.,.F.,.F.)
B_SPLINE_CURVE_WITH_KNOTS((3,3),(0.249954652430657,0.256253455718068),
 .UNSPECIFIED.)
CURVE()
GEOMETRIC_REPRESENTATION_ITEM()
RATIONAL_B_SPLINE_CURVE((1.11971735964623,1.1202411994697,1.12071541658445))
REPRESENTATION_ITEM('')
);
#856=(
BOUNDED_CURVE()
B_SPLINE_CURVE(2,(#52728,#52729,#52730),.UNSPECIFIED.,.F.,.F.)
B_SPLINE_CURVE_WITH_KNOTS((3,3),(0.376641898803534,0.382940702095946),
 .UNSPECIFIED.)
CURVE()
GEOMETRIC_REPRESENTATION_ITEM()
RATIONAL_B_SPLINE_CURVE((1.12071541658428,1.12024119946915,1.11971735964523))
REPRESENTATION_ITEM('')
);
#857=(
BOUNDED_CURVE()
B_SPLINE_CURVE(2,(#52734,#52735,#52736),.UNSPECIFIED.,.F.,.F.)
B_SPLINE_CURVE_WITH_KNOTS((3,3),(0.249954652430652,0.256253455718065),
 .UNSPECIFIED.)
CURVE()
GEOMETRIC_REPRESENTATION_ITEM()
RATIONAL_B_SPLINE_CURVE((1.11971735964615,1.12024119946961,1.12071541658437))
REPRESENTATION_ITEM('')
);
#858=(
BOUNDED_CURVE()
B_SPLINE_CURVE(2,(#52740,#52741,#52742),.UNSPECIFIED.,.F.,.F.)
B_SPLINE_CURVE_WITH_KNOTS((3,3),(0.376641898803528,0.38294070209594),
 .UNSPECIFIED.)
CURVE()
GEOMETRIC_REPRESENTATION_ITEM()
RATIONAL_B_SPLINE_CURVE((1.12071541658438,1.12024119946925,1.11971735964533))
REPRESENTATION_ITEM('')
);
#859=(
BOUNDED_CURVE()
B_SPLINE_CURVE(2,(#52746,#52747,#52748),.UNSPECIFIED.,.F.,.F.)
B_SPLINE_CURVE_WITH_KNOTS((3,3),(0.249954652430646,0.256253455718057),
 .UNSPECIFIED.)
CURVE()
GEOMETRIC_REPRESENTATION_ITEM()
RATIONAL_B_SPLINE_CURVE((1.11971735964604,1.12024119946951,1.12071541658426))
REPRESENTATION_ITEM('')
);
#860=(
BOUNDED_CURVE()
B_SPLINE_CURVE(2,(#52752,#52753,#52754),.UNSPECIFIED.,.F.,.F.)
B_SPLINE_CURVE_WITH_KNOTS((3,3),(0.376641898803525,0.382940702095939),
 .UNSPECIFIED.)
CURVE()
GEOMETRIC_REPRESENTATION_ITEM()
RATIONAL_B_SPLINE_CURVE((1.12071541658443,1.1202411994693,1.11971735964538))
REPRESENTATION_ITEM('')
);
#861=(
BOUNDED_CURVE()
B_SPLINE_CURVE(2,(#52758,#52759,#52760),.UNSPECIFIED.,.F.,.F.)
B_SPLINE_CURVE_WITH_KNOTS((3,3),(0.249954652430639,0.256253455718051),
 .UNSPECIFIED.)
CURVE()
GEOMETRIC_REPRESENTATION_ITEM()
RATIONAL_B_SPLINE_CURVE((1.11971735964598,1.12024119946945,1.1207154165842))
REPRESENTATION_ITEM('')
);
#862=(
BOUNDED_CURVE()
B_SPLINE_CURVE(2,(#52764,#52765,#52766),.UNSPECIFIED.,.F.,.F.)
B_SPLINE_CURVE_WITH_KNOTS((3,3),(0.376641898803521,0.382940702095934),
 .UNSPECIFIED.)
CURVE()
GEOMETRIC_REPRESENTATION_ITEM()
RATIONAL_B_SPLINE_CURVE((1.12071541658441,1.12024119946928,1.11971735964536))
REPRESENTATION_ITEM('')
);
#863=(
BOUNDED_CURVE()
B_SPLINE_CURVE(2,(#52770,#52771,#52772),.UNSPECIFIED.,.F.,.F.)
B_SPLINE_CURVE_WITH_KNOTS((3,3),(0.249954652430652,0.256253455718065),
 .UNSPECIFIED.)
CURVE()
GEOMETRIC_REPRESENTATION_ITEM()
RATIONAL_B_SPLINE_CURVE((1.11971735964616,1.12024119946962,1.12071541658438))
REPRESENTATION_ITEM('')
);
#864=(
BOUNDED_CURVE()
B_SPLINE_CURVE(2,(#52776,#52777,#52778),.UNSPECIFIED.,.F.,.F.)
B_SPLINE_CURVE_WITH_KNOTS((3,3),(0.376641898803544,0.382940702095957),
 .UNSPECIFIED.)
CURVE()
GEOMETRIC_REPRESENTATION_ITEM()
RATIONAL_B_SPLINE_CURVE((1.12071541658424,1.1202411994691,1.11971735964518))
REPRESENTATION_ITEM('')
);
#865=(
BOUNDED_CURVE()
B_SPLINE_CURVE(2,(#52782,#52783,#52784),.UNSPECIFIED.,.F.,.F.)
B_SPLINE_CURVE_WITH_KNOTS((3,3),(0.249954652430643,0.256253455718053),
 .UNSPECIFIED.)
CURVE()
GEOMETRIC_REPRESENTATION_ITEM()
RATIONAL_B_SPLINE_CURVE((1.11971735964601,1.12024119946947,1.12071541658423))
REPRESENTATION_ITEM('')
);
#866=(
BOUNDED_CURVE()
B_SPLINE_CURVE(2,(#52788,#52789,#52790),.UNSPECIFIED.,.F.,.F.)
B_SPLINE_CURVE_WITH_KNOTS((3,3),(0.376641898803543,0.382940702095953),
 .UNSPECIFIED.)
CURVE()
GEOMETRIC_REPRESENTATION_ITEM()
RATIONAL_B_SPLINE_CURVE((1.12071541658425,1.12024119946911,1.1197173596452))
REPRESENTATION_ITEM('')
);
#867=(
BOUNDED_CURVE()
B_SPLINE_CURVE(2,(#52794,#52795,#52796),.UNSPECIFIED.,.F.,.F.)
B_SPLINE_CURVE_WITH_KNOTS((3,3),(0.249954652430649,0.256253455718062),
 .UNSPECIFIED.)
CURVE()
GEOMETRIC_REPRESENTATION_ITEM()
RATIONAL_B_SPLINE_CURVE((1.11971735964607,1.12024119946954,1.12071541658429))
REPRESENTATION_ITEM('')
);
#1522=ELLIPSE('',#32268,0.0195162536838815,0.0137573643715162);
#1523=ELLIPSE('',#32269,0.0195162536830269,0.0137573643713391);
#1524=ELLIPSE('',#32271,0.0195162536835621,0.0137573643714695);
#1525=ELLIPSE('',#32272,0.019516253683001,0.0137573643713521);
#1526=ELLIPSE('',#32274,0.0195162536836977,0.0137573643714721);
#1527=ELLIPSE('',#32275,0.0195162536830636,0.0137573643713535);
#1528=ELLIPSE('',#32277,0.0195162536837443,0.0137573643714943);
#1529=ELLIPSE('',#32278,0.0195162536831223,0.0137573643713688);
#1530=ELLIPSE('',#32280,0.019516253683803,0.013757364371504);
#1531=ELLIPSE('',#32281,0.0195162536829111,0.0137573643713217);
#1532=ELLIPSE('',#32283,0.0195162536837688,0.0137573643714986);
#1533=ELLIPSE('',#32284,0.0195162536830749,0.0137573643713556);
#1534=ELLIPSE('',#32286,0.0195162536837257,0.0137573643714922);
#1535=ELLIPSE('',#32287,0.0195162536830703,0.0137573643713494);
#1536=ELLIPSE('',#32289,0.0195162536838104,0.013757364371505);
#1537=ELLIPSE('',#32290,0.0195162536830614,0.0137573643713493);
#1538=ELLIPSE('',#32292,0.0195162536837473,0.0137573643714877);
#1539=ELLIPSE('',#32293,0.0195162536830537,0.0137573643713548);
#1540=ELLIPSE('',#32295,0.0195162536838422,0.0137573643715182);
#1541=ELLIPSE('',#32296,0.0195162536831755,0.0137573643713807);
#1542=ELLIPSE('',#32298,0.0195162536837639,0.0137573643714952);
#1543=ELLIPSE('',#32299,0.0195162536830792,0.0137573643713542);
#1544=ELLIPSE('',#32301,0.0195162536835653,0.0137573643714501);
#1545=ELLIPSE('',#32302,0.0195162536831025,0.0137573643713567);
#1546=ELLIPSE('',#32304,0.0195162536835776,0.0137573643714587);
#1547=ELLIPSE('',#32305,0.0195162536828947,0.01375736437132);
#1548=ELLIPSE('',#32307,0.0195162536837483,0.0137573643714995);
#1549=ELLIPSE('',#32308,0.0195162536831204,0.0137573643713664);
#1550=ELLIPSE('',#32310,0.0195162536835793,0.0137573643714601);
#1551=ELLIPSE('',#32311,0.0195162536830448,0.0137573643713492);
#1552=ELLIPSE('',#32320,0.0195034997306777,0.013754915723726);
#1553=ELLIPSE('',#32322,0.0195030685020683,0.0137548403891227);
#1554=ELLIPSE('',#32324,0.0195027524929284,0.0137547851848027);
#1555=ELLIPSE('',#32326,0.0195025132809572,0.0137547433941177);
#1556=ELLIPSE('',#32328,0.0195023280193677,0.0137547110253133);
#1557=ELLIPSE('',#32330,0.0195021823053853,0.0137546855626127);
#1558=ELLIPSE('',#32332,0.0195020666474465,0.0137546653482711);
#1559=ELLIPSE('',#32334,0.0195019745733047,0.0137546492518586);
#1560=ELLIPSE('',#32336,0.0195019015620118,0.0137546364836367);
#1561=ELLIPSE('',#32338,0.0195018443987318,0.0137546264818649);
#1562=ELLIPSE('',#32340,0.0195018007910573,0.0137546188457545);
#1563=ELLIPSE('',#32342,0.0195017691158091,0.0137546132912077);
#1564=ELLIPSE('',#32344,0.0195017482624769,0.0137546096234092);
#1565=ELLIPSE('',#32346,0.0195017375337946,0.0137546077193674);
#1566=ELLIPSE('',#32348,0.0195017365885567,0.0137546075177427);
#1567=ELLIPSE('',#32350,0.0195017454175912,0.0137546090143427);
#1568=ELLIPSE('',#32352,0.0195017643506138,0.0137546122627749);
#1569=ELLIPSE('',#32354,0.0195017941005044,0.0137546173811011);
#1570=ELLIPSE('',#32356,0.0195018358641676,0.0137546245672221);
#1571=ELLIPSE('',#32358,0.0195018727625836,0.013754631431718);
#1572=ELLIPSE('',#32360,0.0195034997306828,0.0137549157237274);
#1573=ELLIPSE('',#32362,0.0195030685021256,0.0137548403891337);
#1574=ELLIPSE('',#32364,0.0195027524929019,0.0137547851847966);
#1575=ELLIPSE('',#32366,0.0195025132809425,0.0137547433941156);
#1576=ELLIPSE('',#32368,0.0195023280193708,0.0137547110253143);
#1577=ELLIPSE('',#32370,0.0195021823053841,0.0137546855626124);
#1578=ELLIPSE('',#32372,0.0195020666474398,0.0137546653482691);
#1579=ELLIPSE('',#32374,0.0195019745733335,0.0137546492518631);
#1580=ELLIPSE('',#32376,0.0195019015619959,0.0137546364836322);
#1581=ELLIPSE('',#32378,0.0195018443987879,0.0137546264818748);
#1582=ELLIPSE('',#32380,0.0195018007910457,0.0137546188457536);
#1583=ELLIPSE('',#32382,0.0195017691158159,0.0137546132912084);
#1584=ELLIPSE('',#32384,0.0195017482624727,0.013754609623408);
#1585=ELLIPSE('',#32386,0.0195017375337736,0.0137546077193644);
#1586=ELLIPSE('',#32388,0.0195017365885347,0.0137546075177382);
#1587=ELLIPSE('',#32390,0.019501745417596,0.0137546090143437);
#1588=ELLIPSE('',#32392,0.0195017643505816,0.0137546122627688);
#1589=ELLIPSE('',#32394,0.0195017941005605,0.0137546173811125);
#1590=ELLIPSE('',#32396,0.019501835864167,0.0137546245672222);
#1591=ELLIPSE('',#32398,0.0195162536830855,0.0137573643713537);
#1592=ELLIPSE('',#32400,0.0195034997307414,0.013754915723739);
#1593=ELLIPSE('',#32402,0.0195030685021161,0.0137548403891323);
#1594=ELLIPSE('',#32404,0.0195027524929008,0.0137547851847961);
#1595=ELLIPSE('',#32406,0.0195025132809546,0.0137547433941189);
#1596=ELLIPSE('',#32408,0.0195023280193482,0.0137547110253084);
#1597=ELLIPSE('',#32425,0.0195034997306463,0.0137549157237206);
#1598=ELLIPSE('',#32427,0.0195030685021557,0.0137548403891397);
#1599=ELLIPSE('',#32429,0.0195027524928776,0.0137547851847918);
#1600=ELLIPSE('',#32431,0.0195025132809776,0.0137547433941213);
#1601=ELLIPSE('',#32433,0.019502328019347,0.0137547110253081);
#1602=ELLIPSE('',#32435,0.0195021823053738,0.0137546855626116);
#1603=ELLIPSE('',#32437,0.0195020666474525,0.0137546653482711);
#1604=ELLIPSE('',#32439,0.0195019745733739,0.013754649251872);
#1605=ELLIPSE('',#32441,0.0195019015619764,0.0137546364836293);
#1606=ELLIPSE('',#32443,0.0195018443987816,0.0137546264818739);
#1607=ELLIPSE('',#32445,0.0195018007910337,0.0137546188457504);
#1608=ELLIPSE('',#32447,0.0195017691158341,0.0137546132912121);
#1609=ELLIPSE('',#32449,0.0195017482624509,0.0137546096234037);
#1610=ELLIPSE('',#32451,0.0195017375337853,0.0137546077193653);
#1611=ELLIPSE('',#32453,0.0195017365886309,0.0137546075177561);
#1612=ELLIPSE('',#32455,0.0195017454176055,0.0137546090143461);
#1613=ELLIPSE('',#32457,0.0195017643505986,0.0137546122627731);
#1614=ELLIPSE('',#32459,0.0195017941005311,0.0137546173811059);
#1615=ELLIPSE('',#32461,0.0195018358641241,0.0137546245672129);
#1616=ELLIPSE('',#32465,0.0195034997306858,0.0137549157237271);
#1617=ELLIPSE('',#32467,0.0195030685021635,0.0137548403891432);
#1618=ELLIPSE('',#32469,0.019502752492881,0.0137547851847926);
#1619=ELLIPSE('',#32471,0.0195025132809236,0.0137547433941134);
#1620=ELLIPSE('',#32473,0.0195023280193679,0.0137547110253125);
#1621=ELLIPSE('',#32475,0.0195021823054267,0.0137546855626225);
#1622=ELLIPSE('',#32477,0.0195020666474927,0.0137546653482813);
#1623=ELLIPSE('',#32479,0.019501974573308,0.0137546492518591);
#1624=ELLIPSE('',#32481,0.0195019015619601,0.0137546364836262);
#1625=ELLIPSE('',#32483,0.0195018443987825,0.0137546264818736);
#1626=ELLIPSE('',#32485,0.0195018007910841,0.0137546188457617);
#1627=ELLIPSE('',#32487,0.0195017691158046,0.0137546132912069);
#1628=ELLIPSE('',#32489,0.0195017482624746,0.0137546096234107);
#1629=ELLIPSE('',#32491,0.0195017375337627,0.0137546077193623);
#1630=ELLIPSE('',#32493,0.0195017365885639,0.0137546075177438);
#1631=ELLIPSE('',#32495,0.0195017454175912,0.0137546090143448);
#1632=ELLIPSE('',#32497,0.0195017643506125,0.0137546122627745);
#1633=ELLIPSE('',#32499,0.0195017941005712,0.0137546173811145);
#1634=ELLIPSE('',#32501,0.0195018358641553,0.013754624567221);
#1635=ELLIPSE('',#32503,0.0195018727626295,0.0137546314317287);
#1636=ELLIPSE('',#32505,0.0195034997307231,0.0137549157237351);
#1637=ELLIPSE('',#32507,0.0195030685021692,0.0137548403891432);
#1638=ELLIPSE('',#32509,0.0195027524928953,0.013754785184795);
#1639=ELLIPSE('',#32511,0.0195025132809505,0.0137547433941165);
#1640=ELLIPSE('',#32513,0.0195023280194302,0.0137547110253254);
#1641=ELLIPSE('',#32515,0.019502182305463,0.0137546855626286);
#1642=ELLIPSE('',#32517,0.0195020666474861,0.0137546653482797);
#1643=ELLIPSE('',#32519,0.0195019745732981,0.0137546492518571);
#1644=ELLIPSE('',#32521,0.019501901562003,0.0137546364836345);
#1645=ELLIPSE('',#32523,0.0195018443988218,0.0137546264818824);
#1646=ELLIPSE('',#32525,0.0195018007911448,0.0137546188457728);
#1647=ELLIPSE('',#32527,0.0195017691157916,0.0137546132912057);
#1648=ELLIPSE('',#32529,0.0195017482624564,0.013754609623407);
#1649=ELLIPSE('',#32531,0.0195017375338029,0.0137546077193704);
#1650=ELLIPSE('',#32533,0.0195017365886144,0.0137546075177533);
#1651=ELLIPSE('',#32535,0.0195017454176306,0.0137546090143512);
#1652=ELLIPSE('',#32537,0.0195017643505891,0.0137546122627708);
#1653=ELLIPSE('',#32539,0.0195017941005193,0.013754617381105);
#1654=ELLIPSE('',#32541,0.0195018358642213,0.0137546245672329);
#1655=ELLIPSE('',#32543,0.0195162536837232,0.0137573643714884);
#1656=ELLIPSE('',#32545,0.0195034997306679,0.0137549157237246);
#1657=ELLIPSE('',#32547,0.0195030685021047,0.0137548403891311);
#1658=ELLIPSE('',#32549,0.0195027524929266,0.0137547851848028);
#1659=ELLIPSE('',#32551,0.0195025132809874,0.0137547433941253);
#1660=ELLIPSE('',#32553,0.0195023280194086,0.013754711025321);
#1661=ELLIPSE('',#32555,0.0195021823054203,0.0137546855626212);
#1662=ELLIPSE('',#32557,0.0195020666475111,0.0137546653482846);
#1663=ELLIPSE('',#32559,0.0195019745733549,0.0137546492518684);
#1664=ELLIPSE('',#32561,0.0195019015619592,0.0137546364836273);
#1665=ELLIPSE('',#32563,0.0195018443988324,0.0137546264818843);
#1666=ELLIPSE('',#32565,0.0195018007910703,0.0137546188457585);
#1667=ELLIPSE('',#32567,0.0195017691158645,0.0137546132912193);
#1668=ELLIPSE('',#32569,0.0195017482624579,0.0137546096234066);
#1669=ELLIPSE('',#32571,0.0195017375338027,0.0137546077193706);
#1670=ELLIPSE('',#32573,0.0195017365886083,0.0137546075177516);
#1671=ELLIPSE('',#32575,0.019501745417535,0.0137546090143326);
#1672=ELLIPSE('',#32577,0.0195017643506093,0.0137546122627733);
#1673=ELLIPSE('',#32579,0.0195017941005168,0.013754617381103);
#1674=ELLIPSE('',#32581,0.0195018358640787,0.0137546245672056);
#1675=ELLIPSE('',#32598,0.0195017365886013,0.0137546075177502);
#1676=ELLIPSE('',#32600,0.0195017454175941,0.0137546090143434);
#1677=ELLIPSE('',#32602,0.0195017643505789,0.0137546122627681);
#1678=ELLIPSE('',#32604,0.0195017941005255,0.0137546173811058);
#1679=ELLIPSE('',#32606,0.0195018358641318,0.0137546245672154);
#1680=ELLIPSE('',#32622,0.051274964768551,0.0469971417993774);
#1681=ELLIPSE('',#32624,0.0512707788579671,0.0469842741354326);
#1682=ELLIPSE('',#32626,0.0512707788562332,0.0469842741344865);
#1683=ELLIPSE('',#32627,0.0512749647685533,0.0469971417993787);
#1684=ELLIPSE('',#32630,0.0512707788571307,0.0469842741349983);
#1685=ELLIPSE('',#32631,0.0512749647672664,0.0469971417987026);
#1686=ELLIPSE('',#32634,0.0512707788571389,0.0469842741349856);
#1687=ELLIPSE('',#32635,0.0512749647681367,0.0469971417991575);
#1688=ELLIPSE('',#32638,0.0512707788569124,0.0469842741348335);
#1689=ELLIPSE('',#32639,0.051274964768467,0.0469971417993732);
#1690=ELLIPSE('',#32642,0.051270778857559,0.0469842741351648);
#1691=ELLIPSE('',#32643,0.0512749647697504,0.0469971418000396);
#1692=ELLIPSE('',#32646,0.051270778857562,0.0469842741352078);
#1693=ELLIPSE('',#32647,0.0512749647676798,0.0469971417989218);
#1694=ELLIPSE('',#32650,0.0512707788610954,0.0469842741371193);
#1695=ELLIPSE('',#32651,0.0512749647674827,0.0469971417988075);
#1696=ELLIPSE('',#32654,0.0512707788555596,0.0469842741341208);
#1697=ELLIPSE('',#32655,0.0512749647677061,0.0469971417989105);
#1698=ELLIPSE('',#32658,0.0512707788650729,0.0469842741392919);
#1699=ELLIPSE('',#32659,0.0512749647702881,0.0469971418003199);
#1700=ELLIPSE('',#32662,0.0512707788560203,0.0469842741343728);
#1701=ELLIPSE('',#32663,0.0512749647689969,0.0469971417996401);
#1702=ELLIPSE('',#32666,0.0512707788567884,0.046984274134799);
#1703=ELLIPSE('',#32667,0.0512749647681247,0.0469971417991492);
#1704=ELLIPSE('',#32670,0.0512707788573083,0.0469842741350659);
#1705=ELLIPSE('',#32671,0.0512749647690658,0.0469971417996437);
#1706=ELLIPSE('',#32674,0.0512707788615306,0.046984274137359);
#1707=ELLIPSE('',#32675,0.051274964767619,0.0469971417988856);
#1708=ELLIPSE('',#32678,0.0512707788928482,0.0469842741544496);
#1709=ELLIPSE('',#32679,0.0512749647695684,0.0469971417999069);
#1710=ELLIPSE('',#32682,0.051270778857717,0.0469842741353091);
#1711=ELLIPSE('',#32683,0.0512749647683041,0.0469971417992544);
#1712=ELLIPSE('',#32686,0.051270778855901,0.046984274134278);
#1713=ELLIPSE('',#32687,0.0512749647692079,0.0469971417997307);
#1714=ELLIPSE('',#32690,0.0512707788585063,0.0469842741357279);
#1715=ELLIPSE('',#32691,0.0512749647681597,0.0469971417991513);
#1716=ELLIPSE('',#32694,0.0512707788568602,0.0469842741348085);
#1717=ELLIPSE('',#32695,0.0512749647674443,0.0469971417987893);
#1718=ELLIPSE('',#32698,0.0512707788568387,0.0469842741347804);
#1719=ELLIPSE('',#32699,0.0512749647678151,0.0469971417990189);
#1720=ELLIPSE('',#32702,0.0512707788582789,0.0469842741356006);
#1721=ELLIPSE('',#32703,0.05127496476906,0.0469971417996405);
#1722=ELLIPSE('',#32706,0.051270778856965,0.0469842741348763);
#1723=ELLIPSE('',#32707,0.0512749647686908,0.046997141799481);
#1724=ELLIPSE('',#32710,0.0512707788563555,0.0469842741344815);
#1725=ELLIPSE('',#32711,0.0512749647673275,0.0469971417987118);
#1726=ELLIPSE('',#32714,0.0512707788571547,0.0469842741350112);
#1727=ELLIPSE('',#32715,0.0512749647685426,0.046997141799397);
#1728=ELLIPSE('',#32718,0.0512707788556612,0.0469842741341707);
#1729=ELLIPSE('',#32719,0.0512749647699517,0.0469971418001559);
#1730=ELLIPSE('',#32722,0.0512707788576472,0.0469842741352346);
#1731=ELLIPSE('',#32723,0.0512749647672529,0.0469971417986806);
#1732=ELLIPSE('',#32726,0.0512707788618793,0.0469842741375491);
#1733=ELLIPSE('',#32727,0.0512749647679756,0.0469971417990623);
#1734=ELLIPSE('',#32730,0.0512707788555002,0.0469842741340957);
#1735=ELLIPSE('',#32731,0.0512749647688844,0.046997141799544);
#1736=ELLIPSE('',#32734,0.0512707788566344,0.0469842741346946);
#1737=ELLIPSE('',#32735,0.051274964769648,0.046997141799953);
#1738=ELLIPSE('',#32738,0.0512707788584597,0.0469842741356599);
#1739=ELLIPSE('',#32739,0.0512749647679757,0.0469971417990702);
#1740=ELLIPSE('',#32742,0.0512707788568172,0.0469842741347837);
#1741=ELLIPSE('',#32743,0.051274964767697,0.0469971417989173);
#1742=ELLIPSE('',#32746,0.0512707788670663,0.0469842741404324);
#1743=ELLIPSE('',#32747,0.0512749647689531,0.0469971417995761);
#1744=ELLIPSE('',#32750,0.0512707788557115,0.0469842741341769);
#1745=ELLIPSE('',#32751,0.0512749647694815,0.0469971417999415);
#1746=ELLIPSE('',#32754,0.0512707788568934,0.0469842741348491);
#1747=ELLIPSE('',#32755,0.0512749647661315,0.0469971417980767);
#1748=ELLIPSE('',#32758,0.0512707788572177,0.0469842741350563);
#1749=ELLIPSE('',#32759,0.0512749647680353,0.0469971417991282);
#1750=ELLIPSE('',#32762,0.0512707788587383,0.046984274135853);
#1751=ELLIPSE('',#32763,0.0512749647684727,0.0469971417993084);
#1752=ELLIPSE('',#32766,0.0512707788631157,0.0469842741382362);
#1753=ELLIPSE('',#32767,0.0512749647685272,0.0469971417993756);
#1754=ELLIPSE('',#32770,0.0512707788564907,0.0469842741346169);
#1755=ELLIPSE('',#32771,0.0512749647685682,0.0469971417994032);
#1756=ELLIPSE('',#32774,0.0512707788585969,0.0469842741357701);
#1757=ELLIPSE('',#32775,0.0512749647676235,0.0469971417988947);
#1758=ELLIPSE('',#32778,0.0512707788751318,0.0469842741447984);
#1759=ELLIPSE('',#32779,0.0512749647678178,0.0469971417990053);
#1760=ELLIPSE('',#32782,0.0512707788575899,0.0469842741352132);
#1761=ELLIPSE('',#32783,0.0512749647677413,0.0469971417989442);
#1762=ELLIPSE('',#32786,0.0512707788579549,0.0469842741354182);
#1763=ELLIPSE('',#32787,0.0512749647704146,0.0469971418003949);
#1764=ELLIPSE('',#32790,0.0512707788581164,0.0469842741355277);
#1765=ELLIPSE('',#32791,0.0512749647678976,0.0469971417990442);
#1766=ELLIPSE('',#32794,0.0512707788570414,0.0469842741348829);
#1767=ELLIPSE('',#32795,0.0512749647696248,0.0469971417999634);
#1768=ELLIPSE('',#32798,0.0512707789395351,0.0469842741799766);
#1769=ELLIPSE('',#32799,0.0512749647687745,0.0469971417995203);
#1770=ELLIPSE('',#32802,0.0512707788562593,0.0469842741344864);
#1771=ELLIPSE('',#32803,0.0512749647684955,0.046997141799316);
#1772=ELLIPSE('',#32806,0.0512707788603725,0.0469842741367327);
#1773=ELLIPSE('',#32807,0.0512749647690289,0.0469971417996681);
#1774=ELLIPSE('',#32810,0.0512707788577797,0.0469842741353011);
#1775=ELLIPSE('',#32811,0.0512749647683414,0.0469971417992803);
#1776=ELLIPSE('',#32814,0.051270778856875,0.0469842741348193);
#1777=ELLIPSE('',#32815,0.0512749647684586,0.0469971417993373);
#1778=ELLIPSE('',#32818,0.051270778920832,0.0469842741697548);
#1779=ELLIPSE('',#32819,0.0512749647689089,0.0469971417995588);
#1780=ELLIPSE('',#32822,0.0512707788568015,0.0469842741347871);
#1781=ELLIPSE('',#32823,0.0512749647679381,0.0469971417990666);
#1782=ELLIPSE('',#32826,0.0512707788566487,0.046984274134668);
#1783=ELLIPSE('',#32827,0.0512749647684683,0.0469971417993365);
#1784=ELLIPSE('',#32830,0.051270778856618,0.0469842741346731);
#1785=ELLIPSE('',#32831,0.0512749647693393,0.0469971417998184);
#1786=ELLIPSE('',#32834,0.0512707788568358,0.0469842741348282);
#1787=ELLIPSE('',#32835,0.0512749647674564,0.0469971417987839);
#1788=ELLIPSE('',#32838,0.0512707788557633,0.0469842741342339);
#1789=ELLIPSE('',#32839,0.0512749647690638,0.0469971417996539);
#1790=ELLIPSE('',#32842,0.0512707788566786,0.0469842741346996);
#1791=ELLIPSE('',#32843,0.0512749647672967,0.0469971417987006);
#1792=ELLIPSE('',#32846,0.0512707788621377,0.0469842741376985);
#1793=ELLIPSE('',#32847,0.0512749647686591,0.046997141799446);
#1794=ELLIPSE('',#32850,0.0512707788564809,0.0469842741346051);
#1795=ELLIPSE('',#32851,0.0512749647682497,0.0469971417992212);
#1796=ELLIPSE('',#32854,0.0512707788573564,0.0469842741350646);
#1797=ELLIPSE('',#32855,0.0512749647687658,0.0469971417994997);
#1798=ELLIPSE('',#32858,0.051270778874813,0.0469842741446368);
#1799=ELLIPSE('',#32859,0.0512749647675386,0.046997141798832);
#1800=ELLIPSE('',#32862,0.0512707788565269,0.0469842741346491);
#1801=ELLIPSE('',#32863,0.0512749647691996,0.0469971417997275);
#1802=ELLIPSE('',#32866,0.0512707788580797,0.0469842741354721);
#1803=ELLIPSE('',#32867,0.0512749647681002,0.0469971417991393);
#1804=ELLIPSE('',#32870,0.0512707788579047,0.0469842741354009);
#1805=ELLIPSE('',#32871,0.0512749647678865,0.0469971417990283);
#1806=ELLIPSE('',#32874,0.0512707788574115,0.046984274135125);
#1807=ELLIPSE('',#32875,0.0512749647671369,0.0469971417986091);
#1808=ELLIPSE('',#32878,0.0512749647690318,0.0469971417996552);
#1809=ELLIPSE('',#32880,0.0512707788566348,0.0469842741346708);
#1810=ELLIPSE('',#32882,0.0512749647679538,0.0469971417990534);
#1811=ELLIPSE('',#32884,0.0512707788562212,0.0469842741344524);
#1812=ELLIPSE('',#32886,0.051274964768521,0.0469971417993772);
#1813=ELLIPSE('',#32888,0.051270778856042,0.0469842741343731);
#1814=ELLIPSE('',#32890,0.0512749647675581,0.0469971417988677);
#1815=ELLIPSE('',#32892,0.0512707788559885,0.0469842741343514);
#1816=ELLIPSE('',#32894,0.0512749647693218,0.0469971417997968);
#1817=ELLIPSE('',#32896,0.0512707788571387,0.0469842741349643);
#1818=ELLIPSE('',#32898,0.0512749647679417,0.0469971417990759);
#1819=ELLIPSE('',#32900,0.0512707788922353,0.0469842741541131);
#1820=ELLIPSE('',#32902,0.051274964769059,0.046997141799664);
#1821=ELLIPSE('',#32904,0.0512707788612464,0.0469842741372165);
#1822=ELLIPSE('',#32906,0.0512749647686166,0.0469971417994078);
#1823=ELLIPSE('',#32908,0.0512707788558472,0.0469842741342397);
#1824=ELLIPSE('',#32910,0.0512749647686363,0.0469971417994427);
#1825=ELLIPSE('',#32912,0.0512707788567449,0.0469842741347651);
#1826=ELLIPSE('',#32914,0.0512749647684367,0.0469971417993216);
#1827=ELLIPSE('',#32916,0.0512707788561666,0.0469842741344253);
#1828=ELLIPSE('',#32918,0.0512749647683517,0.046997141799283);
#1829=ELLIPSE('',#32920,0.0512707788648064,0.0469842741391505);
#1830=ELLIPSE('',#32922,0.0512749647688174,0.0469971417995523);
#1831=ELLIPSE('',#32924,0.051270778857567,0.0469842741352074);
#1832=ELLIPSE('',#32926,0.0512749647694904,0.0469971417998601);
#1833=ELLIPSE('',#32928,0.0512707788575527,0.0469842741351904);
#1834=ELLIPSE('',#32930,0.0512749647677225,0.0469971417989513);
#1835=ELLIPSE('',#32932,0.0512707788585909,0.0469842741357571);
#1836=ELLIPSE('',#32934,0.051270778940575,0.0469842741805314);
#1837=ELLIPSE('',#32935,0.0512749647683344,0.0469971417992899);
#1838=ELLIPSE('',#33096,0.0512707788678624,0.04698427414088);
#1839=ELLIPSE('',#33097,0.0512749647679163,0.0469971417991227);
#1840=ELLIPSE('',#33099,0.0512749647654335,0.0469971417977818);
#1841=ELLIPSE('',#33100,0.0512707788568347,0.0469842741348514);
#1842=ELLIPSE('',#33102,0.0512749647672852,0.0469971417988039);
#1843=ELLIPSE('',#33103,0.0512707788564686,0.0469842741346539);
#1844=ELLIPSE('',#33105,0.0512749647659393,0.0469971417980464);
#1845=ELLIPSE('',#33106,0.0512707788556944,0.0469842741342504);
#1846=ELLIPSE('',#33108,0.0512749647686629,0.0469971417995544);
#1847=ELLIPSE('',#33109,0.0512707788564297,0.0469842741346479);
#1848=ELLIPSE('',#33111,0.0512749647671486,0.0469971417987065);
#1849=ELLIPSE('',#33112,0.0512707788597197,0.0469842741364453);
#1850=ELLIPSE('',#33114,0.0512749647666077,0.0469971417984174);
#1851=ELLIPSE('',#33115,0.0512707788555701,0.0469842741341628);
#1852=ELLIPSE('',#33117,0.0512749647679515,0.0469971417991682);
#1853=ELLIPSE('',#33118,0.0512707788587403,0.0469842741359266);
#1854=ELLIPSE('',#33120,0.0512749647675462,0.0469971417988912);
#1855=ELLIPSE('',#33121,0.0512707788561996,0.0469842741345216);
#1856=ELLIPSE('',#33123,0.0512749647665171,0.0469971417983294);
#1857=ELLIPSE('',#33124,0.0512707788563593,0.0469842741346364);
#1858=ELLIPSE('',#33126,0.0512749647671419,0.0469971417986936);
#1859=ELLIPSE('',#33127,0.0512707788554834,0.0469842741341348);
#1860=ELLIPSE('',#33129,0.0512749647679126,0.0469971417991247);
#1861=ELLIPSE('',#33130,0.0512707788566136,0.0469842741347507);
#1862=ELLIPSE('',#33132,0.051274964765861,0.0469971417980122);
#1863=ELLIPSE('',#33133,0.0512707788569887,0.0469842741349521);
#1864=ELLIPSE('',#33135,0.0512749647673257,0.046997141798794);
#1865=ELLIPSE('',#33136,0.0512707788578384,0.0469842741354011);
#1866=ELLIPSE('',#33138,0.0512749647685051,0.046997141799409);
#1867=ELLIPSE('',#33139,0.0512707788566497,0.0469842741347448);
#1868=ELLIPSE('',#33141,0.0512749647664023,0.0469971417983194);
#1869=ELLIPSE('',#33142,0.0512707788557973,0.0469842741343033);
#1870=ELLIPSE('',#33144,0.0512749647657081,0.0469971417979273);
#1871=ELLIPSE('',#33145,0.0512707788560454,0.0469842741344356);
#1872=ELLIPSE('',#33147,0.0512749647672847,0.0469971417988018);
#1873=ELLIPSE('',#33148,0.0512707788908472,0.0469842741534398);
#1874=ELLIPSE('',#33150,0.0512749647656979,0.0469971417979225);
#1875=ELLIPSE('',#33151,0.0512707788619598,0.0469842741376821);
#1876=ELLIPSE('',#33153,0.0512749647673844,0.0469971417987892);
#1877=ELLIPSE('',#33154,0.0512707788554361,0.0469842741341347);
#1878=ELLIPSE('',#33156,0.0512749647665351,0.0469971417983737);
#1879=ELLIPSE('',#33157,0.051270778857401,0.0469842741351899);
#1880=ELLIPSE('',#33159,0.0512749647648224,0.0469971417974593);
#1881=ELLIPSE('',#33160,0.051270778857135,0.0469842741350546);
#1882=ELLIPSE('',#33162,0.051274964767923,0.046997141799147);
#1883=ELLIPSE('',#33163,0.0512707788632245,0.0469842741383353);
#1884=ELLIPSE('',#33165,0.0512749647670837,0.0469971417986601);
#1885=ELLIPSE('',#33166,0.0512707788575274,0.0469842741352789);
#1886=ELLIPSE('',#33168,0.0512749647661063,0.046997141798163);
#1887=ELLIPSE('',#33169,0.0512707788614728,0.0469842741374068);
#1888=ELLIPSE('',#33171,0.0512749647661745,0.0469971417981727);
#1889=ELLIPSE('',#33172,0.0512707788561374,0.0469842741344828);
#1890=ELLIPSE('',#33174,0.0512749647684627,0.0469971417993818);
#1891=ELLIPSE('',#33175,0.0512707788547222,0.0469842741337518);
#1892=ELLIPSE('',#33177,0.0512749647675423,0.0469971417989238);
#1893=ELLIPSE('',#33178,0.0512707788556497,0.0469842741342235);
#1894=ELLIPSE('',#33180,0.0512749647674664,0.0469971417988657);
#1895=ELLIPSE('',#33181,0.0512707788563694,0.0469842741346094);
#1896=ELLIPSE('',#33183,0.0512749647689012,0.0469971417996608);
#1897=ELLIPSE('',#33184,0.0512707788554915,0.0469842741341037);
#1898=ELLIPSE('',#33186,0.0512749647674053,0.0469971417988339);
#1899=ELLIPSE('',#33187,0.0512707788551391,0.0469842741339346);
#1900=ELLIPSE('',#33189,0.051274964767584,0.046997141798928);
#1901=ELLIPSE('',#33190,0.0512707788578603,0.0469842741354062);
#1902=ELLIPSE('',#33192,0.0512749647667973,0.046997141798492);
#1903=ELLIPSE('',#33193,0.0512707788554342,0.0469842741340614);
#1904=ELLIPSE('',#33195,0.0512749647663277,0.0469971417982546);
#1905=ELLIPSE('',#33196,0.051270778856014,0.0469842741344105);
#1906=ELLIPSE('',#33198,0.0512749647644558,0.0469971417972658);
#1907=ELLIPSE('',#33199,0.051270778856549,0.046984274134693);
#1908=ELLIPSE('',#33201,0.0512749647655728,0.0469971417978321);
#1909=ELLIPSE('',#33202,0.0512707788565064,0.0469842741346634);
#1910=ELLIPSE('',#33204,0.0512749647677657,0.0469971417990299);
#1911=ELLIPSE('',#33205,0.0512707788566898,0.0469842741347819);
#1912=ELLIPSE('',#33207,0.0512749647676116,0.0469971417989766);
#1913=ELLIPSE('',#33208,0.0512707788912617,0.0469842741536714);
#1914=ELLIPSE('',#33210,0.0512749647664018,0.0469971417982991);
#1915=ELLIPSE('',#33211,0.0512707788616718,0.0469842741375278);
#1916=ELLIPSE('',#33213,0.0512749647667201,0.046997141798501);
#1917=ELLIPSE('',#33214,0.0512707788559321,0.046984274134359);
#1918=ELLIPSE('',#33216,0.0512749647688712,0.0469971417996063);
#1919=ELLIPSE('',#33217,0.0512707788570311,0.0469842741349509);
#1920=ELLIPSE('',#33219,0.0512749647675863,0.0469971417989162);
#1921=ELLIPSE('',#33220,0.0512707788563448,0.0469842741345939);
#1922=ELLIPSE('',#33222,0.0512749647671262,0.0469971417987068);
#1923=ELLIPSE('',#33223,0.0512707788650867,0.0469842741393638);
#1924=ELLIPSE('',#33225,0.0512749647686962,0.0469971417995509);
#1925=ELLIPSE('',#33226,0.0512707788567886,0.0469842741348241);
#1926=ELLIPSE('',#33228,0.0512749647672976,0.0469971417987731);
#1927=ELLIPSE('',#33229,0.0512707788570162,0.0469842741349496);
#1928=ELLIPSE('',#33231,0.0512749647667697,0.0469971417984931);
#1929=ELLIPSE('',#33232,0.0512707788584097,0.0469842741357168);
#1930=ELLIPSE('',#33234,0.0512749647672832,0.0469971417987584);
#1931=ELLIPSE('',#33235,0.0512707788570115,0.0469842741349691);
#1932=ELLIPSE('',#33237,0.0512749647672073,0.0469971417987249);
#1933=ELLIPSE('',#33238,0.0512707789405328,0.0469842741805533);
#1934=ELLIPSE('',#33240,0.0512749647662809,0.0469971417982346);
#1935=ELLIPSE('',#33241,0.0512707788564733,0.0469842741346687);
#1936=ELLIPSE('',#33243,0.0512749647659994,0.0469971417980507);
#1937=ELLIPSE('',#33244,0.0512707788571204,0.0469842741349872);
#1938=ELLIPSE('',#33246,0.0512749647671319,0.0469971417987083);
#1939=ELLIPSE('',#33247,0.0512707788566097,0.0469842741347329);
#1940=ELLIPSE('',#33249,0.0512749647668497,0.0469971417985515);
#1941=ELLIPSE('',#33250,0.0512707788560048,0.0469842741344256);
#1942=ELLIPSE('',#33252,0.051274964765999,0.0469971417980718);
#1943=ELLIPSE('',#33253,0.0512707788746663,0.0469842741446355);
#1944=ELLIPSE('',#33255,0.0512749647672519,0.0469971417987563);
#1945=ELLIPSE('',#33256,0.051270778855846,0.0469842741343271);
#1946=ELLIPSE('',#33258,0.0512749647662359,0.0469971417982146);
#1947=ELLIPSE('',#33259,0.0512707788574978,0.0469842741352291);
#1948=ELLIPSE('',#33261,0.0512749647668179,0.0469971417985263);
#1949=ELLIPSE('',#33262,0.0512707788607044,0.0469842741369976);
#1950=ELLIPSE('',#33264,0.0512749647674441,0.0469971417988379);
#1951=ELLIPSE('',#33265,0.0512707788568965,0.0469842741348871);
#1952=ELLIPSE('',#33267,0.0512749647672645,0.0469971417987703);
#1953=ELLIPSE('',#33268,0.0512707788559945,0.0469842741344026);
#1954=ELLIPSE('',#33270,0.0512749647680151,0.0469971417991764);
#1955=ELLIPSE('',#33271,0.0512707788560419,0.04698427413443);
#1956=ELLIPSE('',#33273,0.0512749647667931,0.0469971417984966);
#1957=ELLIPSE('',#33274,0.0512707788563537,0.0469842741346079);
#1958=ELLIPSE('',#33276,0.0512749647674696,0.0469971417988977);
#1959=ELLIPSE('',#33277,0.0512707788571896,0.0469842741350665);
#1960=ELLIPSE('',#33279,0.0512749647673948,0.046997141798837);
#1961=ELLIPSE('',#33280,0.0512707788555549,0.0469842741341569);
#1962=ELLIPSE('',#33282,0.0512749647668783,0.0469971417985539);
#1963=ELLIPSE('',#33283,0.0512707789210852,0.0469842741699459);
#1964=ELLIPSE('',#33285,0.0512749647677305,0.0469971417990099);
#1965=ELLIPSE('',#33286,0.0512707788552415,0.0469842741340032);
#1966=ELLIPSE('',#33288,0.0512707788564181,0.0469842741346374);
#1967=ELLIPSE('',#33289,0.0512749647669761,0.0469971417985938);
#1968=ELLIPSE('',#33291,0.051270778856969,0.0469842741349151);
#1969=ELLIPSE('',#33292,0.0512749647670935,0.046997141798684);
#1970=ELLIPSE('',#33294,0.0512707788562384,0.0469842741345515);
#1971=ELLIPSE('',#33295,0.0512749647675247,0.0469971417988957);
#1972=ELLIPSE('',#33297,0.0512707788573216,0.0469842741351317);
#1973=ELLIPSE('',#33298,0.0512749647668487,0.046997141798569);
#1974=ELLIPSE('',#33300,0.0512707788622439,0.0469842741378278);
#1975=ELLIPSE('',#33301,0.0512749647677751,0.0469971417990674);
#1976=ELLIPSE('',#33303,0.0512707788576837,0.046984274135325);
#1977=ELLIPSE('',#33304,0.0512749647668911,0.0469971417985504);
#1978=ELLIPSE('',#33306,0.0512707788569353,0.0469842741349273);
#1979=ELLIPSE('',#33307,0.0512749647675315,0.0469971417989158);
#1980=ELLIPSE('',#33309,0.0512707788759282,0.0469842741452617);
#1981=ELLIPSE('',#33310,0.0512749647661136,0.0469971417981488);
#1982=ELLIPSE('',#33312,0.0512707788557471,0.0469842741342912);
#1983=ELLIPSE('',#33313,0.051274964767063,0.0469971417986624);
#1984=ELLIPSE('',#33315,0.0512707788562218,0.0469842741345251);
#1985=ELLIPSE('',#33316,0.0512749647674796,0.0469971417988927);
#1986=ELLIPSE('',#33318,0.0512707788562634,0.0469842741345331);
#1987=ELLIPSE('',#33319,0.0512749647672643,0.0469971417987429);
#1988=ELLIPSE('',#33321,0.0512707788550995,0.0469842741339394);
#1989=ELLIPSE('',#33322,0.0512749647667936,0.0469971417984887);
#1990=ELLIPSE('',#33324,0.0512707789393949,0.0469842741799506);
#1991=ELLIPSE('',#33325,0.0512749647666032,0.0469971417983921);
#1992=ELLIPSE('',#33327,0.0512707788579345,0.0469842741354427);
#1993=ELLIPSE('',#33328,0.0512749647659267,0.0469971417980537);
#1994=ELLIPSE('',#33330,0.0512749647694732,0.0469971417999488);
#1995=ELLIPSE('',#33331,0.0512707788565522,0.0469842741347113);
#1996=ELLIPSE('',#33335,0.0512707788554107,0.0469842741340208);
#1997=ELLIPSE('',#33336,0.0512749647674929,0.0469971417988238);
#1998=ELLIPSE('',#33341,0.0512749647664458,0.0469971417983288);
#1999=ELLIPSE('',#33342,0.0512707788586759,0.0469842741358754);
#2956=CONICAL_SURFACE('',#32228,1.17524047358084,0.785398163397443);
#2957=CONICAL_SURFACE('',#32263,1.17524047358084,0.785398163397443);
#2958=CONICAL_SURFACE('',#32312,1.55162884844711,0.78539816339745);
#2959=CONICAL_SURFACE('',#32318,2.73627063036812,0.785398163397448);
#2960=CONICAL_SURFACE('',#32463,2.68872936963188,0.785398163397435);
#2961=CONICAL_SURFACE('',#33351,1732.05080756885,1.04719755119659);
#2974=B_SPLINE_CURVE_WITH_KNOTS('',3,(#46248,#46249,#46250,#46251,#46252,
#46253,#46254,#46255,#46256,#46257,#46258,#46259,#46260,#46261,#46262,#46263,
#46264,#46265,#46266,#46267,#46268,#46269,#46270,#46271,#46272,#46273,#46274,
#46275,#46276,#46277,#46278,#46279,#46280,#46281,#46282,#46283),
 .UNSPECIFIED.,.F.,.F.,(4,2,2,2,2,2,2,2,2,2,2,2,2,2,2,2,2,4),(-0.945073641183675,
-0.895238035194944,-0.83625541046657,-0.779319325111488,-0.719695813140934,
-0.661359932358853,-0.603989382535731,-0.544046656752618,-0.486380595229568,
-0.427463950957105,-0.368285170516134,-0.311258814957492,-0.251615042406746,
-0.193080680180277,-0.135881569867343,-0.0757214675349668,-0.0372079607299379,
-9.99999995143774E-7),.UNSPECIFIED.);
#2975=B_SPLINE_CURVE_WITH_KNOTS('',3,(#46289,#46290,#46291,#46292,#46293,
#46294,#46295,#46296,#46297,#46298,#46299,#46300,#46301,#46302,#46303,#46304,
#46305,#46306,#46307,#46308,#46309,#46310,#46311,#46312,#46313,#46314,#46315,
#46316,#46317,#46318,#46319,#46320,#46321,#46322),.UNSPECIFIED.,.F.,.F.,
(4,2,2,2,2,2,2,2,2,2,2,2,2,2,2,2,4),(-27.258759550315,-27.2281298462553,
-27.1982051538512,-27.1403355656588,-27.0801605899845,-27.0231066733285,
-26.9645639497272,-26.9050010855415,-26.8479917157334,-26.7888070303952,
-26.7302213719406,-26.6725610910419,-26.6126177738291,-26.5554428144319,
-26.4971129260297,-26.4375855046171,-26.4315188069733),.UNSPECIFIED.);
#2976=B_SPLINE_CURVE_WITH_KNOTS('',3,(#46327,#46328,#46329,#46330,#46331,
#46332,#46333,#46334,#46335,#46336,#46337,#46338,#46339,#46340,#46341,#46342,
#46343,#46344,#46345,#46346,#46347,#46348,#46349,#46350,#46351,#46352,#46353,
#46354,#46355,#46356,#46357,#46358,#46359,#46360,#46361,#46362),
 .UNSPECIFIED.,.F.,.F.,(4,2,2,2,2,2,2,2,2,2,2,2,2,2,2,2,2,4),(-1.89025095676006,
-1.83161362612537,-1.77291723413503,-1.71588088128378,-1.65621305093223,
-1.59816806724067,-1.54019307596245,-1.48057902624682,-1.42320721251111,
-1.36315245228605,-1.30433237640506,-1.24738924893859,-1.18775702178512,
-1.12958586526634,-1.07195013380193,-1.0121910944455,-0.954689933605391,
-0.945073641183675),.UNSPECIFIED.);
#2977=B_SPLINE_CURVE_WITH_KNOTS('',3,(#46363,#46364,#46365,#46366,#46367,
#46368,#46369,#46370,#46371,#46372,#46373,#46374,#46375,#46376,#46377,#46378,
#46379,#46380,#46381,#46382,#46383,#46384,#46385,#46386,#46387,#46388,#46389,
#46390,#46391,#46392,#46393,#46394,#46395,#46396,#46397,#46398),
 .UNSPECIFIED.,.F.,.F.,(4,2,2,2,2,2,2,2,2,2,2,2,2,2,2,2,2,4),(-26.4315188069733,
-26.3807149169946,-26.3217404209326,-26.2626652889544,-26.2051855221022,
-26.1454428390691,-26.08804784233,-26.0298996832198,-25.970377539516,-25.9135472636022,
-25.8547523829465,-25.7951046336945,-25.7377721236726,-25.6781939173096,
-25.6204935481626,-25.5624909627037,-25.5029463840743,-25.4881909358829),
 .UNSPECIFIED.);
#2978=B_SPLINE_CURVE_WITH_KNOTS('',3,(#46403,#46404,#46405,#46406,#46407,
#46408,#46409,#46410,#46411,#46412,#46413,#46414,#46415,#46416,#46417,#46418,
#46419,#46420,#46421,#46422,#46423,#46424,#46425,#46426,#46427,#46428,#46429,
#46430,#46431,#46432,#46433,#46434,#46435,#46436,#46437,#46438,#46439,#46440),
 .UNSPECIFIED.,.F.,.F.,(4,2,2,2,2,2,2,2,2,2,2,2,2,2,2,2,2,2,4),(-2.83625896355377,
-2.82853093222041,-2.76886611006394,-2.71046756100465,-2.65308502383756,
-2.59307616772703,-2.5353480705631,-2.47645222776391,-2.41720668492958,
-2.36012338869581,-2.30043449435393,-2.24183347940531,-2.1846099393252,
-2.12437972037366,-2.06645193254166,-2.00798057621261,-1.94850769470731,
-1.89126109663031,-1.89025095676006),.UNSPECIFIED.);
#2979=B_SPLINE_CURVE_WITH_KNOTS('',3,(#46441,#46442,#46443,#46444,#46445,
#46446,#46447,#46448,#46449,#46450,#46451,#46452,#46453,#46454,#46455,#46456,
#46457,#46458,#46459,#46460,#46461,#46462,#46463,#46464,#46465,#46466,#46467,
#46468,#46469,#46470,#46471,#46472,#46473,#46474,#46475,#46476),
 .UNSPECIFIED.,.F.,.F.,(4,2,2,2,2,2,2,2,2,2,2,2,2,2,2,2,2,4),(-25.4881909358829,
-25.4460636732589,-25.3874120918811,-25.3278816537184,-25.2706841301686,
-25.2112575632321,-25.1531186176646,-25.0952452143788,-25.0350644348795,
-24.9780430196917,-24.9194961959997,-24.8599520194551,-24.8029424006809,
-24.7437542679059,-24.6852489172368,-24.6275880933991,-24.5676424609794,
-24.544394043377),.UNSPECIFIED.);
#2980=B_SPLINE_CURVE_WITH_KNOTS('',3,(#46481,#46482,#46483,#46484,#46485,
#46486,#46487,#46488,#46489,#46490,#46491,#46492,#46493,#46494,#46495,#46496,
#46497,#46498,#46499,#46500,#46501,#46502,#46503,#46504,#46505,#46506,#46507,
#46508,#46509,#46510,#46511,#46512,#46513,#46514,#46515,#46516),
 .UNSPECIFIED.,.F.,.F.,(4,2,2,2,2,2,2,2,2,2,2,2,2,2,2,2,2,4),(-3.78192035948685,
-3.76562796298537,-3.70592564973338,-3.6478278361799,-3.5898592957152,-3.53018901929876,
-3.47276427223133,-3.41274694188657,-3.3538687217505,-3.29689298752725,
-3.2372230084892,-3.17899386626536,-3.12135698149028,-3.06153650613278,
-3.00397762776562,-2.94455692608413,-2.88551146939021,-2.83625896355377),
 .UNSPECIFIED.);
#2981=B_SPLINE_CURVE_WITH_KNOTS('',3,(#46517,#46518,#46519,#46520,#46521,
#46522,#46523,#46524,#46525,#46526,#46527,#46528,#46529,#46530,#46531,#46532,
#46533,#46534,#46535,#46536,#46537,#46538,#46539,#46540,#46541,#46542,#46543,
#46544,#46545,#46546,#46547,#46548,#46549,#46550,#46551,#46552),
 .UNSPECIFIED.,.F.,.F.,(4,2,2,2,2,2,2,2,2,2,2,2,2,2,2,2,2,4),(-24.544394043377,
-24.5105131978097,-24.4521827141638,-24.3926780124691,-24.3358195936076,
-24.2768451471733,-24.2178632708879,-24.1603868788961,-24.1006461200198,
-24.0433090290329,-23.9851645307063,-23.9256688814307,-23.8688632830925,
-23.8100726156683,-23.7505272749807,-23.6932025949219,-23.6336311604901,
-23.6014349735858),.UNSPECIFIED.);
#2982=B_SPLINE_CURVE_WITH_KNOTS('',3,(#46557,#46558,#46559,#46560,#46561,
#46562,#46563,#46564,#46565,#46566,#46567,#46568,#46569,#46570,#46571,#46572,
#46573,#46574,#46575,#46576,#46577,#46578,#46579,#46580,#46581,#46582,#46583,
#46584,#46585,#46586,#46587,#46588,#46589,#46590,#46591,#46592),
 .UNSPECIFIED.,.F.,.F.,(4,2,2,2,2,2,2,2,2,2,2,2,2,2,2,2,2,4),(-4.72839430207058,
-4.70337431740566,-4.64331595464347,-4.58554178921411,-4.52667966073054,
-4.4673838894256,-4.41025831032806,-4.35054027250619,-4.29188896156004,
-4.23465469260147,-4.17437122548907,-4.11639389057874,-4.05794278357937,
-3.99841660337735,-3.94111979450562,-3.88143640467257,-3.82268708479341,
-3.78192035948685),.UNSPECIFIED.);
#2983=B_SPLINE_CURVE_WITH_KNOTS('',3,(#46593,#46594,#46595,#46596,#46597,
#46598,#46599,#46600,#46601,#46602,#46603,#46604,#46605,#46606,#46607,#46608,
#46609,#46610,#46611,#46612,#46613,#46614,#46615,#46616,#46617,#46618,#46619,
#46620,#46621,#46622,#46623,#46624,#46625,#46626,#46627,#46628),
 .UNSPECIFIED.,.F.,.F.,(4,2,2,2,2,2,2,2,2,2,2,2,2,2,2,2,2,4),(-23.6014349735858,
-23.5759985868542,-23.5180045036599,-23.458489879113,-23.4016430359386,
-23.3430005479742,-23.2834982736845,-23.226310920464,-23.166893628097,-23.1088378874003,
-23.0509758826866,-22.9908049952875,-22.9338319947597,-22.8752964277514,
-22.8157879004539,-22.7587920199088,-22.6996160282244,-22.6581171675807),
 .UNSPECIFIED.);
#2984=B_SPLINE_CURVE_WITH_KNOTS('',3,(#46633,#46634,#46635,#46636,#46637,
#46638,#46639,#46640,#46641,#46642,#46643,#46644,#46645,#46646,#46647,#46648,
#46649,#46650,#46651,#46652,#46653,#46654,#46655,#46656,#46657,#46658,#46659,
#46660,#46661,#46662,#46663,#46664,#46665,#46666,#46667,#46668),
 .UNSPECIFIED.,.F.,.F.,(4,2,2,2,2,2,2,2,2,2,2,2,2,2,2,2,2,4),(-5.67439159596968,
-5.64047766140835,-5.58076721688331,-5.52330498546526,-5.4633387313466,
-5.40441833910885,-5.34742402529794,-5.28773207490788,-5.22946075409439,
-5.17183622553644,-5.11197061930769,-5.05436969869878,-4.99499338073396,
-4.9359013779351,-4.878890651626,-4.8192004273671,-4.76075532631967,-4.72839430207058),
 .UNSPECIFIED.);
#2985=B_SPLINE_CURVE_WITH_KNOTS('',3,(#46669,#46670,#46671,#46672,#46673,
#46674,#46675,#46676,#46677,#46678,#46679,#46680,#46681,#46682,#46683,#46684,
#46685,#46686,#46687,#46688,#46689,#46690,#46691,#46692,#46693,#46694,#46695,
#46696,#46697,#46698,#46699,#46700,#46701,#46702,#46703,#46704),
 .UNSPECIFIED.,.F.,.F.,(4,2,2,2,2,2,2,2,2,2,2,2,2,2,2,2,2,4),(-22.6581171675807,
-22.6412102410835,-22.5835641689142,-22.5236319902899,-22.4665652482388,
-22.4082496043878,-22.3487848861067,-22.2919531828174,-22.2329943725634,
-22.1741263229248,-22.1166686457465,-22.0569456248039,-21.9996842855768,
-21.9415589369491,-21.8821072544915,-21.8253417468782,-21.7665709936596,
-21.7157628302399),.UNSPECIFIED.);
#2986=B_SPLINE_CURVE_WITH_KNOTS('',3,(#46709,#46710,#46711,#46712,#46713,
#46714,#46715,#46716,#46717,#46718,#46719,#46720,#46721,#46722,#46723,#46724,
#46725,#46726,#46727,#46728,#46729,#46730,#46731,#46732,#46733,#46734,#46735,
#46736,#46737,#46738,#46739,#46740,#46741,#46742,#46743,#46744),
 .UNSPECIFIED.,.F.,.F.,(4,2,2,2,2,2,2,2,2,2,2,2,2,2,2,2,2,4),(-6.62109380521341,
-6.57761768259959,-6.51828740763027,-6.46113362202641,-6.40140207096381,
-6.34271600715298,-6.28548482095171,-6.22516410228413,-6.16715260360109,
-6.10873547077658,-6.04917186097877,-5.99184011673613,-5.93213648107799,
-5.8733499659965,-5.81628212661826,-5.75656105013342,-5.69842598086126,
-5.67439159596968),.UNSPECIFIED.);
#2987=B_SPLINE_CURVE_WITH_KNOTS('',3,(#46745,#46746,#46747,#46748,#46749,
#46750,#46751,#46752,#46753,#46754,#46755,#46756,#46757,#46758,#46759,#46760,
#46761,#46762,#46763,#46764,#46765,#46766,#46767,#46768,#46769,#46770,#46771,
#46772,#46773,#46774,#46775,#46776,#46777,#46778,#46779,#46780),
 .UNSPECIFIED.,.F.,.F.,(4,2,2,2,2,2,2,2,2,2,2,2,2,2,2,2,2,4),(-21.7157628302399,
-21.7071499734112,-21.6498486291818,-21.5902999589255,-21.5327541629797,
-21.4747842600729,-21.4153173211779,-21.3585227590009,-21.2999052492263,
-21.2398720875173,-21.1826905454483,-21.1232764692568,-21.065378520901,
-21.0075245508875,-20.9480158554619,-20.8911101904613,-20.8326059984683,
-20.7731793950157),.UNSPECIFIED.);
#2988=B_SPLINE_CURVE_WITH_KNOTS('',3,(#46785,#46786,#46787,#46788,#46789,
#46790,#46791,#46792,#46793,#46794,#46795,#46796,#46797,#46798,#46799,#46800,
#46801,#46802,#46803,#46804,#46805,#46806,#46807,#46808,#46809,#46810,#46811,
#46812,#46813,#46814,#46815,#46816,#46817,#46818,#46819,#46820),
 .UNSPECIFIED.,.F.,.F.,(4,2,2,2,2,2,2,2,2,2,2,2,2,2,2,2,2,4),(-7.56721318319246,
-7.51440195941646,-7.4554548070908,-7.39845589958658,-7.33875763160917,
-7.28045937419718,-7.22286133868259,-7.16296628560166,-7.10533842940707,
-7.04602095897405,-6.9868979771895,-6.92987099130527,-6.87017100691209,
-6.81169474396116,-6.75432913502786,-6.69423710481114,-6.63643211656935,
-6.62109380521341),.UNSPECIFIED.);
#2989=B_SPLINE_CURVE_WITH_KNOTS('',3,(#46821,#46822,#46823,#46824,#46825,
#46826,#46827,#46828,#46829,#46830,#46831,#46832,#46833,#46834,#46835,#46836,
#46837,#46838,#46839,#46840,#46841,#46842,#46843,#46844,#46845,#46846,#46847,
#46848,#46849,#46850,#46851,#46852,#46853,#46854,#46855,#46856,#46857,#46858),
 .UNSPECIFIED.,.F.,.F.,(4,2,2,2,2,2,2,2,2,2,2,2,2,2,2,2,2,2,4),(-20.7731793950157,
-20.7731201315055,-20.7160582025871,-20.6567792566783,-20.5983599289237,
-20.5406164839802,-20.4805811221967,-20.4234656784966,-20.3650514109911,
-20.305511597516,-20.2485949896086,-20.1895371334662,-20.1306696919239,
-20.0731189832228,-20.0132974755221,-19.9560008596223,-19.8977815738613,
-19.8382589546996,-19.8295444030046),.UNSPECIFIED.);
#2990=B_SPLINE_CURVE_WITH_KNOTS('',3,(#46863,#46864,#46865,#46866,#46867,
#46868,#46869,#46870,#46871,#46872,#46873,#46874,#46875,#46876,#46877,#46878,
#46879,#46880,#46881,#46882,#46883,#46884,#46885,#46886,#46887,#46888,#46889,
#46890,#46891,#46892,#46893,#46894,#46895,#46896,#46897,#46898,#46899,#46900),
 .UNSPECIFIED.,.F.,.F.,(4,2,2,2,2,2,2,2,2,2,2,2,2,2,2,2,2,2,4),(-8.51391269073544,
-8.51222365838152,-8.45249428513948,-8.39378861667143,-8.33657472393003,
-8.27623231073072,-8.21820164401039,-8.1598332741766,-8.10024765479814,
-8.04289584139225,-7.98318755401621,-7.92437912604881,-7.86731677437594,
-7.80759259896721,-7.74943539170332,-7.6915218402897,-7.631786775557,-7.57430204194946,
-7.56721318319246),.UNSPECIFIED.);
#2991=B_SPLINE_CURVE_WITH_KNOTS('',3,(#46901,#46902,#46903,#46904,#46905,
#46906,#46907,#46908,#46909,#46910,#46911,#46912,#46913,#46914,#46915,#46916,
#46917,#46918,#46919,#46920,#46921,#46922,#46923,#46924,#46925,#46926,#46927,
#46928,#46929,#46930,#46931,#46932,#46933,#46934,#46935,#46936),
 .UNSPECIFIED.,.F.,.F.,(4,2,2,2,2,2,2,2,2,2,2,2,2,2,2,2,2,4),(-19.8295444030046,
-19.781422440649,-19.7225572817117,-19.6631471763022,-19.6057577545878,
-19.5461159927651,-19.4885461013889,-19.4304876297435,-19.3709535721035,
-19.3141007093386,-19.2553941827952,-19.1953773792029,-19.1381132548424,
-19.0786120692882,-19.0206974716804,-18.9627608300149,-18.9031885891784,
-18.8860416189937),.UNSPECIFIED.);
#2992=B_SPLINE_CURVE_WITH_KNOTS('',3,(#46941,#46942,#46943,#46944,#46945,
#46946,#46947,#46948,#46949,#46950,#46951,#46952,#46953,#46954,#46955,#46956,
#46957,#46958,#46959,#46960,#46961,#46962,#46963,#46964,#46965,#46966,#46967,
#46968,#46969,#46970,#46971,#46972,#46973,#46974,#46975,#46976),
 .UNSPECIFIED.,.F.,.F.,(4,2,2,2,2,2,2,2,2,2,2,2,2,2,2,2,2,4),(-9.4600020867739,
-9.44946097484441,-9.38977226427863,-9.3314620836995,-9.27390543364871,
-9.21399634460654,-9.15635642704838,-9.09711384600216,-9.03797514352587,
-8.98094579786149,-8.92125183936447,-8.86275948675276,-8.8054237975235,
-8.7453135764027,-8.68749269541132,-8.62874128051507,-8.56939184171518,
-8.51391269073544),.UNSPECIFIED.);
#2993=B_SPLINE_CURVE_WITH_KNOTS('',3,(#46977,#46978,#46979,#46980,#46981,
#46982,#46983,#46984,#46985,#46986,#46987,#46988,#46989,#46990,#46991,#46992,
#46993,#46994,#46995,#46996,#46997,#46998,#46999,#47000,#47001,#47002,#47003,
#47004,#47005,#47006,#47007,#47008,#47009,#47010,#47011,#47012),
 .UNSPECIFIED.,.F.,.F.,(4,2,2,2,2,2,2,2,2,2,2,2,2,2,2,2,2,4),(-18.8860416189937,
-18.8462348900712,-18.7876476548069,-18.7280968440835,-18.6709555484027,
-18.6115929558287,-18.5531716016611,-18.495349324202,-18.4352301709226,
-18.3780798368063,-18.319585679885,-18.2599881331103,-18.2030028878512,
-18.1438648978918,-18.0850090800984,-18.0273834680497,-17.9674824112817,
-17.941522876477),.UNSPECIFIED.);
#2994=B_SPLINE_CURVE_WITH_KNOTS('',3,(#47017,#47018,#47019,#47020,#47021,
#47022,#47023,#47024,#47025,#47026,#47027,#47028,#47029,#47030,#47031,#47032,
#47033,#47034,#47035,#47036,#47037,#47038,#47039,#47040,#47041,#47042,#47043,
#47044,#47045,#47046,#47047,#47048,#47049,#47050,#47051,#47052),
 .UNSPECIFIED.,.F.,.F.,(4,2,2,2,2,2,2,2,2,2,2,2,2,2,2,2,2,4),(-10.4063262286273,
-10.387392591544,-10.3270439303512,-10.2690090232558,-10.210705562305,-10.1511132343272,
-10.09375612853,-10.034059046947,-9.97524386932148,-9.91820163035005,-9.8584903134111,
-9.80032595747233,-9.74246277833438,-9.68271846928724,-9.62522607647149,
-9.56540900336133,-9.50645028314585,-9.4600020867739),.UNSPECIFIED.);
#2995=B_SPLINE_CURVE_WITH_KNOTS('',3,(#47053,#47054,#47055,#47056,#47057,
#47058,#47059,#47060,#47061,#47062,#47063,#47064,#47065,#47066,#47067,#47068,
#47069,#47070,#47071,#47072,#47073,#47074,#47075,#47076,#47077,#47078,#47079,
#47080,#47081,#47082,#47083,#47084,#47085,#47086,#47087,#47088),
 .UNSPECIFIED.,.F.,.F.,(4,2,2,2,2,2,2,2,2,2,2,2,2,2,2,2,2,4),(-17.941522876477,
-17.9101636562757,-17.8518687182981,-17.7922922877475,-17.7354001068821,
-17.6764590004862,-17.6170707989498,-17.5596109797981,-17.4998945731994,
-17.4423134048219,-17.3841841685699,-17.3245998970605,-17.2677034424408,
-17.2089258668494,-17.1489368038417,-17.0916073172332,-17.0320369692312,
-16.997272415308),.UNSPECIFIED.);
#2996=B_SPLINE_CURVE_WITH_KNOTS('',3,(#47093,#47094,#47095,#47096,#47097,
#47098,#47099,#47100,#47101,#47102,#47103,#47104,#47105,#47106,#47107,#47108,
#47109,#47110,#47111,#47112,#47113,#47114,#47115,#47116,#47117,#47118,#47119,
#47120,#47121,#47122,#47123,#47124,#47125,#47126,#47127,#47128),
 .UNSPECIFIED.,.F.,.F.,(4,2,2,2,2,2,2,2,2,2,2,2,2,2,2,2,2,4),(-11.3522871924595,
-11.324430394275,-11.264522730746,-11.2068857092522,-11.1477360236872,-11.08859687367,
-11.0315792760543,-10.9719076335357,-10.9134142640608,-10.8561239489264,
-10.796010976838,-10.7381891351563,-10.6795177406942,-10.620164420077,-10.5629956093436,
-10.5032845165816,-10.4445743180876,-10.4063262286273),.UNSPECIFIED.);
#2997=B_SPLINE_CURVE_WITH_KNOTS('',3,(#47129,#47130,#47131,#47132,#47133,
#47134,#47135,#47136,#47137,#47138,#47139,#47140,#47141,#47142,#47143,#47144,
#47145,#47146,#47147,#47148,#47149,#47150,#47151,#47152,#47153,#47154,#47155,
#47156,#47157,#47158,#47159,#47160,#47161,#47162,#47163,#47164),
 .UNSPECIFIED.,.F.,.F.,(4,2,2,2,2,2,2,2,2,2,2,2,2,2,2,2,2,4),(-16.997272415308,
-16.974118579872,-16.9161165902415,-16.8564975009602,-16.7995101512218,
-16.7408573501075,-16.6812582779792,-16.6240545216982,-16.5646258893359,
-16.5062147666311,-16.448330624569,-16.388145391231,-16.3309738020301,-16.2724169024022,
-16.2127779950283,-16.155739296564,-16.0965384948368,-16.052121842989),
 .UNSPECIFIED.);
#2998=B_SPLINE_CURVE_WITH_KNOTS('',3,(#47169,#47170,#47171,#47172,#47173,
#47174,#47175,#47176,#47177,#47178,#47179,#47180,#47181,#47182,#47183,#47184,
#47185,#47186,#47187,#47188,#47189,#47190,#47191,#47192,#47193,#47194,#47195,
#47196,#47197,#47198,#47199,#47200,#47201,#47202,#47203,#47204),
 .UNSPECIFIED.,.F.,.F.,(4,2,2,2,2,2,2,2,2,2,2,2,2,2,2,2,2,4),(-12.2980151684053,
-12.2608049534251,-12.2012214180354,-12.1438740189948,-12.0842046319712,
-12.0253980696236,-11.9683912868138,-11.9087094544592,-11.8505531273409,
-11.7927573534416,-11.7330193273245,-11.6755342944868,-11.6158192576419,
-11.5568642629696,-11.4998992163216,-11.4402365277277,-11.3819295252021,
-11.3522871924595),.UNSPECIFIED.);
#2999=B_SPLINE_CURVE_WITH_KNOTS('',3,(#47205,#47206,#47207,#47208,#47209,
#47210,#47211,#47212,#47213,#47214,#47215,#47216,#47217,#47218,#47219,#47220,
#47221,#47222,#47223,#47224,#47225,#47226,#47227,#47228,#47229,#47230,#47231,
#47232,#47233,#47234,#47235,#47236,#47237,#47238,#47239,#47240),
 .UNSPECIFIED.,.F.,.F.,(4,2,2,2,2,2,2,2,2,2,2,2,2,2,2,2,2,4),(-16.052121842989,
-16.0377063442003,-15.9800225041649,-15.9200592855784,-15.8627316418797,
-15.8043778785959,-15.7447638720137,-15.6878306019307,-15.6288305455336,
-15.5694764347843,-15.5119625793001,-15.452188569769,-15.3946092699113,
-15.3364257590099,-15.2768073817686,-15.2198815508401,-15.1610495793805,
-15.1073443691545),.UNSPECIFIED.);
#3000=B_SPLINE_CURVE_WITH_KNOTS('',3,(#47245,#47246,#47247,#47248,#47249,
#47250,#47251,#47252,#47253,#47254,#47255,#47256,#47257,#47258,#47259,#47260,
#47261,#47262,#47263,#47264,#47265,#47266,#47267,#47268,#47269,#47270,#47271,
#47272,#47273,#47274,#47275,#47276,#47277,#47278,#47279,#47280),
 .UNSPECIFIED.,.F.,.F.,(4,2,2,2,2,2,2,2,2,2,2,2,2,2,2,2,2,4),(-13.2436220538442,
-13.1973293402993,-13.1382053560805,-13.0812140676331,-13.0215819437106,
-12.9631029490451,-12.905874761448,-12.8457747640532,-12.787967213325,-12.7293949980337,
-12.670053341907,-12.6128978517491,-12.5532219431716,-12.494522530246,-12.4373888207658,
-12.3770495663262,-12.3190255916381,-12.2980151684053),.UNSPECIFIED.);
#3001=B_SPLINE_CURVE_WITH_KNOTS('',3,(#47281,#47282,#47283,#47284,#47285,
#47286,#47287,#47288,#47289,#47290,#47291,#47292,#47293,#47294,#47295,#47296,
#47297,#47298,#47299,#47300,#47301,#47302,#47303,#47304,#47305,#47306,#47307,
#47308,#47309,#47310,#47311,#47312,#47313,#47314,#47315,#47316,#47317,#47318),
 .UNSPECIFIED.,.F.,.F.,(4,2,2,2,2,2,2,2,2,2,2,2,2,2,2,2,2,2,4),(-15.1073443691545,
-15.1011008892937,-15.0437220848592,-14.9840992717133,-14.926190394778,
-14.8681392181562,-14.8084892686686,-14.7514823595925,-14.6927803091387,
-14.6331489331619,-14.5758985339276,-14.5164203125443,-14.4580324516964,
-14.4001023522461,-14.339867608388,-14.2826884114687,-14.2240848432797,
-14.1644203791933,-14.161791521072),.UNSPECIFIED.);
#3002=B_SPLINE_CURVE_WITH_KNOTS('',3,(#47323,#47324,#47325,#47326,#47327,
#47328,#47329,#47330,#47331,#47332,#47333,#47334,#47335,#47336,#47337,#47338,
#47339,#47340,#47341,#47342,#47343,#47344,#47345,#47346,#47347,#47348,#47349,
#47350,#47351,#47352,#47353,#47354,#47355,#47356,#47357,#47358),
 .UNSPECIFIED.,.F.,.F.,(4,2,2,2,2,2,2,2,2,2,2,2,2,2,2,2,2,4),(-14.1885859699234,
-14.1330844909293,-14.0738030834317,-14.0151322001193,-13.9573780431577,
-13.8973369154889,-13.8400747014035,-13.781649842778,-13.7220284098382,
-13.6650669338426,-13.6061313895152,-13.5492060305576,-13.4895868440872,
-13.4312985326842,-13.3738747554208,-13.3139843572995,-13.2563655957482,
-13.2436220538442),.UNSPECIFIED.);
#3003=B_SPLINE_CURVE_WITH_KNOTS('',3,(#47359,#47360,#47361,#47362,#47363,
#47364,#47365,#47366,#47367,#47368,#47369,#47370,#47371,#47372,#47373,#47374,
#47375,#47376,#47377,#47378,#47379,#47380,#47381,#47382,#47383,#47384,#47385,
#47386,#47387,#47388,#47389,#47390,#47391,#47392,#47393,#47394),
 .UNSPECIFIED.,.F.,.F.,(4,2,2,2,2,2,2,2,2,2,2,2,2,2,2,2,2,4),(-14.161791521072,
-14.1073426685626,-14.0480953063394,-13.9892999039839,-13.9315735440484,
-13.8715645099561,-13.8142414960538,-13.7558447627025,-13.6962089327002,
-13.6392486779599,-13.5802573437773,-13.5233108369954,-13.4636758610349,
-13.4053314288153,-13.3479464458854,-13.2879951425265,-13.2303206406094,
-13.2166062380566),.UNSPECIFIED.);
#3004=B_SPLINE_CURVE_WITH_KNOTS('',3,(#47399,#47400,#47401,#47402,#47403,
#47404,#47405,#47406,#47407,#47408,#47409,#47410,#47411,#47412,#47413,#47414,
#47415,#47416,#47417,#47418,#47419,#47420,#47421,#47422,#47423,#47424,#47425,
#47426,#47427,#47428,#47429,#47430,#47431,#47432,#47433,#47434,#47435,#47436),
 .UNSPECIFIED.,.F.,.F.,(4,2,2,2,2,2,2,2,2,2,2,2,2,2,2,2,2,2,4),(-15.1341561055544,
-15.1269994338561,-15.0695799723091,-15.0099125340775,-14.9520739190766,
-14.8939828445778,-14.8343297519005,-14.7773366004228,-14.7185951213641,
-14.6589576423824,-14.6016713251844,-14.5421535644632,-14.4838629359255,
-14.4258987192761,-14.3656251166082,-14.3084824988271,-14.2498440170218,
-14.1901865832963,-14.1885859699234),.UNSPECIFIED.);
#3005=B_SPLINE_CURVE_WITH_KNOTS('',3,(#47437,#47438,#47439,#47440,#47441,
#47442,#47443,#47444,#47445,#47446,#47447,#47448,#47449,#47450,#47451,#47452,
#47453,#47454,#47455,#47456,#47457,#47458,#47459,#47460,#47461,#47462,#47463,
#47464,#47465,#47466,#47467,#47468,#47469,#47470,#47471,#47472),
 .UNSPECIFIED.,.F.,.F.,(4,2,2,2,2,2,2,2,2,2,2,2,2,2,2,2,2,4),(-13.2166062380566,
-13.1713851979337,-13.1121981319385,-13.0551628296182,-12.9955080421381,
-12.9369655576865,-12.8797535453401,-12.819585289645,-12.761715189623,-12.7032194250943,
-12.6438086463492,-12.586620577358,-12.5270150261763,-12.4683803900242,
-12.4113696886299,-12.35174219741,-12.2937588655423,-12.2712695292436),
 .UNSPECIFIED.);
#3006=B_SPLINE_CURVE_WITH_KNOTS('',3,(#47477,#47478,#47479,#47480,#47481,
#47482,#47483,#47484,#47485,#47486,#47487,#47488,#47489,#47490,#47491,#47492,
#47493,#47494,#47495,#47496,#47497,#47498,#47499,#47500,#47501,#47502,#47503,
#47504,#47505,#47506,#47507,#47508,#47509,#47510,#47511,#47512),
 .UNSPECIFIED.,.F.,.F.,(4,2,2,2,2,2,2,2,2,2,2,2,2,2,2,2,2,4),(-16.0791645683298,
-16.0637629880179,-16.0060223350212,-15.9459969234656,-15.8887024341941,
-15.8302912537239,-15.7706612508563,-15.7136999051047,-15.654642811055,
-15.5954057874932,-15.5378426704977,-15.4780146687669,-15.4204898319656,
-15.3622571133794,-15.3026293793744,-15.2456979578477,-15.1868171504776,
-15.1341561055544),.UNSPECIFIED.);
#3007=B_SPLINE_CURVE_WITH_KNOTS('',3,(#47513,#47514,#47515,#47516,#47517,
#47518,#47519,#47520,#47521,#47522,#47523,#47524,#47525,#47526,#47527,#47528,
#47529,#47530,#47531,#47532,#47533,#47534,#47535,#47536,#47537,#47538,#47539,
#47540,#47541,#47542,#47543,#47544,#47545,#47546,#47547,#47548),
 .UNSPECIFIED.,.F.,.F.,(4,2,2,2,2,2,2,2,2,2,2,2,2,2,2,2,2,4),(-12.2712695292436,
-12.2357754508004,-12.1762270533728,-12.1189170680661,-12.0588176303639,
-12.0000655464483,-11.943159299172,-11.8835712422689,-11.8254678956475,
-11.7678321870858,-11.708145031833,-11.6507114242844,-11.5912213696332,
-11.5323122460786,-11.4754266605439,-11.4158513420701,-11.3575887654668,
-11.3269908932583),.UNSPECIFIED.);
#3008=B_SPLINE_CURVE_WITH_KNOTS('',3,(#47553,#47554,#47555,#47556,#47557,
#47558,#47559,#47560,#47561,#47562,#47563,#47564,#47565,#47566,#47567,#47568,
#47569,#47570,#47571,#47572,#47573,#47574,#47575,#47576,#47577,#47578,#47579,
#47580,#47581,#47582,#47583,#47584,#47585,#47586,#47587,#47588),
 .UNSPECIFIED.,.F.,.F.,(4,2,2,2,2,2,2,2,2,2,2,2,2,2,2,2,2,4),(-17.0247741151702,
-17.0006922494049,-16.942620899042,-16.8829683888398,-16.8259674619989,
-16.7672454552544,-16.7076101234707,-16.6503415003102,-16.590843286514,
-16.5325014804607,-16.4745540351945,-16.4142996421448,-16.357137434069,
-16.2985161360182,-16.2388539992256,-16.1817640975146,-16.1224994016558,
-16.0791645683298),.UNSPECIFIED.);
#3009=B_SPLINE_CURVE_WITH_KNOTS('',3,(#47589,#47590,#47591,#47592,#47593,
#47594,#47595,#47596,#47597,#47598,#47599,#47600,#47601,#47602,#47603,#47604,
#47605,#47606,#47607,#47608,#47609,#47610,#47611,#47612,#47613,#47614,#47615,
#47616,#47617,#47618,#47619,#47620,#47621,#47622,#47623,#47624),
 .UNSPECIFIED.,.F.,.F.,(4,2,2,2,2,2,2,2,2,2,2,2,2,2,2,2,2,4),(-11.3269908932583,
-11.3002304831747,-11.2403651502537,-11.1827717007332,-11.1238285355636,
-11.064728011521,-11.0077668972893,-10.9481757635054,-10.8897195155163,
-10.8325471683827,-10.7724692707686,-10.7146842840278,-10.6561946025542,
-10.5968740051404,-10.5397395269343,-10.4801014814801,-10.4214223488875,
-10.3822526002173),.UNSPECIFIED.);
#3010=B_SPLINE_CURVE_WITH_KNOTS('',3,(#47629,#47630,#47631,#47632,#47633,
#47634,#47635,#47636,#47637,#47638,#47639,#47640,#47641,#47642,#47643,#47644,
#47645,#47646,#47647,#47648,#47649,#47650,#47651,#47652,#47653,#47654,#47655,
#47656,#47657,#47658,#47659,#47660,#47661,#47662,#47663,#47664),
 .UNSPECIFIED.,.F.,.F.,(4,2,2,2,2,2,2,2,2,2,2,2,2,2,2,2,2,4),(-17.9696970255303,
-17.937289370862,-17.8789069021961,-17.8192841522869,-17.7623368372575,
-17.7033082433986,-17.6440100001385,-17.5864714106887,-17.526670356869,
-17.4691167328281,-17.4109085209012,-17.3512845924667,-17.2943555190345,
-17.2354990142404,-17.1756126480208,-17.1182132969445,-17.0585679978772,
-17.0247741151702),.UNSPECIFIED.);
#3011=B_SPLINE_CURVE_WITH_KNOTS('',3,(#47665,#47666,#47667,#47668,#47669,
#47670,#47671,#47672,#47673,#47674,#47675,#47676,#47677,#47678,#47679,#47680,
#47681,#47682,#47683,#47684,#47685,#47686,#47687,#47688,#47689,#47690,#47691,
#47692,#47693,#47694,#47695,#47696,#47697,#47698,#47699,#47700),
 .UNSPECIFIED.,.F.,.F.,(4,2,2,2,2,2,2,2,2,2,2,2,2,2,2,2,2,4),(-10.3822526002173,
-10.3643343540307,-10.3046400968479,-10.246613334744,-10.1885181147052,
-10.128927402479,-10.0715754084394,-10.011325400927,-9.9525347708931,-9.89556195447909,
-9.83591091083034,-9.77776999750488,-9.72003077893023,-9.66030722303232,
-9.60283704872725,-9.54320316116386,-9.48426076178981,-9.43689892858011),
 .UNSPECIFIED.);
#3012=B_SPLINE_CURVE_WITH_KNOTS('',3,(#47705,#47706,#47707,#47708,#47709,
#47710,#47711,#47712,#47713,#47714,#47715,#47716,#47717,#47718,#47719,#47720,
#47721,#47722,#47723,#47724,#47725,#47726,#47727,#47728,#47729,#47730,#47731,
#47732,#47733,#47734,#47735,#47736,#47737,#47738,#47739,#47740),
 .UNSPECIFIED.,.F.,.F.,(4,2,2,2,2,2,2,2,2,2,2,2,2,2,2,2,2,4),(-18.9151145034862,
-18.8743164654268,-18.8156291548377,-18.7560115648048,-18.6987754493173,
-18.6393121439161,-18.5809341256596,-18.5230183981635,-18.4627987144582,
-18.4056311968295,-18.3470421802252,-18.2873910545073,-18.2303271150055,
-18.171094421965,-18.1123080260466,-18.0545957689432,-17.9946015046478,
-17.9696970255303),.UNSPECIFIED.);
#3013=B_SPLINE_CURVE_WITH_KNOTS('',3,(#47741,#47742,#47743,#47744,#47745,
#47746,#47747,#47748,#47749,#47750,#47751,#47752,#47753,#47754,#47755,#47756,
#47757,#47758,#47759,#47760,#47761,#47762,#47763,#47764,#47765,#47766,#47767,
#47768,#47769,#47770,#47771,#47772,#47773,#47774,#47775,#47776),
 .UNSPECIFIED.,.F.,.F.,(4,2,2,2,2,2,2,2,2,2,2,2,2,2,2,2,2,4),(-9.43689892858011,
-9.42732171849391,-9.36768738295302,-9.30939248028644,-9.25194272911408,
-9.19204622378449,-9.13442101602013,-9.07534568068709,-9.01621630273034,
-8.95921594082851,-8.89957004368503,-8.84108593111714,-8.78383634874988,
-8.72373170856049,-8.6659190669351,-8.60731272480359,-8.54796686813959,
-8.49156038630827),.UNSPECIFIED.);
#3014=B_SPLINE_CURVE_WITH_KNOTS('',3,(#47781,#47782,#47783,#47784,#47785,
#47786,#47787,#47788,#47789,#47790,#47791,#47792,#47793,#47794,#47795,#47796,
#47797,#47798,#47799,#47800,#47801,#47802,#47803,#47804,#47805,#47806,#47807,
#47808,#47809,#47810,#47811,#47812,#47813,#47814,#47815,#47816),
 .UNSPECIFIED.,.F.,.F.,(4,2,2,2,2,2,2,2,2,2,2,2,2,2,2,2,2,4),(-19.8597382210236,
-19.810451373043,-19.7514667566491,-19.6921219719675,-19.6346229403372,
-19.5748644342208,-19.5172962645061,-19.4591277252691,-19.3995232496075,
-19.3426105099162,-19.2837936446735,-19.2238539608265,-19.1664896413472,
-19.1068819617647,-19.0489837573588,-18.9909471893313,-18.9313109305834,
-18.9151145034862),.UNSPECIFIED.);
#3015=B_SPLINE_CURVE_WITH_KNOTS('',3,(#47817,#47818,#47819,#47820,#47821,
#47822,#47823,#47824,#47825,#47826,#47827,#47828,#47829,#47830,#47831,#47832,
#47833,#47834,#47835,#47836,#47837,#47838,#47839,#47840,#47841,#47842,#47843,
#47844,#47845,#47846,#47847,#47848,#47849,#47850,#47851,#47852,#47853,#47854),
 .UNSPECIFIED.,.F.,.F.,(4,2,2,2,2,2,2,2,2,2,2,2,2,2,2,2,2,2,4),(-8.49156038630827,
-8.49080675575303,-8.43111857134256,-8.37241526446117,-8.31526501763932,
-8.25492233706489,-8.19689441801019,-8.13864530142174,-8.07905854481672,
-8.02170761683104,-7.96202852596394,-7.9032187975688,-7.84619976450985,
-7.78650760972943,-7.72834831916545,-7.67052935317836,-7.61078895216033,
-7.55330118212272,-7.54539583975842),.UNSPECIFIED.);
#3016=B_SPLINE_CURVE_WITH_KNOTS('',3,(#47859,#47860,#47861,#47862,#47863,
#47864,#47865,#47866,#47867,#47868,#47869,#47870,#47871,#47872,#47873,#47874,
#47875,#47876,#47877,#47878,#47879,#47880,#47881,#47882,#47883,#47884,#47885,
#47886,#47887,#47888,#47889,#47890,#47891,#47892,#47893,#47894,#47895,#47896),
 .UNSPECIFIED.,.F.,.F.,(4,2,2,2,2,2,2,2,2,2,2,2,2,2,2,2,2,2,4),(-20.8047268284554,
-20.8036363389145,-20.7464479008663,-20.6870352594353,-20.6286348915891,
-20.5707661629285,-20.510597073108,-20.4534380889162,-20.3948967931479,
-20.3352722771837,-20.2782483009287,-20.219063232801,-20.1602410153004,
-20.1025723093681,-20.0426249323872,-19.9853090960203,-19.9269706384341,
-19.867370764855,-19.8597382210236),.UNSPECIFIED.);
#3017=B_SPLINE_CURVE_WITH_KNOTS('',3,(#47897,#47898,#47899,#47900,#47901,
#47902,#47903,#47904,#47905,#47906,#47907,#47908,#47909,#47910,#47911,#47912,
#47913,#47914,#47915,#47916,#47917,#47918,#47919,#47920,#47921,#47922,#47923,
#47924,#47925,#47926,#47927,#47928,#47929,#47930,#47931,#47932),
 .UNSPECIFIED.,.F.,.F.,(4,2,2,2,2,2,2,2,2,2,2,2,2,2,2,2,2,4),(-7.54539583975842,
-7.49355110204946,-7.43459460077228,-7.37762115395009,-7.31794932817515,
-7.25964100917192,-7.20212210603924,-7.14221371611197,-7.08457547245393,
-7.02539392871746,-6.96625468515904,-6.90923296876007,-6.84955345859718,
-6.79106019408235,-6.73375428080265,-6.6736419972573,-6.61582024058893,
-6.59962043014718),.UNSPECIFIED.);
#3018=B_SPLINE_CURVE_WITH_KNOTS('',3,(#47937,#47938,#47939,#47940,#47941,
#47942,#47943,#47944,#47945,#47946,#47947,#47948,#47949,#47950,#47951,#47952,
#47953,#47954,#47955,#47956,#47957,#47958,#47959,#47960,#47961,#47962,#47963,
#47964,#47965,#47966,#47967,#47968,#47969,#47970,#47971,#47972),
 .UNSPECIFIED.,.F.,.F.,(4,2,2,2,2,2,2,2,2,2,2,2,2,2,2,2,2,4),(-21.7489046572791,
-21.7392153866495,-21.6817714549229,-21.6220716583751,-21.5645025223573,
-21.5063893301253,-21.4468200256293,-21.3899376073178,-21.3311762213552,
-21.2711970668162,-21.2138831121422,-21.1543289862749,-21.0964221879644,
-21.0384358621701,-20.9788315240901,-20.9218575630073,-20.8632205676017,
-20.8047268284554),.UNSPECIFIED.);
#3019=B_SPLINE_CURVE_WITH_KNOTS('',3,(#47973,#47974,#47975,#47976,#47977,
#47978,#47979,#47980,#47981,#47982,#47983,#47984,#47985,#47986,#47987,#47988,
#47989,#47990,#47991,#47992,#47993,#47994,#47995,#47996,#47997,#47998,#47999,
#48000,#48001,#48002,#48003,#48004,#48005,#48006,#48007,#48008),
 .UNSPECIFIED.,.F.,.F.,(4,2,2,2,2,2,2,2,2,2,2,2,2,2,2,2,2,4),(-6.59962043014718,
-6.55712143056447,-6.49776917806976,-6.44060046014423,-6.3808828825634,
-6.32217397813377,-6.26498116754636,-6.20463437850135,-6.14660066752985,
-6.0882749718812,-6.02868466855325,-5.9713291133043,-5.91162795849117,-5.85281481524407,
-5.79576557777481,-5.73604961995392,-5.67788743624381,-5.65305968192749),
 .UNSPECIFIED.);
#3020=B_SPLINE_CURVE_WITH_KNOTS('',3,(#48013,#48014,#48015,#48016,#48017,
#48018,#48019,#48020,#48021,#48022,#48023,#48024,#48025,#48026,#48027,#48028,
#48029,#48030,#48031,#48032,#48033,#48034,#48035,#48036,#48037,#48038,#48039,
#48040,#48041,#48042,#48043,#48044,#48045,#48046,#48047,#48048),
 .UNSPECIFIED.,.F.,.F.,(4,2,2,2,2,2,2,2,2,2,2,2,2,2,2,2,2,4),(-22.6930944862137,
-22.6750742815793,-22.6172685137948,-22.5571666469156,-22.5000298336195,
-22.4415523883347,-22.3819703093803,-22.3250007752965,-22.2658796385637,
-22.2070346049225,-22.1494252073759,-22.0895411174023,-22.0322350703383,
-21.9739565284333,-21.9143953015877,-21.8575179583935,-21.7985933937003,
-21.7489046572791),.UNSPECIFIED.);
#3021=B_SPLINE_CURVE_WITH_KNOTS('',3,(#48049,#48050,#48051,#48052,#48053,
#48054,#48055,#48056,#48057,#48058,#48059,#48060,#48061,#48062,#48063,#48064,
#48065,#48066,#48067,#48068,#48069,#48070,#48071,#48072,#48073,#48074,#48075,
#48076,#48077,#48078,#48079,#48080,#48081,#48082,#48083,#48084),
 .UNSPECIFIED.,.F.,.F.,(4,2,2,2,2,2,2,2,2,2,2,2,2,2,2,2,2,4),(-5.65305968192749,
-5.62000697109407,-5.56026553634326,-5.50277548740805,-5.4429300395589,
-5.38397497750277,-5.32698226097639,-5.2672900308627,-5.20898363219345,
-5.15141280935565,-5.09150820934248,-5.03387211917237,-4.97460397585247,
-4.91547032791341,-4.8584416373336,-4.79874535977046,-4.74025819094778,
-4.7070192889843),.UNSPECIFIED.);
#3022=B_SPLINE_CURVE_WITH_KNOTS('',3,(#48089,#48090,#48091,#48092,#48093,
#48094,#48095,#48096,#48097,#48098,#48099,#48100,#48101,#48102,#48103,#48104,
#48105,#48106,#48107,#48108,#48109,#48110,#48111,#48112,#48113,#48114,#48115,
#48116,#48117,#48118,#48119,#48120,#48121,#48122,#48123,#48124),
 .UNSPECIFIED.,.F.,.F.,(4,2,2,2,2,2,2,2,2,2,2,2,2,2,2,2,2,4),(-23.6367224740298,
-23.6102009889967,-23.5521597036553,-23.4926417159663,-23.435803856614,
-23.3771146729451,-23.3171085926091,-23.2598611088234,-23.2003772998387,
-23.1424751745089,-23.0845553127723,-23.0249989156642,-22.9680595588619,
-22.9094892557851,-22.8499543793008,-22.7928294928815,-22.7334840265615,
-22.6930944862137),.UNSPECIFIED.);
#3023=B_SPLINE_CURVE_WITH_KNOTS('',3,(#48125,#48126,#48127,#48128,#48129,
#48130,#48131,#48132,#48133,#48134,#48135,#48136,#48137,#48138,#48139,#48140,
#48141,#48142,#48143,#48144,#48145,#48146,#48147,#48148,#48149,#48150,#48151,
#48152,#48153,#48154,#48155,#48156,#48157,#48158,#48159,#48160),
 .UNSPECIFIED.,.F.,.F.,(4,2,2,2,2,2,2,2,2,2,2,2,2,2,2,2,2,4),(-4.7070192889843,
-4.68291221701188,-4.62280788263384,-4.56499211835275,-4.50621920975702,
-4.44687598188547,-4.3897125228076,-4.32998213906469,-4.27128283566224,
-4.21406294394457,-4.15372759490239,-4.09570314650131,-4.03731813708901,
-3.97773968458231,-3.92039439080922,-3.86068740451247,-3.80188610698126,
-3.76030733114506),.UNSPECIFIED.);
#3024=B_SPLINE_CURVE_WITH_KNOTS('',3,(#48165,#48166,#48167,#48168,#48169,
#48170,#48171,#48172,#48173,#48174,#48175,#48176,#48177,#48178,#48179,#48180,
#48181,#48182,#48183,#48184,#48185,#48186,#48187,#48188,#48189,#48190,#48191,
#48192,#48193,#48194,#48195,#48196,#48197,#48198,#48199,#48200),
 .UNSPECIFIED.,.F.,.F.,(4,2,2,2,2,2,2,2,2,2,2,2,2,2,2,2,2,4),(-24.5799045977848,
-24.544864402261,-24.4864680402579,-24.4269448204466,-24.3700449713328,
-24.3110051741305,-24.2521492970098,-24.1946159613695,-24.1348126294181,
-24.0775296073419,-24.0193278864891,-23.9598215850082,-23.9030009070175,
-23.8441534701742,-23.7847543450619,-23.7273819445697,-23.667757974583,
-23.6367224740298),.UNSPECIFIED.);
#3025=B_SPLINE_CURVE_WITH_KNOTS('',3,(#48201,#48202,#48203,#48204,#48205,
#48206,#48207,#48208,#48209,#48210,#48211,#48212,#48213,#48214,#48215,#48216,
#48217,#48218,#48219,#48220,#48221,#48222,#48223,#48224,#48225,#48226,#48227,
#48228,#48229,#48230,#48231,#48232,#48233,#48234,#48235,#48236),
 .UNSPECIFIED.,.F.,.F.,(4,2,2,2,2,2,2,2,2,2,2,2,2,2,2,2,2,4),(-3.76030733114506,
-3.74482173076156,-3.6850983260828,-3.62694832744347,-3.56902286769636,
-3.50929583899485,-3.45181843527126,-3.39189585023894,-3.33295745069471,
-3.27595993809932,-3.21626352613547,-3.15797408399984,-3.1003669659872,
-3.04048156422391,-2.98286252158158,-2.92352507208656,-2.86441225193454,
-2.81422223630842),.UNSPECIFIED.);
#3026=B_SPLINE_CURVE_WITH_KNOTS('',3,(#48241,#48242,#48243,#48244,#48245,
#48246,#48247,#48248,#48249,#48250,#48251,#48252,#48253,#48254,#48255,#48256,
#48257,#48258,#48259,#48260,#48261,#48262,#48263,#48264,#48265,#48266,#48267,
#48268,#48269,#48270,#48271,#48272,#48273,#48274,#48275,#48276),
 .UNSPECIFIED.,.F.,.F.,(4,2,2,2,2,2,2,2,2,2,2,2,2,2,2,2,2,4),(-25.5227587485597,
-25.47965708315,-25.421058174348,-25.361036462416,-25.3038727637219,-25.2444773184052,
-25.1865926949701,-25.128756714116,-25.0692650147963,-25.0123746718861,
-24.9538886316087,-24.8944198504469,-24.8373755091807,-24.7781149174187,
-24.7197080007783,-24.6619822469935,-24.6019654058989,-24.5799045977848),
 .UNSPECIFIED.);
#3027=B_SPLINE_CURVE_WITH_KNOTS('',3,(#48277,#48278,#48279,#48280,#48281,
#48282,#48283,#48284,#48285,#48286,#48287,#48288,#48289,#48290,#48291,#48292,
#48293,#48294,#48295,#48296,#48297,#48298,#48299,#48300,#48301,#48302,#48303,
#48304,#48305,#48306,#48307,#48308,#48309,#48310,#48311,#48312,#48313,#48314),
 .UNSPECIFIED.,.F.,.F.,(4,2,2,2,2,2,2,2,2,2,2,2,2,2,2,2,2,2,4),(-2.81422223630842,
-2.80739059809379,-2.74769363128926,-2.68922759545975,-2.63185666495599,
-2.57177569602702,-2.51398082031509,-2.45515020591261,-2.39583126811454,
-2.3386868262193,-2.27895955966271,-2.22028492138649,-2.16305256653281,
-2.1027441052407,-2.04474383487291,-1.98631516239258,-1.92676386570169,
-1.86944360522889,-1.86759610747369),.UNSPECIFIED.);
#3028=B_SPLINE_CURVE_WITH_KNOTS('',3,(#48319,#48320,#48321,#48322,#48323,
#48324,#48325,#48326,#48327,#48328,#48329,#48330,#48331,#48332,#48333,#48334,
#48335,#48336,#48337,#48338,#48339,#48340,#48341,#48342,#48343,#48344,#48345,
#48346,#48347,#48348,#48349,#48350,#48351,#48352,#48353,#48354),
 .UNSPECIFIED.,.F.,.F.,(4,2,2,2,2,2,2,2,2,2,2,2,2,2,2,2,2,4),(-26.4647006629411,
-26.4128164821547,-26.3538770628634,-26.295021282913,-26.2375822529352,
-26.1778787398139,-26.1206318744523,-26.0625253754812,-26.0030911980923,
-25.9463425849355,-25.8875908503495,-25.8281815100278,-25.7708984260118,
-25.7113688412011,-25.6538368035759,-25.595885334023,-25.5364356344578,
-25.5227587485597),.UNSPECIFIED.);
#3029=B_SPLINE_CURVE_WITH_KNOTS('',3,(#48355,#48356,#48357,#48358,#48359,
#48360,#48361,#48362,#48363,#48364,#48365,#48366,#48367,#48368,#48369,#48370,
#48371,#48372,#48373,#48374,#48375,#48376,#48377,#48378,#48379,#48380,#48381,
#48382,#48383,#48384,#48385,#48386,#48387,#48388,#48389,#48390),
 .UNSPECIFIED.,.F.,.F.,(4,2,2,2,2,2,2,2,2,2,2,2,2,2,2,2,2,4),(-1.86759610747369,
-1.8097465170722,-1.7509722323765,-1.69390716991027,-1.63419213717573,-1.57606932036452,
-1.51811407870063,-1.45841685307261,-1.40096694869804,-1.34098343757821,
-1.28207692999559,-1.22508871615811,-1.16540388332849,-1.10714645181714,
-1.0495176707267,-0.989666932708261,-0.932079853846146,-0.921606618540025),
 .UNSPECIFIED.);
#3030=B_SPLINE_CURVE_WITH_KNOTS('',3,(#48396,#48397,#48398,#48399,#48400,
#48401,#48402,#48403,#48404,#48405,#48406,#48407,#48408,#48409,#48410,#48411,
#48412,#48413,#48414,#48415),.UNSPECIFIED.,.F.,.F.,(4,2,2,2,2,2,2,2,2,4),
(9.99987117032003E-7,0.0282047267175922,0.0500972781633209,0.077222937740314,
0.107624298477487,0.137340418712146,0.157932276880896,0.175135732483776,
0.191462844907497,0.203440126186273),.UNSPECIFIED.);
#3031=B_SPLINE_CURVE_WITH_KNOTS('',3,(#48421,#48422,#48423,#48424,#48425,
#48426,#48427,#48428),.UNSPECIFIED.,.F.,.F.,(4,2,2,4),(21.4315064013737,
21.4634357935859,21.4930318613417,21.5226265917604),.UNSPECIFIED.);
#3032=B_SPLINE_CURVE_WITH_KNOTS('',3,(#48434,#48435,#48436,#48437,#48438,
#48439,#48440,#48441,#48442,#48443,#48444,#48445,#48446,#48447,#48448,#48449,
#48450,#48451,#48452,#48453,#48454,#48455,#48456,#48457,#48458,#48459,#48460,
#48461,#48462,#48463,#48464,#48465,#48466,#48467,#48468,#48469),
 .UNSPECIFIED.,.F.,.F.,(4,2,2,2,2,2,2,2,2,2,2,2,2,2,2,2,2,4),(20.6936878716818,
20.7322285263897,20.7783057175789,20.8227795047066,20.8693557730982,20.9149428892879,
20.9597524851927,21.0065846852777,21.0516438851204,21.0976519395239,21.1438788790039,
21.188432473727,21.2350392941589,21.2807854576605,21.3254925240272,21.3724982892632,
21.417717724476,21.4315064013737),.UNSPECIFIED.);
#3033=B_SPLINE_CURVE_WITH_KNOTS('',3,(#48470,#48471,#48472,#48473,#48474,
#48475,#48476,#48477,#48478,#48479,#48480,#48481,#48482,#48483,#48484,#48485,
#48486,#48487,#48488,#48489,#48490,#48491,#48492,#48493,#48494,#48495,#48496,
#48497,#48498,#48499,#48500,#48501,#48502,#48503,#48504,#48505),
 .UNSPECIFIED.,.F.,.F.,(4,2,2,2,2,2,2,2,2,2,2,2,2,2,2,2,2,4),(9.99999999753597E-7,
0.0364903991492045,0.0742057367939146,0.120984278340417,0.165716260437277,
0.212135354668823,0.258243398942271,0.303486376579508,0.350510827449709,
0.395451299070227,0.441223703670797,0.487964967533294,0.532602258835938,
0.578864855147042,0.625329100321987,0.670440021753448,0.717320863549735,
0.740262878339932),.UNSPECIFIED.);
#3034=B_SPLINE_CURVE_WITH_KNOTS('',3,(#48510,#48511,#48512,#48513,#48514,
#48515,#48516,#48517,#48518,#48519,#48520,#48521,#48522,#48523,#48524,#48525,
#48526,#48527,#48528,#48529,#48530,#48531,#48532,#48533,#48534,#48535,#48536,
#48537,#48538,#48539,#48540,#48541,#48542,#48543,#48544,#48545),
 .UNSPECIFIED.,.F.,.F.,(4,2,2,2,2,2,2,2,2,2,2,2,2,2,2,2,2,4),(19.9559680414516,
20.0008504784901,20.0467368410681,20.0912761832143,20.1378918451635,20.1832739295335,
20.2285046006904,20.275104513086,20.3199511087905,20.366754624975,20.4127173643503,
20.4571887454312,20.5037686894442,20.5492336658488,20.5942218762843,20.6409180608554,
20.6858523218674,20.6936878716818),.UNSPECIFIED.);
#3035=B_SPLINE_CURVE_WITH_KNOTS('',3,(#48546,#48547,#48548,#48549,#48550,
#48551,#48552,#48553,#48554,#48555,#48556,#48557,#48558,#48559,#48560,#48561,
#48562,#48563,#48564,#48565,#48566,#48567,#48568,#48569,#48570,#48571,#48572,
#48573,#48574,#48575,#48576,#48577,#48578,#48579,#48580,#48581),
 .UNSPECIFIED.,.F.,.F.,(4,2,2,2,2,2,2,2,2,2,2,2,2,2,2,2,2,4),(0.740262878339932,
0.762427102215096,0.808069985401053,0.854808846272841,0.899429812570394,
0.945570872042072,0.992454683227221,1.03747065146669,1.08424743869661,1.12958660656193,
1.175138889682,1.22190780149668,1.26658471043468,1.31264188421903,1.35939848501362,
1.4043392205548,1.45103260193205,1.48067239646651),.UNSPECIFIED.);
#3036=B_SPLINE_CURVE_WITH_KNOTS('',3,(#48586,#48587,#48588,#48589,#48590,
#48591,#48592,#48593,#48594,#48595,#48596,#48597,#48598,#48599,#48600,#48601,
#48602,#48603,#48604,#48605,#48606,#48607,#48608,#48609,#48610,#48611,#48612,
#48613,#48614,#48615,#48616,#48617,#48618,#48619,#48620,#48621,#48622,#48623),
 .UNSPECIFIED.,.F.,.F.,(4,2,2,2,2,2,2,2,2,2,2,2,2,2,2,2,2,2,4),(19.2175408288878,
19.2219373965907,19.2685210725085,19.3141891378125,19.3589248216993,19.4058460198647,
19.4509870738391,19.4968133764095,19.5431350504829,19.5877640910998,19.6343990565288,
19.6802461513431,19.72492597093,19.7720411959568,19.8173618084826,19.8629496498953,
19.9094715861334,19.954248068259,19.9559680414516),.UNSPECIFIED.);
#3037=B_SPLINE_CURVE_WITH_KNOTS('',3,(#48624,#48625,#48626,#48627,#48628,
#48629,#48630,#48631,#48632,#48633,#48634,#48635,#48636,#48637,#48638,#48639,
#48640,#48641,#48642,#48643,#48644,#48645,#48646,#48647,#48648,#48649,#48650,
#48651,#48652,#48653,#48654,#48655,#48656,#48657,#48658,#48659),
 .UNSPECIFIED.,.F.,.F.,(4,2,2,2,2,2,2,2,2,2,2,2,2,2,2,2,2,4),(1.48067239646651,
1.49671326012625,1.54219831558785,1.5894859449329,1.63428944893413,1.68030245144421,
1.72708174969527,1.77186789842175,1.81835464146615,1.86425678940839,1.90955548631379,
1.95664189809396,2.00148568453804,2.0473126858144,2.0940334671172,2.13867975719358,
2.18499121801513,2.22108960850334),.UNSPECIFIED.);
#3038=B_SPLINE_CURVE_WITH_KNOTS('',3,(#48664,#48665,#48666,#48667,#48668,
#48669,#48670,#48671,#48672,#48673,#48674,#48675,#48676,#48677,#48678,#48679,
#48680,#48681,#48682,#48683,#48684,#48685,#48686,#48687,#48688,#48689,#48690,
#48691,#48692,#48693,#48694,#48695,#48696,#48697,#48698,#48699),
 .UNSPECIFIED.,.F.,.F.,(4,2,2,2,2,2,2,2,2,2,2,2,2,2,2,2,2,4),(18.4801374015765,
18.4907658335562,18.5373515680576,18.5827705444335,18.6278503823358,18.6744946234866,
18.7193811539994,18.7659288026933,18.8119468369207,18.8564049550709,18.9029730508313,
18.9484975984601,18.9933693854802,19.0401328543241,19.0851285772229,19.1312801323088,
19.1774331204032,19.2175408288878),.UNSPECIFIED.);
#3039=B_SPLINE_CURVE_WITH_KNOTS('',3,(#48700,#48701,#48702,#48703,#48704,
#48705,#48706,#48707,#48708,#48709,#48710,#48711,#48712,#48713,#48714,#48715,
#48716,#48717,#48718,#48719,#48720,#48721,#48722,#48723,#48724,#48725,#48726,
#48727,#48728,#48729,#48730,#48731,#48732,#48733,#48734,#48735),
 .UNSPECIFIED.,.F.,.F.,(4,2,2,2,2,2,2,2,2,2,2,2,2,2,2,2,2,4),(2.22108960850334,
2.23120408655543,2.27635041769103,2.32327161206725,2.368237212408,2.41391337637609,
2.46061197050217,2.50519713949817,2.5513666691862,2.59796482416004,2.64299465171328,
2.68978881476098,2.73495033654449,2.78051325760178,2.82722340804027,2.87182391079689,
2.91788757586549,2.96056667106229),.UNSPECIFIED.);
#3040=B_SPLINE_CURVE_WITH_KNOTS('',3,(#48740,#48741,#48742,#48743,#48744,
#48745,#48746,#48747,#48748,#48749,#48750,#48751,#48752,#48753,#48754,#48755,
#48756,#48757,#48758,#48759,#48760,#48761,#48762,#48763,#48764,#48765,#48766,
#48767,#48768,#48769,#48770,#48771,#48772,#48773,#48774,#48775),
 .UNSPECIFIED.,.F.,.F.,(4,2,2,2,2,2,2,2,2,2,2,2,2,2,2,2,2,4),(17.7416164546727,
17.7581937026132,17.8052897667917,17.8505949548622,17.8963342504639,17.9428341472151,
17.9875910340227,18.0342105180494,18.0800707723051,18.124652551507,18.1712871824617,
18.2166406572815,18.2619848045744,18.3085503929415,18.3533657882032,18.4003592098579,
18.446278791736,18.4801374015765),.UNSPECIFIED.);
#3041=B_SPLINE_CURVE_WITH_KNOTS('',3,(#48776,#48777,#48778,#48779,#48780,
#48781,#48782,#48783,#48784,#48785,#48786,#48787,#48788,#48789,#48790,#48791,
#48792,#48793,#48794,#48795,#48796,#48797,#48798,#48799,#48800,#48801,#48802,
#48803,#48804,#48805,#48806,#48807,#48808,#48809,#48810,#48811,#48812,#48813),
 .UNSPECIFIED.,.F.,.F.,(4,2,2,2,2,2,2,2,2,2,2,2,2,2,2,2,2,2,4),(2.96056667106229,
2.96492507840458,3.00987622748865,3.05658369115965,3.10200096713613,3.14749048109044,
3.19424386894225,3.23892780465305,3.28492439308362,3.33166335864177,3.3765506531,
3.42318675517329,3.46898366970959,3.51441887461108,3.56165143931351,3.60649480370264,
3.65245839321213,3.69924258617203,3.70124435567),.UNSPECIFIED.);
#3042=B_SPLINE_CURVE_WITH_KNOTS('',3,(#48818,#48819,#48820,#48821,#48822,
#48823,#48824,#48825,#48826,#48827,#48828,#48829,#48830,#48831,#48832,#48833,
#48834,#48835,#48836,#48837,#48838,#48839,#48840,#48841,#48842,#48843,#48844,
#48845,#48846,#48847,#48848,#48849,#48850,#48851,#48852,#48853),
 .UNSPECIFIED.,.F.,.F.,(4,2,2,2,2,2,2,2,2,2,2,2,2,2,2,2,2,4),(17.002935008964,
17.0259159067871,17.0726902796453,17.117698909592,17.1640720079207,17.2102290646699,
17.2547667636235,17.301404789293,17.3470724875982,17.391917818806,17.4388344123328,
17.4839738011972,17.5299894371059,17.5763017108472,17.6209316820209,17.6676058954979,
17.7134384045876,17.7416164546727),.UNSPECIFIED.);
#3043=B_SPLINE_CURVE_WITH_KNOTS('',3,(#48854,#48855,#48856,#48857,#48858,
#48859,#48860,#48861,#48862,#48863,#48864,#48865,#48866,#48867,#48868,#48869,
#48870,#48871,#48872,#48873,#48874,#48875,#48876,#48877,#48878,#48879,#48880,
#48881,#48882,#48883,#48884,#48885,#48886,#48887,#48888,#48889),
 .UNSPECIFIED.,.F.,.F.,(4,2,2,2,2,2,2,2,2,2,2,2,2,2,2,2,2,4),(3.70124435567,
3.74399270352421,3.79043516379055,3.83649298289209,3.88175593971899,3.92880219425985,
3.97372113000247,4.01951325018307,4.0662546751028,4.11089815702418,4.15717909203302,
4.20358177465394,4.24870726106109,4.29560414076508,4.34067748019848,4.38633433906348,
4.43306819834531,4.44139309323576),.UNSPECIFIED.);
#3044=B_SPLINE_CURVE_WITH_KNOTS('',3,(#48894,#48895,#48896,#48897,#48898,
#48899,#48900,#48901,#48902,#48903,#48904,#48905,#48906,#48907,#48908,#48909,
#48910,#48911,#48912,#48913,#48914,#48915,#48916,#48917,#48918,#48919,#48920,
#48921,#48922,#48923,#48924,#48925,#48926,#48927,#48928,#48929),
 .UNSPECIFIED.,.F.,.F.,(4,2,2,2,2,2,2,2,2,2,2,2,2,2,2,2,2,4),(16.2641372477882,
16.2938030439013,16.3403922128616,16.3852327649267,16.4318876926505,16.4778418228271,
16.5224230010358,16.5690903677485,16.6145405429621,16.6597873151308,16.7064589317587,
16.7513738187352,16.7981669545333,16.8442036947422,16.8887271733991,16.9353636748532,
16.9809031318305,17.002935008964),.UNSPECIFIED.);
#3045=B_SPLINE_CURVE_WITH_KNOTS('',3,(#48930,#48931,#48932,#48933,#48934,
#48935,#48936,#48937,#48938,#48939,#48940,#48941,#48942,#48943,#48944,#48945,
#48946,#48947,#48948,#48949,#48950,#48951,#48952,#48953,#48954,#48955,#48956,
#48957,#48958,#48959,#48960,#48961,#48962,#48963,#48964,#48965),
 .UNSPECIFIED.,.F.,.F.,(4,2,2,2,2,2,2,2,2,2,2,2,2,2,2,2,2,4),(4.44139309323576,
4.47768369479005,4.52383758291686,4.57065155177945,4.61567630686354,4.66246297203597,
4.70776020748785,4.7533204420323,4.80007956137218,4.8447406734777,4.8908048094463,
4.93755248955131,4.98249808878681,5.02919719884178,5.0748218415068,5.12031038865077,
5.16760288129374,5.1818539671131),.UNSPECIFIED.);
#3046=B_SPLINE_CURVE_WITH_KNOTS('',3,(#48970,#48971,#48972,#48973,#48974,
#48975,#48976,#48977,#48978,#48979,#48980,#48981,#48982,#48983,#48984,#48985,
#48986,#48987,#48988,#48989,#48990,#48991,#48992,#48993,#48994,#48995,#48996,
#48997,#48998,#48999,#49000,#49001,#49002,#49003,#49004,#49005),
 .UNSPECIFIED.,.F.,.F.,(4,2,2,2,2,2,2,2,2,2,2,2,2,2,2,2,2,4),(15.5253008226521,
15.5614208712953,15.6076307463169,15.6521806514462,15.6988024510405,15.7445285973342,
15.7892808885852,15.8362633798431,15.8814623032694,15.9272761463232,15.9736600003967,
16.0183472154503,16.0650263145743,16.1109370835491,16.1556467547297,16.2028290254408,
16.2482129532865,16.2641372477882),.UNSPECIFIED.);
#3047=B_SPLINE_CURVE_WITH_KNOTS('',3,(#49006,#49007,#49008,#49009,#49010,
#49011,#49012,#49013,#49014,#49015,#49016,#49017,#49018,#49019,#49020,#49021,
#49022,#49023,#49024,#49025,#49026,#49027,#49028,#49029,#49030,#49031,#49032,
#49033,#49034,#49035,#49036,#49037,#49038,#49039,#49040,#49041),
 .UNSPECIFIED.,.F.,.F.,(4,2,2,2,2,2,2,2,2,2,2,2,2,2,2,2,2,4),(5.1818539671131,
5.21237880454505,5.258394968262,5.30515700825967,5.34994371692685,5.39643143835995,
5.44226233196025,5.48755936077848,5.53464520113254,5.57944804045745,5.62527291369698,
5.67197040786348,5.71660500923211,5.76291244064308,5.80904038797896,5.85417959966551,
5.90109443452282,5.92163532828753),.UNSPECIFIED.);
#3048=B_SPLINE_CURVE_WITH_KNOTS('',3,(#49046,#49047,#49048,#49049,#49050,
#49051,#49052,#49053,#49054,#49055,#49056,#49057,#49058,#49059,#49060,#49061,
#49062,#49063,#49064,#49065,#49066,#49067,#49068,#49069,#49070,#49071,#49072,
#49073,#49074,#49075,#49076,#49077,#49078,#49079,#49080,#49081),
 .UNSPECIFIED.,.F.,.F.,(4,2,2,2,2,2,2,2,2,2,2,2,2,2,2,2,2,4),(14.7873695620709,
14.8300506862385,14.8760153817406,14.9205240016754,14.9671371535707,15.0126019576596,
15.0576755801971,15.1043686547149,15.149301357282,15.1958140370104,15.2418832855322,
15.286374482974,15.3329751561295,15.3785518380475,15.4234279626835,15.4702466599603,
15.5152945505239,15.5253008226521),.UNSPECIFIED.);
#3049=B_SPLINE_CURVE_WITH_KNOTS('',3,(#49082,#49083,#49084,#49085,#49086,
#49087,#49088,#49089,#49090,#49091,#49092,#49093,#49094,#49095,#49096,#49097,
#49098,#49099,#49100,#49101,#49102,#49103,#49104,#49105,#49106,#49107,#49108,
#49109,#49110,#49111,#49112,#49113,#49114,#49115,#49116,#49117),
 .UNSPECIFIED.,.F.,.F.,(4,2,2,2,2,2,2,2,2,2,2,2,2,2,2,2,2,4),(5.92163532828753,
5.94600637034905,5.99167472503286,6.03834442621258,6.08290534138804,6.12906543193699,
6.17556776582538,6.22058468374404,6.26736631647045,6.31246290290152,6.358011917132,
6.40468792773244,6.44925237282631,6.4953007135921,6.54223498706927,6.58716711269207,
6.63385553062737,6.66068791027176),.UNSPECIFIED.);
#3050=B_SPLINE_CURVE_WITH_KNOTS('',3,(#49122,#49123,#49124,#49125,#49126,
#49127,#49128,#49129,#49130,#49131,#49132,#49133,#49134,#49135,#49136,#49137,
#49138,#49139,#49140,#49141,#49142,#49143,#49144,#49145,#49146,#49147,#49148,
#49149,#49150,#49151,#49152,#49153,#49154,#49155,#49156,#49157,#49158,#49159),
 .UNSPECIFIED.,.F.,.F.,(4,2,2,2,2,2,2,2,2,2,2,2,2,2,2,2,2,2,4),(14.0482100339955,
14.0502949245492,14.096984232057,14.142851009537,14.1876060347159,14.2347388331608,
14.2800782706825,14.3257899974572,14.3723273782223,14.41711976203,14.463762437258,
14.5096613573186,14.55425504223,14.6009122351073,14.6463049690835,14.6916352778898,
14.7382430334376,14.7830983471007,14.7873695620709),.UNSPECIFIED.);
#3051=B_SPLINE_CURVE_WITH_KNOTS('',3,(#49160,#49161,#49162,#49163,#49164,
#49165,#49166,#49167,#49168,#49169,#49170,#49171,#49172,#49173,#49174,#49175,
#49176,#49177,#49178,#49179,#49180,#49181,#49182,#49183,#49184,#49185,#49186,
#49187,#49188,#49189,#49190,#49191,#49192,#49193,#49194,#49195),
 .UNSPECIFIED.,.F.,.F.,(4,2,2,2,2,2,2,2,2,2,2,2,2,2,2,2,2,4),(6.66068791027176,
6.67919937428358,6.72466854077273,6.77138281680808,6.8160205136328,6.86199546468963,
6.90869606620136,6.95356006101863,7.00017259357045,7.04588152905359,7.09129151458587,
7.13849904618301,7.1832836822818,7.22922137847032,7.27595882272717,7.32067836819823,
7.3670926336791,7.40074313214862),.UNSPECIFIED.);
#3052=B_SPLINE_CURVE_WITH_KNOTS('',3,(#49200,#49201,#49202,#49203,#49204,
#49205,#49206,#49207,#49208,#49209,#49210,#49211,#49212,#49213,#49214,#49215,
#49216,#49217,#49218,#49219,#49220,#49221,#49222,#49223,#49224,#49225,#49226,
#49227,#49228,#49229,#49230,#49231,#49232,#49233,#49234,#49235),
 .UNSPECIFIED.,.F.,.F.,(4,2,2,2,2,2,2,2,2,2,2,2,2,2,2,2,2,4),(13.3095464675158,
13.3179418806692,13.3645829204745,13.4101456027589,13.4551345123131,13.5019343594699,
13.5469666402861,13.5932875705783,13.6394722908042,13.6840250076321,13.7306726518614,
13.7763692796775,13.8212020202917,13.8681498816812,13.9133183606713,13.9592929931832,
14.0056379903772,14.0482100339955),.UNSPECIFIED.);
#3053=B_SPLINE_CURVE_WITH_KNOTS('',3,(#49236,#49237,#49238,#49239,#49240,
#49241,#49242,#49243,#49244,#49245,#49246,#49247,#49248,#49249,#49250,#49251,
#49252,#49253,#49254,#49255,#49256,#49257,#49258,#49259,#49260,#49261,#49262,
#49263,#49264,#49265,#49266,#49267,#49268,#49269,#49270,#49271),
 .UNSPECIFIED.,.F.,.F.,(4,2,2,2,2,2,2,2,2,2,2,2,2,2,2,2,2,4),(7.40074313214862,
7.41304791193527,7.45828058796883,7.50529645981043,7.55014367964178,7.59590467610001,
7.64259365979734,7.68719438829927,7.73344217485688,7.77972977945611,7.82481959518803,
7.87168035903332,7.91667006179515,7.96229014337893,8.00896624300127,8.05352690669973,
8.09964223179755,8.13994719566162),.UNSPECIFIED.);
#3054=B_SPLINE_CURVE_WITH_KNOTS('',3,(#49276,#49277,#49278,#49279,#49280,
#49281,#49282,#49283,#49284,#49285,#49286,#49287,#49288,#49289,#49290,#49291,
#49292,#49293,#49294,#49295,#49296,#49297,#49298,#49299,#49300,#49301,#49302,
#49303,#49304,#49305,#49306,#49307,#49308,#49309,#49310,#49311),
 .UNSPECIFIED.,.F.,.F.,(4,2,2,2,2,2,2,2,2,2,2,2,2,2,2,2,2,4),(12.5705412100685,
12.5848546363202,12.6320513419363,12.6774479779185,12.7229914291377,12.7695957874756,
12.8144503148156,12.8611058709474,12.9070763074098,12.951650697705,12.9983178350321,
13.0437851961517,13.0889992823918,13.1356902587469,13.1806230630583,13.2273560115123,
13.2734149408359,13.3095464675158),.UNSPECIFIED.);
#3055=B_SPLINE_CURVE_WITH_KNOTS('',3,(#49312,#49313,#49314,#49315,#49316,
#49317,#49318,#49319,#49320,#49321,#49322,#49323,#49324,#49325,#49326,#49327,
#49328,#49329,#49330,#49331,#49332,#49333,#49334,#49335,#49336,#49337,#49338,
#49339,#49340,#49341,#49342,#49343,#49344,#49345,#49346,#49347,#49348,#49349),
 .UNSPECIFIED.,.F.,.F.,(4,2,2,2,2,2,2,2,2,2,2,2,2,2,2,2,2,2,4),(8.13994719566162,
8.1463316268328,8.19131496388372,8.2380593874591,8.28326280667136,8.33020598996195,
8.37537161294956,8.42146167930536,8.46779890512908,8.51245656585315,8.55916791039741,
8.60502388501555,8.64982522039719,8.69694438308839,8.7422725099988,8.78807715134522,
8.83459899420235,8.87937738670119,8.87958134265245),.UNSPECIFIED.);
#3056=B_SPLINE_CURVE_WITH_KNOTS('',3,(#49354,#49355,#49356,#49357,#49358,
#49359,#49360,#49361,#49362,#49363,#49364,#49365,#49366,#49367,#49368,#49369,
#49370,#49371,#49372,#49373,#49374,#49375,#49376,#49377,#49378,#49379,#49380,
#49381,#49382,#49383,#49384,#49385,#49386,#49387,#49388,#49389),
 .UNSPECIFIED.,.F.,.F.,(4,2,2,2,2,2,2,2,2,2,2,2,2,2,2,2,2,4),(11.8321815561307,
11.8527802750529,11.8996021687833,11.9446521456017,11.9907033317147,12.0369186139489,
12.0814657613186,12.1280739153687,12.1738072480122,12.2185277557899,12.2655192350349,
12.3107256977114,12.3564778448273,12.4028721237148,12.4475687949672,12.4942402335744,
12.5401634891127,12.5705412100685),.UNSPECIFIED.);
#3057=B_SPLINE_CURVE_WITH_KNOTS('',3,(#49390,#49391,#49392,#49393,#49394,
#49395,#49396,#49397,#49398,#49399,#49400,#49401,#49402,#49403,#49404,#49405,
#49406,#49407,#49408,#49409,#49410,#49411,#49412,#49413,#49414,#49415,#49416,
#49417,#49418,#49419,#49420,#49421,#49422,#49423,#49424,#49425),
 .UNSPECIFIED.,.F.,.F.,(4,2,2,2,2,2,2,2,2,2,2,2,2,2,2,2,2,4),(8.87958134265245,
8.92602852613987,8.97190922554665,9.01652860508801,9.06319528540556,9.10856829663463,
9.15396816684055,9.20055253946269,9.24538645185148,9.29245567553163,9.33839133852289,
9.38290947461184,9.42952391977244,9.47495799934766,9.52008834525836,9.56674688093536,
9.6116477128901,9.61793661341104),.UNSPECIFIED.);
#3058=B_SPLINE_CURVE_WITH_KNOTS('',3,(#49430,#49431,#49432,#49433,#49434,
#49435,#49436,#49437,#49438,#49439,#49440,#49441,#49442,#49443,#49444,#49445,
#49446,#49447,#49448,#49449,#49450,#49451,#49452,#49453,#49454,#49455,#49456,
#49457,#49458,#49459,#49460,#49461,#49462,#49463,#49464,#49465),
 .UNSPECIFIED.,.F.,.F.,(4,2,2,2,2,2,2,2,2,2,2,2,2,2,2,2,2,4),(11.0945157929649,
11.1213867420797,11.1679850354348,11.212830558321,11.2596899586864,11.3056487691199,
11.3501304725593,11.3967192229775,11.4421794409724,11.4871976310158,11.5338877382452,
11.5788167443302,11.6252436424475,11.6713128846608,11.7157888443594,11.7623703136435,
11.8079484981885,11.8321815561307),.UNSPECIFIED.);
#3059=B_SPLINE_CURVE_WITH_KNOTS('',3,(#49466,#49467,#49468,#49469,#49470,
#49471,#49472,#49473,#49474,#49475,#49476,#49477,#49478,#49479,#49480,#49481,
#49482,#49483,#49484,#49485,#49486,#49487,#49488,#49489,#49490,#49491,#49492,
#49493,#49494,#49495,#49496,#49497,#49498,#49499,#49500,#49501),
 .UNSPECIFIED.,.F.,.F.,(4,2,2,2,2,2,2,2,2,2,2,2,2,2,2,2,2,4),(9.61793661341104,
9.65826687912693,9.70429689093938,9.74877836477337,9.79537166131895,9.84090708321871,
9.88582218876157,9.93259567749554,9.97760169196064,10.0238180381891,10.0699792278232,
10.1144983947581,10.1611035398683,10.2067785301348,10.2515491657397,10.2984763720027,
10.3436239452287,10.3558181882677),.UNSPECIFIED.);
#3060=B_SPLINE_CURVE_WITH_KNOTS('',3,(#49506,#49507,#49508,#49509,#49510,
#49511,#49512,#49513,#49514,#49515,#49516,#49517,#49518,#49519,#49520,#49521,
#49522,#49523,#49524,#49525,#49526,#49527,#49528,#49529,#49530,#49531,#49532,
#49533,#49534,#49535,#49536,#49537,#49538,#49539,#49540,#49541),
 .UNSPECIFIED.,.F.,.F.,(4,2,2,2,2,2,2,2,2,2,2,2,2,2,2,2,2,4),(10.3558181865992,
10.3895062288278,10.4358326314552,10.4804680791543,10.5271205064737,10.5729708577389,
10.6176765737363,10.6647940480184,10.710117621532,10.7557512885806,10.8022746889798,
10.8470530120057,10.8936670905081,10.9395538338801,10.9841105681321,11.0307384394129,
11.0761201700909,11.0945157929649),.UNSPECIFIED.);
#3061=B_SPLINE_CURVE_WITH_KNOTS('',3,(#49542,#49543,#49544,#49545,#49546,
#49547,#49548,#49549,#49550,#49551,#49552,#49553,#49554,#49555,#49556,#49557,
#49558,#49559,#49560,#49561,#49562,#49563,#49564,#49565,#49566,#49567,#49568,
#49569,#49570,#49571,#49572,#49573,#49574,#49575,#49576,#49577),
 .UNSPECIFIED.,.F.,.F.,(4,2,2,2,2,2,2,2,2,2,2,2,2,2,2,2,2,4),(10.3558181882677,
10.3895062304569,10.4358326331012,10.4804680808162,10.5271205081509,10.572970859433,
10.6176765754436,10.6647940497431,10.7101176232735,10.7557512903329,10.8022746907493,
10.8470530137919,10.8936670923103,10.9395538356998,10.9841105699663,11.0307384412633,
11.0761201719588,11.0945157948807),.UNSPECIFIED.);
#3062=B_SPLINE_CURVE_WITH_KNOTS('',3,(#49582,#49583,#49584,#49585,#49586,
#49587,#49588,#49589,#49590,#49591,#49592,#49593,#49594,#49595,#49596,#49597,
#49598,#49599,#49600,#49601,#49602,#49603,#49604,#49605,#49606,#49607,#49608,
#49609,#49610,#49611,#49612,#49613,#49614,#49615,#49616,#49617),
 .UNSPECIFIED.,.F.,.F.,(4,2,2,2,2,2,2,2,2,2,2,2,2,2,2,2,2,4),(9.61793661197057,
9.65826687772365,9.7042968895204,9.74877836334091,9.79537165987244,9.84090708175655,
9.88582218728856,9.93259567600637,9.977601690456,10.0238180366761,10.069979226294,
10.1144983932143,10.16110353831,10.2067785285603,10.2515491641532,10.2984763703993,
10.3436239436092,10.3558181865992),.UNSPECIFIED.);
#3063=B_SPLINE_CURVE_WITH_KNOTS('',3,(#49618,#49619,#49620,#49621,#49622,
#49623,#49624,#49625,#49626,#49627,#49628,#49629,#49630,#49631,#49632,#49633,
#49634,#49635,#49636,#49637,#49638,#49639,#49640,#49641,#49642,#49643,#49644,
#49645,#49646,#49647,#49648,#49649,#49650,#49651,#49652,#49653),
 .UNSPECIFIED.,.F.,.F.,(4,2,2,2,2,2,2,2,2,2,2,2,2,2,2,2,2,4),(11.0945157948807,
11.1213867439599,11.1679850373331,11.2128305602366,11.2596899606121,11.3056487710637,
11.3501304745185,11.3967192249533,11.4421794429662,11.4871976330225,11.5338877402705,
11.5788167463733,11.625243644501,11.6713128867326,11.7157888464474,11.762370315748,
11.8079485003112,11.8321815583089),.UNSPECIFIED.);
#3064=B_SPLINE_CURVE_WITH_KNOTS('',3,(#49658,#49659,#49660,#49661,#49662,
#49663,#49664,#49665,#49666,#49667,#49668,#49669,#49670,#49671,#49672,#49673,
#49674,#49675,#49676,#49677,#49678,#49679,#49680,#49681,#49682,#49683,#49684,
#49685,#49686,#49687,#49688,#49689,#49690,#49691,#49692,#49693),
 .UNSPECIFIED.,.F.,.F.,(4,2,2,2,2,2,2,2,2,2,2,2,2,2,2,2,2,4),(8.87958134142251,
8.92602852493827,8.97190922433066,9.01652860386053,9.06319528416507,9.10856829537987,
9.15396816557657,9.20055253818396,9.24538645055861,9.29245567423173,9.33839133720815,
9.38290947328484,9.42952391843202,9.47495799799238,9.5200883438932,9.56674687955462,
9.61164771149445,9.61793661197057),.UNSPECIFIED.);
#3065=B_SPLINE_CURVE_WITH_KNOTS('',3,(#49694,#49695,#49696,#49697,#49698,
#49699,#49700,#49701,#49702,#49703,#49704,#49705,#49706,#49707,#49708,#49709,
#49710,#49711,#49712,#49713,#49714,#49715,#49716,#49717,#49718,#49719,#49720,
#49721,#49722,#49723,#49724,#49725,#49726,#49727,#49728,#49729),
 .UNSPECIFIED.,.F.,.F.,(4,2,2,2,2,2,2,2,2,2,2,2,2,2,2,2,2,4),(11.8321815583089,
11.8527802771891,11.8996021709384,11.9446521477749,11.9907033338989,12.0369186161519,
12.0814657635389,12.128073917606,12.1738072502682,12.2185277580605,12.2655192373249,
12.31072570002,12.3564778471481,12.402872126055,12.4475687973262,12.4942402359512,
12.5401634915089,12.5705412125212),.UNSPECIFIED.);
#3066=B_SPLINE_CURVE_WITH_KNOTS('',3,(#49734,#49735,#49736,#49737,#49738,
#49739,#49740,#49741,#49742,#49743,#49744,#49745,#49746,#49747,#49748,#49749,
#49750,#49751,#49752,#49753,#49754,#49755,#49756,#49757,#49758,#49759,#49760,
#49761,#49762,#49763,#49764,#49765,#49766,#49767,#49768,#49769,#49770,#49771),
 .UNSPECIFIED.,.F.,.F.,(4,2,2,2,2,2,2,2,2,2,2,2,2,2,2,2,2,2,4),(8.13994719462425,
8.14633162583834,8.19131496287961,8.23805938644507,8.28326280564246,8.33020598891935,
8.37537161189387,8.42146167824292,8.46779890405304,8.51245656476452,8.55916790929672,
8.60502388390122,8.64982521927269,8.69694438194964,8.74227250884644,8.78807715018487,
8.83459899302762,8.87937738551268,8.87958134142251),.UNSPECIFIED.);
#3067=B_SPLINE_CURVE_WITH_KNOTS('',3,(#49772,#49773,#49774,#49775,#49776,
#49777,#49778,#49779,#49780,#49781,#49782,#49783,#49784,#49785,#49786,#49787,
#49788,#49789,#49790,#49791,#49792,#49793,#49794,#49795,#49796,#49797,#49798,
#49799,#49800,#49801,#49802,#49803,#49804,#49805,#49806,#49807),
 .UNSPECIFIED.,.F.,.F.,(4,2,2,2,2,2,2,2,2,2,2,2,2,2,2,2,2,4),(12.5705412125212,
12.5848546387325,12.6320513443688,12.6774479803703,12.7229914316032,12.7695957899609,
12.81445031732,12.8611058734703,12.9070763099523,12.9516507002645,12.99831783761,
13.0437851987491,13.0889992850039,13.1356902613794,13.1806230657103,13.2273560141773,
13.2734149435215,13.3095464702606),.UNSPECIFIED.);
#3068=B_SPLINE_CURVE_WITH_KNOTS('',3,(#49812,#49813,#49814,#49815,#49816,
#49817,#49818,#49819,#49820,#49821,#49822,#49823,#49824,#49825,#49826,#49827,
#49828,#49829,#49830,#49831,#49832,#49833,#49834,#49835,#49836,#49837,#49838,
#49839,#49840,#49841,#49842,#49843,#49844,#49845,#49846,#49847),
 .UNSPECIFIED.,.F.,.F.,(4,2,2,2,2,2,2,2,2,2,2,2,2,2,2,2,2,4),(7.4007431312885,
7.41304791111891,7.45828058714382,7.50529645897655,7.55014367879521,7.59590467524459,
7.64259365893083,7.68719438742294,7.73344217397141,7.7797297785534,7.82481959427612,
7.87168035811193,7.91667006085986,7.96229014243438,8.00896624204524,8.05352690573283,
8.09964223082121,8.13994719462425),.UNSPECIFIED.);
#3069=B_SPLINE_CURVE_WITH_KNOTS('',3,(#49848,#49849,#49850,#49851,#49852,
#49853,#49854,#49855,#49856,#49857,#49858,#49859,#49860,#49861,#49862,#49863,
#49864,#49865,#49866,#49867,#49868,#49869,#49870,#49871,#49872,#49873,#49874,
#49875,#49876,#49877,#49878,#49879,#49880,#49881,#49882,#49883),
 .UNSPECIFIED.,.F.,.F.,(4,2,2,2,2,2,2,2,2,2,2,2,2,2,2,2,2,4),(13.3095464702606,
13.317941883373,13.3645829231975,13.4101456055024,13.4551345150724,13.5019343622502,
13.5469666430868,13.5932875733925,13.6394722936394,13.6840250104865,13.7306726547352,
13.7763692825722,13.8212020232032,13.8681498846145,13.9133183636254,13.9592929961519,
14.0056379933677,14.0482100370503),.UNSPECIFIED.);
#3070=B_SPLINE_CURVE_WITH_KNOTS('',3,(#49888,#49889,#49890,#49891,#49892,
#49893,#49894,#49895,#49896,#49897,#49898,#49899,#49900,#49901,#49902,#49903,
#49904,#49905,#49906,#49907,#49908,#49909,#49910,#49911,#49912,#49913,#49914,
#49915,#49916,#49917,#49918,#49919,#49920,#49921,#49922,#49923),
 .UNSPECIFIED.,.F.,.F.,(4,2,2,2,2,2,2,2,2,2,2,2,2,2,2,2,2,4),(6.66068790957161,
6.67919937362265,6.72466854010414,6.77138281612983,6.81602051294445,6.86199546399339,
6.90869606549543,6.95356006030469,7.00017259284827,7.04588152831696,7.09129151384102,
7.13849904542972,7.18328368151711,7.22922137769738,7.27595882194379,7.32067836740631,
7.36709263287862,7.4007431312885),.UNSPECIFIED.);
#3071=B_SPLINE_CURVE_WITH_KNOTS('',3,(#49924,#49925,#49926,#49927,#49928,
#49929,#49930,#49931,#49932,#49933,#49934,#49935,#49936,#49937,#49938,#49939,
#49940,#49941,#49942,#49943,#49944,#49945,#49946,#49947,#49948,#49949,#49950,
#49951,#49952,#49953,#49954,#49955,#49956,#49957,#49958,#49959,#49960,#49961),
 .UNSPECIFIED.,.F.,.F.,(4,2,2,2,2,2,2,2,2,2,2,2,2,2,2,2,2,2,4),(14.0482100370503,
14.0502949275604,14.0969842350884,14.1428510125903,14.1876060377872,14.2347388362546,
14.2800782737978,14.3257900005883,14.3723273813755,14.4171197652046,14.4637624404534,
14.5096613605359,14.5542550454664,14.6009122383646,14.6463049723626,14.6916352811859,
14.7382430367566,14.7830983504416,14.7873695654535),.UNSPECIFIED.);
#3072=B_SPLINE_CURVE_WITH_KNOTS('',3,(#49966,#49967,#49968,#49969,#49970,
#49971,#49972,#49973,#49974,#49975,#49976,#49977,#49978,#49979,#49980,#49981,
#49982,#49983,#49984,#49985,#49986,#49987,#49988,#49989,#49990,#49991,#49992,
#49993,#49994,#49995,#49996,#49997,#49998,#49999,#50000,#50001),
 .UNSPECIFIED.,.F.,.F.,(4,2,2,2,2,2,2,2,2,2,2,2,2,2,2,2,2,4),(5.92163532773223,
5.94600636983764,5.99167472451486,6.03834442568581,6.08290534085326,6.12906543139539,
6.17556776526837,6.22058468317993,6.26736631589905,6.31246290231792,6.35801191654115,
6.40468792713218,6.44925237221679,6.49530071297518,6.5422349864363,6.58716711205166,
6.6338555299793,6.66068790957161),.UNSPECIFIED.);
#3073=B_SPLINE_CURVE_WITH_KNOTS('',3,(#50002,#50003,#50004,#50005,#50006,
#50007,#50008,#50009,#50010,#50011,#50012,#50013,#50014,#50015,#50016,#50017,
#50018,#50019,#50020,#50021,#50022,#50023,#50024,#50025,#50026,#50027,#50028,
#50029,#50030,#50031,#50032,#50033,#50034,#50035,#50036,#50037),
 .UNSPECIFIED.,.F.,.F.,(4,2,2,2,2,2,2,2,2,2,2,2,2,2,2,2,2,4),(14.7873695654535,
14.8300506895943,14.8760153851188,14.9205240050731,14.9671371569893,15.0126019611003,
15.057675583655,15.1043686581955,15.1493013607845,15.1958140405279,15.2418832890724,
15.2863744865348,15.3329751597116,15.3785518416522,15.4234279663063,15.4702466636066,
15.5152945541928,15.52530082637),.UNSPECIFIED.);
#3074=B_SPLINE_CURVE_WITH_KNOTS('',3,(#50042,#50043,#50044,#50045,#50046,
#50047,#50048,#50049,#50050,#50051,#50052,#50053,#50054,#50055,#50056,#50057,
#50058,#50059,#50060,#50061,#50062,#50063,#50064,#50065,#50066,#50067,#50068,
#50069,#50070,#50071,#50072,#50073,#50074,#50075,#50076,#50077),
 .UNSPECIFIED.,.F.,.F.,(4,2,2,2,2,2,2,2,2,2,2,2,2,2,2,2,2,4),(5.18185396668694,
5.21237880416024,5.25839496787151,5.30515700786141,5.34994371652288,5.39643143795004,
5.44226233153737,5.48755936034949,5.53464520069729,5.57944804001234,5.62527291324563,
5.6719704074037,5.71660500876536,5.76291244016987,5.80904038749152,5.85417959917163,
5.90109443402236,5.92163532773223),.UNSPECIFIED.);
#3075=B_SPLINE_CURVE_WITH_KNOTS('',3,(#50078,#50079,#50080,#50081,#50082,
#50083,#50084,#50085,#50086,#50087,#50088,#50089,#50090,#50091,#50092,#50093,
#50094,#50095,#50096,#50097,#50098,#50099,#50100,#50101,#50102,#50103,#50104,
#50105,#50106,#50107,#50108,#50109,#50110,#50111,#50112,#50113),
 .UNSPECIFIED.,.F.,.F.,(4,2,2,2,2,2,2,2,2,2,2,2,2,2,2,2,2,4),(15.52530082637,
15.5614208749801,15.6076307500252,15.6521806551763,15.6988024547926,15.7445286011097,
15.7892808923799,15.8362633836619,15.8814623071114,15.927276150182,15.9736600042795,
16.0183472193562,16.0650263185026,16.1109370875013,16.1556467587023,16.2028290294383,
16.2482129573077,16.2641372518591),.UNSPECIFIED.);
#3076=B_SPLINE_CURVE_WITH_KNOTS('',3,(#50118,#50119,#50120,#50121,#50122,
#50123,#50124,#50125,#50126,#50127,#50128,#50129,#50130,#50131,#50132,#50133,
#50134,#50135,#50136,#50137,#50138,#50139,#50140,#50141,#50142,#50143,#50144,
#50145,#50146,#50147,#50148,#50149,#50150,#50151,#50152,#50153),
 .UNSPECIFIED.,.F.,.F.,(4,2,2,2,2,2,2,2,2,2,2,2,2,2,2,2,2,4),(4.44139309291887,
4.4776836945143,4.52383758263681,4.5706515514869,4.61567630656631,4.66246297173395,
4.70776020717613,4.75332044171567,4.80007956104877,4.84474067314722,4.89080480911077,
4.93755248920882,4.9824980884388,5.02919719848812,5.0748218411417,5.12031038828011,
5.16760288091741,5.18185396668694),.UNSPECIFIED.);
#3077=B_SPLINE_CURVE_WITH_KNOTS('',3,(#50154,#50155,#50156,#50157,#50158,
#50159,#50160,#50161,#50162,#50163,#50164,#50165,#50166,#50167,#50168,#50169,
#50170,#50171,#50172,#50173,#50174,#50175,#50176,#50177,#50178,#50179,#50180,
#50181,#50182,#50183,#50184,#50185,#50186,#50187,#50188,#50189),
 .UNSPECIFIED.,.F.,.F.,(4,2,2,2,2,2,2,2,2,2,2,2,2,2,2,2,2,4),(16.2641372518591,
16.2938030479407,16.3403922169256,16.3852327690144,16.4318876967614,16.4778418269624,
16.5224230051924,16.5690903719281,16.6145405471659,16.6597873193538,16.7064589360066,
16.7513738230071,16.7981669588227,16.8442036990566,16.8887271777361,16.9353636792139,
16.9809031362162,17.002935013404),.UNSPECIFIED.);
#3078=B_SPLINE_CURVE_WITH_KNOTS('',3,(#50194,#50195,#50196,#50197,#50198,
#50199,#50200,#50201,#50202,#50203,#50204,#50205,#50206,#50207,#50208,#50209,
#50210,#50211,#50212,#50213,#50214,#50215,#50216,#50217,#50218,#50219,#50220,
#50221,#50222,#50223,#50224,#50225,#50226,#50227,#50228,#50229),
 .UNSPECIFIED.,.F.,.F.,(4,2,2,2,2,2,2,2,2,2,2,2,2,2,2,2,2,4),(3.70124435544509,
3.74399270334172,3.79043516360456,3.83649298269546,3.88175593951858,3.92880219405563,
3.97372112979052,4.0195132499672,4.06625467488101,4.11089815679736,4.15717909180209,
4.20358177441128,4.24870726081431,4.29560414051408,4.34067747993884,4.38633433879972,
4.43306819807542,4.44139309291887),.UNSPECIFIED.);
#3079=B_SPLINE_CURVE_WITH_KNOTS('',3,(#50230,#50231,#50232,#50233,#50234,
#50235,#50236,#50237,#50238,#50239,#50240,#50241,#50242,#50243,#50244,#50245,
#50246,#50247,#50248,#50249,#50250,#50251,#50252,#50253,#50254,#50255,#50256,
#50257,#50258,#50259,#50260,#50261,#50262,#50263,#50264,#50265),
 .UNSPECIFIED.,.F.,.F.,(4,2,2,2,2,2,2,2,2,2,2,2,2,2,2,2,2,4),(17.002935013404,
17.025915911193,17.072690284077,17.1176989140485,17.1640720123954,17.2102290691703,
17.2547667681474,17.3014047938411,17.3470724921718,17.3919178234011,17.4388344169549,
17.4839738058451,17.5299894417733,17.576301715541,17.6209316867396,17.6676059002416,
17.7134384093576,17.7416164595014),.UNSPECIFIED.);
#3080=B_SPLINE_CURVE_WITH_KNOTS('',3,(#50270,#50271,#50272,#50273,#50274,
#50275,#50276,#50277,#50278,#50279,#50280,#50281,#50282,#50283,#50284,#50285,
#50286,#50287,#50288,#50289,#50290,#50291,#50292,#50293,#50294,#50295,#50296,
#50297,#50298,#50299,#50300,#50301,#50302,#50303,#50304,#50305,#50306,#50307),
 .UNSPECIFIED.,.F.,.F.,(4,2,2,2,2,2,2,2,2,2,2,2,2,2,2,2,2,2,4),(2.96056667091537,
2.96492507829847,3.00987622737974,3.05658369104791,3.10200096701632,3.14749048096761,
3.19424386881459,3.23892780451988,3.28492439294727,3.33166335850067,3.37655065295563,
3.42318675502558,3.46898366955253,3.51441887445073,3.56165143914983,3.60649480353247,
3.65245839303867,3.69924258599329,3.70124435544509),.UNSPECIFIED.);
#3081=B_SPLINE_CURVE_WITH_KNOTS('',3,(#50308,#50309,#50310,#50311,#50312,
#50313,#50314,#50315,#50316,#50317,#50318,#50319,#50320,#50321,#50322,#50323,
#50324,#50325,#50326,#50327,#50328,#50329,#50330,#50331,#50332,#50333,#50334,
#50335,#50336,#50337,#50338,#50339,#50340,#50341,#50342,#50343),
 .UNSPECIFIED.,.F.,.F.,(4,2,2,2,2,2,2,2,2,2,2,2,2,2,2,2,2,4),(17.7416164595014,
17.7581937074056,17.8052897716113,17.8505949597077,17.8963342553297,17.9428341521077,
17.9875910389412,18.0342105229933,18.0800707772756,18.1246525565008,18.1712871874809,
18.216640662327,18.2619848096412,18.3085503980356,18.3533657933236,18.400359214998,
18.4462787969036,18.4801374068086),.UNSPECIFIED.);
#3082=B_SPLINE_CURVE_WITH_KNOTS('',3,(#50348,#50349,#50350,#50351,#50352,
#50353,#50354,#50355,#50356,#50357,#50358,#50359,#50360,#50361,#50362,#50363,
#50364,#50365,#50366,#50367,#50368,#50369,#50370,#50371,#50372,#50373,#50374,
#50375,#50376,#50377,#50378,#50379,#50380,#50381,#50382,#50383),
 .UNSPECIFIED.,.F.,.F.,(4,2,2,2,2,2,2,2,2,2,2,2,2,2,2,2,2,4),(2.22108960842022,
2.23120408651738,2.27635041765121,2.32327161202571,2.36823721236016,2.41391337632635,
2.46061197044848,2.50519713944098,2.5513666691269,2.59796482409036,2.64299465164124,
2.68978881468655,2.73495033646277,2.78051325751773,2.82722340795193,2.87182391070409,
2.91788757577027,2.96056667091537),.UNSPECIFIED.);
#3083=B_SPLINE_CURVE_WITH_KNOTS('',3,(#50384,#50385,#50386,#50387,#50388,
#50389,#50390,#50391,#50392,#50393,#50394,#50395,#50396,#50397,#50398,#50399,
#50400,#50401,#50402,#50403,#50404,#50405,#50406,#50407,#50408,#50409,#50410,
#50411,#50412,#50413,#50414,#50415,#50416,#50417,#50418,#50419),
 .UNSPECIFIED.,.F.,.F.,(4,2,2,2,2,2,2,2,2,2,2,2,2,2,2,2,2,4),(18.4801374068086,
18.4907658387484,18.5373515732759,18.5827705496792,18.6278503876037,18.6744946287827,
18.7193811593225,18.7659288080364,18.8119468422919,18.8564049604675,18.9029730562544,
18.9484976039111,18.9933693909541,19.040132859827,19.0851285827534,19.1312801378602,
19.1774331259836,19.2175408345414),.UNSPECIFIED.);
#3084=B_SPLINE_CURVE_WITH_KNOTS('',3,(#50424,#50425,#50426,#50427,#50428,
#50429,#50430,#50431,#50432,#50433,#50434,#50435,#50436,#50437,#50438,#50439,
#50440,#50441,#50442,#50443,#50444,#50445,#50446,#50447,#50448,#50449,#50450,
#50451,#50452,#50453,#50454,#50455,#50456,#50457,#50458,#50459),
 .UNSPECIFIED.,.F.,.F.,(4,2,2,2,2,2,2,2,2,2,2,2,2,2,2,2,2,4),(1.48067239643092,
1.4967132601331,1.54219831559389,1.58948594493822,1.63428944893559,1.68030245144475,
1.72708174969294,1.77186789841824,1.81835464146151,1.86425678939566,1.90955548629973,
1.95664189807863,2.00148568451759,2.04731268579268,2.09403346709215,2.13867975716629,
2.18499121798638,2.22108960842022),.UNSPECIFIED.);
#3085=B_SPLINE_CURVE_WITH_KNOTS('',3,(#50460,#50461,#50462,#50463,#50464,
#50465,#50466,#50467,#50468,#50469,#50470,#50471,#50472,#50473,#50474,#50475,
#50476,#50477,#50478,#50479,#50480,#50481,#50482,#50483,#50484,#50485,#50486,
#50487,#50488,#50489,#50490,#50491,#50492,#50493,#50494,#50495,#50496,#50497),
 .UNSPECIFIED.,.F.,.F.,(4,2,2,2,2,2,2,2,2,2,2,2,2,2,2,2,2,2,4),(19.2175408345414,
19.221937402198,19.2685210781433,19.3141891434761,19.3589248273872,19.4058460255822,
19.4509870795851,19.4968133821774,19.5431350562803,19.5877640969252,19.634399062382,
19.6802461572256,19.724925976838,19.7720412018952,19.81736181445,19.862949655886,
19.9094715921544,19.954248074309,19.955968047547),.UNSPECIFIED.);
#3086=B_SPLINE_CURVE_WITH_KNOTS('',3,(#50502,#50503,#50504,#50505,#50506,
#50507,#50508,#50509,#50510,#50511,#50512,#50513,#50514,#50515,#50516,#50517,
#50518,#50519,#50520,#50521,#50522,#50523,#50524,#50525,#50526,#50527,#50528,
#50529,#50530,#50531,#50532,#50533,#50534,#50535,#50536,#50537),
 .UNSPECIFIED.,.F.,.F.,(4,2,2,2,2,2,2,2,2,2,2,2,2,2,2,2,2,4),(0.740262878330326,
0.76242710224918,0.808069985435835,0.854808846306471,0.899429812602798,
0.94557087207502,0.992454683252572,1.03747065149212,1.08424743872217,1.12958660658263,
1.17513888970271,1.22190780151563,1.26658471045133,1.31264188423565,1.35939848502835,
1.40433922056887,1.45103260194552,1.48067239643092),.UNSPECIFIED.);
#3087=B_SPLINE_CURVE_WITH_KNOTS('',3,(#50538,#50539,#50540,#50541,#50542,
#50543,#50544,#50545,#50546,#50547,#50548,#50549,#50550,#50551,#50552,#50553,
#50554,#50555,#50556,#50557,#50558,#50559,#50560,#50561,#50562,#50563,#50564,
#50565,#50566,#50567,#50568,#50569,#50570,#50571,#50572,#50573),
 .UNSPECIFIED.,.F.,.F.,(4,2,2,2,2,2,2,2,2,2,2,2,2,2,2,2,2,4),(19.955968047547,
20.000850484569,20.0467368471769,20.0912761893499,20.1378918513278,20.1832739357276,
20.2285046069091,20.2751045193351,20.3199511150685,20.3667546312751,20.4127173706803,
20.4571887517883,20.5037686958299,20.5492336722642,20.5942218827244,20.6409180673264,
20.685852328368,20.6936878782319),.UNSPECIFIED.);
#3088=B_SPLINE_CURVE_WITH_KNOTS('',3,(#50578,#50579,#50580,#50581,#50582,
#50583,#50584,#50585,#50586,#50587,#50588,#50589,#50590,#50591,#50592,#50593,
#50594,#50595,#50596,#50597,#50598,#50599,#50600,#50601,#50602,#50603,#50604,
#50605,#50606,#50607,#50608,#50609,#50610,#50611,#50612,#50613),
 .UNSPECIFIED.,.F.,.F.,(4,2,2,2,2,2,2,2,2,2,2,2,2,2,2,2,2,4),(1.00000014275486E-6,
0.0364903991724837,0.0742057368406976,0.120984278386942,0.16571626048475,
0.212135354717781,0.258243398985401,0.303486376623694,0.350510827495094,
0.395451299112592,0.441223703714196,0.487964967575798,0.532602258878132,
0.578864855190162,0.62532910035835,0.67044002179057,0.717320863587734,0.740262878330326),
 .UNSPECIFIED.);
#3089=B_SPLINE_CURVE_WITH_KNOTS('',3,(#50614,#50615,#50616,#50617,#50618,
#50619,#50620,#50621,#50622,#50623,#50624,#50625,#50626,#50627,#50628,#50629,
#50630,#50631,#50632,#50633,#50634,#50635,#50636,#50637,#50638,#50639,#50640,
#50641,#50642,#50643,#50644,#50645,#50646,#50647,#50648,#50649),
 .UNSPECIFIED.,.F.,.F.,(4,2,2,2,2,2,2,2,2,2,2,2,2,2,2,2,2,4),(20.6936878782319,
20.732228532913,20.778305724133,20.8227795112891,20.8693557797099,20.9149428959302,
20.9597524918607,21.0065846919771,21.0516438918501,21.0976519462771,21.1438788857884,
21.188432480541,21.2350393010027,21.2807854645354,21.325492530929,21.3724982961973,
21.417717731441,21.4315064083924),.UNSPECIFIED.);
#3090=B_SPLINE_CURVE_WITH_KNOTS('',3,(#50652,#50653,#50654,#50655,#50656,
#50657,#50658,#50659),.UNSPECIFIED.,.F.,.F.,(4,2,2,4),(21.4315064083924,
21.4634358005757,21.493031868375,21.522626598838),.UNSPECIFIED.);
#3091=B_SPLINE_CURVE_WITH_KNOTS('',3,(#50664,#50665,#50666,#50667,#50668,
#50669,#50670,#50671,#50672,#50673,#50674,#50675),.UNSPECIFIED.,.F.,.F.,
(4,2,2,2,2,4),(-0.220493779628296,-0.188155373461082,-0.153829429857051,
-0.103952453260852,-0.0536656706932583,-1.00000014990886E-6),
 .UNSPECIFIED.);
#3092=B_SPLINE_CURVE_WITH_KNOTS('',3,(#50678,#50679,#50680,#50681,#50682,
#50683,#50684,#50685,#50686,#50687,#50688,#50689,#50690,#50691,#50692,#50693,
#50694,#50695,#50696,#50697,#50698,#50699),.UNSPECIFIED.,.F.,.F.,(4,2,2,
2,2,2,2,2,2,2,4),(0.203440126186273,0.213167596868103,0.241856386112924,
0.272211919544501,0.305118112000406,0.341399456620154,0.378879659132554,
0.40534149334872,0.429291364608543,0.44378295238274,0.459192789470913),
 .UNSPECIFIED.);
#3093=B_SPLINE_CURVE_WITH_KNOTS('',3,(#50701,#50702,#50703,#50704,#50705,
#50706,#50707,#50708,#50709,#50710,#50711,#50712,#50713,#50714,#50715,#50716,
#50717,#50718,#50719,#50720,#50721,#50722,#50723,#50724,#50725,#50726,#50727,
#50728,#50729,#50730,#50731,#50732,#50733,#50734),.UNSPECIFIED.,.F.,.F.,
(4,2,2,2,2,2,2,2,2,2,2,2,2,2,2,2,4),(-0.921606618540025,-0.872688627355351,
-0.813612023857313,-0.756611351546357,-0.69692945872276,-0.638499761548747,
-0.581118209737007,-0.521076231967445,-0.463317306881228,-0.4044438926574,
-0.345164740388026,-0.288053249414949,-0.228344796882901,-0.169710130792356,
-0.112479424024743,-0.0563089256119929,-9.99999990258793E-7),
 .UNSPECIFIED.);
#3094=B_SPLINE_CURVE_WITH_KNOTS('',3,(#50735,#50736,#50737,#50738,#50739,
#50740,#50741,#50742,#50743,#50744,#50745,#50746,#50747,#50748,#50749,#50750,
#50751,#50752,#50753,#50754,#50755,#50756,#50757,#50758,#50759,#50760,#50761,
#50762,#50763,#50764,#50765,#50766),.UNSPECIFIED.,.F.,.F.,(4,2,2,2,2,2,
2,2,2,2,2,2,2,2,2,4),(-27.2675995337344,-27.2205810783644,-27.1716030839864,
-27.1114524980469,-27.0544959346273,-26.9959799991961,-26.9364896777515,
-26.8795127522937,-26.8203565510693,-26.7619639947482,-26.7043369916545,
-26.6444247756288,-26.5873734790364,-26.5290771329393,-26.4696302887724,
-26.4647006629411),.UNSPECIFIED.);
#3095=B_SPLINE_CURVE_WITH_KNOTS('',3,(#50943,#50944,#50945,#50946,#50947,
#50948,#50949,#50950),.UNSPECIFIED.,.F.,.F.,(4,2,2,4),(-0.00426615559741139,
-0.00353262795509977,-0.00302253710286643,-0.00251244625063308),
 .UNSPECIFIED.);
#3096=B_SPLINE_CURVE_WITH_KNOTS('',3,(#51864,#51865,#51866,#51867,#51868,
#51869,#51870,#51871),.UNSPECIFIED.,.F.,.F.,(4,2,2,4),(-0.00251244625063308,
-0.00200235539839974,-0.0014922645461664,-0.000758736903856822),
 .UNSPECIFIED.);
#3097=B_SPLINE_CURVE_WITH_KNOTS('',3,(#51876,#51877,#51878,#51879,#51880,
#51881,#51882,#51883),.UNSPECIFIED.,.F.,.F.,(4,2,2,4),(-0.00932716297425779,
-0.00859363533194745,-0.0080835444797141,-0.00757345362748076),
 .UNSPECIFIED.);
#3098=B_SPLINE_CURVE_WITH_KNOTS('',3,(#52797,#52798,#52799,#52800,#52801,
#52802,#52803,#52804),.UNSPECIFIED.,.F.,.F.,(4,2,2,4),(-0.00757345362748076,
-0.00706336277524741,-0.00655327192301407,-0.00581974428070595),
 .UNSPECIFIED.);
#3099=B_SPLINE_CURVE_WITH_KNOTS('',3,(#54800,#54801,#54802,#54803,#54804,
#54805,#54806,#54807,#54808,#54809,#54810,#54811,#54812,#54813,#54814,#54815,
#54816,#54817,#54818,#54819,#54820,#54821,#54822,#54823,#54824,#54825,#54826,
#54827),.UNSPECIFIED.,.F.,.F.,(4,2,2,2,2,2,2,2,2,2,2,2,2,4),(1.00000052656661E-6,
0.0405527857266322,0.0799421814660319,0.1262631587317,0.186952165234641,
0.270820823781497,0.348937293245129,0.459507052180891,0.623823282878412,
0.790896670749941,0.927459468885873,1.05843758188768,1.16179395572833,1.24835467272154),
 .UNSPECIFIED.);
#3360=SHAPE_REPRESENTATION_RELATIONSHIP('SRR','None',#75373,#3368);
#3368=ADVANCED_BREP_SHAPE_REPRESENTATION('',(#3384),#75333);
#3376=STYLED_ITEM('',(#75419),#3384);
#3384=MANIFOLD_SOLID_BREP('Body1',#32026);
#3394=FACE_BOUND('',#7230,.T.);
#3395=FACE_BOUND('',#7235,.T.);
#3435=CIRCLE('',#32199,1.5);
#3436=CIRCLE('',#32200,1.5);
#3437=CIRCLE('',#32229,1.17524047358084);
#3438=CIRCLE('',#32231,1.17524047358084);
#3439=CIRCLE('',#32262,1.1752404735812);
#3440=CIRCLE('',#32264,1.17524047358084);
#3441=CIRCLE('',#32265,1.5);
#3442=CIRCLE('',#32313,1.55162884844711);
#3443=CIRCLE('',#32315,2.61372936963188);
#3444=CIRCLE('',#32316,0.0468749999999982);
#3445=CIRCLE('',#32317,2.58058373926377);
#3446=CIRCLE('',#32319,2.73627063036812);
#3447=CIRCLE('',#32321,2.73627063036812);
#3448=CIRCLE('',#32323,2.73627063036812);
#3449=CIRCLE('',#32325,2.73627063036812);
#3450=CIRCLE('',#32327,2.73627063036812);
#3451=CIRCLE('',#32329,2.73627063036812);
#3452=CIRCLE('',#32331,2.73627063036812);
#3453=CIRCLE('',#32333,2.73627063036812);
#3454=CIRCLE('',#32335,2.73627063036812);
#3455=CIRCLE('',#32337,2.73627063036812);
#3456=CIRCLE('',#32339,2.73627063036812);
#3457=CIRCLE('',#32341,2.73627063036812);
#3458=CIRCLE('',#32343,2.73627063036812);
#3459=CIRCLE('',#32345,2.73627063036812);
#3460=CIRCLE('',#32347,2.73627063036812);
#3461=CIRCLE('',#32349,2.73627063036812);
#3462=CIRCLE('',#32351,2.73627063036812);
#3463=CIRCLE('',#32353,2.73627063036812);
#3464=CIRCLE('',#32355,2.73627063036812);
#3465=CIRCLE('',#32357,2.73627063036812);
#3466=CIRCLE('',#32359,2.73627063036812);
#3467=CIRCLE('',#32361,2.73627063036812);
#3468=CIRCLE('',#32363,2.73627063036812);
#3469=CIRCLE('',#32365,2.73627063036812);
#3470=CIRCLE('',#32367,2.73627063036812);
#3471=CIRCLE('',#32369,2.73627063036812);
#3472=CIRCLE('',#32371,2.73627063036812);
#3473=CIRCLE('',#32373,2.73627063036812);
#3474=CIRCLE('',#32375,2.73627063036812);
#3475=CIRCLE('',#32377,2.73627063036812);
#3476=CIRCLE('',#32379,2.73627063036812);
#3477=CIRCLE('',#32381,2.73627063036812);
#3478=CIRCLE('',#32383,2.73627063036812);
#3479=CIRCLE('',#32385,2.73627063036812);
#3480=CIRCLE('',#32387,2.73627063036812);
#3481=CIRCLE('',#32389,2.73627063036812);
#3482=CIRCLE('',#32391,2.73627063036812);
#3483=CIRCLE('',#32393,2.73627063036812);
#3484=CIRCLE('',#32395,2.73627063036812);
#3485=CIRCLE('',#32397,2.73627063036812);
#3486=CIRCLE('',#32399,2.73627063036812);
#3487=CIRCLE('',#32401,2.73627063036812);
#3488=CIRCLE('',#32403,2.73627063036812);
#3489=CIRCLE('',#32405,2.73627063036812);
#3490=CIRCLE('',#32407,2.73627063036812);
#3491=CIRCLE('',#32409,2.73627063036812);
#3492=CIRCLE('',#32410,2.73627063036812);
#3493=CIRCLE('',#32411,2.73627063036812);
#3494=CIRCLE('',#32412,2.73627063036812);
#3495=CIRCLE('',#32413,2.73627063036812);
#3496=CIRCLE('',#32414,2.73627063036812);
#3497=CIRCLE('',#32415,2.73627063036812);
#3498=CIRCLE('',#32416,2.73627063036812);
#3499=CIRCLE('',#32417,2.73627063036812);
#3500=CIRCLE('',#32418,2.73627063036812);
#3501=CIRCLE('',#32419,2.73627063036812);
#3502=CIRCLE('',#32420,2.73627063036812);
#3503=CIRCLE('',#32421,2.73627063036812);
#3504=CIRCLE('',#32422,2.73627063036812);
#3505=CIRCLE('',#32423,2.73627063036812);
#3506=CIRCLE('',#32424,2.73627063036812);
#3507=CIRCLE('',#32426,2.73627063036812);
#3508=CIRCLE('',#32428,2.73627063036812);
#3509=CIRCLE('',#32430,2.73627063036812);
#3510=CIRCLE('',#32432,2.73627063036812);
#3511=CIRCLE('',#32434,2.73627063036812);
#3512=CIRCLE('',#32436,2.73627063036812);
#3513=CIRCLE('',#32438,2.73627063036812);
#3514=CIRCLE('',#32440,2.73627063036812);
#3515=CIRCLE('',#32442,2.73627063036812);
#3516=CIRCLE('',#32444,2.73627063036812);
#3517=CIRCLE('',#32446,2.73627063036812);
#3518=CIRCLE('',#32448,2.73627063036812);
#3519=CIRCLE('',#32450,2.73627063036812);
#3520=CIRCLE('',#32452,2.73627063036812);
#3521=CIRCLE('',#32454,2.73627063036812);
#3522=CIRCLE('',#32456,2.73627063036812);
#3523=CIRCLE('',#32458,2.73627063036812);
#3524=CIRCLE('',#32460,2.73627063036812);
#3525=CIRCLE('',#32462,2.73627063036812);
#3526=CIRCLE('',#32464,2.73627063036812);
#3527=CIRCLE('',#32466,2.73627063036812);
#3528=CIRCLE('',#32468,2.73627063036812);
#3529=CIRCLE('',#32470,2.73627063036812);
#3530=CIRCLE('',#32472,2.73627063036812);
#3531=CIRCLE('',#32474,2.73627063036812);
#3532=CIRCLE('',#32476,2.73627063036812);
#3533=CIRCLE('',#32478,2.73627063036812);
#3534=CIRCLE('',#32480,2.73627063036812);
#3535=CIRCLE('',#32482,2.73627063036812);
#3536=CIRCLE('',#32484,2.73627063036812);
#3537=CIRCLE('',#32486,2.73627063036812);
#3538=CIRCLE('',#32488,2.73627063036812);
#3539=CIRCLE('',#32490,2.73627063036812);
#3540=CIRCLE('',#32492,2.73627063036812);
#3541=CIRCLE('',#32494,2.73627063036812);
#3542=CIRCLE('',#32496,2.73627063036812);
#3543=CIRCLE('',#32498,2.73627063036812);
#3544=CIRCLE('',#32500,2.73627063036812);
#3545=CIRCLE('',#32502,2.73627063036812);
#3546=CIRCLE('',#32504,2.73627063036812);
#3547=CIRCLE('',#32506,2.73627063036812);
#3548=CIRCLE('',#32508,2.73627063036812);
#3549=CIRCLE('',#32510,2.73627063036812);
#3550=CIRCLE('',#32512,2.73627063036812);
#3551=CIRCLE('',#32514,2.73627063036812);
#3552=CIRCLE('',#32516,2.73627063036812);
#3553=CIRCLE('',#32518,2.73627063036812);
#3554=CIRCLE('',#32520,2.73627063036812);
#3555=CIRCLE('',#32522,2.73627063036812);
#3556=CIRCLE('',#32524,2.73627063036812);
#3557=CIRCLE('',#32526,2.73627063036812);
#3558=CIRCLE('',#32528,2.73627063036812);
#3559=CIRCLE('',#32530,2.73627063036812);
#3560=CIRCLE('',#32532,2.73627063036812);
#3561=CIRCLE('',#32534,2.73627063036812);
#3562=CIRCLE('',#32536,2.73627063036812);
#3563=CIRCLE('',#32538,2.73627063036812);
#3564=CIRCLE('',#32540,2.73627063036812);
#3565=CIRCLE('',#32542,2.73627063036812);
#3566=CIRCLE('',#32544,2.73627063036812);
#3567=CIRCLE('',#32546,2.73627063036812);
#3568=CIRCLE('',#32548,2.73627063036812);
#3569=CIRCLE('',#32550,2.73627063036812);
#3570=CIRCLE('',#32552,2.73627063036812);
#3571=CIRCLE('',#32554,2.73627063036812);
#3572=CIRCLE('',#32556,2.73627063036812);
#3573=CIRCLE('',#32558,2.73627063036812);
#3574=CIRCLE('',#32560,2.73627063036812);
#3575=CIRCLE('',#32562,2.73627063036812);
#3576=CIRCLE('',#32564,2.73627063036812);
#3577=CIRCLE('',#32566,2.73627063036812);
#3578=CIRCLE('',#32568,2.73627063036812);
#3579=CIRCLE('',#32570,2.73627063036812);
#3580=CIRCLE('',#32572,2.73627063036812);
#3581=CIRCLE('',#32574,2.73627063036812);
#3582=CIRCLE('',#32576,2.73627063036812);
#3583=CIRCLE('',#32578,2.73627063036812);
#3584=CIRCLE('',#32580,2.73627063036812);
#3585=CIRCLE('',#32582,2.73627063036812);
#3586=CIRCLE('',#32583,2.73627063036812);
#3587=CIRCLE('',#32584,2.73627063036812);
#3588=CIRCLE('',#32585,2.73627063036812);
#3589=CIRCLE('',#32586,2.73627063036812);
#3590=CIRCLE('',#32587,2.73627063036812);
#3591=CIRCLE('',#32588,2.73627063036812);
#3592=CIRCLE('',#32589,2.73627063036812);
#3593=CIRCLE('',#32590,2.73627063036812);
#3594=CIRCLE('',#32591,2.73627063036812);
#3595=CIRCLE('',#32592,2.73627063036812);
#3596=CIRCLE('',#32593,2.73627063036812);
#3597=CIRCLE('',#32594,2.73627063036812);
#3598=CIRCLE('',#32595,2.73627063036812);
#3599=CIRCLE('',#32596,2.73627063036812);
#3600=CIRCLE('',#32597,2.73627063036812);
#3601=CIRCLE('',#32599,2.73627063036812);
#3602=CIRCLE('',#32601,2.73627063036812);
#3603=CIRCLE('',#32603,2.73627063036812);
#3604=CIRCLE('',#32605,2.73627063036812);
#3605=CIRCLE('',#32607,2.73627063036812);
#3606=CIRCLE('',#32608,2.68872936963188);
#3607=CIRCLE('',#32609,2.68872936963188);
#3608=CIRCLE('',#32611,2.675);
#3609=CIRCLE('',#32612,0.0468749999999996);
#3610=CIRCLE('',#32614,2.675);
#3611=CIRCLE('',#32616,2.60625);
#3612=CIRCLE('',#32617,0.0687500000000002);
#3613=CIRCLE('',#32619,0.15);
#3614=CIRCLE('',#32620,1.65);
#3615=CIRCLE('',#32623,2.75);
#3616=CIRCLE('',#32628,2.75);
#3617=CIRCLE('',#32632,2.75);
#3618=CIRCLE('',#32636,2.75);
#3619=CIRCLE('',#32640,2.75);
#3620=CIRCLE('',#32644,2.75);
#3621=CIRCLE('',#32648,2.75);
#3622=CIRCLE('',#32652,2.75);
#3623=CIRCLE('',#32656,2.75);
#3624=CIRCLE('',#32660,2.75);
#3625=CIRCLE('',#32664,2.75);
#3626=CIRCLE('',#32668,2.75);
#3627=CIRCLE('',#32672,2.75);
#3628=CIRCLE('',#32676,2.75);
#3629=CIRCLE('',#32680,2.75);
#3630=CIRCLE('',#32684,2.75);
#3631=CIRCLE('',#32688,2.75);
#3632=CIRCLE('',#32692,2.75);
#3633=CIRCLE('',#32696,2.75);
#3634=CIRCLE('',#32700,2.75);
#3635=CIRCLE('',#32704,2.75);
#3636=CIRCLE('',#32708,2.75);
#3637=CIRCLE('',#32712,2.75);
#3638=CIRCLE('',#32716,2.75);
#3639=CIRCLE('',#32720,2.75);
#3640=CIRCLE('',#32724,2.75);
#3641=CIRCLE('',#32728,2.75);
#3642=CIRCLE('',#32732,2.75);
#3643=CIRCLE('',#32736,2.75);
#3644=CIRCLE('',#32740,2.75);
#3645=CIRCLE('',#32744,2.75);
#3646=CIRCLE('',#32748,2.75);
#3647=CIRCLE('',#32752,2.75);
#3648=CIRCLE('',#32756,2.75);
#3649=CIRCLE('',#32760,2.75);
#3650=CIRCLE('',#32764,2.75);
#3651=CIRCLE('',#32768,2.75);
#3652=CIRCLE('',#32772,2.75);
#3653=CIRCLE('',#32776,2.75);
#3654=CIRCLE('',#32780,2.75);
#3655=CIRCLE('',#32784,2.75);
#3656=CIRCLE('',#32788,2.75);
#3657=CIRCLE('',#32792,2.75);
#3658=CIRCLE('',#32796,2.75);
#3659=CIRCLE('',#32800,2.75);
#3660=CIRCLE('',#32804,2.75);
#3661=CIRCLE('',#32808,2.75);
#3662=CIRCLE('',#32812,2.75);
#3663=CIRCLE('',#32816,2.75);
#3664=CIRCLE('',#32820,2.75);
#3665=CIRCLE('',#32824,2.75);
#3666=CIRCLE('',#32828,2.75);
#3667=CIRCLE('',#32832,2.75);
#3668=CIRCLE('',#32836,2.75);
#3669=CIRCLE('',#32840,2.75);
#3670=CIRCLE('',#32844,2.75);
#3671=CIRCLE('',#32848,2.75);
#3672=CIRCLE('',#32852,2.75);
#3673=CIRCLE('',#32856,2.75);
#3674=CIRCLE('',#32860,2.75);
#3675=CIRCLE('',#32864,2.75);
#3676=CIRCLE('',#32868,2.75);
#3677=CIRCLE('',#32872,2.75);
#3678=CIRCLE('',#32876,2.75);
#3679=CIRCLE('',#32879,2.75);
#3680=CIRCLE('',#32883,2.75);
#3681=CIRCLE('',#32887,2.75);
#3682=CIRCLE('',#32891,2.75);
#3683=CIRCLE('',#32895,2.75);
#3684=CIRCLE('',#32899,2.75);
#3685=CIRCLE('',#32903,2.75);
#3686=CIRCLE('',#32907,2.75);
#3687=CIRCLE('',#32911,2.75);
#3688=CIRCLE('',#32915,2.75);
#3689=CIRCLE('',#32919,2.75);
#3690=CIRCLE('',#32923,2.75);
#3691=CIRCLE('',#32927,2.75);
#3692=CIRCLE('',#32931,2.75);
#3693=CIRCLE('',#32936,2.75);
#3694=CIRCLE('',#32938,2.75);
#3695=CIRCLE('',#32940,2.75);
#3696=CIRCLE('',#32942,2.75);
#3697=CIRCLE('',#32944,2.75);
#3698=CIRCLE('',#32946,2.75);
#3699=CIRCLE('',#32948,2.75);
#3700=CIRCLE('',#32950,2.75);
#3701=CIRCLE('',#32952,2.75);
#3702=CIRCLE('',#32954,2.75);
#3703=CIRCLE('',#32956,2.75);
#3704=CIRCLE('',#32958,2.75);
#3705=CIRCLE('',#32960,2.75);
#3706=CIRCLE('',#32962,2.75);
#3707=CIRCLE('',#32964,2.75);
#3708=CIRCLE('',#32966,2.75);
#3709=CIRCLE('',#32968,2.75);
#3710=CIRCLE('',#32970,2.75);
#3711=CIRCLE('',#32972,2.75);
#3712=CIRCLE('',#32974,2.75);
#3713=CIRCLE('',#32976,2.75);
#3714=CIRCLE('',#32978,2.75);
#3715=CIRCLE('',#32980,2.75);
#3716=CIRCLE('',#32982,2.75);
#3717=CIRCLE('',#32984,2.75);
#3718=CIRCLE('',#32986,2.75);
#3719=CIRCLE('',#32988,2.75);
#3720=CIRCLE('',#32990,2.75);
#3721=CIRCLE('',#32992,2.75);
#3722=CIRCLE('',#32994,2.75);
#3723=CIRCLE('',#32996,2.75);
#3724=CIRCLE('',#32998,2.75);
#3725=CIRCLE('',#33000,2.75);
#3726=CIRCLE('',#33002,2.75);
#3727=CIRCLE('',#33004,2.75);
#3728=CIRCLE('',#33006,2.75);
#3729=CIRCLE('',#33008,2.75);
#3730=CIRCLE('',#33010,2.75);
#3731=CIRCLE('',#33012,2.75);
#3732=CIRCLE('',#33014,2.75);
#3733=CIRCLE('',#33016,2.75);
#3734=CIRCLE('',#33018,2.75);
#3735=CIRCLE('',#33020,2.75);
#3736=CIRCLE('',#33022,2.75);
#3737=CIRCLE('',#33024,2.75);
#3738=CIRCLE('',#33026,2.75);
#3739=CIRCLE('',#33028,2.75);
#3740=CIRCLE('',#33030,2.75);
#3741=CIRCLE('',#33032,2.75);
#3742=CIRCLE('',#33034,2.75);
#3743=CIRCLE('',#33036,2.75);
#3744=CIRCLE('',#33038,2.75);
#3745=CIRCLE('',#33040,2.75);
#3746=CIRCLE('',#33042,2.75);
#3747=CIRCLE('',#33044,2.75);
#3748=CIRCLE('',#33046,2.75);
#3749=CIRCLE('',#33048,2.75);
#3750=CIRCLE('',#33050,2.75);
#3751=CIRCLE('',#33052,2.75);
#3752=CIRCLE('',#33054,2.75);
#3753=CIRCLE('',#33056,2.75);
#3754=CIRCLE('',#33058,2.75);
#3755=CIRCLE('',#33060,2.75);
#3756=CIRCLE('',#33062,2.75);
#3757=CIRCLE('',#33064,2.75);
#3758=CIRCLE('',#33066,2.75);
#3759=CIRCLE('',#33068,2.75);
#3760=CIRCLE('',#33070,2.75);
#3761=CIRCLE('',#33072,2.75);
#3762=CIRCLE('',#33074,2.75);
#3763=CIRCLE('',#33076,2.75);
#3764=CIRCLE('',#33078,2.75);
#3765=CIRCLE('',#33080,2.75);
#3766=CIRCLE('',#33082,2.75);
#3767=CIRCLE('',#33084,2.75);
#3768=CIRCLE('',#33086,2.75);
#3769=CIRCLE('',#33088,2.75);
#3770=CIRCLE('',#33090,2.75);
#3771=CIRCLE('',#33092,2.75);
#3772=CIRCLE('',#33094,2.75);
#3773=CIRCLE('',#33337,2.75);
#3774=CIRCLE('',#33339,2.75);
#4471=CYLINDRICAL_SURFACE('',#32198,1.5);
#4472=CYLINDRICAL_SURFACE('',#32201,1.5);
#4473=CYLINDRICAL_SURFACE('',#32202,1.5);
#4474=CYLINDRICAL_SURFACE('',#32203,1.5);
#4475=CYLINDRICAL_SURFACE('',#32204,1.5);
#4476=CYLINDRICAL_SURFACE('',#32205,1.5);
#4477=CYLINDRICAL_SURFACE('',#32206,1.5);
#4478=CYLINDRICAL_SURFACE('',#32207,1.5);
#4479=CYLINDRICAL_SURFACE('',#32208,1.5);
#4480=CYLINDRICAL_SURFACE('',#32209,1.5);
#4481=CYLINDRICAL_SURFACE('',#32210,1.5);
#4482=CYLINDRICAL_SURFACE('',#32211,1.5);
#4483=CYLINDRICAL_SURFACE('',#32212,1.5);
#4484=CYLINDRICAL_SURFACE('',#32213,1.5);
#4485=CYLINDRICAL_SURFACE('',#32214,1.5);
#4486=CYLINDRICAL_SURFACE('',#32215,1.5);
#4487=CYLINDRICAL_SURFACE('',#32216,1.5);
#4488=CYLINDRICAL_SURFACE('',#32217,1.5);
#4489=CYLINDRICAL_SURFACE('',#32218,1.5);
#4490=CYLINDRICAL_SURFACE('',#32219,1.5);
#4491=CYLINDRICAL_SURFACE('',#32220,1.5);
#4492=CYLINDRICAL_SURFACE('',#32221,1.5);
#4493=CYLINDRICAL_SURFACE('',#32222,1.5);
#4494=CYLINDRICAL_SURFACE('',#32223,1.5);
#4495=CYLINDRICAL_SURFACE('',#32224,1.5);
#4496=CYLINDRICAL_SURFACE('',#32225,1.5);
#4497=CYLINDRICAL_SURFACE('',#32226,1.5);
#4498=CYLINDRICAL_SURFACE('',#32227,1.5);
#4499=CYLINDRICAL_SURFACE('',#32230,1.17524047358084);
#4500=CYLINDRICAL_SURFACE('',#32232,1.17524047358084);
#4501=CYLINDRICAL_SURFACE('',#32233,1.17524047358084);
#4502=CYLINDRICAL_SURFACE('',#32234,1.17524047358084);
#4503=CYLINDRICAL_SURFACE('',#32235,1.17524047358084);
#4504=CYLINDRICAL_SURFACE('',#32236,1.17524047358084);
#4505=CYLINDRICAL_SURFACE('',#32237,1.17524047358084);
#4506=CYLINDRICAL_SURFACE('',#32238,1.17524047358084);
#4507=CYLINDRICAL_SURFACE('',#32239,1.17524047358084);
#4508=CYLINDRICAL_SURFACE('',#32240,1.17524047358084);
#4509=CYLINDRICAL_SURFACE('',#32241,1.17524047358084);
#4510=CYLINDRICAL_SURFACE('',#32242,1.17524047358084);
#4511=CYLINDRICAL_SURFACE('',#32243,1.17524047358084);
#4512=CYLINDRICAL_SURFACE('',#32244,1.17524047358084);
#4513=CYLINDRICAL_SURFACE('',#32245,1.17524047358084);
#4514=CYLINDRICAL_SURFACE('',#32246,1.17524047358084);
#4515=CYLINDRICAL_SURFACE('',#32247,1.17524047358084);
#4516=CYLINDRICAL_SURFACE('',#32248,1.17524047358084);
#4517=CYLINDRICAL_SURFACE('',#32249,1.17524047358084);
#4518=CYLINDRICAL_SURFACE('',#32250,1.17524047358084);
#4519=CYLINDRICAL_SURFACE('',#32251,1.17524047358084);
#4520=CYLINDRICAL_SURFACE('',#32252,1.17524047358084);
#4521=CYLINDRICAL_SURFACE('',#32253,1.17524047358084);
#4522=CYLINDRICAL_SURFACE('',#32254,1.17524047358084);
#4523=CYLINDRICAL_SURFACE('',#32255,1.17524047358084);
#4524=CYLINDRICAL_SURFACE('',#32256,1.17524047358084);
#4525=CYLINDRICAL_SURFACE('',#32257,1.17524047358084);
#4526=CYLINDRICAL_SURFACE('',#32258,1.17524047358084);
#4527=CYLINDRICAL_SURFACE('',#32259,1.17524047358084);
#4528=CYLINDRICAL_SURFACE('',#32260,1.17524047358084);
#4529=CYLINDRICAL_SURFACE('',#32261,1.17524047358084);
#4530=CYLINDRICAL_SURFACE('',#32266,1.5);
#4531=CYLINDRICAL_SURFACE('',#32267,0.0137499999999999);
#4532=CYLINDRICAL_SURFACE('',#32270,0.0137499999999999);
#4533=CYLINDRICAL_SURFACE('',#32273,0.0137499999999999);
#4534=CYLINDRICAL_SURFACE('',#32276,0.0137499999999999);
#4535=CYLINDRICAL_SURFACE('',#32279,0.0137499999999999);
#4536=CYLINDRICAL_SURFACE('',#32282,0.0137499999999999);
#4537=CYLINDRICAL_SURFACE('',#32285,0.0137499999999999);
#4538=CYLINDRICAL_SURFACE('',#32288,0.0137499999999999);
#4539=CYLINDRICAL_SURFACE('',#32291,0.0137499999999999);
#4540=CYLINDRICAL_SURFACE('',#32294,0.0137499999999999);
#4541=CYLINDRICAL_SURFACE('',#32297,0.0137499999999997);
#4542=CYLINDRICAL_SURFACE('',#32300,0.0137499999999997);
#4543=CYLINDRICAL_SURFACE('',#32303,0.0137499999999997);
#4544=CYLINDRICAL_SURFACE('',#32306,0.0137499999999997);
#4545=CYLINDRICAL_SURFACE('',#32309,0.0137499999999997);
#4546=CYLINDRICAL_SURFACE('',#32613,2.675);
#4547=CYLINDRICAL_SURFACE('',#32937,2.75);
#4548=CYLINDRICAL_SURFACE('',#32939,2.75);
#4549=CYLINDRICAL_SURFACE('',#32941,2.75);
#4550=CYLINDRICAL_SURFACE('',#32943,2.75);
#4551=CYLINDRICAL_SURFACE('',#32945,2.75);
#4552=CYLINDRICAL_SURFACE('',#32947,2.75);
#4553=CYLINDRICAL_SURFACE('',#32949,2.75);
#4554=CYLINDRICAL_SURFACE('',#32951,2.75);
#4555=CYLINDRICAL_SURFACE('',#32953,2.75);
#4556=CYLINDRICAL_SURFACE('',#32955,2.75);
#4557=CYLINDRICAL_SURFACE('',#32957,2.75);
#4558=CYLINDRICAL_SURFACE('',#32959,2.75);
#4559=CYLINDRICAL_SURFACE('',#32961,2.75);
#4560=CYLINDRICAL_SURFACE('',#32963,2.75);
#4561=CYLINDRICAL_SURFACE('',#32965,2.75);
#4562=CYLINDRICAL_SURFACE('',#32967,2.75);
#4563=CYLINDRICAL_SURFACE('',#32969,2.75);
#4564=CYLINDRICAL_SURFACE('',#32971,2.75);
#4565=CYLINDRICAL_SURFACE('',#32973,2.75);
#4566=CYLINDRICAL_SURFACE('',#32975,2.75);
#4567=CYLINDRICAL_SURFACE('',#32977,2.75);
#4568=CYLINDRICAL_SURFACE('',#32979,2.75);
#4569=CYLINDRICAL_SURFACE('',#32981,2.75);
#4570=CYLINDRICAL_SURFACE('',#32983,2.75);
#4571=CYLINDRICAL_SURFACE('',#32985,2.75);
#4572=CYLINDRICAL_SURFACE('',#32987,2.75);
#4573=CYLINDRICAL_SURFACE('',#32989,2.75);
#4574=CYLINDRICAL_SURFACE('',#32991,2.75);
#4575=CYLINDRICAL_SURFACE('',#32993,2.75);
#4576=CYLINDRICAL_SURFACE('',#32995,2.75);
#4577=CYLINDRICAL_SURFACE('',#32997,2.75);
#4578=CYLINDRICAL_SURFACE('',#32999,2.75);
#4579=CYLINDRICAL_SURFACE('',#33001,2.75);
#4580=CYLINDRICAL_SURFACE('',#33003,2.75);
#4581=CYLINDRICAL_SURFACE('',#33005,2.75);
#4582=CYLINDRICAL_SURFACE('',#33007,2.75);
#4583=CYLINDRICAL_SURFACE('',#33009,2.75);
#4584=CYLINDRICAL_SURFACE('',#33011,2.75);
#4585=CYLINDRICAL_SURFACE('',#33013,2.75);
#4586=CYLINDRICAL_SURFACE('',#33015,2.75);
#4587=CYLINDRICAL_SURFACE('',#33017,2.75);
#4588=CYLINDRICAL_SURFACE('',#33019,2.75);
#4589=CYLINDRICAL_SURFACE('',#33021,2.75);
#4590=CYLINDRICAL_SURFACE('',#33023,2.75);
#4591=CYLINDRICAL_SURFACE('',#33025,2.75);
#4592=CYLINDRICAL_SURFACE('',#33027,2.75);
#4593=CYLINDRICAL_SURFACE('',#33029,2.75);
#4594=CYLINDRICAL_SURFACE('',#33031,2.75);
#4595=CYLINDRICAL_SURFACE('',#33033,2.75);
#4596=CYLINDRICAL_SURFACE('',#33035,2.75);
#4597=CYLINDRICAL_SURFACE('',#33037,2.75);
#4598=CYLINDRICAL_SURFACE('',#33039,2.75);
#4599=CYLINDRICAL_SURFACE('',#33041,2.75);
#4600=CYLINDRICAL_SURFACE('',#33043,2.75);
#4601=CYLINDRICAL_SURFACE('',#33045,2.75);
#4602=CYLINDRICAL_SURFACE('',#33047,2.75);
#4603=CYLINDRICAL_SURFACE('',#33049,2.75);
#4604=CYLINDRICAL_SURFACE('',#33051,2.75);
#4605=CYLINDRICAL_SURFACE('',#33053,2.75);
#4606=CYLINDRICAL_SURFACE('',#33055,2.75);
#4607=CYLINDRICAL_SURFACE('',#33057,2.75);
#4608=CYLINDRICAL_SURFACE('',#33059,2.75);
#4609=CYLINDRICAL_SURFACE('',#33061,2.75);
#4610=CYLINDRICAL_SURFACE('',#33063,2.75);
#4611=CYLINDRICAL_SURFACE('',#33065,2.75);
#4612=CYLINDRICAL_SURFACE('',#33067,2.75);
#4613=CYLINDRICAL_SURFACE('',#33069,2.75);
#4614=CYLINDRICAL_SURFACE('',#33071,2.75);
#4615=CYLINDRICAL_SURFACE('',#33073,2.75);
#4616=CYLINDRICAL_SURFACE('',#33075,2.75);
#4617=CYLINDRICAL_SURFACE('',#33077,2.75);
#4618=CYLINDRICAL_SURFACE('',#33079,2.75);
#4619=CYLINDRICAL_SURFACE('',#33081,2.75);
#4620=CYLINDRICAL_SURFACE('',#33083,2.75);
#4621=CYLINDRICAL_SURFACE('',#33085,2.75);
#4622=CYLINDRICAL_SURFACE('',#33087,2.75);
#4623=CYLINDRICAL_SURFACE('',#33089,2.75);
#4624=CYLINDRICAL_SURFACE('',#33091,2.75);
#4625=CYLINDRICAL_SURFACE('',#33093,2.75);
#4626=CYLINDRICAL_SURFACE('',#33338,2.75);
#4627=CYLINDRICAL_SURFACE('',#33353,0.0137499999999997);
#4628=CYLINDRICAL_SURFACE('',#33356,0.0137499999999997);
#4629=CYLINDRICAL_SURFACE('',#33359,0.0137499999999997);
#4630=CYLINDRICAL_SURFACE('',#33362,0.0137499999999997);
#4631=CYLINDRICAL_SURFACE('',#33365,0.0137499999999998);
#4632=CYLINDRICAL_SURFACE('',#33368,0.0137499999999998);
#4633=CYLINDRICAL_SURFACE('',#33371,0.0137499999999997);
#4634=CYLINDRICAL_SURFACE('',#33392,0.0137499999999997);
#4635=CYLINDRICAL_SURFACE('',#33395,0.0137499999999998);
#4636=CYLINDRICAL_SURFACE('',#33398,0.0137499999999998);
#4637=CYLINDRICAL_SURFACE('',#33401,0.0137499999999997);
#4638=CYLINDRICAL_SURFACE('',#33404,0.0137499999999997);
#4639=CYLINDRICAL_SURFACE('',#33407,0.0137499999999997);
#4640=CYLINDRICAL_SURFACE('',#33410,0.0137499999999997);
#4641=CYLINDRICAL_SURFACE('',#33413,0.0137499999999997);
#4642=CYLINDRICAL_SURFACE('',#33416,0.0137499999999997);
#4643=CYLINDRICAL_SURFACE('',#33419,0.0137499999999999);
#4644=CYLINDRICAL_SURFACE('',#33422,0.0137499999999999);
#4645=CYLINDRICAL_SURFACE('',#33425,0.0137499999999999);
#4646=CYLINDRICAL_SURFACE('',#33428,0.0137499999999999);
#4647=CYLINDRICAL_SURFACE('',#33431,0.0137499999999999);
#4648=CYLINDRICAL_SURFACE('',#33434,0.0137499999999999);
#4649=CYLINDRICAL_SURFACE('',#33437,0.0137499999999999);
#4650=CYLINDRICAL_SURFACE('',#33440,0.0137499999999999);
#4651=CYLINDRICAL_SURFACE('',#33443,0.0137499999999999);
#4652=CYLINDRICAL_SURFACE('',#33446,0.0137499999999997);
#4653=CYLINDRICAL_SURFACE('',#33449,0.0137499999999997);
#4654=CYLINDRICAL_SURFACE('',#33452,0.0137499999999997);
#4655=CYLINDRICAL_SURFACE('',#33455,0.0137499999999998);
#4656=CYLINDRICAL_SURFACE('',#33458,0.0137499999999998);
#4657=CYLINDRICAL_SURFACE('',#33461,0.0137499999999997);
#4658=CYLINDRICAL_SURFACE('',#33464,0.0137499999999997);
#4659=CYLINDRICAL_SURFACE('',#33467,0.0137499999999997);
#4660=CYLINDRICAL_SURFACE('',#33470,0.0137499999999997);
#4661=CYLINDRICAL_SURFACE('',#33473,0.0137499999999997);
#4662=CYLINDRICAL_SURFACE('',#33476,0.0137499999999997);
#4663=CYLINDRICAL_SURFACE('',#33479,0.0137499999999999);
#4664=CYLINDRICAL_SURFACE('',#33482,0.0137499999999999);
#4665=CYLINDRICAL_SURFACE('',#33485,0.0137499999999999);
#4666=CYLINDRICAL_SURFACE('',#33488,0.0137499999999999);
#4667=CYLINDRICAL_SURFACE('',#33491,0.0137499999999999);
#4668=CYLINDRICAL_SURFACE('',#33494,0.0137499999999999);
#4669=CYLINDRICAL_SURFACE('',#33497,0.0137499999999999);
#4670=CYLINDRICAL_SURFACE('',#33500,0.0137499999999999);
#4671=CYLINDRICAL_SURFACE('',#33503,0.0137499999999999);
#4672=CYLINDRICAL_SURFACE('',#33506,0.0137499999999999);
#4673=CYLINDRICAL_SURFACE('',#33509,0.0137499999999999);
#4674=CYLINDRICAL_SURFACE('',#33512,0.0137499999999999);
#4675=CYLINDRICAL_SURFACE('',#33515,0.0137499999999999);
#4676=CYLINDRICAL_SURFACE('',#33518,0.0137499999999999);
#4677=CYLINDRICAL_SURFACE('',#33521,0.0137499999999999);
#4678=CYLINDRICAL_SURFACE('',#33524,0.0137499999999999);
#4679=CYLINDRICAL_SURFACE('',#33527,0.0137499999999999);
#4680=CYLINDRICAL_SURFACE('',#33530,0.0137499999999999);
#4681=CYLINDRICAL_SURFACE('',#33533,0.0137499999999999);
#4682=CYLINDRICAL_SURFACE('',#33536,0.0137499999999997);
#4683=CYLINDRICAL_SURFACE('',#33539,0.0137499999999997);
#4684=CYLINDRICAL_SURFACE('',#33542,0.0137499999999997);
#4685=CYLINDRICAL_SURFACE('',#33545,0.0137499999999997);
#4686=CYLINDRICAL_SURFACE('',#33548,0.0137499999999997);
#4687=CYLINDRICAL_SURFACE('',#33551,0.0137499999999997);
#4688=CYLINDRICAL_SURFACE('',#33554,0.0137499999999998);
#4689=CYLINDRICAL_SURFACE('',#33557,0.0137499999999998);
#4690=CYLINDRICAL_SURFACE('',#33560,0.0137499999999997);
#4691=CYLINDRICAL_SURFACE('',#33563,0.0137499999999997);
#5172=FACE_OUTER_BOUND('',#6906,.T.);
#5173=FACE_OUTER_BOUND('',#6907,.T.);
#5174=FACE_OUTER_BOUND('',#6908,.T.);
#5175=FACE_OUTER_BOUND('',#6909,.T.);
#5176=FACE_OUTER_BOUND('',#6910,.T.);
#5177=FACE_OUTER_BOUND('',#6911,.T.);
#5178=FACE_OUTER_BOUND('',#6912,.T.);
#5179=FACE_OUTER_BOUND('',#6913,.T.);
#5180=FACE_OUTER_BOUND('',#6914,.T.);
#5181=FACE_OUTER_BOUND('',#6915,.T.);
#5182=FACE_OUTER_BOUND('',#6916,.T.);
#5183=FACE_OUTER_BOUND('',#6917,.T.);
#5184=FACE_OUTER_BOUND('',#6918,.T.);
#5185=FACE_OUTER_BOUND('',#6919,.T.);
#5186=FACE_OUTER_BOUND('',#6920,.T.);
#5187=FACE_OUTER_BOUND('',#6921,.T.);
#5188=FACE_OUTER_BOUND('',#6922,.T.);
#5189=FACE_OUTER_BOUND('',#6923,.T.);
#5190=FACE_OUTER_BOUND('',#6924,.T.);
#5191=FACE_OUTER_BOUND('',#6925,.T.);
#5192=FACE_OUTER_BOUND('',#6926,.T.);
#5193=FACE_OUTER_BOUND('',#6927,.T.);
#5194=FACE_OUTER_BOUND('',#6928,.T.);
#5195=FACE_OUTER_BOUND('',#6929,.T.);
#5196=FACE_OUTER_BOUND('',#6930,.T.);
#5197=FACE_OUTER_BOUND('',#6931,.T.);
#5198=FACE_OUTER_BOUND('',#6932,.T.);
#5199=FACE_OUTER_BOUND('',#6933,.T.);
#5200=FACE_OUTER_BOUND('',#6934,.T.);
#5201=FACE_OUTER_BOUND('',#6935,.T.);
#5202=FACE_OUTER_BOUND('',#6936,.T.);
#5203=FACE_OUTER_BOUND('',#6937,.T.);
#5204=FACE_OUTER_BOUND('',#6938,.T.);
#5205=FACE_OUTER_BOUND('',#6939,.T.);
#5206=FACE_OUTER_BOUND('',#6940,.T.);
#5207=FACE_OUTER_BOUND('',#6941,.T.);
#5208=FACE_OUTER_BOUND('',#6942,.T.);
#5209=FACE_OUTER_BOUND('',#6943,.T.);
#5210=FACE_OUTER_BOUND('',#6944,.T.);
#5211=FACE_OUTER_BOUND('',#6945,.T.);
#5212=FACE_OUTER_BOUND('',#6946,.T.);
#5213=FACE_OUTER_BOUND('',#6947,.T.);
#5214=FACE_OUTER_BOUND('',#6948,.T.);
#5215=FACE_OUTER_BOUND('',#6949,.T.);
#5216=FACE_OUTER_BOUND('',#6950,.T.);
#5217=FACE_OUTER_BOUND('',#6951,.T.);
#5218=FACE_OUTER_BOUND('',#6952,.T.);
#5219=FACE_OUTER_BOUND('',#6953,.T.);
#5220=FACE_OUTER_BOUND('',#6954,.T.);
#5221=FACE_OUTER_BOUND('',#6955,.T.);
#5222=FACE_OUTER_BOUND('',#6956,.T.);
#5223=FACE_OUTER_BOUND('',#6957,.T.);
#5224=FACE_OUTER_BOUND('',#6958,.T.);
#5225=FACE_OUTER_BOUND('',#6959,.T.);
#5226=FACE_OUTER_BOUND('',#6960,.T.);
#5227=FACE_OUTER_BOUND('',#6961,.T.);
#5228=FACE_OUTER_BOUND('',#6962,.T.);
#5229=FACE_OUTER_BOUND('',#6963,.T.);
#5230=FACE_OUTER_BOUND('',#6964,.T.);
#5231=FACE_OUTER_BOUND('',#6965,.T.);
#5232=FACE_OUTER_BOUND('',#6966,.T.);
#5233=FACE_OUTER_BOUND('',#6967,.T.);
#5234=FACE_OUTER_BOUND('',#6968,.T.);
#5235=FACE_OUTER_BOUND('',#6969,.T.);
#5236=FACE_OUTER_BOUND('',#6970,.T.);
#5237=FACE_OUTER_BOUND('',#6971,.T.);
#5238=FACE_OUTER_BOUND('',#6972,.T.);
#5239=FACE_OUTER_BOUND('',#6973,.T.);
#5240=FACE_OUTER_BOUND('',#6974,.T.);
#5241=FACE_OUTER_BOUND('',#6975,.T.);
#5242=FACE_OUTER_BOUND('',#6976,.T.);
#5243=FACE_OUTER_BOUND('',#6977,.T.);
#5244=FACE_OUTER_BOUND('',#6978,.T.);
#5245=FACE_OUTER_BOUND('',#6979,.T.);
#5246=FACE_OUTER_BOUND('',#6980,.T.);
#5247=FACE_OUTER_BOUND('',#6981,.T.);
#5248=FACE_OUTER_BOUND('',#6982,.T.);
#5249=FACE_OUTER_BOUND('',#6983,.T.);
#5250=FACE_OUTER_BOUND('',#6984,.T.);
#5251=FACE_OUTER_BOUND('',#6985,.T.);
#5252=FACE_OUTER_BOUND('',#6986,.T.);
#5253=FACE_OUTER_BOUND('',#6987,.T.);
#5254=FACE_OUTER_BOUND('',#6988,.T.);
#5255=FACE_OUTER_BOUND('',#6989,.T.);
#5256=FACE_OUTER_BOUND('',#6990,.T.);
#5257=FACE_OUTER_BOUND('',#6991,.T.);
#5258=FACE_OUTER_BOUND('',#6992,.T.);
#5259=FACE_OUTER_BOUND('',#6993,.T.);
#5260=FACE_OUTER_BOUND('',#6994,.T.);
#5261=FACE_OUTER_BOUND('',#6995,.T.);
#5262=FACE_OUTER_BOUND('',#6996,.T.);
#5263=FACE_OUTER_BOUND('',#6997,.T.);
#5264=FACE_OUTER_BOUND('',#6998,.T.);
#5265=FACE_OUTER_BOUND('',#6999,.T.);
#5266=FACE_OUTER_BOUND('',#7000,.T.);
#5267=FACE_OUTER_BOUND('',#7001,.T.);
#5268=FACE_OUTER_BOUND('',#7002,.T.);
#5269=FACE_OUTER_BOUND('',#7003,.T.);
#5270=FACE_OUTER_BOUND('',#7004,.T.);
#5271=FACE_OUTER_BOUND('',#7005,.T.);
#5272=FACE_OUTER_BOUND('',#7006,.T.);
#5273=FACE_OUTER_BOUND('',#7007,.T.);
#5274=FACE_OUTER_BOUND('',#7008,.T.);
#5275=FACE_OUTER_BOUND('',#7009,.T.);
#5276=FACE_OUTER_BOUND('',#7010,.T.);
#5277=FACE_OUTER_BOUND('',#7011,.T.);
#5278=FACE_OUTER_BOUND('',#7012,.T.);
#5279=FACE_OUTER_BOUND('',#7013,.T.);
#5280=FACE_OUTER_BOUND('',#7014,.T.);
#5281=FACE_OUTER_BOUND('',#7015,.T.);
#5282=FACE_OUTER_BOUND('',#7016,.T.);
#5283=FACE_OUTER_BOUND('',#7017,.T.);
#5284=FACE_OUTER_BOUND('',#7018,.T.);
#5285=FACE_OUTER_BOUND('',#7019,.T.);
#5286=FACE_OUTER_BOUND('',#7020,.T.);
#5287=FACE_OUTER_BOUND('',#7021,.T.);
#5288=FACE_OUTER_BOUND('',#7022,.T.);
#5289=FACE_OUTER_BOUND('',#7023,.T.);
#5290=FACE_OUTER_BOUND('',#7024,.T.);
#5291=FACE_OUTER_BOUND('',#7025,.T.);
#5292=FACE_OUTER_BOUND('',#7026,.T.);
#5293=FACE_OUTER_BOUND('',#7027,.T.);
#5294=FACE_OUTER_BOUND('',#7028,.T.);
#5295=FACE_OUTER_BOUND('',#7029,.T.);
#5296=FACE_OUTER_BOUND('',#7030,.T.);
#5297=FACE_OUTER_BOUND('',#7031,.T.);
#5298=FACE_OUTER_BOUND('',#7032,.T.);
#5299=FACE_OUTER_BOUND('',#7033,.T.);
#5300=FACE_OUTER_BOUND('',#7034,.T.);
#5301=FACE_OUTER_BOUND('',#7035,.T.);
#5302=FACE_OUTER_BOUND('',#7036,.T.);
#5303=FACE_OUTER_BOUND('',#7037,.T.);
#5304=FACE_OUTER_BOUND('',#7038,.T.);
#5305=FACE_OUTER_BOUND('',#7039,.T.);
#5306=FACE_OUTER_BOUND('',#7040,.T.);
#5307=FACE_OUTER_BOUND('',#7041,.T.);
#5308=FACE_OUTER_BOUND('',#7042,.T.);
#5309=FACE_OUTER_BOUND('',#7043,.T.);
#5310=FACE_OUTER_BOUND('',#7044,.T.);
#5311=FACE_OUTER_BOUND('',#7045,.T.);
#5312=FACE_OUTER_BOUND('',#7046,.T.);
#5313=FACE_OUTER_BOUND('',#7047,.T.);
#5314=FACE_OUTER_BOUND('',#7048,.T.);
#5315=FACE_OUTER_BOUND('',#7049,.T.);
#5316=FACE_OUTER_BOUND('',#7050,.T.);
#5317=FACE_OUTER_BOUND('',#7051,.T.);
#5318=FACE_OUTER_BOUND('',#7052,.T.);
#5319=FACE_OUTER_BOUND('',#7053,.T.);
#5320=FACE_OUTER_BOUND('',#7054,.T.);
#5321=FACE_OUTER_BOUND('',#7055,.T.);
#5322=FACE_OUTER_BOUND('',#7056,.T.);
#5323=FACE_OUTER_BOUND('',#7057,.T.);
#5324=FACE_OUTER_BOUND('',#7058,.T.);
#5325=FACE_OUTER_BOUND('',#7059,.T.);
#5326=FACE_OUTER_BOUND('',#7060,.T.);
#5327=FACE_OUTER_BOUND('',#7061,.T.);
#5328=FACE_OUTER_BOUND('',#7062,.T.);
#5329=FACE_OUTER_BOUND('',#7063,.T.);
#5330=FACE_OUTER_BOUND('',#7064,.T.);
#5331=FACE_OUTER_BOUND('',#7065,.T.);
#5332=FACE_OUTER_BOUND('',#7066,.T.);
#5333=FACE_OUTER_BOUND('',#7067,.T.);
#5334=FACE_OUTER_BOUND('',#7068,.T.);
#5335=FACE_OUTER_BOUND('',#7069,.T.);
#5336=FACE_OUTER_BOUND('',#7070,.T.);
#5337=FACE_OUTER_BOUND('',#7071,.T.);
#5338=FACE_OUTER_BOUND('',#7072,.T.);
#5339=FACE_OUTER_BOUND('',#7073,.T.);
#5340=FACE_OUTER_BOUND('',#7074,.T.);
#5341=FACE_OUTER_BOUND('',#7075,.T.);
#5342=FACE_OUTER_BOUND('',#7076,.T.);
#5343=FACE_OUTER_BOUND('',#7077,.T.);
#5344=FACE_OUTER_BOUND('',#7078,.T.);
#5345=FACE_OUTER_BOUND('',#7079,.T.);
#5346=FACE_OUTER_BOUND('',#7080,.T.);
#5347=FACE_OUTER_BOUND('',#7081,.T.);
#5348=FACE_OUTER_BOUND('',#7082,.T.);
#5349=FACE_OUTER_BOUND('',#7083,.T.);
#5350=FACE_OUTER_BOUND('',#7084,.T.);
#5351=FACE_OUTER_BOUND('',#7085,.T.);
#5352=FACE_OUTER_BOUND('',#7086,.T.);
#5353=FACE_OUTER_BOUND('',#7087,.T.);
#5354=FACE_OUTER_BOUND('',#7088,.T.);
#5355=FACE_OUTER_BOUND('',#7089,.T.);
#5356=FACE_OUTER_BOUND('',#7090,.T.);
#5357=FACE_OUTER_BOUND('',#7091,.T.);
#5358=FACE_OUTER_BOUND('',#7092,.T.);
#5359=FACE_OUTER_BOUND('',#7093,.T.);
#5360=FACE_OUTER_BOUND('',#7094,.T.);
#5361=FACE_OUTER_BOUND('',#7095,.T.);
#5362=FACE_OUTER_BOUND('',#7096,.T.);
#5363=FACE_OUTER_BOUND('',#7097,.T.);
#5364=FACE_OUTER_BOUND('',#7098,.T.);
#5365=FACE_OUTER_BOUND('',#7099,.T.);
#5366=FACE_OUTER_BOUND('',#7100,.T.);
#5367=FACE_OUTER_BOUND('',#7101,.T.);
#5368=FACE_OUTER_BOUND('',#7102,.T.);
#5369=FACE_OUTER_BOUND('',#7103,.T.);
#5370=FACE_OUTER_BOUND('',#7104,.T.);
#5371=FACE_OUTER_BOUND('',#7105,.T.);
#5372=FACE_OUTER_BOUND('',#7106,.T.);
#5373=FACE_OUTER_BOUND('',#7107,.T.);
#5374=FACE_OUTER_BOUND('',#7108,.T.);
#5375=FACE_OUTER_BOUND('',#7109,.T.);
#5376=FACE_OUTER_BOUND('',#7110,.T.);
#5377=FACE_OUTER_BOUND('',#7111,.T.);
#5378=FACE_OUTER_BOUND('',#7112,.T.);
#5379=FACE_OUTER_BOUND('',#7113,.T.);
#5380=FACE_OUTER_BOUND('',#7114,.T.);
#5381=FACE_OUTER_BOUND('',#7115,.T.);
#5382=FACE_OUTER_BOUND('',#7116,.T.);
#5383=FACE_OUTER_BOUND('',#7117,.T.);
#5384=FACE_OUTER_BOUND('',#7118,.T.);
#5385=FACE_OUTER_BOUND('',#7119,.T.);
#5386=FACE_OUTER_BOUND('',#7120,.T.);
#5387=FACE_OUTER_BOUND('',#7121,.T.);
#5388=FACE_OUTER_BOUND('',#7122,.T.);
#5389=FACE_OUTER_BOUND('',#7123,.T.);
#5390=FACE_OUTER_BOUND('',#7124,.T.);
#5391=FACE_OUTER_BOUND('',#7125,.T.);
#5392=FACE_OUTER_BOUND('',#7126,.T.);
#5393=FACE_OUTER_BOUND('',#7127,.T.);
#5394=FACE_OUTER_BOUND('',#7128,.T.);
#5395=FACE_OUTER_BOUND('',#7129,.T.);
#5396=FACE_OUTER_BOUND('',#7130,.T.);
#5397=FACE_OUTER_BOUND('',#7131,.T.);
#5398=FACE_OUTER_BOUND('',#7132,.T.);
#5399=FACE_OUTER_BOUND('',#7133,.T.);
#5400=FACE_OUTER_BOUND('',#7134,.T.);
#5401=FACE_OUTER_BOUND('',#7135,.T.);
#5402=FACE_OUTER_BOUND('',#7136,.T.);
#5403=FACE_OUTER_BOUND('',#7137,.T.);
#5404=FACE_OUTER_BOUND('',#7138,.T.);
#5405=FACE_OUTER_BOUND('',#7139,.T.);
#5406=FACE_OUTER_BOUND('',#7140,.T.);
#5407=FACE_OUTER_BOUND('',#7141,.T.);
#5408=FACE_OUTER_BOUND('',#7142,.T.);
#5409=FACE_OUTER_BOUND('',#7143,.T.);
#5410=FACE_OUTER_BOUND('',#7144,.T.);
#5411=FACE_OUTER_BOUND('',#7145,.T.);
#5412=FACE_OUTER_BOUND('',#7146,.T.);
#5413=FACE_OUTER_BOUND('',#7147,.T.);
#5414=FACE_OUTER_BOUND('',#7148,.T.);
#5415=FACE_OUTER_BOUND('',#7149,.T.);
#5416=FACE_OUTER_BOUND('',#7150,.T.);
#5417=FACE_OUTER_BOUND('',#7151,.T.);
#5418=FACE_OUTER_BOUND('',#7152,.T.);
#5419=FACE_OUTER_BOUND('',#7153,.T.);
#5420=FACE_OUTER_BOUND('',#7154,.T.);
#5421=FACE_OUTER_BOUND('',#7155,.T.);
#5422=FACE_OUTER_BOUND('',#7156,.T.);
#5423=FACE_OUTER_BOUND('',#7157,.T.);
#5424=FACE_OUTER_BOUND('',#7158,.T.);
#5425=FACE_OUTER_BOUND('',#7159,.T.);
#5426=FACE_OUTER_BOUND('',#7160,.T.);
#5427=FACE_OUTER_BOUND('',#7161,.T.);
#5428=FACE_OUTER_BOUND('',#7162,.T.);
#5429=FACE_OUTER_BOUND('',#7163,.T.);
#5430=FACE_OUTER_BOUND('',#7164,.T.);
#5431=FACE_OUTER_BOUND('',#7165,.T.);
#5432=FACE_OUTER_BOUND('',#7166,.T.);
#5433=FACE_OUTER_BOUND('',#7167,.T.);
#5434=FACE_OUTER_BOUND('',#7168,.T.);
#5435=FACE_OUTER_BOUND('',#7169,.T.);
#5436=FACE_OUTER_BOUND('',#7170,.T.);
#5437=FACE_OUTER_BOUND('',#7171,.T.);
#5438=FACE_OUTER_BOUND('',#7172,.T.);
#5439=FACE_OUTER_BOUND('',#7173,.T.);
#5440=FACE_OUTER_BOUND('',#7174,.T.);
#5441=FACE_OUTER_BOUND('',#7175,.T.);
#5442=FACE_OUTER_BOUND('',#7176,.T.);
#5443=FACE_OUTER_BOUND('',#7177,.T.);
#5444=FACE_OUTER_BOUND('',#7178,.T.);
#5445=FACE_OUTER_BOUND('',#7179,.T.);
#5446=FACE_OUTER_BOUND('',#7180,.T.);
#5447=FACE_OUTER_BOUND('',#7181,.T.);
#5448=FACE_OUTER_BOUND('',#7182,.T.);
#5449=FACE_OUTER_BOUND('',#7183,.T.);
#5450=FACE_OUTER_BOUND('',#7184,.T.);
#5451=FACE_OUTER_BOUND('',#7185,.T.);
#5452=FACE_OUTER_BOUND('',#7186,.T.);
#5453=FACE_OUTER_BOUND('',#7187,.T.);
#5454=FACE_OUTER_BOUND('',#7188,.T.);
#5455=FACE_OUTER_BOUND('',#7189,.T.);
#5456=FACE_OUTER_BOUND('',#7190,.T.);
#5457=FACE_OUTER_BOUND('',#7191,.T.);
#5458=FACE_OUTER_BOUND('',#7192,.T.);
#5459=FACE_OUTER_BOUND('',#7193,.T.);
#5460=FACE_OUTER_BOUND('',#7194,.T.);
#5461=FACE_OUTER_BOUND('',#7195,.T.);
#5462=FACE_OUTER_BOUND('',#7196,.T.);
#5463=FACE_OUTER_BOUND('',#7197,.T.);
#5464=FACE_OUTER_BOUND('',#7198,.T.);
#5465=FACE_OUTER_BOUND('',#7199,.T.);
#5466=FACE_OUTER_BOUND('',#7200,.T.);
#5467=FACE_OUTER_BOUND('',#7201,.T.);
#5468=FACE_OUTER_BOUND('',#7202,.T.);
#5469=FACE_OUTER_BOUND('',#7203,.T.);
#5470=FACE_OUTER_BOUND('',#7204,.T.);
#5471=FACE_OUTER_BOUND('',#7205,.T.);
#5472=FACE_OUTER_BOUND('',#7206,.T.);
#5473=FACE_OUTER_BOUND('',#7207,.T.);
#5474=FACE_OUTER_BOUND('',#7208,.T.);
#5475=FACE_OUTER_BOUND('',#7209,.T.);
#5476=FACE_OUTER_BOUND('',#7210,.T.);
#5477=FACE_OUTER_BOUND('',#7211,.T.);
#5478=FACE_OUTER_BOUND('',#7212,.T.);
#5479=FACE_OUTER_BOUND('',#7213,.T.);
#5480=FACE_OUTER_BOUND('',#7214,.T.);
#5481=FACE_OUTER_BOUND('',#7215,.T.);
#5482=FACE_OUTER_BOUND('',#7216,.T.);
#5483=FACE_OUTER_BOUND('',#7217,.T.);
#5484=FACE_OUTER_BOUND('',#7218,.T.);
#5485=FACE_OUTER_BOUND('',#7219,.T.);
#5486=FACE_OUTER_BOUND('',#7220,.T.);
#5487=FACE_OUTER_BOUND('',#7221,.T.);
#5488=FACE_OUTER_BOUND('',#7222,.T.);
#5489=FACE_OUTER_BOUND('',#7223,.T.);
#5490=FACE_OUTER_BOUND('',#7224,.T.);
#5491=FACE_OUTER_BOUND('',#7225,.T.);
#5492=FACE_OUTER_BOUND('',#7226,.T.);
#5493=FACE_OUTER_BOUND('',#7227,.T.);
#5494=FACE_OUTER_BOUND('',#7228,.T.);
#5495=FACE_OUTER_BOUND('',#7229,.T.);
#5496=FACE_OUTER_BOUND('',#7231,.T.);
#5497=FACE_OUTER_BOUND('',#7232,.T.);
#5498=FACE_OUTER_BOUND('',#7233,.T.);
#5499=FACE_OUTER_BOUND('',#7234,.T.);
#5500=FACE_OUTER_BOUND('',#7236,.T.);
#5501=FACE_OUTER_BOUND('',#7237,.T.);
#5502=FACE_OUTER_BOUND('',#7238,.T.);
#5503=FACE_OUTER_BOUND('',#7239,.T.);
#5504=FACE_OUTER_BOUND('',#7240,.T.);
#5505=FACE_OUTER_BOUND('',#7241,.T.);
#5506=FACE_OUTER_BOUND('',#7242,.T.);
#5507=FACE_OUTER_BOUND('',#7243,.T.);
#5508=FACE_OUTER_BOUND('',#7244,.T.);
#5509=FACE_OUTER_BOUND('',#7245,.T.);
#5510=FACE_OUTER_BOUND('',#7246,.T.);
#5511=FACE_OUTER_BOUND('',#7247,.T.);
#5512=FACE_OUTER_BOUND('',#7248,.T.);
#5513=FACE_OUTER_BOUND('',#7249,.T.);
#5514=FACE_OUTER_BOUND('',#7250,.T.);
#5515=FACE_OUTER_BOUND('',#7251,.T.);
#5516=FACE_OUTER_BOUND('',#7252,.T.);
#5517=FACE_OUTER_BOUND('',#7253,.T.);
#5518=FACE_OUTER_BOUND('',#7254,.T.);
#5519=FACE_OUTER_BOUND('',#7255,.T.);
#5520=FACE_OUTER_BOUND('',#7256,.T.);
#5521=FACE_OUTER_BOUND('',#7257,.T.);
#5522=FACE_OUTER_BOUND('',#7258,.T.);
#5523=FACE_OUTER_BOUND('',#7259,.T.);
#5524=FACE_OUTER_BOUND('',#7260,.T.);
#5525=FACE_OUTER_BOUND('',#7261,.T.);
#5526=FACE_OUTER_BOUND('',#7262,.T.);
#5527=FACE_OUTER_BOUND('',#7263,.T.);
#5528=FACE_OUTER_BOUND('',#7264,.T.);
#5529=FACE_OUTER_BOUND('',#7265,.T.);
#5530=FACE_OUTER_BOUND('',#7266,.T.);
#5531=FACE_OUTER_BOUND('',#7267,.T.);
#5532=FACE_OUTER_BOUND('',#7268,.T.);
#5533=FACE_OUTER_BOUND('',#7269,.T.);
#5534=FACE_OUTER_BOUND('',#7270,.T.);
#5535=FACE_OUTER_BOUND('',#7271,.T.);
#5536=FACE_OUTER_BOUND('',#7272,.T.);
#5537=FACE_OUTER_BOUND('',#7273,.T.);
#5538=FACE_OUTER_BOUND('',#7274,.T.);
#5539=FACE_OUTER_BOUND('',#7275,.T.);
#5540=FACE_OUTER_BOUND('',#7276,.T.);
#5541=FACE_OUTER_BOUND('',#7277,.T.);
#5542=FACE_OUTER_BOUND('',#7278,.T.);
#5543=FACE_OUTER_BOUND('',#7279,.T.);
#5544=FACE_OUTER_BOUND('',#7280,.T.);
#5545=FACE_OUTER_BOUND('',#7281,.T.);
#5546=FACE_OUTER_BOUND('',#7282,.T.);
#5547=FACE_OUTER_BOUND('',#7283,.T.);
#5548=FACE_OUTER_BOUND('',#7284,.T.);
#5549=FACE_OUTER_BOUND('',#7285,.T.);
#5550=FACE_OUTER_BOUND('',#7286,.T.);
#5551=FACE_OUTER_BOUND('',#7287,.T.);
#5552=FACE_OUTER_BOUND('',#7288,.T.);
#5553=FACE_OUTER_BOUND('',#7289,.T.);
#5554=FACE_OUTER_BOUND('',#7290,.T.);
#5555=FACE_OUTER_BOUND('',#7291,.T.);
#5556=FACE_OUTER_BOUND('',#7292,.T.);
#5557=FACE_OUTER_BOUND('',#7293,.T.);
#5558=FACE_OUTER_BOUND('',#7294,.T.);
#5559=FACE_OUTER_BOUND('',#7295,.T.);
#5560=FACE_OUTER_BOUND('',#7296,.T.);
#5561=FACE_OUTER_BOUND('',#7297,.T.);
#5562=FACE_OUTER_BOUND('',#7298,.T.);
#5563=FACE_OUTER_BOUND('',#7299,.T.);
#5564=FACE_OUTER_BOUND('',#7300,.T.);
#5565=FACE_OUTER_BOUND('',#7301,.T.);
#5566=FACE_OUTER_BOUND('',#7302,.T.);
#5567=FACE_OUTER_BOUND('',#7303,.T.);
#5568=FACE_OUTER_BOUND('',#7304,.T.);
#5569=FACE_OUTER_BOUND('',#7305,.T.);
#5570=FACE_OUTER_BOUND('',#7306,.T.);
#5571=FACE_OUTER_BOUND('',#7307,.T.);
#5572=FACE_OUTER_BOUND('',#7308,.T.);
#5573=FACE_OUTER_BOUND('',#7309,.T.);
#5574=FACE_OUTER_BOUND('',#7310,.T.);
#5575=FACE_OUTER_BOUND('',#7311,.T.);
#5576=FACE_OUTER_BOUND('',#7312,.T.);
#5577=FACE_OUTER_BOUND('',#7313,.T.);
#5578=FACE_OUTER_BOUND('',#7314,.T.);
#5579=FACE_OUTER_BOUND('',#7315,.T.);
#5580=FACE_OUTER_BOUND('',#7316,.T.);
#5581=FACE_OUTER_BOUND('',#7317,.T.);
#5582=FACE_OUTER_BOUND('',#7318,.T.);
#5583=FACE_OUTER_BOUND('',#7319,.T.);
#5584=FACE_OUTER_BOUND('',#7320,.T.);
#5585=FACE_OUTER_BOUND('',#7321,.T.);
#5586=FACE_OUTER_BOUND('',#7322,.T.);
#5587=FACE_OUTER_BOUND('',#7323,.T.);
#5588=FACE_OUTER_BOUND('',#7324,.T.);
#5589=FACE_OUTER_BOUND('',#7325,.T.);
#5590=FACE_OUTER_BOUND('',#7326,.T.);
#5591=FACE_OUTER_BOUND('',#7327,.T.);
#5592=FACE_OUTER_BOUND('',#7328,.T.);
#5593=FACE_OUTER_BOUND('',#7329,.T.);
#5594=FACE_OUTER_BOUND('',#7330,.T.);
#5595=FACE_OUTER_BOUND('',#7331,.T.);
#5596=FACE_OUTER_BOUND('',#7332,.T.);
#5597=FACE_OUTER_BOUND('',#7333,.T.);
#5598=FACE_OUTER_BOUND('',#7334,.T.);
#5599=FACE_OUTER_BOUND('',#7335,.T.);
#5600=FACE_OUTER_BOUND('',#7336,.T.);
#5601=FACE_OUTER_BOUND('',#7337,.T.);
#5602=FACE_OUTER_BOUND('',#7338,.T.);
#5603=FACE_OUTER_BOUND('',#7339,.T.);
#5604=FACE_OUTER_BOUND('',#7340,.T.);
#5605=FACE_OUTER_BOUND('',#7341,.T.);
#5606=FACE_OUTER_BOUND('',#7342,.T.);
#5607=FACE_OUTER_BOUND('',#7343,.T.);
#5608=FACE_OUTER_BOUND('',#7344,.T.);
#5609=FACE_OUTER_BOUND('',#7345,.T.);
#5610=FACE_OUTER_BOUND('',#7346,.T.);
#5611=FACE_OUTER_BOUND('',#7347,.T.);
#5612=FACE_OUTER_BOUND('',#7348,.T.);
#5613=FACE_OUTER_BOUND('',#7349,.T.);
#5614=FACE_OUTER_BOUND('',#7350,.T.);
#5615=FACE_OUTER_BOUND('',#7351,.T.);
#5616=FACE_OUTER_BOUND('',#7352,.T.);
#5617=FACE_OUTER_BOUND('',#7353,.T.);
#5618=FACE_OUTER_BOUND('',#7354,.T.);
#5619=FACE_OUTER_BOUND('',#7355,.T.);
#5620=FACE_OUTER_BOUND('',#7356,.T.);
#5621=FACE_OUTER_BOUND('',#7357,.T.);
#5622=FACE_OUTER_BOUND('',#7358,.T.);
#5623=FACE_OUTER_BOUND('',#7359,.T.);
#5624=FACE_OUTER_BOUND('',#7360,.T.);
#5625=FACE_OUTER_BOUND('',#7361,.T.);
#5626=FACE_OUTER_BOUND('',#7362,.T.);
#5627=FACE_OUTER_BOUND('',#7363,.T.);
#5628=FACE_OUTER_BOUND('',#7364,.T.);
#5629=FACE_OUTER_BOUND('',#7365,.T.);
#5630=FACE_OUTER_BOUND('',#7366,.T.);
#5631=FACE_OUTER_BOUND('',#7367,.T.);
#5632=FACE_OUTER_BOUND('',#7368,.T.);
#5633=FACE_OUTER_BOUND('',#7369,.T.);
#5634=FACE_OUTER_BOUND('',#7370,.T.);
#5635=FACE_OUTER_BOUND('',#7371,.T.);
#5636=FACE_OUTER_BOUND('',#7372,.T.);
#5637=FACE_OUTER_BOUND('',#7373,.T.);
#5638=FACE_OUTER_BOUND('',#7374,.T.);
#5639=FACE_OUTER_BOUND('',#7375,.T.);
#5640=FACE_OUTER_BOUND('',#7376,.T.);
#5641=FACE_OUTER_BOUND('',#7377,.T.);
#5642=FACE_OUTER_BOUND('',#7378,.T.);
#5643=FACE_OUTER_BOUND('',#7379,.T.);
#5644=FACE_OUTER_BOUND('',#7380,.T.);
#5645=FACE_OUTER_BOUND('',#7381,.T.);
#5646=FACE_OUTER_BOUND('',#7382,.T.);
#5647=FACE_OUTER_BOUND('',#7383,.T.);
#5648=FACE_OUTER_BOUND('',#7384,.T.);
#5649=FACE_OUTER_BOUND('',#7385,.T.);
#5650=FACE_OUTER_BOUND('',#7386,.T.);
#5651=FACE_OUTER_BOUND('',#7387,.T.);
#5652=FACE_OUTER_BOUND('',#7388,.T.);
#5653=FACE_OUTER_BOUND('',#7389,.T.);
#5654=FACE_OUTER_BOUND('',#7390,.T.);
#5655=FACE_OUTER_BOUND('',#7391,.T.);
#5656=FACE_OUTER_BOUND('',#7392,.T.);
#5657=FACE_OUTER_BOUND('',#7393,.T.);
#5658=FACE_OUTER_BOUND('',#7394,.T.);
#5659=FACE_OUTER_BOUND('',#7395,.T.);
#5660=FACE_OUTER_BOUND('',#7396,.T.);
#5661=FACE_OUTER_BOUND('',#7397,.T.);
#5662=FACE_OUTER_BOUND('',#7398,.T.);
#5663=FACE_OUTER_BOUND('',#7399,.T.);
#5664=FACE_OUTER_BOUND('',#7400,.T.);
#5665=FACE_OUTER_BOUND('',#7401,.T.);
#5666=FACE_OUTER_BOUND('',#7402,.T.);
#5667=FACE_OUTER_BOUND('',#7403,.T.);
#5668=FACE_OUTER_BOUND('',#7404,.T.);
#5669=FACE_OUTER_BOUND('',#7405,.T.);
#5670=FACE_OUTER_BOUND('',#7406,.T.);
#5671=FACE_OUTER_BOUND('',#7407,.T.);
#5672=FACE_OUTER_BOUND('',#7408,.T.);
#5673=FACE_OUTER_BOUND('',#7409,.T.);
#5674=FACE_OUTER_BOUND('',#7410,.T.);
#5675=FACE_OUTER_BOUND('',#7411,.T.);
#5676=FACE_OUTER_BOUND('',#7412,.T.);
#5677=FACE_OUTER_BOUND('',#7413,.T.);
#5678=FACE_OUTER_BOUND('',#7414,.T.);
#5679=FACE_OUTER_BOUND('',#7415,.T.);
#5680=FACE_OUTER_BOUND('',#7416,.T.);
#5681=FACE_OUTER_BOUND('',#7417,.T.);
#5682=FACE_OUTER_BOUND('',#7418,.T.);
#5683=FACE_OUTER_BOUND('',#7419,.T.);
#5684=FACE_OUTER_BOUND('',#7420,.T.);
#5685=FACE_OUTER_BOUND('',#7421,.T.);
#5686=FACE_OUTER_BOUND('',#7422,.T.);
#5687=FACE_OUTER_BOUND('',#7423,.T.);
#5688=FACE_OUTER_BOUND('',#7424,.T.);
#5689=FACE_OUTER_BOUND('',#7425,.T.);
#5690=FACE_OUTER_BOUND('',#7426,.T.);
#5691=FACE_OUTER_BOUND('',#7427,.T.);
#5692=FACE_OUTER_BOUND('',#7428,.T.);
#5693=FACE_OUTER_BOUND('',#7429,.T.);
#5694=FACE_OUTER_BOUND('',#7430,.T.);
#5695=FACE_OUTER_BOUND('',#7431,.T.);
#5696=FACE_OUTER_BOUND('',#7432,.T.);
#5697=FACE_OUTER_BOUND('',#7433,.T.);
#5698=FACE_OUTER_BOUND('',#7434,.T.);
#5699=FACE_OUTER_BOUND('',#7435,.T.);
#5700=FACE_OUTER_BOUND('',#7436,.T.);
#5701=FACE_OUTER_BOUND('',#7437,.T.);
#5702=FACE_OUTER_BOUND('',#7438,.T.);
#5703=FACE_OUTER_BOUND('',#7439,.T.);
#5704=FACE_OUTER_BOUND('',#7440,.T.);
#5705=FACE_OUTER_BOUND('',#7441,.T.);
#5706=FACE_OUTER_BOUND('',#7442,.T.);
#5707=FACE_OUTER_BOUND('',#7443,.T.);
#5708=FACE_OUTER_BOUND('',#7444,.T.);
#5709=FACE_OUTER_BOUND('',#7445,.T.);
#5710=FACE_OUTER_BOUND('',#7446,.T.);
#5711=FACE_OUTER_BOUND('',#7447,.T.);
#5712=FACE_OUTER_BOUND('',#7448,.T.);
#5713=FACE_OUTER_BOUND('',#7449,.T.);
#5714=FACE_OUTER_BOUND('',#7450,.T.);
#5715=FACE_OUTER_BOUND('',#7451,.T.);
#5716=FACE_OUTER_BOUND('',#7452,.T.);
#5717=FACE_OUTER_BOUND('',#7453,.T.);
#5718=FACE_OUTER_BOUND('',#7454,.T.);
#5719=FACE_OUTER_BOUND('',#7455,.T.);
#5720=FACE_OUTER_BOUND('',#7456,.T.);
#5721=FACE_OUTER_BOUND('',#7457,.T.);
#5722=FACE_OUTER_BOUND('',#7458,.T.);
#5723=FACE_OUTER_BOUND('',#7459,.T.);
#5724=FACE_OUTER_BOUND('',#7460,.T.);
#5725=FACE_OUTER_BOUND('',#7461,.T.);
#5726=FACE_OUTER_BOUND('',#7462,.T.);
#5727=FACE_OUTER_BOUND('',#7463,.T.);
#5728=FACE_OUTER_BOUND('',#7464,.T.);
#5729=FACE_OUTER_BOUND('',#7465,.T.);
#5730=FACE_OUTER_BOUND('',#7466,.T.);
#5731=FACE_OUTER_BOUND('',#7467,.T.);
#5732=FACE_OUTER_BOUND('',#7468,.T.);
#5733=FACE_OUTER_BOUND('',#7469,.T.);
#5734=FACE_OUTER_BOUND('',#7470,.T.);
#6906=EDGE_LOOP('',(#19757,#19758,#19759,#19760,#19761,#19762,#19763));
#6907=EDGE_LOOP('',(#19764,#19765,#19766,#19767));
#6908=EDGE_LOOP('',(#19768,#19769,#19770,#19771));
#6909=EDGE_LOOP('',(#19772,#19773,#19774,#19775));
#6910=EDGE_LOOP('',(#19776,#19777,#19778,#19779));
#6911=EDGE_LOOP('',(#19780,#19781,#19782,#19783));
#6912=EDGE_LOOP('',(#19784,#19785,#19786,#19787));
#6913=EDGE_LOOP('',(#19788,#19789,#19790,#19791));
#6914=EDGE_LOOP('',(#19792,#19793,#19794,#19795));
#6915=EDGE_LOOP('',(#19796,#19797,#19798,#19799));
#6916=EDGE_LOOP('',(#19800,#19801,#19802,#19803));
#6917=EDGE_LOOP('',(#19804,#19805,#19806,#19807));
#6918=EDGE_LOOP('',(#19808,#19809,#19810,#19811));
#6919=EDGE_LOOP('',(#19812,#19813,#19814,#19815));
#6920=EDGE_LOOP('',(#19816,#19817,#19818,#19819));
#6921=EDGE_LOOP('',(#19820,#19821,#19822,#19823));
#6922=EDGE_LOOP('',(#19824,#19825,#19826,#19827));
#6923=EDGE_LOOP('',(#19828,#19829,#19830,#19831));
#6924=EDGE_LOOP('',(#19832,#19833,#19834,#19835));
#6925=EDGE_LOOP('',(#19836,#19837,#19838,#19839));
#6926=EDGE_LOOP('',(#19840,#19841,#19842,#19843));
#6927=EDGE_LOOP('',(#19844,#19845,#19846,#19847));
#6928=EDGE_LOOP('',(#19848,#19849,#19850,#19851));
#6929=EDGE_LOOP('',(#19852,#19853,#19854,#19855));
#6930=EDGE_LOOP('',(#19856,#19857,#19858,#19859));
#6931=EDGE_LOOP('',(#19860,#19861,#19862,#19863));
#6932=EDGE_LOOP('',(#19864,#19865,#19866,#19867));
#6933=EDGE_LOOP('',(#19868,#19869,#19870,#19871));
#6934=EDGE_LOOP('',(#19872,#19873,#19874));
#6935=EDGE_LOOP('',(#19875,#19876,#19877));
#6936=EDGE_LOOP('',(#19878,#19879,#19880,#19881));
#6937=EDGE_LOOP('',(#19882,#19883,#19884,#19885));
#6938=EDGE_LOOP('',(#19886,#19887,#19888,#19889));
#6939=EDGE_LOOP('',(#19890,#19891,#19892,#19893));
#6940=EDGE_LOOP('',(#19894,#19895,#19896,#19897));
#6941=EDGE_LOOP('',(#19898,#19899,#19900,#19901));
#6942=EDGE_LOOP('',(#19902,#19903,#19904,#19905));
#6943=EDGE_LOOP('',(#19906,#19907,#19908,#19909));
#6944=EDGE_LOOP('',(#19910,#19911,#19912,#19913));
#6945=EDGE_LOOP('',(#19914,#19915,#19916,#19917));
#6946=EDGE_LOOP('',(#19918,#19919,#19920,#19921));
#6947=EDGE_LOOP('',(#19922,#19923,#19924,#19925));
#6948=EDGE_LOOP('',(#19926,#19927,#19928,#19929));
#6949=EDGE_LOOP('',(#19930,#19931,#19932,#19933));
#6950=EDGE_LOOP('',(#19934,#19935,#19936,#19937));
#6951=EDGE_LOOP('',(#19938,#19939,#19940,#19941));
#6952=EDGE_LOOP('',(#19942,#19943,#19944,#19945));
#6953=EDGE_LOOP('',(#19946,#19947,#19948,#19949));
#6954=EDGE_LOOP('',(#19950,#19951,#19952,#19953));
#6955=EDGE_LOOP('',(#19954,#19955,#19956,#19957));
#6956=EDGE_LOOP('',(#19958,#19959,#19960,#19961));
#6957=EDGE_LOOP('',(#19962,#19963,#19964,#19965));
#6958=EDGE_LOOP('',(#19966,#19967,#19968,#19969));
#6959=EDGE_LOOP('',(#19970,#19971,#19972,#19973));
#6960=EDGE_LOOP('',(#19974,#19975,#19976,#19977));
#6961=EDGE_LOOP('',(#19978,#19979,#19980,#19981));
#6962=EDGE_LOOP('',(#19982,#19983,#19984,#19985));
#6963=EDGE_LOOP('',(#19986,#19987,#19988,#19989));
#6964=EDGE_LOOP('',(#19990,#19991,#19992,#19993));
#6965=EDGE_LOOP('',(#19994,#19995,#19996));
#6966=EDGE_LOOP('',(#19997,#19998,#19999,#20000,#20001));
#6967=EDGE_LOOP('',(#20002,#20003,#20004,#20005));
#6968=EDGE_LOOP('',(#20006,#20007,#20008,#20009));
#6969=EDGE_LOOP('',(#20010,#20011,#20012,#20013));
#6970=EDGE_LOOP('',(#20014,#20015,#20016,#20017));
#6971=EDGE_LOOP('',(#20018,#20019,#20020,#20021));
#6972=EDGE_LOOP('',(#20022,#20023,#20024,#20025));
#6973=EDGE_LOOP('',(#20026,#20027,#20028,#20029));
#6974=EDGE_LOOP('',(#20030,#20031,#20032,#20033));
#6975=EDGE_LOOP('',(#20034,#20035,#20036,#20037));
#6976=EDGE_LOOP('',(#20038,#20039,#20040,#20041));
#6977=EDGE_LOOP('',(#20042,#20043,#20044,#20045));
#6978=EDGE_LOOP('',(#20046,#20047,#20048,#20049));
#6979=EDGE_LOOP('',(#20050,#20051,#20052,#20053));
#6980=EDGE_LOOP('',(#20054,#20055,#20056,#20057));
#6981=EDGE_LOOP('',(#20058,#20059,#20060,#20061));
#6982=EDGE_LOOP('',(#20062,#20063,#20064,#20065));
#6983=EDGE_LOOP('',(#20066,#20067,#20068,#20069,#20070,#20071,#20072,#20073,
#20074,#20075));
#6984=EDGE_LOOP('',(#20076,#20077,#20078,#20079));
#6985=EDGE_LOOP('',(#20080,#20081,#20082,#20083,#20084,#20085,#20086,#20087,
#20088,#20089,#20090,#20091,#20092,#20093,#20094,#20095,#20096,#20097,#20098,
#20099,#20100,#20101,#20102,#20103,#20104,#20105,#20106,#20107,#20108,#20109,
#20110,#20111,#20112,#20113,#20114,#20115,#20116,#20117,#20118,#20119,#20120,
#20121,#20122,#20123,#20124,#20125,#20126,#20127,#20128,#20129,#20130,#20131,
#20132,#20133,#20134,#20135,#20136,#20137,#20138,#20139,#20140,#20141,#20142,
#20143,#20144,#20145,#20146,#20147,#20148,#20149,#20150,#20151,#20152,#20153,
#20154,#20155,#20156,#20157,#20158,#20159,#20160,#20161,#20162,#20163,#20164,
#20165,#20166,#20167,#20168,#20169,#20170,#20171,#20172,#20173,#20174,#20175,
#20176,#20177,#20178,#20179,#20180,#20181,#20182,#20183,#20184,#20185,#20186,
#20187,#20188,#20189,#20190,#20191,#20192,#20193,#20194,#20195,#20196,#20197,
#20198,#20199,#20200,#20201,#20202,#20203,#20204,#20205,#20206,#20207,#20208,
#20209,#20210,#20211,#20212,#20213,#20214,#20215,#20216,#20217,#20218,#20219,
#20220,#20221,#20222,#20223,#20224,#20225,#20226,#20227,#20228,#20229,#20230,
#20231,#20232,#20233,#20234,#20235,#20236,#20237,#20238,#20239,#20240,#20241,
#20242,#20243,#20244,#20245,#20246,#20247,#20248,#20249,#20250,#20251,#20252,
#20253,#20254,#20255,#20256,#20257,#20258,#20259,#20260,#20261,#20262,#20263,
#20264,#20265,#20266,#20267,#20268,#20269,#20270,#20271,#20272,#20273,#20274,
#20275,#20276,#20277,#20278,#20279,#20280,#20281,#20282,#20283,#20284,#20285,
#20286,#20287,#20288,#20289,#20290,#20291,#20292,#20293,#20294,#20295,#20296,
#20297,#20298,#20299,#20300,#20301,#20302,#20303,#20304,#20305,#20306,#20307,
#20308,#20309,#20310,#20311,#20312,#20313,#20314,#20315,#20316,#20317,#20318,
#20319,#20320,#20321,#20322,#20323,#20324,#20325,#20326,#20327,#20328,#20329,
#20330,#20331,#20332,#20333,#20334,#20335,#20336,#20337,#20338,#20339,#20340,
#20341,#20342,#20343,#20344,#20345,#20346,#20347,#20348,#20349,#20350,#20351,
#20352,#20353,#20354,#20355,#20356,#20357,#20358,#20359,#20360,#20361,#20362,
#20363,#20364,#20365,#20366,#20367,#20368,#20369,#20370,#20371,#20372,#20373,
#20374,#20375,#20376,#20377,#20378,#20379,#20380,#20381,#20382,#20383,#20384,
#20385,#20386,#20387,#20388,#20389,#20390,#20391,#20392,#20393,#20394,#20395,
#20396,#20397,#20398,#20399,#20400,#20401,#20402,#20403));
#6986=EDGE_LOOP('',(#20404,#20405,#20406,#20407,#20408,#20409,#20410,#20411,
#20412,#20413,#20414,#20415,#20416,#20417,#20418,#20419,#20420,#20421,#20422,
#20423,#20424,#20425,#20426,#20427,#20428,#20429,#20430,#20431,#20432,#20433,
#20434,#20435,#20436,#20437,#20438,#20439,#20440,#20441,#20442,#20443,#20444,
#20445,#20446,#20447,#20448,#20449,#20450,#20451,#20452,#20453,#20454,#20455,
#20456,#20457,#20458,#20459,#20460,#20461,#20462,#20463,#20464,#20465,#20466,
#20467,#20468,#20469,#20470,#20471,#20472,#20473,#20474,#20475,#20476,#20477,
#20478,#20479,#20480,#20481,#20482,#20483,#20484,#20485,#20486,#20487,#20488,
#20489,#20490,#20491,#20492,#20493,#20494,#20495,#20496,#20497,#20498,#20499,
#20500,#20501,#20502,#20503,#20504,#20505,#20506,#20507,#20508,#20509,#20510,
#20511,#20512,#20513,#20514,#20515,#20516,#20517,#20518,#20519,#20520,#20521,
#20522,#20523,#20524,#20525,#20526,#20527,#20528,#20529,#20530,#20531,#20532,
#20533,#20534,#20535,#20536,#20537,#20538,#20539,#20540,#20541,#20542,#20543,
#20544,#20545,#20546,#20547,#20548,#20549,#20550,#20551,#20552,#20553,#20554,
#20555,#20556,#20557,#20558,#20559,#20560,#20561,#20562,#20563,#20564,#20565,
#20566,#20567,#20568,#20569,#20570,#20571,#20572,#20573,#20574,#20575,#20576,
#20577,#20578,#20579,#20580,#20581,#20582,#20583,#20584,#20585,#20586,#20587,
#20588,#20589,#20590,#20591,#20592,#20593,#20594,#20595,#20596,#20597,#20598,
#20599,#20600,#20601,#20602,#20603,#20604,#20605,#20606,#20607,#20608,#20609,
#20610,#20611,#20612,#20613,#20614,#20615,#20616,#20617,#20618,#20619,#20620,
#20621,#20622,#20623,#20624,#20625,#20626,#20627,#20628,#20629,#20630,#20631,
#20632,#20633,#20634,#20635,#20636,#20637,#20638,#20639,#20640,#20641,#20642,
#20643,#20644,#20645,#20646,#20647,#20648,#20649,#20650,#20651,#20652,#20653,
#20654,#20655,#20656,#20657,#20658,#20659,#20660,#20661,#20662,#20663,#20664,
#20665,#20666,#20667,#20668,#20669,#20670,#20671,#20672,#20673,#20674,#20675,
#20676,#20677,#20678,#20679,#20680,#20681,#20682,#20683,#20684,#20685,#20686,
#20687,#20688,#20689,#20690,#20691,#20692,#20693,#20694,#20695,#20696,#20697,
#20698,#20699,#20700,#20701,#20702,#20703,#20704,#20705,#20706,#20707,#20708,
#20709,#20710,#20711,#20712,#20713,#20714,#20715,#20716,#20717,#20718,#20719,
#20720,#20721,#20722,#20723,#20724,#20725,#20726,#20727,#20728));
#6987=EDGE_LOOP('',(#20729,#20730,#20731,#20732,#20733));
#6988=EDGE_LOOP('',(#20734,#20735,#20736,#20737));
#6989=EDGE_LOOP('',(#20738,#20739,#20740,#20741));
#6990=EDGE_LOOP('',(#20742,#20743,#20744,#20745));
#6991=EDGE_LOOP('',(#20746,#20747,#20748,#20749));
#6992=EDGE_LOOP('',(#20750,#20751,#20752,#20753));
#6993=EDGE_LOOP('',(#20754,#20755,#20756,#20757));
#6994=EDGE_LOOP('',(#20758,#20759,#20760,#20761));
#6995=EDGE_LOOP('',(#20762,#20763,#20764,#20765));
#6996=EDGE_LOOP('',(#20766,#20767,#20768,#20769));
#6997=EDGE_LOOP('',(#20770,#20771,#20772,#20773));
#6998=EDGE_LOOP('',(#20774,#20775,#20776,#20777));
#6999=EDGE_LOOP('',(#20778,#20779,#20780,#20781));
#7000=EDGE_LOOP('',(#20782,#20783,#20784,#20785));
#7001=EDGE_LOOP('',(#20786,#20787,#20788,#20789));
#7002=EDGE_LOOP('',(#20790,#20791,#20792,#20793));
#7003=EDGE_LOOP('',(#20794,#20795,#20796,#20797));
#7004=EDGE_LOOP('',(#20798,#20799,#20800,#20801));
#7005=EDGE_LOOP('',(#20802,#20803,#20804,#20805));
#7006=EDGE_LOOP('',(#20806,#20807,#20808,#20809));
#7007=EDGE_LOOP('',(#20810,#20811,#20812,#20813));
#7008=EDGE_LOOP('',(#20814,#20815,#20816,#20817));
#7009=EDGE_LOOP('',(#20818,#20819,#20820,#20821));
#7010=EDGE_LOOP('',(#20822,#20823,#20824,#20825));
#7011=EDGE_LOOP('',(#20826,#20827,#20828,#20829));
#7012=EDGE_LOOP('',(#20830,#20831,#20832,#20833));
#7013=EDGE_LOOP('',(#20834,#20835,#20836,#20837));
#7014=EDGE_LOOP('',(#20838,#20839,#20840,#20841));
#7015=EDGE_LOOP('',(#20842,#20843,#20844,#20845));
#7016=EDGE_LOOP('',(#20846,#20847,#20848,#20849));
#7017=EDGE_LOOP('',(#20850,#20851,#20852,#20853));
#7018=EDGE_LOOP('',(#20854,#20855,#20856,#20857));
#7019=EDGE_LOOP('',(#20858,#20859,#20860,#20861));
#7020=EDGE_LOOP('',(#20862,#20863,#20864,#20865));
#7021=EDGE_LOOP('',(#20866,#20867,#20868,#20869));
#7022=EDGE_LOOP('',(#20870,#20871,#20872,#20873));
#7023=EDGE_LOOP('',(#20874,#20875,#20876,#20877));
#7024=EDGE_LOOP('',(#20878,#20879,#20880,#20881));
#7025=EDGE_LOOP('',(#20882,#20883,#20884,#20885));
#7026=EDGE_LOOP('',(#20886,#20887,#20888,#20889));
#7027=EDGE_LOOP('',(#20890,#20891,#20892,#20893));
#7028=EDGE_LOOP('',(#20894,#20895,#20896,#20897));
#7029=EDGE_LOOP('',(#20898,#20899,#20900,#20901));
#7030=EDGE_LOOP('',(#20902,#20903,#20904,#20905));
#7031=EDGE_LOOP('',(#20906,#20907,#20908,#20909));
#7032=EDGE_LOOP('',(#20910,#20911,#20912,#20913));
#7033=EDGE_LOOP('',(#20914,#20915,#20916,#20917));
#7034=EDGE_LOOP('',(#20918,#20919,#20920,#20921));
#7035=EDGE_LOOP('',(#20922,#20923,#20924,#20925));
#7036=EDGE_LOOP('',(#20926,#20927,#20928,#20929));
#7037=EDGE_LOOP('',(#20930,#20931,#20932,#20933));
#7038=EDGE_LOOP('',(#20934,#20935,#20936,#20937));
#7039=EDGE_LOOP('',(#20938,#20939,#20940,#20941));
#7040=EDGE_LOOP('',(#20942,#20943,#20944,#20945));
#7041=EDGE_LOOP('',(#20946,#20947,#20948,#20949));
#7042=EDGE_LOOP('',(#20950,#20951,#20952,#20953));
#7043=EDGE_LOOP('',(#20954,#20955,#20956,#20957));
#7044=EDGE_LOOP('',(#20958,#20959,#20960,#20961));
#7045=EDGE_LOOP('',(#20962,#20963,#20964,#20965));
#7046=EDGE_LOOP('',(#20966,#20967,#20968,#20969));
#7047=EDGE_LOOP('',(#20970,#20971,#20972,#20973));
#7048=EDGE_LOOP('',(#20974,#20975,#20976,#20977));
#7049=EDGE_LOOP('',(#20978,#20979,#20980,#20981));
#7050=EDGE_LOOP('',(#20982,#20983,#20984,#20985));
#7051=EDGE_LOOP('',(#20986,#20987,#20988,#20989));
#7052=EDGE_LOOP('',(#20990,#20991,#20992,#20993));
#7053=EDGE_LOOP('',(#20994,#20995,#20996,#20997));
#7054=EDGE_LOOP('',(#20998,#20999,#21000,#21001));
#7055=EDGE_LOOP('',(#21002,#21003,#21004,#21005));
#7056=EDGE_LOOP('',(#21006,#21007,#21008,#21009));
#7057=EDGE_LOOP('',(#21010,#21011,#21012,#21013));
#7058=EDGE_LOOP('',(#21014,#21015,#21016,#21017));
#7059=EDGE_LOOP('',(#21018,#21019,#21020,#21021));
#7060=EDGE_LOOP('',(#21022,#21023,#21024,#21025));
#7061=EDGE_LOOP('',(#21026,#21027,#21028,#21029));
#7062=EDGE_LOOP('',(#21030,#21031,#21032,#21033));
#7063=EDGE_LOOP('',(#21034,#21035,#21036,#21037));
#7064=EDGE_LOOP('',(#21038,#21039,#21040,#21041));
#7065=EDGE_LOOP('',(#21042,#21043,#21044,#21045));
#7066=EDGE_LOOP('',(#21046,#21047,#21048,#21049));
#7067=EDGE_LOOP('',(#21050,#21051,#21052,#21053));
#7068=EDGE_LOOP('',(#21054,#21055,#21056,#21057));
#7069=EDGE_LOOP('',(#21058,#21059,#21060,#21061));
#7070=EDGE_LOOP('',(#21062,#21063,#21064,#21065));
#7071=EDGE_LOOP('',(#21066,#21067,#21068,#21069));
#7072=EDGE_LOOP('',(#21070,#21071,#21072,#21073));
#7073=EDGE_LOOP('',(#21074,#21075,#21076,#21077));
#7074=EDGE_LOOP('',(#21078,#21079,#21080,#21081));
#7075=EDGE_LOOP('',(#21082,#21083,#21084,#21085));
#7076=EDGE_LOOP('',(#21086,#21087,#21088,#21089));
#7077=EDGE_LOOP('',(#21090,#21091,#21092,#21093));
#7078=EDGE_LOOP('',(#21094,#21095,#21096,#21097));
#7079=EDGE_LOOP('',(#21098,#21099,#21100,#21101));
#7080=EDGE_LOOP('',(#21102,#21103,#21104,#21105));
#7081=EDGE_LOOP('',(#21106,#21107,#21108,#21109));
#7082=EDGE_LOOP('',(#21110,#21111,#21112,#21113));
#7083=EDGE_LOOP('',(#21114,#21115,#21116,#21117));
#7084=EDGE_LOOP('',(#21118,#21119,#21120,#21121));
#7085=EDGE_LOOP('',(#21122,#21123,#21124,#21125));
#7086=EDGE_LOOP('',(#21126,#21127,#21128,#21129));
#7087=EDGE_LOOP('',(#21130,#21131,#21132,#21133));
#7088=EDGE_LOOP('',(#21134,#21135,#21136,#21137));
#7089=EDGE_LOOP('',(#21138,#21139,#21140,#21141));
#7090=EDGE_LOOP('',(#21142,#21143,#21144,#21145));
#7091=EDGE_LOOP('',(#21146,#21147,#21148,#21149));
#7092=EDGE_LOOP('',(#21150,#21151,#21152,#21153));
#7093=EDGE_LOOP('',(#21154,#21155,#21156,#21157));
#7094=EDGE_LOOP('',(#21158,#21159,#21160,#21161));
#7095=EDGE_LOOP('',(#21162,#21163,#21164,#21165));
#7096=EDGE_LOOP('',(#21166,#21167,#21168,#21169));
#7097=EDGE_LOOP('',(#21170,#21171,#21172,#21173));
#7098=EDGE_LOOP('',(#21174,#21175,#21176,#21177));
#7099=EDGE_LOOP('',(#21178,#21179,#21180,#21181));
#7100=EDGE_LOOP('',(#21182,#21183,#21184,#21185));
#7101=EDGE_LOOP('',(#21186,#21187,#21188,#21189));
#7102=EDGE_LOOP('',(#21190,#21191,#21192,#21193));
#7103=EDGE_LOOP('',(#21194,#21195,#21196,#21197));
#7104=EDGE_LOOP('',(#21198,#21199,#21200,#21201));
#7105=EDGE_LOOP('',(#21202,#21203,#21204,#21205));
#7106=EDGE_LOOP('',(#21206,#21207,#21208,#21209));
#7107=EDGE_LOOP('',(#21210,#21211,#21212,#21213));
#7108=EDGE_LOOP('',(#21214,#21215,#21216,#21217));
#7109=EDGE_LOOP('',(#21218,#21219,#21220,#21221));
#7110=EDGE_LOOP('',(#21222,#21223,#21224,#21225));
#7111=EDGE_LOOP('',(#21226,#21227,#21228,#21229));
#7112=EDGE_LOOP('',(#21230,#21231,#21232,#21233));
#7113=EDGE_LOOP('',(#21234,#21235,#21236,#21237));
#7114=EDGE_LOOP('',(#21238,#21239,#21240,#21241));
#7115=EDGE_LOOP('',(#21242,#21243,#21244,#21245));
#7116=EDGE_LOOP('',(#21246,#21247,#21248,#21249));
#7117=EDGE_LOOP('',(#21250,#21251,#21252,#21253));
#7118=EDGE_LOOP('',(#21254,#21255,#21256,#21257));
#7119=EDGE_LOOP('',(#21258,#21259,#21260,#21261));
#7120=EDGE_LOOP('',(#21262,#21263,#21264,#21265));
#7121=EDGE_LOOP('',(#21266,#21267,#21268,#21269));
#7122=EDGE_LOOP('',(#21270,#21271,#21272,#21273));
#7123=EDGE_LOOP('',(#21274,#21275,#21276,#21277));
#7124=EDGE_LOOP('',(#21278,#21279,#21280,#21281));
#7125=EDGE_LOOP('',(#21282,#21283,#21284,#21285));
#7126=EDGE_LOOP('',(#21286,#21287,#21288,#21289));
#7127=EDGE_LOOP('',(#21290,#21291,#21292,#21293));
#7128=EDGE_LOOP('',(#21294,#21295,#21296,#21297));
#7129=EDGE_LOOP('',(#21298,#21299,#21300,#21301));
#7130=EDGE_LOOP('',(#21302,#21303,#21304,#21305));
#7131=EDGE_LOOP('',(#21306,#21307,#21308,#21309));
#7132=EDGE_LOOP('',(#21310,#21311,#21312,#21313));
#7133=EDGE_LOOP('',(#21314,#21315,#21316,#21317));
#7134=EDGE_LOOP('',(#21318,#21319,#21320,#21321));
#7135=EDGE_LOOP('',(#21322,#21323,#21324,#21325));
#7136=EDGE_LOOP('',(#21326,#21327,#21328,#21329));
#7137=EDGE_LOOP('',(#21330,#21331,#21332,#21333));
#7138=EDGE_LOOP('',(#21334,#21335,#21336,#21337));
#7139=EDGE_LOOP('',(#21338,#21339,#21340,#21341));
#7140=EDGE_LOOP('',(#21342,#21343,#21344,#21345));
#7141=EDGE_LOOP('',(#21346,#21347,#21348,#21349));
#7142=EDGE_LOOP('',(#21350,#21351,#21352,#21353));
#7143=EDGE_LOOP('',(#21354,#21355,#21356,#21357));
#7144=EDGE_LOOP('',(#21358,#21359,#21360,#21361));
#7145=EDGE_LOOP('',(#21362,#21363,#21364,#21365));
#7146=EDGE_LOOP('',(#21366,#21367,#21368,#21369));
#7147=EDGE_LOOP('',(#21370,#21371,#21372,#21373));
#7148=EDGE_LOOP('',(#21374,#21375,#21376,#21377));
#7149=EDGE_LOOP('',(#21378,#21379,#21380,#21381));
#7150=EDGE_LOOP('',(#21382,#21383,#21384,#21385));
#7151=EDGE_LOOP('',(#21386,#21387,#21388,#21389));
#7152=EDGE_LOOP('',(#21390,#21391,#21392,#21393));
#7153=EDGE_LOOP('',(#21394,#21395,#21396,#21397));
#7154=EDGE_LOOP('',(#21398,#21399,#21400,#21401));
#7155=EDGE_LOOP('',(#21402,#21403,#21404,#21405));
#7156=EDGE_LOOP('',(#21406,#21407,#21408,#21409));
#7157=EDGE_LOOP('',(#21410,#21411,#21412,#21413));
#7158=EDGE_LOOP('',(#21414,#21415,#21416,#21417));
#7159=EDGE_LOOP('',(#21418,#21419,#21420,#21421));
#7160=EDGE_LOOP('',(#21422,#21423,#21424,#21425));
#7161=EDGE_LOOP('',(#21426,#21427,#21428,#21429));
#7162=EDGE_LOOP('',(#21430,#21431,#21432,#21433));
#7163=EDGE_LOOP('',(#21434,#21435,#21436,#21437));
#7164=EDGE_LOOP('',(#21438,#21439,#21440,#21441));
#7165=EDGE_LOOP('',(#21442,#21443,#21444,#21445));
#7166=EDGE_LOOP('',(#21446,#21447,#21448,#21449));
#7167=EDGE_LOOP('',(#21450,#21451,#21452,#21453));
#7168=EDGE_LOOP('',(#21454,#21455,#21456,#21457));
#7169=EDGE_LOOP('',(#21458,#21459,#21460,#21461));
#7170=EDGE_LOOP('',(#21462,#21463,#21464,#21465));
#7171=EDGE_LOOP('',(#21466,#21467,#21468,#21469));
#7172=EDGE_LOOP('',(#21470,#21471,#21472,#21473));
#7173=EDGE_LOOP('',(#21474,#21475,#21476,#21477));
#7174=EDGE_LOOP('',(#21478,#21479,#21480,#21481));
#7175=EDGE_LOOP('',(#21482,#21483,#21484,#21485));
#7176=EDGE_LOOP('',(#21486,#21487,#21488,#21489));
#7177=EDGE_LOOP('',(#21490,#21491,#21492,#21493));
#7178=EDGE_LOOP('',(#21494,#21495,#21496,#21497));
#7179=EDGE_LOOP('',(#21498,#21499,#21500,#21501));
#7180=EDGE_LOOP('',(#21502,#21503,#21504,#21505));
#7181=EDGE_LOOP('',(#21506,#21507,#21508,#21509));
#7182=EDGE_LOOP('',(#21510,#21511,#21512,#21513));
#7183=EDGE_LOOP('',(#21514,#21515,#21516,#21517));
#7184=EDGE_LOOP('',(#21518,#21519,#21520,#21521));
#7185=EDGE_LOOP('',(#21522,#21523,#21524,#21525));
#7186=EDGE_LOOP('',(#21526,#21527,#21528,#21529));
#7187=EDGE_LOOP('',(#21530,#21531,#21532,#21533));
#7188=EDGE_LOOP('',(#21534,#21535,#21536,#21537));
#7189=EDGE_LOOP('',(#21538,#21539,#21540,#21541));
#7190=EDGE_LOOP('',(#21542,#21543,#21544,#21545));
#7191=EDGE_LOOP('',(#21546,#21547,#21548,#21549));
#7192=EDGE_LOOP('',(#21550,#21551,#21552,#21553));
#7193=EDGE_LOOP('',(#21554,#21555,#21556,#21557));
#7194=EDGE_LOOP('',(#21558,#21559,#21560,#21561));
#7195=EDGE_LOOP('',(#21562,#21563,#21564,#21565));
#7196=EDGE_LOOP('',(#21566,#21567,#21568,#21569));
#7197=EDGE_LOOP('',(#21570,#21571,#21572,#21573));
#7198=EDGE_LOOP('',(#21574,#21575,#21576,#21577));
#7199=EDGE_LOOP('',(#21578,#21579,#21580,#21581));
#7200=EDGE_LOOP('',(#21582,#21583,#21584,#21585));
#7201=EDGE_LOOP('',(#21586,#21587,#21588,#21589));
#7202=EDGE_LOOP('',(#21590,#21591,#21592,#21593));
#7203=EDGE_LOOP('',(#21594,#21595,#21596,#21597));
#7204=EDGE_LOOP('',(#21598,#21599,#21600,#21601));
#7205=EDGE_LOOP('',(#21602,#21603,#21604,#21605));
#7206=EDGE_LOOP('',(#21606,#21607,#21608,#21609));
#7207=EDGE_LOOP('',(#21610,#21611,#21612,#21613));
#7208=EDGE_LOOP('',(#21614,#21615,#21616,#21617));
#7209=EDGE_LOOP('',(#21618,#21619,#21620,#21621));
#7210=EDGE_LOOP('',(#21622,#21623,#21624,#21625));
#7211=EDGE_LOOP('',(#21626,#21627,#21628,#21629));
#7212=EDGE_LOOP('',(#21630,#21631,#21632,#21633));
#7213=EDGE_LOOP('',(#21634,#21635,#21636,#21637));
#7214=EDGE_LOOP('',(#21638,#21639,#21640,#21641));
#7215=EDGE_LOOP('',(#21642,#21643,#21644,#21645));
#7216=EDGE_LOOP('',(#21646,#21647,#21648,#21649));
#7217=EDGE_LOOP('',(#21650,#21651,#21652,#21653));
#7218=EDGE_LOOP('',(#21654,#21655,#21656,#21657));
#7219=EDGE_LOOP('',(#21658,#21659,#21660,#21661));
#7220=EDGE_LOOP('',(#21662,#21663,#21664,#21665));
#7221=EDGE_LOOP('',(#21666,#21667,#21668,#21669));
#7222=EDGE_LOOP('',(#21670,#21671,#21672,#21673));
#7223=EDGE_LOOP('',(#21674,#21675,#21676,#21677));
#7224=EDGE_LOOP('',(#21678,#21679,#21680,#21681));
#7225=EDGE_LOOP('',(#21682,#21683,#21684,#21685));
#7226=EDGE_LOOP('',(#21686,#21687,#21688,#21689));
#7227=EDGE_LOOP('',(#21690,#21691,#21692,#21693));
#7228=EDGE_LOOP('',(#21694,#21695,#21696));
#7229=EDGE_LOOP('',(#21697));
#7230=EDGE_LOOP('',(#21698));
#7231=EDGE_LOOP('',(#21699,#21700,#21701,#21702));
#7232=EDGE_LOOP('',(#21703,#21704,#21705,#21706));
#7233=EDGE_LOOP('',(#21707,#21708,#21709,#21710));
#7234=EDGE_LOOP('',(#21711));
#7235=EDGE_LOOP('',(#21712));
#7236=EDGE_LOOP('',(#21713,#21714,#21715,#21716,#21717,#21718));
#7237=EDGE_LOOP('',(#21719,#21720,#21721,#21722));
#7238=EDGE_LOOP('',(#21723,#21724,#21725,#21726));
#7239=EDGE_LOOP('',(#21727,#21728,#21729,#21730));
#7240=EDGE_LOOP('',(#21731,#21732,#21733,#21734,#21735));
#7241=EDGE_LOOP('',(#21736,#21737,#21738,#21739));
#7242=EDGE_LOOP('',(#21740,#21741,#21742,#21743));
#7243=EDGE_LOOP('',(#21744,#21745,#21746,#21747,#21748,#21749,#21750,#21751,
#21752,#21753,#21754,#21755,#21756,#21757,#21758,#21759,#21760,#21761,#21762,
#21763,#21764,#21765,#21766,#21767,#21768,#21769,#21770,#21771,#21772,#21773,
#21774,#21775,#21776,#21777,#21778,#21779,#21780,#21781,#21782,#21783,#21784,
#21785,#21786,#21787,#21788,#21789,#21790,#21791,#21792,#21793,#21794,#21795,
#21796,#21797,#21798,#21799,#21800,#21801,#21802,#21803,#21804,#21805));
#7244=EDGE_LOOP('',(#21806,#21807,#21808,#21809,#21810,#21811,#21812,#21813,
#21814,#21815,#21816,#21817,#21818,#21819,#21820,#21821,#21822,#21823,#21824,
#21825,#21826,#21827,#21828,#21829,#21830,#21831,#21832,#21833,#21834,#21835,
#21836,#21837,#21838,#21839,#21840,#21841,#21842,#21843,#21844,#21845,#21846,
#21847,#21848,#21849,#21850,#21851,#21852,#21853,#21854,#21855,#21856,#21857,
#21858,#21859,#21860,#21861,#21862,#21863,#21864,#21865,#21866));
#7245=EDGE_LOOP('',(#21867,#21868,#21869,#21870));
#7246=EDGE_LOOP('',(#21871,#21872,#21873,#21874,#21875,#21876));
#7247=EDGE_LOOP('',(#21877,#21878,#21879,#21880,#21881));
#7248=EDGE_LOOP('',(#21882,#21883,#21884,#21885,#21886,#21887));
#7249=EDGE_LOOP('',(#21888,#21889,#21890,#21891,#21892,#21893));
#7250=EDGE_LOOP('',(#21894,#21895,#21896,#21897));
#7251=EDGE_LOOP('',(#21898,#21899,#21900,#21901,#21902,#21903));
#7252=EDGE_LOOP('',(#21904,#21905,#21906,#21907,#21908,#21909));
#7253=EDGE_LOOP('',(#21910,#21911,#21912,#21913));
#7254=EDGE_LOOP('',(#21914,#21915,#21916,#21917,#21918,#21919));
#7255=EDGE_LOOP('',(#21920,#21921,#21922,#21923,#21924,#21925));
#7256=EDGE_LOOP('',(#21926,#21927,#21928,#21929));
#7257=EDGE_LOOP('',(#21930,#21931,#21932,#21933,#21934,#21935));
#7258=EDGE_LOOP('',(#21936,#21937,#21938,#21939,#21940,#21941));
#7259=EDGE_LOOP('',(#21942,#21943,#21944,#21945));
#7260=EDGE_LOOP('',(#21946,#21947,#21948,#21949,#21950,#21951));
#7261=EDGE_LOOP('',(#21952,#21953,#21954,#21955,#21956,#21957));
#7262=EDGE_LOOP('',(#21958,#21959,#21960,#21961));
#7263=EDGE_LOOP('',(#21962,#21963,#21964,#21965,#21966,#21967));
#7264=EDGE_LOOP('',(#21968,#21969,#21970,#21971,#21972,#21973));
#7265=EDGE_LOOP('',(#21974,#21975,#21976,#21977));
#7266=EDGE_LOOP('',(#21978,#21979,#21980,#21981,#21982,#21983));
#7267=EDGE_LOOP('',(#21984,#21985,#21986,#21987,#21988,#21989));
#7268=EDGE_LOOP('',(#21990,#21991,#21992,#21993,#21994,#21995));
#7269=EDGE_LOOP('',(#21996,#21997,#21998,#21999,#22000,#22001));
#7270=EDGE_LOOP('',(#22002,#22003,#22004,#22005,#22006,#22007));
#7271=EDGE_LOOP('',(#22008,#22009,#22010,#22011,#22012,#22013));
#7272=EDGE_LOOP('',(#22014,#22015,#22016,#22017,#22018,#22019));
#7273=EDGE_LOOP('',(#22020,#22021,#22022,#22023,#22024,#22025));
#7274=EDGE_LOOP('',(#22026,#22027,#22028,#22029,#22030,#22031));
#7275=EDGE_LOOP('',(#22032,#22033,#22034,#22035,#22036,#22037));
#7276=EDGE_LOOP('',(#22038,#22039,#22040,#22041,#22042,#22043));
#7277=EDGE_LOOP('',(#22044,#22045,#22046,#22047,#22048,#22049));
#7278=EDGE_LOOP('',(#22050,#22051,#22052,#22053,#22054,#22055));
#7279=EDGE_LOOP('',(#22056,#22057,#22058,#22059,#22060,#22061));
#7280=EDGE_LOOP('',(#22062,#22063,#22064,#22065,#22066,#22067));
#7281=EDGE_LOOP('',(#22068,#22069,#22070,#22071,#22072,#22073));
#7282=EDGE_LOOP('',(#22074,#22075,#22076,#22077,#22078,#22079));
#7283=EDGE_LOOP('',(#22080,#22081,#22082,#22083,#22084,#22085));
#7284=EDGE_LOOP('',(#22086,#22087,#22088,#22089,#22090,#22091));
#7285=EDGE_LOOP('',(#22092,#22093,#22094,#22095,#22096,#22097));
#7286=EDGE_LOOP('',(#22098,#22099,#22100,#22101));
#7287=EDGE_LOOP('',(#22102,#22103,#22104,#22105,#22106,#22107));
#7288=EDGE_LOOP('',(#22108,#22109,#22110,#22111,#22112,#22113));
#7289=EDGE_LOOP('',(#22114,#22115,#22116,#22117));
#7290=EDGE_LOOP('',(#22118,#22119,#22120,#22121,#22122,#22123));
#7291=EDGE_LOOP('',(#22124,#22125,#22126,#22127,#22128,#22129));
#7292=EDGE_LOOP('',(#22130,#22131,#22132,#22133));
#7293=EDGE_LOOP('',(#22134,#22135,#22136,#22137,#22138,#22139));
#7294=EDGE_LOOP('',(#22140,#22141,#22142,#22143,#22144,#22145));
#7295=EDGE_LOOP('',(#22146,#22147,#22148,#22149));
#7296=EDGE_LOOP('',(#22150,#22151,#22152,#22153,#22154,#22155));
#7297=EDGE_LOOP('',(#22156,#22157,#22158,#22159,#22160,#22161));
#7298=EDGE_LOOP('',(#22162,#22163,#22164,#22165));
#7299=EDGE_LOOP('',(#22166,#22167,#22168,#22169,#22170,#22171));
#7300=EDGE_LOOP('',(#22172,#22173,#22174,#22175,#22176,#22177));
#7301=EDGE_LOOP('',(#22178,#22179,#22180,#22181));
#7302=EDGE_LOOP('',(#22182,#22183,#22184,#22185,#22186,#22187));
#7303=EDGE_LOOP('',(#22188,#22189,#22190,#22191,#22192,#22193));
#7304=EDGE_LOOP('',(#22194,#22195,#22196,#22197));
#7305=EDGE_LOOP('',(#22198,#22199,#22200,#22201,#22202,#22203));
#7306=EDGE_LOOP('',(#22204,#22205,#22206,#22207,#22208,#22209));
#7307=EDGE_LOOP('',(#22210,#22211,#22212,#22213));
#7308=EDGE_LOOP('',(#22214,#22215,#22216,#22217,#22218,#22219));
#7309=EDGE_LOOP('',(#22220,#22221,#22222,#22223,#22224,#22225));
#7310=EDGE_LOOP('',(#22226,#22227,#22228,#22229));
#7311=EDGE_LOOP('',(#22230,#22231,#22232,#22233,#22234,#22235));
#7312=EDGE_LOOP('',(#22236,#22237,#22238,#22239,#22240,#22241));
#7313=EDGE_LOOP('',(#22242,#22243,#22244,#22245));
#7314=EDGE_LOOP('',(#22246,#22247,#22248,#22249,#22250,#22251));
#7315=EDGE_LOOP('',(#22252,#22253,#22254,#22255,#22256,#22257));
#7316=EDGE_LOOP('',(#22258,#22259,#22260,#22261));
#7317=EDGE_LOOP('',(#22262,#22263,#22264,#22265,#22266,#22267));
#7318=EDGE_LOOP('',(#22268,#22269,#22270,#22271,#22272,#22273));
#7319=EDGE_LOOP('',(#22274,#22275,#22276,#22277));
#7320=EDGE_LOOP('',(#22278,#22279,#22280,#22281,#22282,#22283));
#7321=EDGE_LOOP('',(#22284,#22285,#22286,#22287,#22288,#22289));
#7322=EDGE_LOOP('',(#22290,#22291,#22292,#22293));
#7323=EDGE_LOOP('',(#22294,#22295,#22296,#22297,#22298,#22299));
#7324=EDGE_LOOP('',(#22300,#22301,#22302,#22303,#22304,#22305));
#7325=EDGE_LOOP('',(#22306,#22307,#22308,#22309));
#7326=EDGE_LOOP('',(#22310,#22311,#22312,#22313,#22314,#22315));
#7327=EDGE_LOOP('',(#22316,#22317,#22318,#22319,#22320,#22321));
#7328=EDGE_LOOP('',(#22322,#22323,#22324,#22325));
#7329=EDGE_LOOP('',(#22326,#22327,#22328,#22329,#22330,#22331));
#7330=EDGE_LOOP('',(#22332,#22333,#22334,#22335,#22336,#22337));
#7331=EDGE_LOOP('',(#22338,#22339,#22340,#22341));
#7332=EDGE_LOOP('',(#22342,#22343,#22344,#22345,#22346,#22347));
#7333=EDGE_LOOP('',(#22348,#22349,#22350,#22351,#22352,#22353));
#7334=EDGE_LOOP('',(#22354,#22355,#22356,#22357));
#7335=EDGE_LOOP('',(#22358,#22359,#22360,#22361,#22362,#22363));
#7336=EDGE_LOOP('',(#22364,#22365,#22366,#22367,#22368,#22369));
#7337=EDGE_LOOP('',(#22370,#22371,#22372,#22373));
#7338=EDGE_LOOP('',(#22374,#22375,#22376,#22377,#22378,#22379));
#7339=EDGE_LOOP('',(#22380,#22381,#22382,#22383,#22384,#22385));
#7340=EDGE_LOOP('',(#22386,#22387,#22388,#22389));
#7341=EDGE_LOOP('',(#22390,#22391,#22392,#22393,#22394,#22395));
#7342=EDGE_LOOP('',(#22396,#22397,#22398,#22399,#22400,#22401));
#7343=EDGE_LOOP('',(#22402,#22403,#22404,#22405));
#7344=EDGE_LOOP('',(#22406,#22407,#22408,#22409,#22410,#22411));
#7345=EDGE_LOOP('',(#22412,#22413,#22414,#22415,#22416,#22417));
#7346=EDGE_LOOP('',(#22418,#22419,#22420,#22421));
#7347=EDGE_LOOP('',(#22422,#22423,#22424,#22425,#22426,#22427));
#7348=EDGE_LOOP('',(#22428,#22429,#22430,#22431,#22432,#22433));
#7349=EDGE_LOOP('',(#22434,#22435,#22436,#22437));
#7350=EDGE_LOOP('',(#22438,#22439,#22440,#22441,#22442,#22443));
#7351=EDGE_LOOP('',(#22444,#22445,#22446,#22447,#22448,#22449));
#7352=EDGE_LOOP('',(#22450,#22451,#22452,#22453));
#7353=EDGE_LOOP('',(#22454,#22455,#22456,#22457,#22458,#22459));
#7354=EDGE_LOOP('',(#22460,#22461,#22462,#22463,#22464,#22465));
#7355=EDGE_LOOP('',(#22466,#22467,#22468,#22469));
#7356=EDGE_LOOP('',(#22470,#22471,#22472,#22473,#22474,#22475));
#7357=EDGE_LOOP('',(#22476,#22477,#22478,#22479,#22480,#22481));
#7358=EDGE_LOOP('',(#22482,#22483,#22484,#22485));
#7359=EDGE_LOOP('',(#22486,#22487,#22488,#22489,#22490,#22491));
#7360=EDGE_LOOP('',(#22492,#22493,#22494,#22495,#22496,#22497));
#7361=EDGE_LOOP('',(#22498,#22499,#22500,#22501));
#7362=EDGE_LOOP('',(#22502,#22503,#22504,#22505,#22506,#22507));
#7363=EDGE_LOOP('',(#22508,#22509,#22510,#22511,#22512,#22513));
#7364=EDGE_LOOP('',(#22514,#22515,#22516,#22517));
#7365=EDGE_LOOP('',(#22518,#22519,#22520,#22521,#22522,#22523));
#7366=EDGE_LOOP('',(#22524,#22525,#22526,#22527,#22528,#22529));
#7367=EDGE_LOOP('',(#22530,#22531,#22532,#22533));
#7368=EDGE_LOOP('',(#22534,#22535,#22536,#22537,#22538,#22539));
#7369=EDGE_LOOP('',(#22540,#22541,#22542,#22543,#22544,#22545));
#7370=EDGE_LOOP('',(#22546,#22547,#22548,#22549));
#7371=EDGE_LOOP('',(#22550,#22551,#22552,#22553,#22554,#22555));
#7372=EDGE_LOOP('',(#22556,#22557,#22558,#22559,#22560,#22561));
#7373=EDGE_LOOP('',(#22562,#22563,#22564,#22565));
#7374=EDGE_LOOP('',(#22566,#22567,#22568,#22569,#22570,#22571));
#7375=EDGE_LOOP('',(#22572,#22573,#22574,#22575,#22576,#22577));
#7376=EDGE_LOOP('',(#22578,#22579,#22580,#22581));
#7377=EDGE_LOOP('',(#22582,#22583,#22584,#22585,#22586,#22587));
#7378=EDGE_LOOP('',(#22588,#22589,#22590,#22591,#22592,#22593));
#7379=EDGE_LOOP('',(#22594,#22595,#22596,#22597));
#7380=EDGE_LOOP('',(#22598,#22599,#22600,#22601,#22602,#22603));
#7381=EDGE_LOOP('',(#22604,#22605,#22606,#22607,#22608,#22609));
#7382=EDGE_LOOP('',(#22610,#22611,#22612,#22613));
#7383=EDGE_LOOP('',(#22614,#22615,#22616,#22617,#22618,#22619));
#7384=EDGE_LOOP('',(#22620,#22621,#22622,#22623,#22624,#22625));
#7385=EDGE_LOOP('',(#22626,#22627,#22628,#22629));
#7386=EDGE_LOOP('',(#22630,#22631,#22632,#22633,#22634,#22635));
#7387=EDGE_LOOP('',(#22636,#22637,#22638,#22639,#22640,#22641));
#7388=EDGE_LOOP('',(#22642,#22643,#22644,#22645));
#7389=EDGE_LOOP('',(#22646,#22647,#22648,#22649,#22650,#22651));
#7390=EDGE_LOOP('',(#22652,#22653,#22654,#22655,#22656,#22657));
#7391=EDGE_LOOP('',(#22658,#22659,#22660,#22661));
#7392=EDGE_LOOP('',(#22662,#22663,#22664,#22665,#22666,#22667));
#7393=EDGE_LOOP('',(#22668,#22669,#22670,#22671,#22672,#22673));
#7394=EDGE_LOOP('',(#22674,#22675,#22676,#22677));
#7395=EDGE_LOOP('',(#22678,#22679,#22680,#22681,#22682,#22683));
#7396=EDGE_LOOP('',(#22684,#22685,#22686,#22687,#22688,#22689));
#7397=EDGE_LOOP('',(#22690,#22691,#22692,#22693));
#7398=EDGE_LOOP('',(#22694,#22695,#22696,#22697,#22698,#22699));
#7399=EDGE_LOOP('',(#22700,#22701,#22702,#22703,#22704,#22705));
#7400=EDGE_LOOP('',(#22706,#22707,#22708,#22709,#22710));
#7401=EDGE_LOOP('',(#22711,#22712,#22713,#22714,#22715,#22716));
#7402=EDGE_LOOP('',(#22717,#22718,#22719,#22720,#22721,#22722));
#7403=EDGE_LOOP('',(#22723,#22724,#22725,#22726));
#7404=EDGE_LOOP('',(#22727,#22728,#22729,#22730,#22731,#22732));
#7405=EDGE_LOOP('',(#22733,#22734,#22735,#22736,#22737,#22738));
#7406=EDGE_LOOP('',(#22739,#22740,#22741,#22742));
#7407=EDGE_LOOP('',(#22743,#22744,#22745,#22746,#22747,#22748));
#7408=EDGE_LOOP('',(#22749,#22750,#22751,#22752,#22753,#22754));
#7409=EDGE_LOOP('',(#22755,#22756,#22757,#22758));
#7410=EDGE_LOOP('',(#22759,#22760,#22761,#22762,#22763,#22764));
#7411=EDGE_LOOP('',(#22765,#22766,#22767,#22768,#22769,#22770));
#7412=EDGE_LOOP('',(#22771,#22772,#22773,#22774));
#7413=EDGE_LOOP('',(#22775,#22776,#22777,#22778,#22779,#22780));
#7414=EDGE_LOOP('',(#22781,#22782,#22783,#22784,#22785,#22786));
#7415=EDGE_LOOP('',(#22787,#22788,#22789,#22790));
#7416=EDGE_LOOP('',(#22791,#22792,#22793,#22794,#22795,#22796));
#7417=EDGE_LOOP('',(#22797,#22798,#22799,#22800,#22801,#22802));
#7418=EDGE_LOOP('',(#22803,#22804,#22805,#22806));
#7419=EDGE_LOOP('',(#22807,#22808,#22809,#22810,#22811,#22812));
#7420=EDGE_LOOP('',(#22813,#22814,#22815,#22816,#22817,#22818));
#7421=EDGE_LOOP('',(#22819,#22820,#22821,#22822));
#7422=EDGE_LOOP('',(#22823,#22824,#22825,#22826,#22827,#22828));
#7423=EDGE_LOOP('',(#22829,#22830,#22831,#22832,#22833,#22834));
#7424=EDGE_LOOP('',(#22835,#22836,#22837,#22838));
#7425=EDGE_LOOP('',(#22839,#22840,#22841,#22842,#22843,#22844));
#7426=EDGE_LOOP('',(#22845,#22846,#22847,#22848,#22849,#22850));
#7427=EDGE_LOOP('',(#22851,#22852,#22853,#22854));
#7428=EDGE_LOOP('',(#22855,#22856,#22857,#22858,#22859,#22860));
#7429=EDGE_LOOP('',(#22861,#22862,#22863,#22864,#22865,#22866));
#7430=EDGE_LOOP('',(#22867,#22868,#22869,#22870));
#7431=EDGE_LOOP('',(#22871,#22872,#22873,#22874,#22875,#22876));
#7432=EDGE_LOOP('',(#22877,#22878,#22879,#22880,#22881,#22882));
#7433=EDGE_LOOP('',(#22883,#22884,#22885,#22886));
#7434=EDGE_LOOP('',(#22887,#22888,#22889,#22890,#22891,#22892));
#7435=EDGE_LOOP('',(#22893,#22894,#22895,#22896,#22897,#22898));
#7436=EDGE_LOOP('',(#22899,#22900,#22901,#22902));
#7437=EDGE_LOOP('',(#22903,#22904,#22905,#22906,#22907,#22908));
#7438=EDGE_LOOP('',(#22909,#22910,#22911,#22912,#22913,#22914));
#7439=EDGE_LOOP('',(#22915,#22916,#22917,#22918));
#7440=EDGE_LOOP('',(#22919,#22920,#22921,#22922,#22923,#22924));
#7441=EDGE_LOOP('',(#22925,#22926,#22927,#22928,#22929,#22930));
#7442=EDGE_LOOP('',(#22931,#22932,#22933,#22934));
#7443=EDGE_LOOP('',(#22935,#22936,#22937,#22938,#22939,#22940));
#7444=EDGE_LOOP('',(#22941,#22942,#22943,#22944,#22945,#22946));
#7445=EDGE_LOOP('',(#22947,#22948,#22949,#22950));
#7446=EDGE_LOOP('',(#22951,#22952,#22953,#22954,#22955,#22956));
#7447=EDGE_LOOP('',(#22957,#22958,#22959,#22960,#22961,#22962));
#7448=EDGE_LOOP('',(#22963,#22964,#22965,#22966));
#7449=EDGE_LOOP('',(#22967,#22968,#22969,#22970,#22971,#22972));
#7450=EDGE_LOOP('',(#22973,#22974,#22975,#22976,#22977,#22978));
#7451=EDGE_LOOP('',(#22979,#22980,#22981,#22982));
#7452=EDGE_LOOP('',(#22983,#22984,#22985,#22986,#22987,#22988));
#7453=EDGE_LOOP('',(#22989,#22990,#22991,#22992,#22993,#22994));
#7454=EDGE_LOOP('',(#22995,#22996,#22997,#22998));
#7455=EDGE_LOOP('',(#22999,#23000,#23001,#23002,#23003,#23004));
#7456=EDGE_LOOP('',(#23005,#23006,#23007,#23008,#23009,#23010));
#7457=EDGE_LOOP('',(#23011,#23012,#23013,#23014));
#7458=EDGE_LOOP('',(#23015,#23016,#23017,#23018,#23019,#23020));
#7459=EDGE_LOOP('',(#23021,#23022,#23023,#23024,#23025,#23026));
#7460=EDGE_LOOP('',(#23027,#23028,#23029,#23030,#23031,#23032));
#7461=EDGE_LOOP('',(#23033,#23034,#23035,#23036,#23037,#23038));
#7462=EDGE_LOOP('',(#23039,#23040,#23041,#23042,#23043,#23044));
#7463=EDGE_LOOP('',(#23045,#23046,#23047,#23048,#23049,#23050));
#7464=EDGE_LOOP('',(#23051,#23052,#23053,#23054,#23055,#23056));
#7465=EDGE_LOOP('',(#23057,#23058,#23059,#23060,#23061,#23062));
#7466=EDGE_LOOP('',(#23063,#23064,#23065,#23066,#23067,#23068));
#7467=EDGE_LOOP('',(#23069,#23070,#23071,#23072,#23073,#23074));
#7468=EDGE_LOOP('',(#23075,#23076,#23077,#23078,#23079,#23080));
#7469=EDGE_LOOP('',(#23081,#23082,#23083,#23084,#23085,#23086));
#7470=EDGE_LOOP('',(#23087,#23088,#23089,#23090,#23091,#23092));
#8656=LINE('',#46246,#9902);
#8657=LINE('',#46285,#9903);
#8658=LINE('',#46326,#9904);
#8659=LINE('',#46402,#9905);
#8660=LINE('',#46480,#9906);
#8661=LINE('',#46556,#9907);
#8662=LINE('',#46632,#9908);
#8663=LINE('',#46708,#9909);
#8664=LINE('',#46784,#9910);
#8665=LINE('',#46862,#9911);
#8666=LINE('',#46940,#9912);
#8667=LINE('',#47016,#9913);
#8668=LINE('',#47092,#9914);
#8669=LINE('',#47168,#9915);
#8670=LINE('',#47244,#9916);
#8671=LINE('',#47322,#9917);
#8672=LINE('',#47398,#9918);
#8673=LINE('',#47476,#9919);
#8674=LINE('',#47552,#9920);
#8675=LINE('',#47628,#9921);
#8676=LINE('',#47704,#9922);
#8677=LINE('',#47780,#9923);
#8678=LINE('',#47858,#9924);
#8679=LINE('',#47936,#9925);
#8680=LINE('',#48012,#9926);
#8681=LINE('',#48088,#9927);
#8682=LINE('',#48164,#9928);
#8683=LINE('',#48240,#9929);
#8684=LINE('',#48318,#9930);
#8685=LINE('',#48394,#9931);
#8686=LINE('',#48419,#9932);
#8687=LINE('',#48433,#9933);
#8688=LINE('',#48509,#9934);
#8689=LINE('',#48585,#9935);
#8690=LINE('',#48663,#9936);
#8691=LINE('',#48739,#9937);
#8692=LINE('',#48817,#9938);
#8693=LINE('',#48893,#9939);
#8694=LINE('',#48969,#9940);
#8695=LINE('',#49045,#9941);
#8696=LINE('',#49121,#9942);
#8697=LINE('',#49199,#9943);
#8698=LINE('',#49275,#9944);
#8699=LINE('',#49353,#9945);
#8700=LINE('',#49429,#9946);
#8701=LINE('',#49505,#9947);
#8702=LINE('',#49581,#9948);
#8703=LINE('',#49657,#9949);
#8704=LINE('',#49733,#9950);
#8705=LINE('',#49811,#9951);
#8706=LINE('',#49887,#9952);
#8707=LINE('',#49965,#9953);
#8708=LINE('',#50041,#9954);
#8709=LINE('',#50117,#9955);
#8710=LINE('',#50193,#9956);
#8711=LINE('',#50269,#9957);
#8712=LINE('',#50347,#9958);
#8713=LINE('',#50423,#9959);
#8714=LINE('',#50501,#9960);
#8715=LINE('',#50577,#9961);
#8716=LINE('',#50772,#9962);
#8717=LINE('',#50775,#9963);
#8718=LINE('',#50781,#9964);
#8719=LINE('',#50784,#9965);
#8720=LINE('',#50790,#9966);
#8721=LINE('',#50793,#9967);
#8722=LINE('',#50799,#9968);
#8723=LINE('',#50802,#9969);
#8724=LINE('',#50808,#9970);
#8725=LINE('',#50811,#9971);
#8726=LINE('',#50817,#9972);
#8727=LINE('',#50820,#9973);
#8728=LINE('',#50826,#9974);
#8729=LINE('',#50829,#9975);
#8730=LINE('',#50835,#9976);
#8731=LINE('',#50838,#9977);
#8732=LINE('',#50844,#9978);
#8733=LINE('',#50847,#9979);
#8734=LINE('',#50853,#9980);
#8735=LINE('',#50856,#9981);
#8736=LINE('',#50862,#9982);
#8737=LINE('',#50865,#9983);
#8738=LINE('',#50871,#9984);
#8739=LINE('',#50874,#9985);
#8740=LINE('',#50880,#9986);
#8741=LINE('',#50883,#9987);
#8742=LINE('',#50889,#9988);
#8743=LINE('',#50892,#9989);
#8744=LINE('',#50898,#9990);
#8745=LINE('',#50901,#9991);
#8746=LINE('',#50932,#9992);
#8747=LINE('',#51872,#9993);
#8748=LINE('',#52806,#9994);
#8749=LINE('',#52817,#9995);
#8750=LINE('',#53302,#9996);
#8751=LINE('',#53305,#9997);
#8752=LINE('',#53308,#9998);
#8753=LINE('',#53310,#9999);
#8754=LINE('',#53314,#10000);
#8755=LINE('',#53316,#10001);
#8756=LINE('',#53320,#10002);
#8757=LINE('',#53322,#10003);
#8758=LINE('',#53326,#10004);
#8759=LINE('',#53328,#10005);
#8760=LINE('',#53332,#10006);
#8761=LINE('',#53334,#10007);
#8762=LINE('',#53338,#10008);
#8763=LINE('',#53340,#10009);
#8764=LINE('',#53344,#10010);
#8765=LINE('',#53346,#10011);
#8766=LINE('',#53350,#10012);
#8767=LINE('',#53352,#10013);
#8768=LINE('',#53356,#10014);
#8769=LINE('',#53358,#10015);
#8770=LINE('',#53362,#10016);
#8771=LINE('',#53364,#10017);
#8772=LINE('',#53368,#10018);
#8773=LINE('',#53370,#10019);
#8774=LINE('',#53374,#10020);
#8775=LINE('',#53376,#10021);
#8776=LINE('',#53380,#10022);
#8777=LINE('',#53382,#10023);
#8778=LINE('',#53386,#10024);
#8779=LINE('',#53388,#10025);
#8780=LINE('',#53392,#10026);
#8781=LINE('',#53394,#10027);
#8782=LINE('',#53398,#10028);
#8783=LINE('',#53400,#10029);
#8784=LINE('',#53404,#10030);
#8785=LINE('',#53406,#10031);
#8786=LINE('',#53410,#10032);
#8787=LINE('',#53412,#10033);
#8788=LINE('',#53416,#10034);
#8789=LINE('',#53418,#10035);
#8790=LINE('',#53422,#10036);
#8791=LINE('',#53424,#10037);
#8792=LINE('',#53428,#10038);
#8793=LINE('',#53430,#10039);
#8794=LINE('',#53434,#10040);
#8795=LINE('',#53436,#10041);
#8796=LINE('',#53440,#10042);
#8797=LINE('',#53442,#10043);
#8798=LINE('',#53446,#10044);
#8799=LINE('',#53448,#10045);
#8800=LINE('',#53452,#10046);
#8801=LINE('',#53454,#10047);
#8802=LINE('',#53458,#10048);
#8803=LINE('',#53460,#10049);
#8804=LINE('',#53464,#10050);
#8805=LINE('',#53466,#10051);
#8806=LINE('',#53470,#10052);
#8807=LINE('',#53472,#10053);
#8808=LINE('',#53476,#10054);
#8809=LINE('',#53478,#10055);
#8810=LINE('',#53482,#10056);
#8811=LINE('',#53484,#10057);
#8812=LINE('',#53488,#10058);
#8813=LINE('',#53490,#10059);
#8814=LINE('',#53494,#10060);
#8815=LINE('',#53496,#10061);
#8816=LINE('',#53500,#10062);
#8817=LINE('',#53502,#10063);
#8818=LINE('',#53506,#10064);
#8819=LINE('',#53508,#10065);
#8820=LINE('',#53512,#10066);
#8821=LINE('',#53514,#10067);
#8822=LINE('',#53518,#10068);
#8823=LINE('',#53520,#10069);
#8824=LINE('',#53524,#10070);
#8825=LINE('',#53526,#10071);
#8826=LINE('',#53530,#10072);
#8827=LINE('',#53532,#10073);
#8828=LINE('',#53536,#10074);
#8829=LINE('',#53538,#10075);
#8830=LINE('',#53542,#10076);
#8831=LINE('',#53544,#10077);
#8832=LINE('',#53548,#10078);
#8833=LINE('',#53550,#10079);
#8834=LINE('',#53554,#10080);
#8835=LINE('',#53556,#10081);
#8836=LINE('',#53560,#10082);
#8837=LINE('',#53562,#10083);
#8838=LINE('',#53566,#10084);
#8839=LINE('',#53568,#10085);
#8840=LINE('',#53572,#10086);
#8841=LINE('',#53574,#10087);
#8842=LINE('',#53578,#10088);
#8843=LINE('',#53580,#10089);
#8844=LINE('',#53584,#10090);
#8845=LINE('',#53586,#10091);
#8846=LINE('',#53590,#10092);
#8847=LINE('',#53592,#10093);
#8848=LINE('',#53596,#10094);
#8849=LINE('',#53598,#10095);
#8850=LINE('',#53602,#10096);
#8851=LINE('',#53604,#10097);
#8852=LINE('',#53608,#10098);
#8853=LINE('',#53610,#10099);
#8854=LINE('',#53614,#10100);
#8855=LINE('',#53616,#10101);
#8856=LINE('',#53620,#10102);
#8857=LINE('',#53622,#10103);
#8858=LINE('',#53626,#10104);
#8859=LINE('',#53628,#10105);
#8860=LINE('',#53632,#10106);
#8861=LINE('',#53634,#10107);
#8862=LINE('',#53638,#10108);
#8863=LINE('',#53640,#10109);
#8864=LINE('',#53644,#10110);
#8865=LINE('',#53646,#10111);
#8866=LINE('',#53650,#10112);
#8867=LINE('',#53652,#10113);
#8868=LINE('',#53656,#10114);
#8869=LINE('',#53658,#10115);
#8870=LINE('',#53662,#10116);
#8871=LINE('',#53664,#10117);
#8872=LINE('',#53668,#10118);
#8873=LINE('',#53670,#10119);
#8874=LINE('',#53674,#10120);
#8875=LINE('',#53676,#10121);
#8876=LINE('',#53680,#10122);
#8877=LINE('',#53682,#10123);
#8878=LINE('',#53686,#10124);
#8879=LINE('',#53689,#10125);
#8880=LINE('',#53692,#10126);
#8881=LINE('',#53695,#10127);
#8882=LINE('',#53698,#10128);
#8883=LINE('',#53701,#10129);
#8884=LINE('',#53704,#10130);
#8885=LINE('',#53707,#10131);
#8886=LINE('',#53710,#10132);
#8887=LINE('',#53713,#10133);
#8888=LINE('',#53716,#10134);
#8889=LINE('',#53719,#10135);
#8890=LINE('',#53722,#10136);
#8891=LINE('',#53725,#10137);
#8892=LINE('',#53728,#10138);
#8893=LINE('',#53731,#10139);
#8894=LINE('',#53734,#10140);
#8895=LINE('',#53737,#10141);
#8896=LINE('',#53740,#10142);
#8897=LINE('',#53743,#10143);
#8898=LINE('',#53746,#10144);
#8899=LINE('',#53749,#10145);
#8900=LINE('',#53752,#10146);
#8901=LINE('',#53755,#10147);
#8902=LINE('',#53758,#10148);
#8903=LINE('',#53761,#10149);
#8904=LINE('',#53764,#10150);
#8905=LINE('',#53767,#10151);
#8906=LINE('',#53770,#10152);
#8907=LINE('',#53772,#10153);
#8908=LINE('',#54021,#10154);
#8909=LINE('',#54023,#10155);
#8910=LINE('',#54032,#10156);
#8911=LINE('',#54034,#10157);
#8912=LINE('',#54036,#10158);
#8913=LINE('',#54038,#10159);
#8914=LINE('',#54040,#10160);
#8915=LINE('',#54041,#10161);
#8916=LINE('',#54043,#10162);
#8917=LINE('',#54044,#10163);
#8918=LINE('',#54046,#10164);
#8919=LINE('',#54048,#10165);
#8920=LINE('',#54050,#10166);
#8921=LINE('',#54052,#10167);
#8922=LINE('',#55574,#10168);
#8923=LINE('',#55577,#10169);
#8924=LINE('',#55579,#10170);
#8925=LINE('',#55582,#10171);
#8926=LINE('',#55584,#10172);
#8927=LINE('',#55587,#10173);
#8928=LINE('',#55589,#10174);
#8929=LINE('',#55592,#10175);
#8930=LINE('',#55594,#10176);
#8931=LINE('',#55597,#10177);
#8932=LINE('',#55599,#10178);
#8933=LINE('',#55602,#10179);
#8934=LINE('',#55604,#10180);
#8935=LINE('',#55607,#10181);
#8936=LINE('',#55609,#10182);
#8937=LINE('',#55630,#10183);
#8938=LINE('',#55632,#10184);
#8939=LINE('',#55635,#10185);
#8940=LINE('',#55637,#10186);
#8941=LINE('',#55640,#10187);
#8942=LINE('',#55642,#10188);
#8943=LINE('',#55645,#10189);
#8944=LINE('',#55647,#10190);
#8945=LINE('',#55650,#10191);
#8946=LINE('',#55652,#10192);
#8947=LINE('',#55655,#10193);
#8948=LINE('',#55657,#10194);
#8949=LINE('',#55660,#10195);
#8950=LINE('',#55662,#10196);
#8951=LINE('',#55665,#10197);
#8952=LINE('',#55667,#10198);
#8953=LINE('',#55670,#10199);
#8954=LINE('',#55672,#10200);
#8955=LINE('',#55675,#10201);
#8956=LINE('',#55677,#10202);
#8957=LINE('',#55680,#10203);
#8958=LINE('',#55682,#10204);
#8959=LINE('',#55685,#10205);
#8960=LINE('',#55687,#10206);
#8961=LINE('',#55690,#10207);
#8962=LINE('',#55692,#10208);
#8963=LINE('',#55695,#10209);
#8964=LINE('',#55697,#10210);
#8965=LINE('',#55700,#10211);
#8966=LINE('',#55702,#10212);
#8967=LINE('',#55705,#10213);
#8968=LINE('',#55707,#10214);
#8969=LINE('',#55710,#10215);
#8970=LINE('',#55712,#10216);
#8971=LINE('',#55715,#10217);
#8972=LINE('',#55717,#10218);
#8973=LINE('',#55720,#10219);
#8974=LINE('',#55722,#10220);
#8975=LINE('',#55725,#10221);
#8976=LINE('',#55727,#10222);
#8977=LINE('',#55730,#10223);
#8978=LINE('',#55732,#10224);
#8979=LINE('',#55735,#10225);
#8980=LINE('',#55737,#10226);
#8981=LINE('',#55740,#10227);
#8982=LINE('',#55742,#10228);
#8983=LINE('',#55745,#10229);
#8984=LINE('',#55747,#10230);
#8985=LINE('',#55750,#10231);
#8986=LINE('',#55752,#10232);
#8987=LINE('',#55755,#10233);
#8988=LINE('',#55757,#10234);
#8989=LINE('',#55760,#10235);
#8990=LINE('',#55762,#10236);
#8991=LINE('',#55765,#10237);
#8992=LINE('',#55767,#10238);
#8993=LINE('',#55770,#10239);
#8994=LINE('',#55772,#10240);
#8995=LINE('',#55775,#10241);
#8996=LINE('',#55777,#10242);
#8997=LINE('',#55780,#10243);
#8998=LINE('',#55782,#10244);
#8999=LINE('',#55785,#10245);
#9000=LINE('',#55787,#10246);
#9001=LINE('',#55790,#10247);
#9002=LINE('',#55792,#10248);
#9003=LINE('',#55795,#10249);
#9004=LINE('',#55797,#10250);
#9005=LINE('',#55800,#10251);
#9006=LINE('',#55802,#10252);
#9007=LINE('',#55805,#10253);
#9008=LINE('',#55807,#10254);
#9009=LINE('',#55810,#10255);
#9010=LINE('',#55812,#10256);
#9011=LINE('',#55815,#10257);
#9012=LINE('',#55817,#10258);
#9013=LINE('',#55820,#10259);
#9014=LINE('',#55822,#10260);
#9015=LINE('',#55825,#10261);
#9016=LINE('',#55827,#10262);
#9017=LINE('',#55830,#10263);
#9018=LINE('',#55832,#10264);
#9019=LINE('',#55835,#10265);
#9020=LINE('',#55837,#10266);
#9021=LINE('',#55840,#10267);
#9022=LINE('',#55842,#10268);
#9023=LINE('',#55845,#10269);
#9024=LINE('',#55847,#10270);
#9025=LINE('',#55850,#10271);
#9026=LINE('',#55852,#10272);
#9027=LINE('',#55855,#10273);
#9028=LINE('',#55857,#10274);
#9029=LINE('',#55860,#10275);
#9030=LINE('',#55862,#10276);
#9031=LINE('',#55865,#10277);
#9032=LINE('',#55867,#10278);
#9033=LINE('',#55870,#10279);
#9034=LINE('',#55872,#10280);
#9035=LINE('',#55875,#10281);
#9036=LINE('',#55877,#10282);
#9037=LINE('',#55880,#10283);
#9038=LINE('',#55882,#10284);
#9039=LINE('',#55885,#10285);
#9040=LINE('',#55887,#10286);
#9041=LINE('',#55890,#10287);
#9042=LINE('',#55892,#10288);
#9043=LINE('',#55895,#10289);
#9044=LINE('',#55897,#10290);
#9045=LINE('',#55900,#10291);
#9046=LINE('',#55902,#10292);
#9047=LINE('',#55905,#10293);
#9048=LINE('',#55907,#10294);
#9049=LINE('',#55910,#10295);
#9050=LINE('',#55912,#10296);
#9051=LINE('',#55915,#10297);
#9052=LINE('',#55917,#10298);
#9902=VECTOR('',#36562,1.5);
#9903=VECTOR('',#36563,1.5);
#9904=VECTOR('',#36570,1.5);
#9905=VECTOR('',#36573,1.5);
#9906=VECTOR('',#36576,1.5);
#9907=VECTOR('',#36579,1.5);
#9908=VECTOR('',#36582,1.5);
#9909=VECTOR('',#36585,1.5);
#9910=VECTOR('',#36588,1.5);
#9911=VECTOR('',#36591,1.5);
#9912=VECTOR('',#36594,1.5);
#9913=VECTOR('',#36597,1.5);
#9914=VECTOR('',#36600,1.5);
#9915=VECTOR('',#36603,1.5);
#9916=VECTOR('',#36606,1.5);
#9917=VECTOR('',#36609,1.5);
#9918=VECTOR('',#36612,1.5);
#9919=VECTOR('',#36615,1.5);
#9920=VECTOR('',#36618,1.5);
#9921=VECTOR('',#36621,1.5);
#9922=VECTOR('',#36624,1.5);
#9923=VECTOR('',#36627,1.5);
#9924=VECTOR('',#36630,1.5);
#9925=VECTOR('',#36633,1.5);
#9926=VECTOR('',#36636,1.5);
#9927=VECTOR('',#36639,1.5);
#9928=VECTOR('',#36642,1.5);
#9929=VECTOR('',#36645,1.5);
#9930=VECTOR('',#36648,1.5);
#9931=VECTOR('',#36651,1.17524047358084);
#9932=VECTOR('',#36656,1.17524047358084);
#9933=VECTOR('',#36661,1.17524047358084);
#9934=VECTOR('',#36664,1.17524047358084);
#9935=VECTOR('',#36667,1.17524047358084);
#9936=VECTOR('',#36670,1.17524047358084);
#9937=VECTOR('',#36673,1.17524047358084);
#9938=VECTOR('',#36676,1.17524047358084);
#9939=VECTOR('',#36679,1.17524047358084);
#9940=VECTOR('',#36682,1.17524047358084);
#9941=VECTOR('',#36685,1.17524047358084);
#9942=VECTOR('',#36688,1.17524047358084);
#9943=VECTOR('',#36691,1.17524047358084);
#9944=VECTOR('',#36694,1.17524047358084);
#9945=VECTOR('',#36697,1.17524047358084);
#9946=VECTOR('',#36700,1.17524047358084);
#9947=VECTOR('',#36703,1.17524047358084);
#9948=VECTOR('',#36706,1.17524047358084);
#9949=VECTOR('',#36709,1.17524047358084);
#9950=VECTOR('',#36712,1.17524047358084);
#9951=VECTOR('',#36715,1.17524047358084);
#9952=VECTOR('',#36718,1.17524047358084);
#9953=VECTOR('',#36721,1.17524047358084);
#9954=VECTOR('',#36724,1.17524047358084);
#9955=VECTOR('',#36727,1.17524047358084);
#9956=VECTOR('',#36730,1.17524047358084);
#9957=VECTOR('',#36733,1.17524047358084);
#9958=VECTOR('',#36736,1.17524047358084);
#9959=VECTOR('',#36739,1.17524047358084);
#9960=VECTOR('',#36742,1.17524047358084);
#9961=VECTOR('',#36745,1.17524047358084);
#9962=VECTOR('',#36762,1000.);
#9963=VECTOR('',#36765,1000.);
#9964=VECTOR('',#36770,1000.);
#9965=VECTOR('',#36773,1000.);
#9966=VECTOR('',#36778,1000.);
#9967=VECTOR('',#36781,1000.);
#9968=VECTOR('',#36786,1000.);
#9969=VECTOR('',#36789,1000.);
#9970=VECTOR('',#36794,1000.);
#9971=VECTOR('',#36797,1000.);
#9972=VECTOR('',#36802,1000.);
#9973=VECTOR('',#36805,1000.);
#9974=VECTOR('',#36810,1000.);
#9975=VECTOR('',#36813,1000.);
#9976=VECTOR('',#36818,1000.);
#9977=VECTOR('',#36821,1000.);
#9978=VECTOR('',#36826,1000.);
#9979=VECTOR('',#36829,1000.);
#9980=VECTOR('',#36834,1000.);
#9981=VECTOR('',#36837,1000.);
#9982=VECTOR('',#36842,1000.);
#9983=VECTOR('',#36845,1000.);
#9984=VECTOR('',#36850,1000.);
#9985=VECTOR('',#36853,1000.);
#9986=VECTOR('',#36858,1000.);
#9987=VECTOR('',#36861,1000.);
#9988=VECTOR('',#36866,1000.);
#9989=VECTOR('',#36869,1000.);
#9990=VECTOR('',#36874,1000.);
#9991=VECTOR('',#36877,1000.);
#9992=VECTOR('',#36880,1.55162884844711);
#9993=VECTOR('',#37181,2.73627063036812);
#9994=VECTOR('',#37472,2.68872936963188);
#9995=VECTOR('',#37487,2.675);
#9996=VECTOR('',#38134,1000.);
#9997=VECTOR('',#38137,1000.);
#9998=VECTOR('',#38140,1000.);
#9999=VECTOR('',#38141,1000.);
#10000=VECTOR('',#38146,1000.);
#10001=VECTOR('',#38147,1000.);
#10002=VECTOR('',#38152,1000.);
#10003=VECTOR('',#38153,1000.);
#10004=VECTOR('',#38158,1000.);
#10005=VECTOR('',#38159,1000.);
#10006=VECTOR('',#38164,1000.);
#10007=VECTOR('',#38165,1000.);
#10008=VECTOR('',#38170,1000.);
#10009=VECTOR('',#38171,1000.);
#10010=VECTOR('',#38176,1000.);
#10011=VECTOR('',#38177,1000.);
#10012=VECTOR('',#38182,1000.);
#10013=VECTOR('',#38183,1000.);
#10014=VECTOR('',#38188,1000.);
#10015=VECTOR('',#38189,1000.);
#10016=VECTOR('',#38194,1000.);
#10017=VECTOR('',#38195,1000.);
#10018=VECTOR('',#38200,1000.);
#10019=VECTOR('',#38201,1000.);
#10020=VECTOR('',#38206,1000.);
#10021=VECTOR('',#38207,1000.);
#10022=VECTOR('',#38212,1000.);
#10023=VECTOR('',#38213,1000.);
#10024=VECTOR('',#38218,1000.);
#10025=VECTOR('',#38219,1000.);
#10026=VECTOR('',#38224,1000.);
#10027=VECTOR('',#38225,1000.);
#10028=VECTOR('',#38230,1000.);
#10029=VECTOR('',#38231,1000.);
#10030=VECTOR('',#38236,1000.);
#10031=VECTOR('',#38237,1000.);
#10032=VECTOR('',#38242,1000.);
#10033=VECTOR('',#38243,1000.);
#10034=VECTOR('',#38248,1000.);
#10035=VECTOR('',#38249,1000.);
#10036=VECTOR('',#38254,1000.);
#10037=VECTOR('',#38255,1000.);
#10038=VECTOR('',#38260,1000.);
#10039=VECTOR('',#38261,1000.);
#10040=VECTOR('',#38266,1000.);
#10041=VECTOR('',#38267,1000.);
#10042=VECTOR('',#38272,1000.);
#10043=VECTOR('',#38273,1000.);
#10044=VECTOR('',#38278,1000.);
#10045=VECTOR('',#38279,1000.);
#10046=VECTOR('',#38284,1000.);
#10047=VECTOR('',#38285,1000.);
#10048=VECTOR('',#38290,1000.);
#10049=VECTOR('',#38291,1000.);
#10050=VECTOR('',#38296,1000.);
#10051=VECTOR('',#38297,1000.);
#10052=VECTOR('',#38302,1000.);
#10053=VECTOR('',#38303,1000.);
#10054=VECTOR('',#38308,1000.);
#10055=VECTOR('',#38309,1000.);
#10056=VECTOR('',#38314,1000.);
#10057=VECTOR('',#38315,1000.);
#10058=VECTOR('',#38320,1000.);
#10059=VECTOR('',#38321,1000.);
#10060=VECTOR('',#38326,1000.);
#10061=VECTOR('',#38327,1000.);
#10062=VECTOR('',#38332,1000.);
#10063=VECTOR('',#38333,1000.);
#10064=VECTOR('',#38338,1000.);
#10065=VECTOR('',#38339,1000.);
#10066=VECTOR('',#38344,1000.);
#10067=VECTOR('',#38345,1000.);
#10068=VECTOR('',#38350,1000.);
#10069=VECTOR('',#38351,1000.);
#10070=VECTOR('',#38356,1000.);
#10071=VECTOR('',#38357,1000.);
#10072=VECTOR('',#38362,1000.);
#10073=VECTOR('',#38363,1000.);
#10074=VECTOR('',#38368,1000.);
#10075=VECTOR('',#38369,1000.);
#10076=VECTOR('',#38374,1000.);
#10077=VECTOR('',#38375,1000.);
#10078=VECTOR('',#38380,1000.);
#10079=VECTOR('',#38381,1000.);
#10080=VECTOR('',#38386,1000.);
#10081=VECTOR('',#38387,1000.);
#10082=VECTOR('',#38392,1000.);
#10083=VECTOR('',#38393,1000.);
#10084=VECTOR('',#38398,1000.);
#10085=VECTOR('',#38399,1000.);
#10086=VECTOR('',#38404,1000.);
#10087=VECTOR('',#38405,1000.);
#10088=VECTOR('',#38410,1000.);
#10089=VECTOR('',#38411,1000.);
#10090=VECTOR('',#38416,1000.);
#10091=VECTOR('',#38417,1000.);
#10092=VECTOR('',#38422,1000.);
#10093=VECTOR('',#38423,1000.);
#10094=VECTOR('',#38428,1000.);
#10095=VECTOR('',#38429,1000.);
#10096=VECTOR('',#38434,1000.);
#10097=VECTOR('',#38435,1000.);
#10098=VECTOR('',#38440,1000.);
#10099=VECTOR('',#38441,1000.);
#10100=VECTOR('',#38446,1000.);
#10101=VECTOR('',#38447,1000.);
#10102=VECTOR('',#38452,1000.);
#10103=VECTOR('',#38453,1000.);
#10104=VECTOR('',#38458,1000.);
#10105=VECTOR('',#38459,1000.);
#10106=VECTOR('',#38464,1000.);
#10107=VECTOR('',#38465,1000.);
#10108=VECTOR('',#38470,1000.);
#10109=VECTOR('',#38471,1000.);
#10110=VECTOR('',#38476,1000.);
#10111=VECTOR('',#38477,1000.);
#10112=VECTOR('',#38482,1000.);
#10113=VECTOR('',#38483,1000.);
#10114=VECTOR('',#38488,1000.);
#10115=VECTOR('',#38489,1000.);
#10116=VECTOR('',#38494,1000.);
#10117=VECTOR('',#38495,1000.);
#10118=VECTOR('',#38500,1000.);
#10119=VECTOR('',#38501,1000.);
#10120=VECTOR('',#38506,1000.);
#10121=VECTOR('',#38507,1000.);
#10122=VECTOR('',#38512,1000.);
#10123=VECTOR('',#38513,1000.);
#10124=VECTOR('',#38518,1000.);
#10125=VECTOR('',#38521,1000.);
#10126=VECTOR('',#38524,1000.);
#10127=VECTOR('',#38527,1000.);
#10128=VECTOR('',#38530,1000.);
#10129=VECTOR('',#38533,1000.);
#10130=VECTOR('',#38536,1000.);
#10131=VECTOR('',#38539,1000.);
#10132=VECTOR('',#38542,1000.);
#10133=VECTOR('',#38545,1000.);
#10134=VECTOR('',#38548,1000.);
#10135=VECTOR('',#38551,1000.);
#10136=VECTOR('',#38554,1000.);
#10137=VECTOR('',#38557,1000.);
#10138=VECTOR('',#38560,1000.);
#10139=VECTOR('',#38563,1000.);
#10140=VECTOR('',#38566,1000.);
#10141=VECTOR('',#38569,1000.);
#10142=VECTOR('',#38572,1000.);
#10143=VECTOR('',#38575,1000.);
#10144=VECTOR('',#38578,1000.);
#10145=VECTOR('',#38581,1000.);
#10146=VECTOR('',#38584,1000.);
#10147=VECTOR('',#38587,1000.);
#10148=VECTOR('',#38590,1000.);
#10149=VECTOR('',#38593,1000.);
#10150=VECTOR('',#38596,1000.);
#10151=VECTOR('',#38599,1000.);
#10152=VECTOR('',#38602,1000.);
#10153=VECTOR('',#38603,1000.);
#10154=VECTOR('',#39094,1000.);
#10155=VECTOR('',#39095,1000.);
#10156=VECTOR('',#39108,1000.);
#10157=VECTOR('',#39109,1000.);
#10158=VECTOR('',#39110,1000.);
#10159=VECTOR('',#39111,1000.);
#10160=VECTOR('',#39112,1000.);
#10161=VECTOR('',#39113,1000.);
#10162=VECTOR('',#39116,1000.);
#10163=VECTOR('',#39117,1000.);
#10164=VECTOR('',#39120,1000.);
#10165=VECTOR('',#39123,1000.);
#10166=VECTOR('',#39126,1000.);
#10167=VECTOR('',#39129,1000.);
#10168=VECTOR('',#39132,10.);
#10169=VECTOR('',#39137,1000.);
#10170=VECTOR('',#39140,1000.);
#10171=VECTOR('',#39145,1000.);
#10172=VECTOR('',#39148,1000.);
#10173=VECTOR('',#39153,1000.);
#10174=VECTOR('',#39156,1000.);
#10175=VECTOR('',#39161,1000.);
#10176=VECTOR('',#39164,1000.);
#10177=VECTOR('',#39169,1000.);
#10178=VECTOR('',#39172,1000.);
#10179=VECTOR('',#39177,1000.);
#10180=VECTOR('',#39180,1000.);
#10181=VECTOR('',#39185,1000.);
#10182=VECTOR('',#39188,1000.);
#10183=VECTOR('',#39229,1000.);
#10184=VECTOR('',#39232,1000.);
#10185=VECTOR('',#39237,1000.);
#10186=VECTOR('',#39240,1000.);
#10187=VECTOR('',#39245,1000.);
#10188=VECTOR('',#39248,1000.);
#10189=VECTOR('',#39253,1000.);
#10190=VECTOR('',#39256,1000.);
#10191=VECTOR('',#39261,1000.);
#10192=VECTOR('',#39264,1000.);
#10193=VECTOR('',#39269,1000.);
#10194=VECTOR('',#39272,1000.);
#10195=VECTOR('',#39277,1000.);
#10196=VECTOR('',#39280,1000.);
#10197=VECTOR('',#39285,1000.);
#10198=VECTOR('',#39288,1000.);
#10199=VECTOR('',#39293,1000.);
#10200=VECTOR('',#39296,1000.);
#10201=VECTOR('',#39301,1000.);
#10202=VECTOR('',#39304,1000.);
#10203=VECTOR('',#39309,1000.);
#10204=VECTOR('',#39312,1000.);
#10205=VECTOR('',#39317,1000.);
#10206=VECTOR('',#39320,1000.);
#10207=VECTOR('',#39325,1000.);
#10208=VECTOR('',#39328,1000.);
#10209=VECTOR('',#39333,1000.);
#10210=VECTOR('',#39336,1000.);
#10211=VECTOR('',#39341,1000.);
#10212=VECTOR('',#39344,1000.);
#10213=VECTOR('',#39349,1000.);
#10214=VECTOR('',#39352,1000.);
#10215=VECTOR('',#39357,1000.);
#10216=VECTOR('',#39360,1000.);
#10217=VECTOR('',#39365,1000.);
#10218=VECTOR('',#39368,1000.);
#10219=VECTOR('',#39373,1000.);
#10220=VECTOR('',#39376,1000.);
#10221=VECTOR('',#39381,1000.);
#10222=VECTOR('',#39384,1000.);
#10223=VECTOR('',#39389,1000.);
#10224=VECTOR('',#39392,1000.);
#10225=VECTOR('',#39397,1000.);
#10226=VECTOR('',#39400,1000.);
#10227=VECTOR('',#39405,1000.);
#10228=VECTOR('',#39408,1000.);
#10229=VECTOR('',#39413,1000.);
#10230=VECTOR('',#39416,1000.);
#10231=VECTOR('',#39421,1000.);
#10232=VECTOR('',#39424,1000.);
#10233=VECTOR('',#39429,1000.);
#10234=VECTOR('',#39432,1000.);
#10235=VECTOR('',#39437,1000.);
#10236=VECTOR('',#39440,1000.);
#10237=VECTOR('',#39445,1000.);
#10238=VECTOR('',#39448,1000.);
#10239=VECTOR('',#39453,1000.);
#10240=VECTOR('',#39456,1000.);
#10241=VECTOR('',#39461,1000.);
#10242=VECTOR('',#39464,1000.);
#10243=VECTOR('',#39469,1000.);
#10244=VECTOR('',#39472,1000.);
#10245=VECTOR('',#39477,1000.);
#10246=VECTOR('',#39480,1000.);
#10247=VECTOR('',#39485,1000.);
#10248=VECTOR('',#39488,1000.);
#10249=VECTOR('',#39493,1000.);
#10250=VECTOR('',#39496,1000.);
#10251=VECTOR('',#39501,1000.);
#10252=VECTOR('',#39504,1000.);
#10253=VECTOR('',#39509,1000.);
#10254=VECTOR('',#39512,1000.);
#10255=VECTOR('',#39517,1000.);
#10256=VECTOR('',#39520,1000.);
#10257=VECTOR('',#39525,1000.);
#10258=VECTOR('',#39528,1000.);
#10259=VECTOR('',#39533,1000.);
#10260=VECTOR('',#39536,1000.);
#10261=VECTOR('',#39541,1000.);
#10262=VECTOR('',#39544,1000.);
#10263=VECTOR('',#39549,1000.);
#10264=VECTOR('',#39552,1000.);
#10265=VECTOR('',#39557,1000.);
#10266=VECTOR('',#39560,1000.);
#10267=VECTOR('',#39565,1000.);
#10268=VECTOR('',#39568,1000.);
#10269=VECTOR('',#39573,1000.);
#10270=VECTOR('',#39576,1000.);
#10271=VECTOR('',#39581,1000.);
#10272=VECTOR('',#39584,1000.);
#10273=VECTOR('',#39589,1000.);
#10274=VECTOR('',#39592,1000.);
#10275=VECTOR('',#39597,1000.);
#10276=VECTOR('',#39600,1000.);
#10277=VECTOR('',#39605,1000.);
#10278=VECTOR('',#39608,1000.);
#10279=VECTOR('',#39613,1000.);
#10280=VECTOR('',#39616,1000.);
#10281=VECTOR('',#39621,1000.);
#10282=VECTOR('',#39624,1000.);
#10283=VECTOR('',#39629,1000.);
#10284=VECTOR('',#39632,1000.);
#10285=VECTOR('',#39637,1000.);
#10286=VECTOR('',#39640,1000.);
#10287=VECTOR('',#39645,1000.);
#10288=VECTOR('',#39648,1000.);
#10289=VECTOR('',#39653,1000.);
#10290=VECTOR('',#39656,1000.);
#10291=VECTOR('',#39661,1000.);
#10292=VECTOR('',#39664,1000.);
#10293=VECTOR('',#39669,1000.);
#10294=VECTOR('',#39672,1000.);
#10295=VECTOR('',#39677,1000.);
#10296=VECTOR('',#39680,1000.);
#10297=VECTOR('',#39685,1000.);
#10298=VECTOR('',#39688,1000.);
#11156=VERTEX_POINT('',#46244);
#11157=VERTEX_POINT('',#46245);
#11158=VERTEX_POINT('',#46247);
#11159=VERTEX_POINT('',#46284);
#11160=VERTEX_POINT('',#46287);
#11161=VERTEX_POINT('',#46324);
#11162=VERTEX_POINT('',#46325);
#11163=VERTEX_POINT('',#46400);
#11164=VERTEX_POINT('',#46401);
#11165=VERTEX_POINT('',#46478);
#11166=VERTEX_POINT('',#46479);
#11167=VERTEX_POINT('',#46554);
#11168=VERTEX_POINT('',#46555);
#11169=VERTEX_POINT('',#46630);
#11170=VERTEX_POINT('',#46631);
#11171=VERTEX_POINT('',#46706);
#11172=VERTEX_POINT('',#46707);
#11173=VERTEX_POINT('',#46782);
#11174=VERTEX_POINT('',#46783);
#11175=VERTEX_POINT('',#46860);
#11176=VERTEX_POINT('',#46861);
#11177=VERTEX_POINT('',#46938);
#11178=VERTEX_POINT('',#46939);
#11179=VERTEX_POINT('',#47014);
#11180=VERTEX_POINT('',#47015);
#11181=VERTEX_POINT('',#47090);
#11182=VERTEX_POINT('',#47091);
#11183=VERTEX_POINT('',#47166);
#11184=VERTEX_POINT('',#47167);
#11185=VERTEX_POINT('',#47242);
#11186=VERTEX_POINT('',#47243);
#11187=VERTEX_POINT('',#47320);
#11188=VERTEX_POINT('',#47321);
#11189=VERTEX_POINT('',#47396);
#11190=VERTEX_POINT('',#47397);
#11191=VERTEX_POINT('',#47474);
#11192=VERTEX_POINT('',#47475);
#11193=VERTEX_POINT('',#47550);
#11194=VERTEX_POINT('',#47551);
#11195=VERTEX_POINT('',#47626);
#11196=VERTEX_POINT('',#47627);
#11197=VERTEX_POINT('',#47702);
#11198=VERTEX_POINT('',#47703);
#11199=VERTEX_POINT('',#47778);
#11200=VERTEX_POINT('',#47779);
#11201=VERTEX_POINT('',#47856);
#11202=VERTEX_POINT('',#47857);
#11203=VERTEX_POINT('',#47934);
#11204=VERTEX_POINT('',#47935);
#11205=VERTEX_POINT('',#48010);
#11206=VERTEX_POINT('',#48011);
#11207=VERTEX_POINT('',#48086);
#11208=VERTEX_POINT('',#48087);
#11209=VERTEX_POINT('',#48162);
#11210=VERTEX_POINT('',#48163);
#11211=VERTEX_POINT('',#48238);
#11212=VERTEX_POINT('',#48239);
#11213=VERTEX_POINT('',#48316);
#11214=VERTEX_POINT('',#48317);
#11215=VERTEX_POINT('',#48392);
#11216=VERTEX_POINT('',#48393);
#11217=VERTEX_POINT('',#48395);
#11218=VERTEX_POINT('',#48418);
#11219=VERTEX_POINT('',#48420);
#11220=VERTEX_POINT('',#48431);
#11221=VERTEX_POINT('',#48432);
#11222=VERTEX_POINT('',#48507);
#11223=VERTEX_POINT('',#48508);
#11224=VERTEX_POINT('',#48583);
#11225=VERTEX_POINT('',#48584);
#11226=VERTEX_POINT('',#48661);
#11227=VERTEX_POINT('',#48662);
#11228=VERTEX_POINT('',#48737);
#11229=VERTEX_POINT('',#48738);
#11230=VERTEX_POINT('',#48815);
#11231=VERTEX_POINT('',#48816);
#11232=VERTEX_POINT('',#48891);
#11233=VERTEX_POINT('',#48892);
#11234=VERTEX_POINT('',#48967);
#11235=VERTEX_POINT('',#48968);
#11236=VERTEX_POINT('',#49043);
#11237=VERTEX_POINT('',#49044);
#11238=VERTEX_POINT('',#49119);
#11239=VERTEX_POINT('',#49120);
#11240=VERTEX_POINT('',#49197);
#11241=VERTEX_POINT('',#49198);
#11242=VERTEX_POINT('',#49273);
#11243=VERTEX_POINT('',#49274);
#11244=VERTEX_POINT('',#49351);
#11245=VERTEX_POINT('',#49352);
#11246=VERTEX_POINT('',#49427);
#11247=VERTEX_POINT('',#49428);
#11248=VERTEX_POINT('',#49503);
#11249=VERTEX_POINT('',#49504);
#11250=VERTEX_POINT('',#49579);
#11251=VERTEX_POINT('',#49580);
#11252=VERTEX_POINT('',#49655);
#11253=VERTEX_POINT('',#49656);
#11254=VERTEX_POINT('',#49731);
#11255=VERTEX_POINT('',#49732);
#11256=VERTEX_POINT('',#49809);
#11257=VERTEX_POINT('',#49810);
#11258=VERTEX_POINT('',#49885);
#11259=VERTEX_POINT('',#49886);
#11260=VERTEX_POINT('',#49963);
#11261=VERTEX_POINT('',#49964);
#11262=VERTEX_POINT('',#50039);
#11263=VERTEX_POINT('',#50040);
#11264=VERTEX_POINT('',#50115);
#11265=VERTEX_POINT('',#50116);
#11266=VERTEX_POINT('',#50191);
#11267=VERTEX_POINT('',#50192);
#11268=VERTEX_POINT('',#50267);
#11269=VERTEX_POINT('',#50268);
#11270=VERTEX_POINT('',#50345);
#11271=VERTEX_POINT('',#50346);
#11272=VERTEX_POINT('',#50421);
#11273=VERTEX_POINT('',#50422);
#11274=VERTEX_POINT('',#50499);
#11275=VERTEX_POINT('',#50500);
#11276=VERTEX_POINT('',#50575);
#11277=VERTEX_POINT('',#50576);
#11278=VERTEX_POINT('',#50651);
#11279=VERTEX_POINT('',#50663);
#11280=VERTEX_POINT('',#50676);
#11281=VERTEX_POINT('',#50768);
#11282=VERTEX_POINT('',#50769);
#11283=VERTEX_POINT('',#50771);
#11284=VERTEX_POINT('',#50773);
#11285=VERTEX_POINT('',#50777);
#11286=VERTEX_POINT('',#50778);
#11287=VERTEX_POINT('',#50780);
#11288=VERTEX_POINT('',#50782);
#11289=VERTEX_POINT('',#50786);
#11290=VERTEX_POINT('',#50787);
#11291=VERTEX_POINT('',#50789);
#11292=VERTEX_POINT('',#50791);
#11293=VERTEX_POINT('',#50795);
#11294=VERTEX_POINT('',#50796);
#11295=VERTEX_POINT('',#50798);
#11296=VERTEX_POINT('',#50800);
#11297=VERTEX_POINT('',#50804);
#11298=VERTEX_POINT('',#50805);
#11299=VERTEX_POINT('',#50807);
#11300=VERTEX_POINT('',#50809);
#11301=VERTEX_POINT('',#50813);
#11302=VERTEX_POINT('',#50814);
#11303=VERTEX_POINT('',#50816);
#11304=VERTEX_POINT('',#50818);
#11305=VERTEX_POINT('',#50822);
#11306=VERTEX_POINT('',#50823);
#11307=VERTEX_POINT('',#50825);
#11308=VERTEX_POINT('',#50827);
#11309=VERTEX_POINT('',#50831);
#11310=VERTEX_POINT('',#50832);
#11311=VERTEX_POINT('',#50834);
#11312=VERTEX_POINT('',#50836);
#11313=VERTEX_POINT('',#50840);
#11314=VERTEX_POINT('',#50841);
#11315=VERTEX_POINT('',#50843);
#11316=VERTEX_POINT('',#50845);
#11317=VERTEX_POINT('',#50849);
#11318=VERTEX_POINT('',#50850);
#11319=VERTEX_POINT('',#50852);
#11320=VERTEX_POINT('',#50854);
#11321=VERTEX_POINT('',#50858);
#11322=VERTEX_POINT('',#50859);
#11323=VERTEX_POINT('',#50861);
#11324=VERTEX_POINT('',#50863);
#11325=VERTEX_POINT('',#50867);
#11326=VERTEX_POINT('',#50868);
#11327=VERTEX_POINT('',#50870);
#11328=VERTEX_POINT('',#50872);
#11329=VERTEX_POINT('',#50876);
#11330=VERTEX_POINT('',#50877);
#11331=VERTEX_POINT('',#50879);
#11332=VERTEX_POINT('',#50881);
#11333=VERTEX_POINT('',#50885);
#11334=VERTEX_POINT('',#50886);
#11335=VERTEX_POINT('',#50888);
#11336=VERTEX_POINT('',#50890);
#11337=VERTEX_POINT('',#50894);
#11338=VERTEX_POINT('',#50895);
#11339=VERTEX_POINT('',#50897);
#11340=VERTEX_POINT('',#50899);
#11341=VERTEX_POINT('',#50903);
#11342=VERTEX_POINT('',#50904);
#11343=VERTEX_POINT('',#50908);
#11344=VERTEX_POINT('',#50912);
#11345=VERTEX_POINT('',#50916);
#11346=VERTEX_POINT('',#50920);
#11347=VERTEX_POINT('',#50924);
#11348=VERTEX_POINT('',#50931);
#11349=VERTEX_POINT('',#50935);
#11350=VERTEX_POINT('',#50937);
#11351=VERTEX_POINT('',#50941);
#11352=VERTEX_POINT('',#50942);
#11353=VERTEX_POINT('',#50951);
#11354=VERTEX_POINT('',#50955);
#11355=VERTEX_POINT('',#50957);
#11356=VERTEX_POINT('',#50961);
#11357=VERTEX_POINT('',#50963);
#11358=VERTEX_POINT('',#50967);
#11359=VERTEX_POINT('',#50969);
#11360=VERTEX_POINT('',#50973);
#11361=VERTEX_POINT('',#50975);
#11362=VERTEX_POINT('',#50979);
#11363=VERTEX_POINT('',#50981);
#11364=VERTEX_POINT('',#50985);
#11365=VERTEX_POINT('',#50987);
#11366=VERTEX_POINT('',#50991);
#11367=VERTEX_POINT('',#50993);
#11368=VERTEX_POINT('',#50997);
#11369=VERTEX_POINT('',#50999);
#11370=VERTEX_POINT('',#51003);
#11371=VERTEX_POINT('',#51005);
#11372=VERTEX_POINT('',#51009);
#11373=VERTEX_POINT('',#51011);
#11374=VERTEX_POINT('',#51015);
#11375=VERTEX_POINT('',#51017);
#11376=VERTEX_POINT('',#51021);
#11377=VERTEX_POINT('',#51023);
#11378=VERTEX_POINT('',#51027);
#11379=VERTEX_POINT('',#51029);
#11380=VERTEX_POINT('',#51033);
#11381=VERTEX_POINT('',#51035);
#11382=VERTEX_POINT('',#51039);
#11383=VERTEX_POINT('',#51041);
#11384=VERTEX_POINT('',#51045);
#11385=VERTEX_POINT('',#51047);
#11386=VERTEX_POINT('',#51051);
#11387=VERTEX_POINT('',#51053);
#11388=VERTEX_POINT('',#51057);
#11389=VERTEX_POINT('',#51059);
#11390=VERTEX_POINT('',#51063);
#11391=VERTEX_POINT('',#51065);
#11392=VERTEX_POINT('',#51069);
#11393=VERTEX_POINT('',#51071);
#11394=VERTEX_POINT('',#51075);
#11395=VERTEX_POINT('',#51077);
#11396=VERTEX_POINT('',#51081);
#11397=VERTEX_POINT('',#51083);
#11398=VERTEX_POINT('',#51087);
#11399=VERTEX_POINT('',#51089);
#11400=VERTEX_POINT('',#51093);
#11401=VERTEX_POINT('',#51095);
#11402=VERTEX_POINT('',#51099);
#11403=VERTEX_POINT('',#51101);
#11404=VERTEX_POINT('',#51105);
#11405=VERTEX_POINT('',#51107);
#11406=VERTEX_POINT('',#51111);
#11407=VERTEX_POINT('',#51113);
#11408=VERTEX_POINT('',#51117);
#11409=VERTEX_POINT('',#51119);
#11410=VERTEX_POINT('',#51123);
#11411=VERTEX_POINT('',#51125);
#11412=VERTEX_POINT('',#51129);
#11413=VERTEX_POINT('',#51131);
#11414=VERTEX_POINT('',#51135);
#11415=VERTEX_POINT('',#51137);
#11416=VERTEX_POINT('',#51141);
#11417=VERTEX_POINT('',#51143);
#11418=VERTEX_POINT('',#51147);
#11419=VERTEX_POINT('',#51149);
#11420=VERTEX_POINT('',#51153);
#11421=VERTEX_POINT('',#51155);
#11422=VERTEX_POINT('',#51159);
#11423=VERTEX_POINT('',#51161);
#11424=VERTEX_POINT('',#51165);
#11425=VERTEX_POINT('',#51167);
#11426=VERTEX_POINT('',#51171);
#11427=VERTEX_POINT('',#51173);
#11428=VERTEX_POINT('',#51177);
#11429=VERTEX_POINT('',#51179);
#11430=VERTEX_POINT('',#51183);
#11431=VERTEX_POINT('',#51185);
#11432=VERTEX_POINT('',#51189);
#11433=VERTEX_POINT('',#51191);
#11434=VERTEX_POINT('',#51195);
#11435=VERTEX_POINT('',#51197);
#11436=VERTEX_POINT('',#51201);
#11437=VERTEX_POINT('',#51203);
#11438=VERTEX_POINT('',#51207);
#11439=VERTEX_POINT('',#51209);
#11440=VERTEX_POINT('',#51213);
#11441=VERTEX_POINT('',#51215);
#11442=VERTEX_POINT('',#51219);
#11443=VERTEX_POINT('',#51221);
#11444=VERTEX_POINT('',#51225);
#11445=VERTEX_POINT('',#51227);
#11446=VERTEX_POINT('',#51231);
#11447=VERTEX_POINT('',#51233);
#11448=VERTEX_POINT('',#51237);
#11449=VERTEX_POINT('',#51239);
#11450=VERTEX_POINT('',#51243);
#11451=VERTEX_POINT('',#51245);
#11452=VERTEX_POINT('',#51249);
#11453=VERTEX_POINT('',#51251);
#11454=VERTEX_POINT('',#51255);
#11455=VERTEX_POINT('',#51257);
#11456=VERTEX_POINT('',#51261);
#11457=VERTEX_POINT('',#51263);
#11458=VERTEX_POINT('',#51267);
#11459=VERTEX_POINT('',#51269);
#11460=VERTEX_POINT('',#51273);
#11461=VERTEX_POINT('',#51275);
#11462=VERTEX_POINT('',#51279);
#11463=VERTEX_POINT('',#51281);
#11464=VERTEX_POINT('',#51285);
#11465=VERTEX_POINT('',#51287);
#11466=VERTEX_POINT('',#51291);
#11467=VERTEX_POINT('',#51293);
#11468=VERTEX_POINT('',#51297);
#11469=VERTEX_POINT('',#51299);
#11470=VERTEX_POINT('',#51303);
#11471=VERTEX_POINT('',#51305);
#11472=VERTEX_POINT('',#51309);
#11473=VERTEX_POINT('',#51311);
#11474=VERTEX_POINT('',#51315);
#11475=VERTEX_POINT('',#51317);
#11476=VERTEX_POINT('',#51321);
#11477=VERTEX_POINT('',#51323);
#11478=VERTEX_POINT('',#51327);
#11479=VERTEX_POINT('',#51329);
#11480=VERTEX_POINT('',#51333);
#11481=VERTEX_POINT('',#51335);
#11482=VERTEX_POINT('',#51339);
#11483=VERTEX_POINT('',#51341);
#11484=VERTEX_POINT('',#51345);
#11485=VERTEX_POINT('',#51347);
#11486=VERTEX_POINT('',#51351);
#11487=VERTEX_POINT('',#51353);
#11488=VERTEX_POINT('',#51357);
#11489=VERTEX_POINT('',#51359);
#11490=VERTEX_POINT('',#51363);
#11491=VERTEX_POINT('',#51365);
#11492=VERTEX_POINT('',#51369);
#11493=VERTEX_POINT('',#51371);
#11494=VERTEX_POINT('',#51375);
#11495=VERTEX_POINT('',#51377);
#11496=VERTEX_POINT('',#51381);
#11497=VERTEX_POINT('',#51383);
#11498=VERTEX_POINT('',#51387);
#11499=VERTEX_POINT('',#51389);
#11500=VERTEX_POINT('',#51393);
#11501=VERTEX_POINT('',#51395);
#11502=VERTEX_POINT('',#51399);
#11503=VERTEX_POINT('',#51401);
#11504=VERTEX_POINT('',#51405);
#11505=VERTEX_POINT('',#51407);
#11506=VERTEX_POINT('',#51411);
#11507=VERTEX_POINT('',#51413);
#11508=VERTEX_POINT('',#51417);
#11509=VERTEX_POINT('',#51419);
#11510=VERTEX_POINT('',#51423);
#11511=VERTEX_POINT('',#51425);
#11512=VERTEX_POINT('',#51429);
#11513=VERTEX_POINT('',#51431);
#11514=VERTEX_POINT('',#51435);
#11515=VERTEX_POINT('',#51437);
#11516=VERTEX_POINT('',#51441);
#11517=VERTEX_POINT('',#51443);
#11518=VERTEX_POINT('',#51447);
#11519=VERTEX_POINT('',#51449);
#11520=VERTEX_POINT('',#51453);
#11521=VERTEX_POINT('',#51455);
#11522=VERTEX_POINT('',#51459);
#11523=VERTEX_POINT('',#51461);
#11524=VERTEX_POINT('',#51465);
#11525=VERTEX_POINT('',#51467);
#11526=VERTEX_POINT('',#51471);
#11527=VERTEX_POINT('',#51473);
#11528=VERTEX_POINT('',#51477);
#11529=VERTEX_POINT('',#51479);
#11530=VERTEX_POINT('',#51483);
#11531=VERTEX_POINT('',#51485);
#11532=VERTEX_POINT('',#51489);
#11533=VERTEX_POINT('',#51491);
#11534=VERTEX_POINT('',#51495);
#11535=VERTEX_POINT('',#51500);
#11536=VERTEX_POINT('',#51504);
#11537=VERTEX_POINT('',#51509);
#11538=VERTEX_POINT('',#51513);
#11539=VERTEX_POINT('',#51518);
#11540=VERTEX_POINT('',#51522);
#11541=VERTEX_POINT('',#51527);
#11542=VERTEX_POINT('',#51531);
#11543=VERTEX_POINT('',#51536);
#11544=VERTEX_POINT('',#51540);
#11545=VERTEX_POINT('',#51545);
#11546=VERTEX_POINT('',#51549);
#11547=VERTEX_POINT('',#51554);
#11548=VERTEX_POINT('',#51558);
#11549=VERTEX_POINT('',#51563);
#11550=VERTEX_POINT('',#51567);
#11551=VERTEX_POINT('',#51572);
#11552=VERTEX_POINT('',#51576);
#11553=VERTEX_POINT('',#51581);
#11554=VERTEX_POINT('',#51585);
#11555=VERTEX_POINT('',#51590);
#11556=VERTEX_POINT('',#51594);
#11557=VERTEX_POINT('',#51599);
#11558=VERTEX_POINT('',#51603);
#11559=VERTEX_POINT('',#51608);
#11560=VERTEX_POINT('',#51612);
#11561=VERTEX_POINT('',#51617);
#11562=VERTEX_POINT('',#51621);
#11563=VERTEX_POINT('',#51626);
#11564=VERTEX_POINT('',#51630);
#11565=VERTEX_POINT('',#51632);
#11566=VERTEX_POINT('',#51636);
#11567=VERTEX_POINT('',#51638);
#11568=VERTEX_POINT('',#51642);
#11569=VERTEX_POINT('',#51644);
#11570=VERTEX_POINT('',#51648);
#11571=VERTEX_POINT('',#51650);
#11572=VERTEX_POINT('',#51654);
#11573=VERTEX_POINT('',#51656);
#11574=VERTEX_POINT('',#51660);
#11575=VERTEX_POINT('',#51662);
#11576=VERTEX_POINT('',#51666);
#11577=VERTEX_POINT('',#51668);
#11578=VERTEX_POINT('',#51672);
#11579=VERTEX_POINT('',#51674);
#11580=VERTEX_POINT('',#51678);
#11581=VERTEX_POINT('',#51680);
#11582=VERTEX_POINT('',#51684);
#11583=VERTEX_POINT('',#51686);
#11584=VERTEX_POINT('',#51690);
#11585=VERTEX_POINT('',#51692);
#11586=VERTEX_POINT('',#51696);
#11587=VERTEX_POINT('',#51698);
#11588=VERTEX_POINT('',#51702);
#11589=VERTEX_POINT('',#51704);
#11590=VERTEX_POINT('',#51708);
#11591=VERTEX_POINT('',#51710);
#11592=VERTEX_POINT('',#51714);
#11593=VERTEX_POINT('',#51716);
#11594=VERTEX_POINT('',#51720);
#11595=VERTEX_POINT('',#51722);
#11596=VERTEX_POINT('',#51726);
#11597=VERTEX_POINT('',#51728);
#11598=VERTEX_POINT('',#51732);
#11599=VERTEX_POINT('',#51734);
#11600=VERTEX_POINT('',#51738);
#11601=VERTEX_POINT('',#51740);
#11602=VERTEX_POINT('',#51744);
#11603=VERTEX_POINT('',#51746);
#11604=VERTEX_POINT('',#51750);
#11605=VERTEX_POINT('',#51752);
#11606=VERTEX_POINT('',#51756);
#11607=VERTEX_POINT('',#51758);
#11608=VERTEX_POINT('',#51762);
#11609=VERTEX_POINT('',#51764);
#11610=VERTEX_POINT('',#51768);
#11611=VERTEX_POINT('',#51770);
#11612=VERTEX_POINT('',#51774);
#11613=VERTEX_POINT('',#51776);
#11614=VERTEX_POINT('',#51780);
#11615=VERTEX_POINT('',#51782);
#11616=VERTEX_POINT('',#51786);
#11617=VERTEX_POINT('',#51788);
#11618=VERTEX_POINT('',#51792);
#11619=VERTEX_POINT('',#51794);
#11620=VERTEX_POINT('',#51798);
#11621=VERTEX_POINT('',#51800);
#11622=VERTEX_POINT('',#51804);
#11623=VERTEX_POINT('',#51806);
#11624=VERTEX_POINT('',#51810);
#11625=VERTEX_POINT('',#51812);
#11626=VERTEX_POINT('',#51816);
#11627=VERTEX_POINT('',#51818);
#11628=VERTEX_POINT('',#51822);
#11629=VERTEX_POINT('',#51824);
#11630=VERTEX_POINT('',#51828);
#11631=VERTEX_POINT('',#51830);
#11632=VERTEX_POINT('',#51834);
#11633=VERTEX_POINT('',#51836);
#11634=VERTEX_POINT('',#51840);
#11635=VERTEX_POINT('',#51842);
#11636=VERTEX_POINT('',#51846);
#11637=VERTEX_POINT('',#51848);
#11638=VERTEX_POINT('',#51852);
#11639=VERTEX_POINT('',#51854);
#11640=VERTEX_POINT('',#51858);
#11641=VERTEX_POINT('',#51860);
#11642=VERTEX_POINT('',#51874);
#11643=VERTEX_POINT('',#51875);
#11644=VERTEX_POINT('',#51884);
#11645=VERTEX_POINT('',#51888);
#11646=VERTEX_POINT('',#51890);
#11647=VERTEX_POINT('',#51894);
#11648=VERTEX_POINT('',#51896);
#11649=VERTEX_POINT('',#51900);
#11650=VERTEX_POINT('',#51902);
#11651=VERTEX_POINT('',#51906);
#11652=VERTEX_POINT('',#51908);
#11653=VERTEX_POINT('',#51912);
#11654=VERTEX_POINT('',#51914);
#11655=VERTEX_POINT('',#51918);
#11656=VERTEX_POINT('',#51920);
#11657=VERTEX_POINT('',#51924);
#11658=VERTEX_POINT('',#51926);
#11659=VERTEX_POINT('',#51930);
#11660=VERTEX_POINT('',#51932);
#11661=VERTEX_POINT('',#51936);
#11662=VERTEX_POINT('',#51938);
#11663=VERTEX_POINT('',#51942);
#11664=VERTEX_POINT('',#51944);
#11665=VERTEX_POINT('',#51948);
#11666=VERTEX_POINT('',#51950);
#11667=VERTEX_POINT('',#51954);
#11668=VERTEX_POINT('',#51956);
#11669=VERTEX_POINT('',#51960);
#11670=VERTEX_POINT('',#51962);
#11671=VERTEX_POINT('',#51966);
#11672=VERTEX_POINT('',#51968);
#11673=VERTEX_POINT('',#51972);
#11674=VERTEX_POINT('',#51974);
#11675=VERTEX_POINT('',#51978);
#11676=VERTEX_POINT('',#51980);
#11677=VERTEX_POINT('',#51984);
#11678=VERTEX_POINT('',#51986);
#11679=VERTEX_POINT('',#51990);
#11680=VERTEX_POINT('',#51992);
#11681=VERTEX_POINT('',#51996);
#11682=VERTEX_POINT('',#51998);
#11683=VERTEX_POINT('',#52002);
#11684=VERTEX_POINT('',#52004);
#11685=VERTEX_POINT('',#52008);
#11686=VERTEX_POINT('',#52010);
#11687=VERTEX_POINT('',#52014);
#11688=VERTEX_POINT('',#52016);
#11689=VERTEX_POINT('',#52020);
#11690=VERTEX_POINT('',#52022);
#11691=VERTEX_POINT('',#52026);
#11692=VERTEX_POINT('',#52028);
#11693=VERTEX_POINT('',#52032);
#11694=VERTEX_POINT('',#52034);
#11695=VERTEX_POINT('',#52038);
#11696=VERTEX_POINT('',#52040);
#11697=VERTEX_POINT('',#52044);
#11698=VERTEX_POINT('',#52046);
#11699=VERTEX_POINT('',#52050);
#11700=VERTEX_POINT('',#52052);
#11701=VERTEX_POINT('',#52056);
#11702=VERTEX_POINT('',#52058);
#11703=VERTEX_POINT('',#52062);
#11704=VERTEX_POINT('',#52064);
#11705=VERTEX_POINT('',#52068);
#11706=VERTEX_POINT('',#52070);
#11707=VERTEX_POINT('',#52074);
#11708=VERTEX_POINT('',#52076);
#11709=VERTEX_POINT('',#52080);
#11710=VERTEX_POINT('',#52082);
#11711=VERTEX_POINT('',#52086);
#11712=VERTEX_POINT('',#52088);
#11713=VERTEX_POINT('',#52092);
#11714=VERTEX_POINT('',#52094);
#11715=VERTEX_POINT('',#52098);
#11716=VERTEX_POINT('',#52100);
#11717=VERTEX_POINT('',#52104);
#11718=VERTEX_POINT('',#52106);
#11719=VERTEX_POINT('',#52110);
#11720=VERTEX_POINT('',#52112);
#11721=VERTEX_POINT('',#52116);
#11722=VERTEX_POINT('',#52118);
#11723=VERTEX_POINT('',#52122);
#11724=VERTEX_POINT('',#52124);
#11725=VERTEX_POINT('',#52128);
#11726=VERTEX_POINT('',#52130);
#11727=VERTEX_POINT('',#52134);
#11728=VERTEX_POINT('',#52136);
#11729=VERTEX_POINT('',#52140);
#11730=VERTEX_POINT('',#52142);
#11731=VERTEX_POINT('',#52146);
#11732=VERTEX_POINT('',#52148);
#11733=VERTEX_POINT('',#52152);
#11734=VERTEX_POINT('',#52154);
#11735=VERTEX_POINT('',#52158);
#11736=VERTEX_POINT('',#52160);
#11737=VERTEX_POINT('',#52164);
#11738=VERTEX_POINT('',#52166);
#11739=VERTEX_POINT('',#52170);
#11740=VERTEX_POINT('',#52172);
#11741=VERTEX_POINT('',#52176);
#11742=VERTEX_POINT('',#52178);
#11743=VERTEX_POINT('',#52182);
#11744=VERTEX_POINT('',#52184);
#11745=VERTEX_POINT('',#52188);
#11746=VERTEX_POINT('',#52190);
#11747=VERTEX_POINT('',#52194);
#11748=VERTEX_POINT('',#52196);
#11749=VERTEX_POINT('',#52200);
#11750=VERTEX_POINT('',#52202);
#11751=VERTEX_POINT('',#52206);
#11752=VERTEX_POINT('',#52208);
#11753=VERTEX_POINT('',#52212);
#11754=VERTEX_POINT('',#52214);
#11755=VERTEX_POINT('',#52218);
#11756=VERTEX_POINT('',#52220);
#11757=VERTEX_POINT('',#52224);
#11758=VERTEX_POINT('',#52226);
#11759=VERTEX_POINT('',#52230);
#11760=VERTEX_POINT('',#52232);
#11761=VERTEX_POINT('',#52236);
#11762=VERTEX_POINT('',#52238);
#11763=VERTEX_POINT('',#52242);
#11764=VERTEX_POINT('',#52244);
#11765=VERTEX_POINT('',#52248);
#11766=VERTEX_POINT('',#52250);
#11767=VERTEX_POINT('',#52254);
#11768=VERTEX_POINT('',#52256);
#11769=VERTEX_POINT('',#52260);
#11770=VERTEX_POINT('',#52262);
#11771=VERTEX_POINT('',#52266);
#11772=VERTEX_POINT('',#52268);
#11773=VERTEX_POINT('',#52272);
#11774=VERTEX_POINT('',#52274);
#11775=VERTEX_POINT('',#52278);
#11776=VERTEX_POINT('',#52280);
#11777=VERTEX_POINT('',#52284);
#11778=VERTEX_POINT('',#52286);
#11779=VERTEX_POINT('',#52290);
#11780=VERTEX_POINT('',#52292);
#11781=VERTEX_POINT('',#52296);
#11782=VERTEX_POINT('',#52298);
#11783=VERTEX_POINT('',#52302);
#11784=VERTEX_POINT('',#52304);
#11785=VERTEX_POINT('',#52308);
#11786=VERTEX_POINT('',#52310);
#11787=VERTEX_POINT('',#52314);
#11788=VERTEX_POINT('',#52316);
#11789=VERTEX_POINT('',#52320);
#11790=VERTEX_POINT('',#52322);
#11791=VERTEX_POINT('',#52326);
#11792=VERTEX_POINT('',#52328);
#11793=VERTEX_POINT('',#52332);
#11794=VERTEX_POINT('',#52334);
#11795=VERTEX_POINT('',#52338);
#11796=VERTEX_POINT('',#52340);
#11797=VERTEX_POINT('',#52344);
#11798=VERTEX_POINT('',#52346);
#11799=VERTEX_POINT('',#52350);
#11800=VERTEX_POINT('',#52352);
#11801=VERTEX_POINT('',#52356);
#11802=VERTEX_POINT('',#52358);
#11803=VERTEX_POINT('',#52362);
#11804=VERTEX_POINT('',#52364);
#11805=VERTEX_POINT('',#52368);
#11806=VERTEX_POINT('',#52370);
#11807=VERTEX_POINT('',#52374);
#11808=VERTEX_POINT('',#52376);
#11809=VERTEX_POINT('',#52380);
#11810=VERTEX_POINT('',#52382);
#11811=VERTEX_POINT('',#52386);
#11812=VERTEX_POINT('',#52388);
#11813=VERTEX_POINT('',#52392);
#11814=VERTEX_POINT('',#52394);
#11815=VERTEX_POINT('',#52398);
#11816=VERTEX_POINT('',#52400);
#11817=VERTEX_POINT('',#52404);
#11818=VERTEX_POINT('',#52406);
#11819=VERTEX_POINT('',#52410);
#11820=VERTEX_POINT('',#52412);
#11821=VERTEX_POINT('',#52416);
#11822=VERTEX_POINT('',#52418);
#11823=VERTEX_POINT('',#52422);
#11824=VERTEX_POINT('',#52424);
#11825=VERTEX_POINT('',#52428);
#11826=VERTEX_POINT('',#52430);
#11827=VERTEX_POINT('',#52434);
#11828=VERTEX_POINT('',#52436);
#11829=VERTEX_POINT('',#52440);
#11830=VERTEX_POINT('',#52442);
#11831=VERTEX_POINT('',#52446);
#11832=VERTEX_POINT('',#52448);
#11833=VERTEX_POINT('',#52452);
#11834=VERTEX_POINT('',#52454);
#11835=VERTEX_POINT('',#52458);
#11836=VERTEX_POINT('',#52460);
#11837=VERTEX_POINT('',#52464);
#11838=VERTEX_POINT('',#52466);
#11839=VERTEX_POINT('',#52470);
#11840=VERTEX_POINT('',#52472);
#11841=VERTEX_POINT('',#52476);
#11842=VERTEX_POINT('',#52478);
#11843=VERTEX_POINT('',#52482);
#11844=VERTEX_POINT('',#52484);
#11845=VERTEX_POINT('',#52488);
#11846=VERTEX_POINT('',#52490);
#11847=VERTEX_POINT('',#52494);
#11848=VERTEX_POINT('',#52496);
#11849=VERTEX_POINT('',#52500);
#11850=VERTEX_POINT('',#52502);
#11851=VERTEX_POINT('',#52506);
#11852=VERTEX_POINT('',#52508);
#11853=VERTEX_POINT('',#52512);
#11854=VERTEX_POINT('',#52514);
#11855=VERTEX_POINT('',#52518);
#11856=VERTEX_POINT('',#52520);
#11857=VERTEX_POINT('',#52524);
#11858=VERTEX_POINT('',#52526);
#11859=VERTEX_POINT('',#52530);
#11860=VERTEX_POINT('',#52532);
#11861=VERTEX_POINT('',#52536);
#11862=VERTEX_POINT('',#52538);
#11863=VERTEX_POINT('',#52542);
#11864=VERTEX_POINT('',#52544);
#11865=VERTEX_POINT('',#52548);
#11866=VERTEX_POINT('',#52550);
#11867=VERTEX_POINT('',#52554);
#11868=VERTEX_POINT('',#52556);
#11869=VERTEX_POINT('',#52560);
#11870=VERTEX_POINT('',#52562);
#11871=VERTEX_POINT('',#52566);
#11872=VERTEX_POINT('',#52568);
#11873=VERTEX_POINT('',#52572);
#11874=VERTEX_POINT('',#52574);
#11875=VERTEX_POINT('',#52578);
#11876=VERTEX_POINT('',#52580);
#11877=VERTEX_POINT('',#52584);
#11878=VERTEX_POINT('',#52586);
#11879=VERTEX_POINT('',#52590);
#11880=VERTEX_POINT('',#52592);
#11881=VERTEX_POINT('',#52596);
#11882=VERTEX_POINT('',#52601);
#11883=VERTEX_POINT('',#52605);
#11884=VERTEX_POINT('',#52610);
#11885=VERTEX_POINT('',#52614);
#11886=VERTEX_POINT('',#52619);
#11887=VERTEX_POINT('',#52623);
#11888=VERTEX_POINT('',#52628);
#11889=VERTEX_POINT('',#52632);
#11890=VERTEX_POINT('',#52637);
#11891=VERTEX_POINT('',#52641);
#11892=VERTEX_POINT('',#52646);
#11893=VERTEX_POINT('',#52650);
#11894=VERTEX_POINT('',#52655);
#11895=VERTEX_POINT('',#52659);
#11896=VERTEX_POINT('',#52664);
#11897=VERTEX_POINT('',#52668);
#11898=VERTEX_POINT('',#52673);
#11899=VERTEX_POINT('',#52677);
#11900=VERTEX_POINT('',#52682);
#11901=VERTEX_POINT('',#52686);
#11902=VERTEX_POINT('',#52691);
#11903=VERTEX_POINT('',#52695);
#11904=VERTEX_POINT('',#52700);
#11905=VERTEX_POINT('',#52704);
#11906=VERTEX_POINT('',#52709);
#11907=VERTEX_POINT('',#52713);
#11908=VERTEX_POINT('',#52718);
#11909=VERTEX_POINT('',#52722);
#11910=VERTEX_POINT('',#52727);
#11911=VERTEX_POINT('',#52731);
#11912=VERTEX_POINT('',#52733);
#11913=VERTEX_POINT('',#52737);
#11914=VERTEX_POINT('',#52739);
#11915=VERTEX_POINT('',#52743);
#11916=VERTEX_POINT('',#52745);
#11917=VERTEX_POINT('',#52749);
#11918=VERTEX_POINT('',#52751);
#11919=VERTEX_POINT('',#52755);
#11920=VERTEX_POINT('',#52757);
#11921=VERTEX_POINT('',#52761);
#11922=VERTEX_POINT('',#52763);
#11923=VERTEX_POINT('',#52767);
#11924=VERTEX_POINT('',#52769);
#11925=VERTEX_POINT('',#52773);
#11926=VERTEX_POINT('',#52775);
#11927=VERTEX_POINT('',#52779);
#11928=VERTEX_POINT('',#52781);
#11929=VERTEX_POINT('',#52785);
#11930=VERTEX_POINT('',#52787);
#11931=VERTEX_POINT('',#52791);
#11932=VERTEX_POINT('',#52793);
#11933=VERTEX_POINT('',#52805);
#11934=VERTEX_POINT('',#52807);
#11935=VERTEX_POINT('',#52811);
#11936=VERTEX_POINT('',#52815);
#11937=VERTEX_POINT('',#52819);
#11938=VERTEX_POINT('',#52823);
#11939=VERTEX_POINT('',#52827);
#11940=VERTEX_POINT('',#52829);
#11941=VERTEX_POINT('',#52833);
#11942=VERTEX_POINT('',#52835);
#11943=VERTEX_POINT('',#52839);
#11944=VERTEX_POINT('',#52841);
#11945=VERTEX_POINT('',#52845);
#11946=VERTEX_POINT('',#52847);
#11947=VERTEX_POINT('',#52851);
#11948=VERTEX_POINT('',#52853);
#11949=VERTEX_POINT('',#52857);
#11950=VERTEX_POINT('',#52859);
#11951=VERTEX_POINT('',#52863);
#11952=VERTEX_POINT('',#52865);
#11953=VERTEX_POINT('',#52869);
#11954=VERTEX_POINT('',#52871);
#11955=VERTEX_POINT('',#52875);
#11956=VERTEX_POINT('',#52877);
#11957=VERTEX_POINT('',#52881);
#11958=VERTEX_POINT('',#52883);
#11959=VERTEX_POINT('',#52887);
#11960=VERTEX_POINT('',#52889);
#11961=VERTEX_POINT('',#52893);
#11962=VERTEX_POINT('',#52895);
#11963=VERTEX_POINT('',#52899);
#11964=VERTEX_POINT('',#52901);
#11965=VERTEX_POINT('',#52905);
#11966=VERTEX_POINT('',#52907);
#11967=VERTEX_POINT('',#52911);
#11968=VERTEX_POINT('',#52913);
#11969=VERTEX_POINT('',#52917);
#11970=VERTEX_POINT('',#52919);
#11971=VERTEX_POINT('',#52923);
#11972=VERTEX_POINT('',#52925);
#11973=VERTEX_POINT('',#52929);
#11974=VERTEX_POINT('',#52931);
#11975=VERTEX_POINT('',#52935);
#11976=VERTEX_POINT('',#52937);
#11977=VERTEX_POINT('',#52941);
#11978=VERTEX_POINT('',#52943);
#11979=VERTEX_POINT('',#52947);
#11980=VERTEX_POINT('',#52949);
#11981=VERTEX_POINT('',#52953);
#11982=VERTEX_POINT('',#52955);
#11983=VERTEX_POINT('',#52959);
#11984=VERTEX_POINT('',#52961);
#11985=VERTEX_POINT('',#52965);
#11986=VERTEX_POINT('',#52967);
#11987=VERTEX_POINT('',#52971);
#11988=VERTEX_POINT('',#52973);
#11989=VERTEX_POINT('',#52977);
#11990=VERTEX_POINT('',#52979);
#11991=VERTEX_POINT('',#52983);
#11992=VERTEX_POINT('',#52985);
#11993=VERTEX_POINT('',#52989);
#11994=VERTEX_POINT('',#52991);
#11995=VERTEX_POINT('',#52995);
#11996=VERTEX_POINT('',#52997);
#11997=VERTEX_POINT('',#53001);
#11998=VERTEX_POINT('',#53003);
#11999=VERTEX_POINT('',#53007);
#12000=VERTEX_POINT('',#53009);
#12001=VERTEX_POINT('',#53013);
#12002=VERTEX_POINT('',#53015);
#12003=VERTEX_POINT('',#53019);
#12004=VERTEX_POINT('',#53021);
#12005=VERTEX_POINT('',#53025);
#12006=VERTEX_POINT('',#53027);
#12007=VERTEX_POINT('',#53031);
#12008=VERTEX_POINT('',#53033);
#12009=VERTEX_POINT('',#53037);
#12010=VERTEX_POINT('',#53039);
#12011=VERTEX_POINT('',#53043);
#12012=VERTEX_POINT('',#53045);
#12013=VERTEX_POINT('',#53049);
#12014=VERTEX_POINT('',#53051);
#12015=VERTEX_POINT('',#53055);
#12016=VERTEX_POINT('',#53057);
#12017=VERTEX_POINT('',#53061);
#12018=VERTEX_POINT('',#53063);
#12019=VERTEX_POINT('',#53067);
#12020=VERTEX_POINT('',#53069);
#12021=VERTEX_POINT('',#53073);
#12022=VERTEX_POINT('',#53075);
#12023=VERTEX_POINT('',#53079);
#12024=VERTEX_POINT('',#53081);
#12025=VERTEX_POINT('',#53085);
#12026=VERTEX_POINT('',#53087);
#12027=VERTEX_POINT('',#53091);
#12028=VERTEX_POINT('',#53093);
#12029=VERTEX_POINT('',#53097);
#12030=VERTEX_POINT('',#53099);
#12031=VERTEX_POINT('',#53103);
#12032=VERTEX_POINT('',#53105);
#12033=VERTEX_POINT('',#53109);
#12034=VERTEX_POINT('',#53111);
#12035=VERTEX_POINT('',#53115);
#12036=VERTEX_POINT('',#53117);
#12037=VERTEX_POINT('',#53121);
#12038=VERTEX_POINT('',#53123);
#12039=VERTEX_POINT('',#53127);
#12040=VERTEX_POINT('',#53129);
#12041=VERTEX_POINT('',#53133);
#12042=VERTEX_POINT('',#53135);
#12043=VERTEX_POINT('',#53139);
#12044=VERTEX_POINT('',#53141);
#12045=VERTEX_POINT('',#53145);
#12046=VERTEX_POINT('',#53147);
#12047=VERTEX_POINT('',#53151);
#12048=VERTEX_POINT('',#53153);
#12049=VERTEX_POINT('',#53157);
#12050=VERTEX_POINT('',#53159);
#12051=VERTEX_POINT('',#53163);
#12052=VERTEX_POINT('',#53165);
#12053=VERTEX_POINT('',#53169);
#12054=VERTEX_POINT('',#53171);
#12055=VERTEX_POINT('',#53175);
#12056=VERTEX_POINT('',#53177);
#12057=VERTEX_POINT('',#53181);
#12058=VERTEX_POINT('',#53183);
#12059=VERTEX_POINT('',#53187);
#12060=VERTEX_POINT('',#53189);
#12061=VERTEX_POINT('',#53193);
#12062=VERTEX_POINT('',#53195);
#12063=VERTEX_POINT('',#53199);
#12064=VERTEX_POINT('',#53201);
#12065=VERTEX_POINT('',#53205);
#12066=VERTEX_POINT('',#53207);
#12067=VERTEX_POINT('',#53211);
#12068=VERTEX_POINT('',#53213);
#12069=VERTEX_POINT('',#53217);
#12070=VERTEX_POINT('',#53219);
#12071=VERTEX_POINT('',#53223);
#12072=VERTEX_POINT('',#53225);
#12073=VERTEX_POINT('',#53229);
#12074=VERTEX_POINT('',#53231);
#12075=VERTEX_POINT('',#53235);
#12076=VERTEX_POINT('',#53237);
#12077=VERTEX_POINT('',#53241);
#12078=VERTEX_POINT('',#53243);
#12079=VERTEX_POINT('',#53247);
#12080=VERTEX_POINT('',#53249);
#12081=VERTEX_POINT('',#53253);
#12082=VERTEX_POINT('',#53255);
#12083=VERTEX_POINT('',#53259);
#12084=VERTEX_POINT('',#53261);
#12085=VERTEX_POINT('',#53265);
#12086=VERTEX_POINT('',#53267);
#12087=VERTEX_POINT('',#53271);
#12088=VERTEX_POINT('',#53273);
#12089=VERTEX_POINT('',#53277);
#12090=VERTEX_POINT('',#53279);
#12091=VERTEX_POINT('',#53283);
#12092=VERTEX_POINT('',#53285);
#12093=VERTEX_POINT('',#53289);
#12094=VERTEX_POINT('',#53291);
#12095=VERTEX_POINT('',#53295);
#12096=VERTEX_POINT('',#53297);
#12097=VERTEX_POINT('',#53301);
#12098=VERTEX_POINT('',#53303);
#12099=VERTEX_POINT('',#53307);
#12100=VERTEX_POINT('',#53309);
#12101=VERTEX_POINT('',#53313);
#12102=VERTEX_POINT('',#53315);
#12103=VERTEX_POINT('',#53319);
#12104=VERTEX_POINT('',#53321);
#12105=VERTEX_POINT('',#53325);
#12106=VERTEX_POINT('',#53327);
#12107=VERTEX_POINT('',#53331);
#12108=VERTEX_POINT('',#53333);
#12109=VERTEX_POINT('',#53337);
#12110=VERTEX_POINT('',#53339);
#12111=VERTEX_POINT('',#53343);
#12112=VERTEX_POINT('',#53345);
#12113=VERTEX_POINT('',#53349);
#12114=VERTEX_POINT('',#53351);
#12115=VERTEX_POINT('',#53355);
#12116=VERTEX_POINT('',#53357);
#12117=VERTEX_POINT('',#53361);
#12118=VERTEX_POINT('',#53363);
#12119=VERTEX_POINT('',#53367);
#12120=VERTEX_POINT('',#53369);
#12121=VERTEX_POINT('',#53373);
#12122=VERTEX_POINT('',#53375);
#12123=VERTEX_POINT('',#53379);
#12124=VERTEX_POINT('',#53381);
#12125=VERTEX_POINT('',#53385);
#12126=VERTEX_POINT('',#53387);
#12127=VERTEX_POINT('',#53391);
#12128=VERTEX_POINT('',#53393);
#12129=VERTEX_POINT('',#53397);
#12130=VERTEX_POINT('',#53399);
#12131=VERTEX_POINT('',#53403);
#12132=VERTEX_POINT('',#53405);
#12133=VERTEX_POINT('',#53409);
#12134=VERTEX_POINT('',#53411);
#12135=VERTEX_POINT('',#53415);
#12136=VERTEX_POINT('',#53417);
#12137=VERTEX_POINT('',#53421);
#12138=VERTEX_POINT('',#53423);
#12139=VERTEX_POINT('',#53427);
#12140=VERTEX_POINT('',#53429);
#12141=VERTEX_POINT('',#53433);
#12142=VERTEX_POINT('',#53435);
#12143=VERTEX_POINT('',#53439);
#12144=VERTEX_POINT('',#53441);
#12145=VERTEX_POINT('',#53445);
#12146=VERTEX_POINT('',#53447);
#12147=VERTEX_POINT('',#53451);
#12148=VERTEX_POINT('',#53453);
#12149=VERTEX_POINT('',#53457);
#12150=VERTEX_POINT('',#53459);
#12151=VERTEX_POINT('',#53463);
#12152=VERTEX_POINT('',#53465);
#12153=VERTEX_POINT('',#53469);
#12154=VERTEX_POINT('',#53471);
#12155=VERTEX_POINT('',#53475);
#12156=VERTEX_POINT('',#53477);
#12157=VERTEX_POINT('',#53481);
#12158=VERTEX_POINT('',#53483);
#12159=VERTEX_POINT('',#53487);
#12160=VERTEX_POINT('',#53489);
#12161=VERTEX_POINT('',#53493);
#12162=VERTEX_POINT('',#53495);
#12163=VERTEX_POINT('',#53499);
#12164=VERTEX_POINT('',#53501);
#12165=VERTEX_POINT('',#53505);
#12166=VERTEX_POINT('',#53507);
#12167=VERTEX_POINT('',#53511);
#12168=VERTEX_POINT('',#53513);
#12169=VERTEX_POINT('',#53517);
#12170=VERTEX_POINT('',#53519);
#12171=VERTEX_POINT('',#53523);
#12172=VERTEX_POINT('',#53525);
#12173=VERTEX_POINT('',#53529);
#12174=VERTEX_POINT('',#53531);
#12175=VERTEX_POINT('',#53535);
#12176=VERTEX_POINT('',#53537);
#12177=VERTEX_POINT('',#53541);
#12178=VERTEX_POINT('',#53543);
#12179=VERTEX_POINT('',#53547);
#12180=VERTEX_POINT('',#53549);
#12181=VERTEX_POINT('',#53553);
#12182=VERTEX_POINT('',#53555);
#12183=VERTEX_POINT('',#53559);
#12184=VERTEX_POINT('',#53561);
#12185=VERTEX_POINT('',#53565);
#12186=VERTEX_POINT('',#53567);
#12187=VERTEX_POINT('',#53571);
#12188=VERTEX_POINT('',#53573);
#12189=VERTEX_POINT('',#53577);
#12190=VERTEX_POINT('',#53579);
#12191=VERTEX_POINT('',#53583);
#12192=VERTEX_POINT('',#53585);
#12193=VERTEX_POINT('',#53589);
#12194=VERTEX_POINT('',#53591);
#12195=VERTEX_POINT('',#53595);
#12196=VERTEX_POINT('',#53597);
#12197=VERTEX_POINT('',#53601);
#12198=VERTEX_POINT('',#53603);
#12199=VERTEX_POINT('',#53607);
#12200=VERTEX_POINT('',#53609);
#12201=VERTEX_POINT('',#53613);
#12202=VERTEX_POINT('',#53615);
#12203=VERTEX_POINT('',#53619);
#12204=VERTEX_POINT('',#53621);
#12205=VERTEX_POINT('',#53625);
#12206=VERTEX_POINT('',#53627);
#12207=VERTEX_POINT('',#53631);
#12208=VERTEX_POINT('',#53633);
#12209=VERTEX_POINT('',#53637);
#12210=VERTEX_POINT('',#53639);
#12211=VERTEX_POINT('',#53643);
#12212=VERTEX_POINT('',#53645);
#12213=VERTEX_POINT('',#53649);
#12214=VERTEX_POINT('',#53651);
#12215=VERTEX_POINT('',#53655);
#12216=VERTEX_POINT('',#53657);
#12217=VERTEX_POINT('',#53661);
#12218=VERTEX_POINT('',#53663);
#12219=VERTEX_POINT('',#53667);
#12220=VERTEX_POINT('',#53669);
#12221=VERTEX_POINT('',#53673);
#12222=VERTEX_POINT('',#53675);
#12223=VERTEX_POINT('',#53679);
#12224=VERTEX_POINT('',#53681);
#12225=VERTEX_POINT('',#53685);
#12226=VERTEX_POINT('',#53687);
#12227=VERTEX_POINT('',#53691);
#12228=VERTEX_POINT('',#53693);
#12229=VERTEX_POINT('',#53697);
#12230=VERTEX_POINT('',#53699);
#12231=VERTEX_POINT('',#53703);
#12232=VERTEX_POINT('',#53705);
#12233=VERTEX_POINT('',#53709);
#12234=VERTEX_POINT('',#53711);
#12235=VERTEX_POINT('',#53715);
#12236=VERTEX_POINT('',#53717);
#12237=VERTEX_POINT('',#53721);
#12238=VERTEX_POINT('',#53723);
#12239=VERTEX_POINT('',#53727);
#12240=VERTEX_POINT('',#53729);
#12241=VERTEX_POINT('',#53733);
#12242=VERTEX_POINT('',#53735);
#12243=VERTEX_POINT('',#53739);
#12244=VERTEX_POINT('',#53741);
#12245=VERTEX_POINT('',#53745);
#12246=VERTEX_POINT('',#53747);
#12247=VERTEX_POINT('',#53751);
#12248=VERTEX_POINT('',#53753);
#12249=VERTEX_POINT('',#53757);
#12250=VERTEX_POINT('',#53759);
#12251=VERTEX_POINT('',#53763);
#12252=VERTEX_POINT('',#53765);
#12253=VERTEX_POINT('',#53769);
#12254=VERTEX_POINT('',#53771);
#12255=VERTEX_POINT('',#54014);
#12256=VERTEX_POINT('',#54016);
#12257=VERTEX_POINT('',#54020);
#12258=VERTEX_POINT('',#54022);
#12259=VERTEX_POINT('',#54030);
#12260=VERTEX_POINT('',#54031);
#12261=VERTEX_POINT('',#54033);
#12262=VERTEX_POINT('',#54035);
#12263=VERTEX_POINT('',#54037);
#12264=VERTEX_POINT('',#54039);
#14573=EDGE_CURVE('',#11156,#11157,#8656,.T.);
#14574=EDGE_CURVE('',#11158,#11156,#2974,.F.);
#14575=EDGE_CURVE('',#11158,#11159,#8657,.T.);
#14576=EDGE_CURVE('',#11159,#11159,#3435,.T.);
#14577=EDGE_CURVE('',#11160,#11158,#3436,.T.);
#14578=EDGE_CURVE('',#11157,#11160,#2975,.F.);
#14579=EDGE_CURVE('',#11161,#11162,#8658,.T.);
#14580=EDGE_CURVE('',#11156,#11161,#2976,.F.);
#14581=EDGE_CURVE('',#11162,#11157,#2977,.F.);
#14582=EDGE_CURVE('',#11163,#11164,#8659,.T.);
#14583=EDGE_CURVE('',#11161,#11163,#2978,.F.);
#14584=EDGE_CURVE('',#11164,#11162,#2979,.F.);
#14585=EDGE_CURVE('',#11165,#11166,#8660,.T.);
#14586=EDGE_CURVE('',#11163,#11165,#2980,.F.);
#14587=EDGE_CURVE('',#11166,#11164,#2981,.F.);
#14588=EDGE_CURVE('',#11167,#11168,#8661,.T.);
#14589=EDGE_CURVE('',#11165,#11167,#2982,.F.);
#14590=EDGE_CURVE('',#11168,#11166,#2983,.F.);
#14591=EDGE_CURVE('',#11169,#11170,#8662,.T.);
#14592=EDGE_CURVE('',#11167,#11169,#2984,.F.);
#14593=EDGE_CURVE('',#11170,#11168,#2985,.F.);
#14594=EDGE_CURVE('',#11171,#11172,#8663,.T.);
#14595=EDGE_CURVE('',#11169,#11171,#2986,.F.);
#14596=EDGE_CURVE('',#11172,#11170,#2987,.F.);
#14597=EDGE_CURVE('',#11173,#11174,#8664,.T.);
#14598=EDGE_CURVE('',#11171,#11173,#2988,.F.);
#14599=EDGE_CURVE('',#11174,#11172,#2989,.F.);
#14600=EDGE_CURVE('',#11175,#11176,#8665,.T.);
#14601=EDGE_CURVE('',#11173,#11175,#2990,.F.);
#14602=EDGE_CURVE('',#11176,#11174,#2991,.F.);
#14603=EDGE_CURVE('',#11177,#11178,#8666,.T.);
#14604=EDGE_CURVE('',#11175,#11177,#2992,.F.);
#14605=EDGE_CURVE('',#11178,#11176,#2993,.F.);
#14606=EDGE_CURVE('',#11179,#11180,#8667,.T.);
#14607=EDGE_CURVE('',#11177,#11179,#2994,.F.);
#14608=EDGE_CURVE('',#11180,#11178,#2995,.F.);
#14609=EDGE_CURVE('',#11181,#11182,#8668,.T.);
#14610=EDGE_CURVE('',#11179,#11181,#2996,.F.);
#14611=EDGE_CURVE('',#11182,#11180,#2997,.F.);
#14612=EDGE_CURVE('',#11183,#11184,#8669,.T.);
#14613=EDGE_CURVE('',#11181,#11183,#2998,.F.);
#14614=EDGE_CURVE('',#11184,#11182,#2999,.F.);
#14615=EDGE_CURVE('',#11185,#11186,#8670,.T.);
#14616=EDGE_CURVE('',#11183,#11185,#3000,.F.);
#14617=EDGE_CURVE('',#11186,#11184,#3001,.F.);
#14618=EDGE_CURVE('',#11187,#11188,#8671,.T.);
#14619=EDGE_CURVE('',#11185,#11187,#3002,.F.);
#14620=EDGE_CURVE('',#11188,#11186,#3003,.F.);
#14621=EDGE_CURVE('',#11189,#11190,#8672,.T.);
#14622=EDGE_CURVE('',#11187,#11189,#3004,.F.);
#14623=EDGE_CURVE('',#11190,#11188,#3005,.F.);
#14624=EDGE_CURVE('',#11191,#11192,#8673,.T.);
#14625=EDGE_CURVE('',#11189,#11191,#3006,.F.);
#14626=EDGE_CURVE('',#11192,#11190,#3007,.F.);
#14627=EDGE_CURVE('',#11193,#11194,#8674,.T.);
#14628=EDGE_CURVE('',#11191,#11193,#3008,.F.);
#14629=EDGE_CURVE('',#11194,#11192,#3009,.F.);
#14630=EDGE_CURVE('',#11195,#11196,#8675,.T.);
#14631=EDGE_CURVE('',#11193,#11195,#3010,.F.);
#14632=EDGE_CURVE('',#11196,#11194,#3011,.F.);
#14633=EDGE_CURVE('',#11197,#11198,#8676,.T.);
#14634=EDGE_CURVE('',#11195,#11197,#3012,.F.);
#14635=EDGE_CURVE('',#11198,#11196,#3013,.F.);
#14636=EDGE_CURVE('',#11199,#11200,#8677,.T.);
#14637=EDGE_CURVE('',#11197,#11199,#3014,.F.);
#14638=EDGE_CURVE('',#11200,#11198,#3015,.F.);
#14639=EDGE_CURVE('',#11201,#11202,#8678,.T.);
#14640=EDGE_CURVE('',#11199,#11201,#3016,.F.);
#14641=EDGE_CURVE('',#11202,#11200,#3017,.F.);
#14642=EDGE_CURVE('',#11203,#11204,#8679,.T.);
#14643=EDGE_CURVE('',#11201,#11203,#3018,.F.);
#14644=EDGE_CURVE('',#11204,#11202,#3019,.F.);
#14645=EDGE_CURVE('',#11205,#11206,#8680,.T.);
#14646=EDGE_CURVE('',#11203,#11205,#3020,.F.);
#14647=EDGE_CURVE('',#11206,#11204,#3021,.F.);
#14648=EDGE_CURVE('',#11207,#11208,#8681,.T.);
#14649=EDGE_CURVE('',#11205,#11207,#3022,.F.);
#14650=EDGE_CURVE('',#11208,#11206,#3023,.F.);
#14651=EDGE_CURVE('',#11209,#11210,#8682,.T.);
#14652=EDGE_CURVE('',#11207,#11209,#3024,.F.);
#14653=EDGE_CURVE('',#11210,#11208,#3025,.F.);
#14654=EDGE_CURVE('',#11211,#11212,#8683,.T.);
#14655=EDGE_CURVE('',#11209,#11211,#3026,.F.);
#14656=EDGE_CURVE('',#11212,#11210,#3027,.F.);
#14657=EDGE_CURVE('',#11213,#11214,#8684,.T.);
#14658=EDGE_CURVE('',#11211,#11213,#3028,.F.);
#14659=EDGE_CURVE('',#11214,#11212,#3029,.F.);
#14660=EDGE_CURVE('',#11215,#11216,#8685,.T.);
#14661=EDGE_CURVE('',#11215,#11217,#3030,.F.);
#14662=EDGE_CURVE('',#11216,#11217,#3437,.T.);
#14663=EDGE_CURVE('',#11218,#11217,#8686,.T.);
#14664=EDGE_CURVE('',#11219,#11218,#3031,.F.);
#14665=EDGE_CURVE('',#11217,#11219,#3438,.T.);
#14666=EDGE_CURVE('',#11220,#11221,#8687,.T.);
#14667=EDGE_CURVE('',#11218,#11220,#3032,.F.);
#14668=EDGE_CURVE('',#11217,#11221,#3033,.T.);
#14669=EDGE_CURVE('',#11222,#11223,#8688,.T.);
#14670=EDGE_CURVE('',#11220,#11222,#3034,.F.);
#14671=EDGE_CURVE('',#11221,#11223,#3035,.T.);
#14672=EDGE_CURVE('',#11224,#11225,#8689,.T.);
#14673=EDGE_CURVE('',#11222,#11224,#3036,.F.);
#14674=EDGE_CURVE('',#11223,#11225,#3037,.T.);
#14675=EDGE_CURVE('',#11226,#11227,#8690,.T.);
#14676=EDGE_CURVE('',#11224,#11226,#3038,.F.);
#14677=EDGE_CURVE('',#11225,#11227,#3039,.T.);
#14678=EDGE_CURVE('',#11228,#11229,#8691,.T.);
#14679=EDGE_CURVE('',#11226,#11228,#3040,.F.);
#14680=EDGE_CURVE('',#11227,#11229,#3041,.T.);
#14681=EDGE_CURVE('',#11230,#11231,#8692,.T.);
#14682=EDGE_CURVE('',#11228,#11230,#3042,.F.);
#14683=EDGE_CURVE('',#11229,#11231,#3043,.T.);
#14684=EDGE_CURVE('',#11232,#11233,#8693,.T.);
#14685=EDGE_CURVE('',#11230,#11232,#3044,.F.);
#14686=EDGE_CURVE('',#11231,#11233,#3045,.T.);
#14687=EDGE_CURVE('',#11234,#11235,#8694,.T.);
#14688=EDGE_CURVE('',#11232,#11234,#3046,.F.);
#14689=EDGE_CURVE('',#11233,#11235,#3047,.T.);
#14690=EDGE_CURVE('',#11236,#11237,#8695,.T.);
#14691=EDGE_CURVE('',#11234,#11236,#3048,.F.);
#14692=EDGE_CURVE('',#11235,#11237,#3049,.T.);
#14693=EDGE_CURVE('',#11238,#11239,#8696,.T.);
#14694=EDGE_CURVE('',#11236,#11238,#3050,.F.);
#14695=EDGE_CURVE('',#11237,#11239,#3051,.T.);
#14696=EDGE_CURVE('',#11240,#11241,#8697,.T.);
#14697=EDGE_CURVE('',#11238,#11240,#3052,.F.);
#14698=EDGE_CURVE('',#11239,#11241,#3053,.T.);
#14699=EDGE_CURVE('',#11242,#11243,#8698,.T.);
#14700=EDGE_CURVE('',#11240,#11242,#3054,.F.);
#14701=EDGE_CURVE('',#11241,#11243,#3055,.T.);
#14702=EDGE_CURVE('',#11244,#11245,#8699,.T.);
#14703=EDGE_CURVE('',#11242,#11244,#3056,.F.);
#14704=EDGE_CURVE('',#11243,#11245,#3057,.T.);
#14705=EDGE_CURVE('',#11246,#11247,#8700,.T.);
#14706=EDGE_CURVE('',#11244,#11246,#3058,.F.);
#14707=EDGE_CURVE('',#11245,#11247,#3059,.T.);
#14708=EDGE_CURVE('',#11248,#11249,#8701,.T.);
#14709=EDGE_CURVE('',#11246,#11248,#3060,.F.);
#14710=EDGE_CURVE('',#11247,#11249,#3061,.T.);
#14711=EDGE_CURVE('',#11250,#11251,#8702,.T.);
#14712=EDGE_CURVE('',#11248,#11250,#3062,.F.);
#14713=EDGE_CURVE('',#11249,#11251,#3063,.T.);
#14714=EDGE_CURVE('',#11252,#11253,#8703,.T.);
#14715=EDGE_CURVE('',#11250,#11252,#3064,.F.);
#14716=EDGE_CURVE('',#11251,#11253,#3065,.T.);
#14717=EDGE_CURVE('',#11254,#11255,#8704,.T.);
#14718=EDGE_CURVE('',#11252,#11254,#3066,.F.);
#14719=EDGE_CURVE('',#11253,#11255,#3067,.T.);
#14720=EDGE_CURVE('',#11256,#11257,#8705,.T.);
#14721=EDGE_CURVE('',#11254,#11256,#3068,.F.);
#14722=EDGE_CURVE('',#11255,#11257,#3069,.T.);
#14723=EDGE_CURVE('',#11258,#11259,#8706,.T.);
#14724=EDGE_CURVE('',#11256,#11258,#3070,.F.);
#14725=EDGE_CURVE('',#11257,#11259,#3071,.T.);
#14726=EDGE_CURVE('',#11260,#11261,#8707,.T.);
#14727=EDGE_CURVE('',#11258,#11260,#3072,.F.);
#14728=EDGE_CURVE('',#11259,#11261,#3073,.T.);
#14729=EDGE_CURVE('',#11262,#11263,#8708,.T.);
#14730=EDGE_CURVE('',#11260,#11262,#3074,.F.);
#14731=EDGE_CURVE('',#11261,#11263,#3075,.T.);
#14732=EDGE_CURVE('',#11264,#11265,#8709,.T.);
#14733=EDGE_CURVE('',#11262,#11264,#3076,.F.);
#14734=EDGE_CURVE('',#11263,#11265,#3077,.T.);
#14735=EDGE_CURVE('',#11266,#11267,#8710,.T.);
#14736=EDGE_CURVE('',#11264,#11266,#3078,.F.);
#14737=EDGE_CURVE('',#11265,#11267,#3079,.T.);
#14738=EDGE_CURVE('',#11268,#11269,#8711,.T.);
#14739=EDGE_CURVE('',#11266,#11268,#3080,.F.);
#14740=EDGE_CURVE('',#11267,#11269,#3081,.T.);
#14741=EDGE_CURVE('',#11270,#11271,#8712,.T.);
#14742=EDGE_CURVE('',#11268,#11270,#3082,.F.);
#14743=EDGE_CURVE('',#11269,#11271,#3083,.T.);
#14744=EDGE_CURVE('',#11272,#11273,#8713,.T.);
#14745=EDGE_CURVE('',#11270,#11272,#3084,.F.);
#14746=EDGE_CURVE('',#11271,#11273,#3085,.T.);
#14747=EDGE_CURVE('',#11274,#11275,#8714,.T.);
#14748=EDGE_CURVE('',#11272,#11274,#3086,.F.);
#14749=EDGE_CURVE('',#11273,#11275,#3087,.T.);
#14750=EDGE_CURVE('',#11276,#11277,#8715,.T.);
#14751=EDGE_CURVE('',#11274,#11276,#3088,.F.);
#14752=EDGE_CURVE('',#11275,#11277,#3089,.T.);
#14753=EDGE_CURVE('',#11277,#11278,#3090,.T.);
#14754=EDGE_CURVE('',#11276,#11278,#3439,.T.);
#14755=EDGE_CURVE('',#11219,#11216,#3440,.T.);
#14756=EDGE_CURVE('',#11219,#11279,#3091,.T.);
#14757=EDGE_CURVE('',#11279,#11280,#3441,.T.);
#14758=EDGE_CURVE('',#11280,#11215,#3092,.F.);
#14759=EDGE_CURVE('',#11280,#11214,#3093,.F.);
#14760=EDGE_CURVE('',#11213,#11279,#3094,.F.);
#14761=EDGE_CURVE('',#11281,#11282,#1522,.T.);
#14762=EDGE_CURVE('',#11282,#11283,#8716,.T.);
#14763=EDGE_CURVE('',#11283,#11284,#1523,.T.);
#14764=EDGE_CURVE('',#11281,#11284,#8717,.T.);
#14765=EDGE_CURVE('',#11285,#11286,#1524,.T.);
#14766=EDGE_CURVE('',#11286,#11287,#8718,.T.);
#14767=EDGE_CURVE('',#11287,#11288,#1525,.T.);
#14768=EDGE_CURVE('',#11285,#11288,#8719,.T.);
#14769=EDGE_CURVE('',#11289,#11290,#1526,.T.);
#14770=EDGE_CURVE('',#11290,#11291,#8720,.T.);
#14771=EDGE_CURVE('',#11291,#11292,#1527,.T.);
#14772=EDGE_CURVE('',#11289,#11292,#8721,.T.);
#14773=EDGE_CURVE('',#11293,#11294,#1528,.T.);
#14774=EDGE_CURVE('',#11294,#11295,#8722,.T.);
#14775=EDGE_CURVE('',#11295,#11296,#1529,.T.);
#14776=EDGE_CURVE('',#11293,#11296,#8723,.T.);
#14777=EDGE_CURVE('',#11297,#11298,#1530,.T.);
#14778=EDGE_CURVE('',#11298,#11299,#8724,.T.);
#14779=EDGE_CURVE('',#11299,#11300,#1531,.T.);
#14780=EDGE_CURVE('',#11297,#11300,#8725,.T.);
#14781=EDGE_CURVE('',#11301,#11302,#1532,.T.);
#14782=EDGE_CURVE('',#11302,#11303,#8726,.T.);
#14783=EDGE_CURVE('',#11303,#11304,#1533,.T.);
#14784=EDGE_CURVE('',#11301,#11304,#8727,.T.);
#14785=EDGE_CURVE('',#11305,#11306,#1534,.T.);
#14786=EDGE_CURVE('',#11306,#11307,#8728,.T.);
#14787=EDGE_CURVE('',#11307,#11308,#1535,.T.);
#14788=EDGE_CURVE('',#11305,#11308,#8729,.T.);
#14789=EDGE_CURVE('',#11309,#11310,#1536,.T.);
#14790=EDGE_CURVE('',#11310,#11311,#8730,.T.);
#14791=EDGE_CURVE('',#11311,#11312,#1537,.T.);
#14792=EDGE_CURVE('',#11309,#11312,#8731,.T.);
#14793=EDGE_CURVE('',#11313,#11314,#1538,.T.);
#14794=EDGE_CURVE('',#11314,#11315,#8732,.T.);
#14795=EDGE_CURVE('',#11315,#11316,#1539,.T.);
#14796=EDGE_CURVE('',#11313,#11316,#8733,.T.);
#14797=EDGE_CURVE('',#11317,#11318,#1540,.T.);
#14798=EDGE_CURVE('',#11318,#11319,#8734,.T.);
#14799=EDGE_CURVE('',#11319,#11320,#1541,.T.);
#14800=EDGE_CURVE('',#11317,#11320,#8735,.T.);
#14801=EDGE_CURVE('',#11321,#11322,#1542,.T.);
#14802=EDGE_CURVE('',#11322,#11323,#8736,.T.);
#14803=EDGE_CURVE('',#11323,#11324,#1543,.T.);
#14804=EDGE_CURVE('',#11321,#11324,#8737,.T.);
#14805=EDGE_CURVE('',#11325,#11326,#1544,.T.);
#14806=EDGE_CURVE('',#11326,#11327,#8738,.T.);
#14807=EDGE_CURVE('',#11327,#11328,#1545,.T.);
#14808=EDGE_CURVE('',#11325,#11328,#8739,.T.);
#14809=EDGE_CURVE('',#11329,#11330,#1546,.T.);
#14810=EDGE_CURVE('',#11330,#11331,#8740,.T.);
#14811=EDGE_CURVE('',#11331,#11332,#1547,.T.);
#14812=EDGE_CURVE('',#11329,#11332,#8741,.T.);
#14813=EDGE_CURVE('',#11333,#11334,#1548,.T.);
#14814=EDGE_CURVE('',#11334,#11335,#8742,.T.);
#14815=EDGE_CURVE('',#11335,#11336,#1549,.T.);
#14816=EDGE_CURVE('',#11333,#11336,#8743,.T.);
#14817=EDGE_CURVE('',#11337,#11338,#1550,.T.);
#14818=EDGE_CURVE('',#11338,#11339,#8744,.T.);
#14819=EDGE_CURVE('',#11339,#11340,#1551,.T.);
#14820=EDGE_CURVE('',#11337,#11340,#8745,.T.);
#14821=EDGE_CURVE('',#11341,#11342,#541,.T.);
#14822=EDGE_CURVE('',#11343,#11341,#542,.T.);
#14823=EDGE_CURVE('',#11344,#11343,#543,.T.);
#14824=EDGE_CURVE('',#11345,#11344,#544,.T.);
#14825=EDGE_CURVE('',#11346,#11345,#545,.T.);
#14826=EDGE_CURVE('',#11347,#11346,#546,.T.);
#14827=EDGE_CURVE('',#11342,#11347,#547,.T.);
#14828=EDGE_CURVE('',#11342,#11348,#8746,.T.);
#14829=EDGE_CURVE('',#11348,#11348,#3442,.T.);
#14830=EDGE_CURVE('',#11349,#11349,#3443,.T.);
#14831=EDGE_CURVE('',#11349,#11350,#3444,.T.);
#14832=EDGE_CURVE('',#11350,#11350,#3445,.T.);
#14833=EDGE_CURVE('',#11351,#11352,#3095,.T.);
#14834=EDGE_CURVE('',#11353,#11351,#548,.T.);
#14835=EDGE_CURVE('',#11354,#11353,#3446,.T.);
#14836=EDGE_CURVE('',#11355,#11354,#549,.T.);
#14837=EDGE_CURVE('',#11356,#11355,#1552,.T.);
#14838=EDGE_CURVE('',#11357,#11356,#550,.T.);
#14839=EDGE_CURVE('',#11358,#11357,#3447,.T.);
#14840=EDGE_CURVE('',#11359,#11358,#551,.T.);
#14841=EDGE_CURVE('',#11360,#11359,#1553,.T.);
#14842=EDGE_CURVE('',#11361,#11360,#552,.T.);
#14843=EDGE_CURVE('',#11362,#11361,#3448,.T.);
#14844=EDGE_CURVE('',#11363,#11362,#553,.T.);
#14845=EDGE_CURVE('',#11364,#11363,#1554,.T.);
#14846=EDGE_CURVE('',#11365,#11364,#554,.T.);
#14847=EDGE_CURVE('',#11366,#11365,#3449,.T.);
#14848=EDGE_CURVE('',#11367,#11366,#555,.T.);
#14849=EDGE_CURVE('',#11368,#11367,#1555,.T.);
#14850=EDGE_CURVE('',#11369,#11368,#556,.T.);
#14851=EDGE_CURVE('',#11370,#11369,#3450,.T.);
#14852=EDGE_CURVE('',#11371,#11370,#557,.T.);
#14853=EDGE_CURVE('',#11372,#11371,#1556,.T.);
#14854=EDGE_CURVE('',#11373,#11372,#558,.T.);
#14855=EDGE_CURVE('',#11374,#11373,#3451,.T.);
#14856=EDGE_CURVE('',#11375,#11374,#559,.T.);
#14857=EDGE_CURVE('',#11376,#11375,#1557,.T.);
#14858=EDGE_CURVE('',#11377,#11376,#560,.T.);
#14859=EDGE_CURVE('',#11378,#11377,#3452,.T.);
#14860=EDGE_CURVE('',#11379,#11378,#561,.T.);
#14861=EDGE_CURVE('',#11380,#11379,#1558,.T.);
#14862=EDGE_CURVE('',#11381,#11380,#562,.T.);
#14863=EDGE_CURVE('',#11382,#11381,#3453,.T.);
#14864=EDGE_CURVE('',#11383,#11382,#563,.T.);
#14865=EDGE_CURVE('',#11384,#11383,#1559,.T.);
#14866=EDGE_CURVE('',#11385,#11384,#564,.T.);
#14867=EDGE_CURVE('',#11386,#11385,#3454,.T.);
#14868=EDGE_CURVE('',#11387,#11386,#565,.T.);
#14869=EDGE_CURVE('',#11388,#11387,#1560,.T.);
#14870=EDGE_CURVE('',#11389,#11388,#566,.T.);
#14871=EDGE_CURVE('',#11390,#11389,#3455,.T.);
#14872=EDGE_CURVE('',#11391,#11390,#567,.T.);
#14873=EDGE_CURVE('',#11392,#11391,#1561,.T.);
#14874=EDGE_CURVE('',#11393,#11392,#568,.T.);
#14875=EDGE_CURVE('',#11394,#11393,#3456,.T.);
#14876=EDGE_CURVE('',#11395,#11394,#569,.T.);
#14877=EDGE_CURVE('',#11396,#11395,#1562,.T.);
#14878=EDGE_CURVE('',#11397,#11396,#570,.T.);
#14879=EDGE_CURVE('',#11398,#11397,#3457,.T.);
#14880=EDGE_CURVE('',#11399,#11398,#571,.T.);
#14881=EDGE_CURVE('',#11400,#11399,#1563,.T.);
#14882=EDGE_CURVE('',#11401,#11400,#572,.T.);
#14883=EDGE_CURVE('',#11402,#11401,#3458,.T.);
#14884=EDGE_CURVE('',#11403,#11402,#573,.T.);
#14885=EDGE_CURVE('',#11404,#11403,#1564,.T.);
#14886=EDGE_CURVE('',#11405,#11404,#574,.T.);
#14887=EDGE_CURVE('',#11406,#11405,#3459,.T.);
#14888=EDGE_CURVE('',#11407,#11406,#575,.T.);
#14889=EDGE_CURVE('',#11408,#11407,#1565,.T.);
#14890=EDGE_CURVE('',#11409,#11408,#576,.T.);
#14891=EDGE_CURVE('',#11410,#11409,#3460,.T.);
#14892=EDGE_CURVE('',#11411,#11410,#577,.T.);
#14893=EDGE_CURVE('',#11412,#11411,#1566,.T.);
#14894=EDGE_CURVE('',#11413,#11412,#578,.T.);
#14895=EDGE_CURVE('',#11414,#11413,#3461,.T.);
#14896=EDGE_CURVE('',#11415,#11414,#579,.T.);
#14897=EDGE_CURVE('',#11416,#11415,#1567,.T.);
#14898=EDGE_CURVE('',#11417,#11416,#580,.T.);
#14899=EDGE_CURVE('',#11418,#11417,#3462,.T.);
#14900=EDGE_CURVE('',#11419,#11418,#581,.T.);
#14901=EDGE_CURVE('',#11420,#11419,#1568,.T.);
#14902=EDGE_CURVE('',#11421,#11420,#582,.T.);
#14903=EDGE_CURVE('',#11422,#11421,#3463,.T.);
#14904=EDGE_CURVE('',#11423,#11422,#583,.T.);
#14905=EDGE_CURVE('',#11424,#11423,#1569,.T.);
#14906=EDGE_CURVE('',#11425,#11424,#584,.T.);
#14907=EDGE_CURVE('',#11426,#11425,#3464,.T.);
#14908=EDGE_CURVE('',#11427,#11426,#585,.T.);
#14909=EDGE_CURVE('',#11428,#11427,#1570,.T.);
#14910=EDGE_CURVE('',#11429,#11428,#586,.T.);
#14911=EDGE_CURVE('',#11430,#11429,#3465,.T.);
#14912=EDGE_CURVE('',#11431,#11430,#587,.T.);
#14913=EDGE_CURVE('',#11432,#11431,#1571,.T.);
#14914=EDGE_CURVE('',#11433,#11432,#588,.T.);
#14915=EDGE_CURVE('',#11434,#11433,#3466,.T.);
#14916=EDGE_CURVE('',#11435,#11434,#589,.T.);
#14917=EDGE_CURVE('',#11436,#11435,#1572,.T.);
#14918=EDGE_CURVE('',#11437,#11436,#590,.T.);
#14919=EDGE_CURVE('',#11438,#11437,#3467,.T.);
#14920=EDGE_CURVE('',#11439,#11438,#591,.T.);
#14921=EDGE_CURVE('',#11440,#11439,#1573,.T.);
#14922=EDGE_CURVE('',#11441,#11440,#592,.T.);
#14923=EDGE_CURVE('',#11442,#11441,#3468,.T.);
#14924=EDGE_CURVE('',#11443,#11442,#593,.T.);
#14925=EDGE_CURVE('',#11444,#11443,#1574,.T.);
#14926=EDGE_CURVE('',#11445,#11444,#594,.T.);
#14927=EDGE_CURVE('',#11446,#11445,#3469,.T.);
#14928=EDGE_CURVE('',#11447,#11446,#595,.T.);
#14929=EDGE_CURVE('',#11448,#11447,#1575,.T.);
#14930=EDGE_CURVE('',#11449,#11448,#596,.T.);
#14931=EDGE_CURVE('',#11450,#11449,#3470,.T.);
#14932=EDGE_CURVE('',#11451,#11450,#597,.T.);
#14933=EDGE_CURVE('',#11452,#11451,#1576,.T.);
#14934=EDGE_CURVE('',#11453,#11452,#598,.T.);
#14935=EDGE_CURVE('',#11454,#11453,#3471,.T.);
#14936=EDGE_CURVE('',#11455,#11454,#599,.T.);
#14937=EDGE_CURVE('',#11456,#11455,#1577,.T.);
#14938=EDGE_CURVE('',#11457,#11456,#600,.T.);
#14939=EDGE_CURVE('',#11458,#11457,#3472,.T.);
#14940=EDGE_CURVE('',#11459,#11458,#601,.T.);
#14941=EDGE_CURVE('',#11460,#11459,#1578,.T.);
#14942=EDGE_CURVE('',#11461,#11460,#602,.T.);
#14943=EDGE_CURVE('',#11462,#11461,#3473,.T.);
#14944=EDGE_CURVE('',#11463,#11462,#603,.T.);
#14945=EDGE_CURVE('',#11464,#11463,#1579,.T.);
#14946=EDGE_CURVE('',#11465,#11464,#604,.T.);
#14947=EDGE_CURVE('',#11466,#11465,#3474,.T.);
#14948=EDGE_CURVE('',#11467,#11466,#605,.T.);
#14949=EDGE_CURVE('',#11468,#11467,#1580,.T.);
#14950=EDGE_CURVE('',#11469,#11468,#606,.T.);
#14951=EDGE_CURVE('',#11470,#11469,#3475,.T.);
#14952=EDGE_CURVE('',#11471,#11470,#607,.T.);
#14953=EDGE_CURVE('',#11472,#11471,#1581,.T.);
#14954=EDGE_CURVE('',#11473,#11472,#608,.T.);
#14955=EDGE_CURVE('',#11474,#11473,#3476,.T.);
#14956=EDGE_CURVE('',#11475,#11474,#609,.T.);
#14957=EDGE_CURVE('',#11476,#11475,#1582,.T.);
#14958=EDGE_CURVE('',#11477,#11476,#610,.T.);
#14959=EDGE_CURVE('',#11478,#11477,#3477,.T.);
#14960=EDGE_CURVE('',#11479,#11478,#611,.T.);
#14961=EDGE_CURVE('',#11480,#11479,#1583,.T.);
#14962=EDGE_CURVE('',#11481,#11480,#612,.T.);
#14963=EDGE_CURVE('',#11482,#11481,#3478,.T.);
#14964=EDGE_CURVE('',#11483,#11482,#613,.T.);
#14965=EDGE_CURVE('',#11484,#11483,#1584,.T.);
#14966=EDGE_CURVE('',#11485,#11484,#614,.T.);
#14967=EDGE_CURVE('',#11486,#11485,#3479,.T.);
#14968=EDGE_CURVE('',#11487,#11486,#615,.T.);
#14969=EDGE_CURVE('',#11488,#11487,#1585,.T.);
#14970=EDGE_CURVE('',#11489,#11488,#616,.T.);
#14971=EDGE_CURVE('',#11490,#11489,#3480,.T.);
#14972=EDGE_CURVE('',#11491,#11490,#617,.T.);
#14973=EDGE_CURVE('',#11492,#11491,#1586,.T.);
#14974=EDGE_CURVE('',#11493,#11492,#618,.T.);
#14975=EDGE_CURVE('',#11494,#11493,#3481,.T.);
#14976=EDGE_CURVE('',#11495,#11494,#619,.T.);
#14977=EDGE_CURVE('',#11496,#11495,#1587,.T.);
#14978=EDGE_CURVE('',#11497,#11496,#620,.T.);
#14979=EDGE_CURVE('',#11498,#11497,#3482,.T.);
#14980=EDGE_CURVE('',#11499,#11498,#621,.T.);
#14981=EDGE_CURVE('',#11500,#11499,#1588,.T.);
#14982=EDGE_CURVE('',#11501,#11500,#622,.T.);
#14983=EDGE_CURVE('',#11502,#11501,#3483,.T.);
#14984=EDGE_CURVE('',#11503,#11502,#623,.T.);
#14985=EDGE_CURVE('',#11504,#11503,#1589,.T.);
#14986=EDGE_CURVE('',#11505,#11504,#624,.T.);
#14987=EDGE_CURVE('',#11506,#11505,#3484,.T.);
#14988=EDGE_CURVE('',#11507,#11506,#625,.T.);
#14989=EDGE_CURVE('',#11508,#11507,#1590,.T.);
#14990=EDGE_CURVE('',#11509,#11508,#626,.T.);
#14991=EDGE_CURVE('',#11510,#11509,#3485,.T.);
#14992=EDGE_CURVE('',#11511,#11510,#627,.T.);
#14993=EDGE_CURVE('',#11512,#11511,#1591,.T.);
#14994=EDGE_CURVE('',#11513,#11512,#628,.T.);
#14995=EDGE_CURVE('',#11514,#11513,#3486,.T.);
#14996=EDGE_CURVE('',#11515,#11514,#629,.T.);
#14997=EDGE_CURVE('',#11516,#11515,#1592,.T.);
#14998=EDGE_CURVE('',#11517,#11516,#630,.T.);
#14999=EDGE_CURVE('',#11518,#11517,#3487,.T.);
#15000=EDGE_CURVE('',#11519,#11518,#631,.T.);
#15001=EDGE_CURVE('',#11520,#11519,#1593,.T.);
#15002=EDGE_CURVE('',#11521,#11520,#632,.T.);
#15003=EDGE_CURVE('',#11522,#11521,#3488,.T.);
#15004=EDGE_CURVE('',#11523,#11522,#633,.T.);
#15005=EDGE_CURVE('',#11524,#11523,#1594,.T.);
#15006=EDGE_CURVE('',#11525,#11524,#634,.T.);
#15007=EDGE_CURVE('',#11526,#11525,#3489,.T.);
#15008=EDGE_CURVE('',#11527,#11526,#635,.T.);
#15009=EDGE_CURVE('',#11528,#11527,#1595,.T.);
#15010=EDGE_CURVE('',#11529,#11528,#636,.T.);
#15011=EDGE_CURVE('',#11530,#11529,#3490,.T.);
#15012=EDGE_CURVE('',#11531,#11530,#637,.T.);
#15013=EDGE_CURVE('',#11532,#11531,#1596,.T.);
#15014=EDGE_CURVE('',#11533,#11532,#638,.T.);
#15015=EDGE_CURVE('',#11534,#11533,#3491,.T.);
#15016=EDGE_CURVE('',#11340,#11534,#639,.T.);
#15017=EDGE_CURVE('',#11535,#11339,#640,.T.);
#15018=EDGE_CURVE('',#11536,#11535,#3492,.T.);
#15019=EDGE_CURVE('',#11336,#11536,#641,.T.);
#15020=EDGE_CURVE('',#11537,#11335,#642,.T.);
#15021=EDGE_CURVE('',#11538,#11537,#3493,.T.);
#15022=EDGE_CURVE('',#11332,#11538,#643,.T.);
#15023=EDGE_CURVE('',#11539,#11331,#644,.T.);
#15024=EDGE_CURVE('',#11540,#11539,#3494,.T.);
#15025=EDGE_CURVE('',#11328,#11540,#645,.T.);
#15026=EDGE_CURVE('',#11541,#11327,#646,.T.);
#15027=EDGE_CURVE('',#11542,#11541,#3495,.T.);
#15028=EDGE_CURVE('',#11324,#11542,#647,.T.);
#15029=EDGE_CURVE('',#11543,#11323,#648,.T.);
#15030=EDGE_CURVE('',#11544,#11543,#3496,.T.);
#15031=EDGE_CURVE('',#11320,#11544,#649,.T.);
#15032=EDGE_CURVE('',#11545,#11319,#650,.T.);
#15033=EDGE_CURVE('',#11546,#11545,#3497,.T.);
#15034=EDGE_CURVE('',#11316,#11546,#651,.T.);
#15035=EDGE_CURVE('',#11547,#11315,#652,.T.);
#15036=EDGE_CURVE('',#11548,#11547,#3498,.T.);
#15037=EDGE_CURVE('',#11312,#11548,#653,.T.);
#15038=EDGE_CURVE('',#11549,#11311,#654,.T.);
#15039=EDGE_CURVE('',#11550,#11549,#3499,.T.);
#15040=EDGE_CURVE('',#11308,#11550,#655,.T.);
#15041=EDGE_CURVE('',#11551,#11307,#656,.T.);
#15042=EDGE_CURVE('',#11552,#11551,#3500,.T.);
#15043=EDGE_CURVE('',#11284,#11552,#657,.T.);
#15044=EDGE_CURVE('',#11553,#11283,#658,.T.);
#15045=EDGE_CURVE('',#11554,#11553,#3501,.T.);
#15046=EDGE_CURVE('',#11288,#11554,#659,.T.);
#15047=EDGE_CURVE('',#11555,#11287,#660,.T.);
#15048=EDGE_CURVE('',#11556,#11555,#3502,.T.);
#15049=EDGE_CURVE('',#11292,#11556,#661,.T.);
#15050=EDGE_CURVE('',#11557,#11291,#662,.T.);
#15051=EDGE_CURVE('',#11558,#11557,#3503,.T.);
#15052=EDGE_CURVE('',#11296,#11558,#663,.T.);
#15053=EDGE_CURVE('',#11559,#11295,#664,.T.);
#15054=EDGE_CURVE('',#11560,#11559,#3504,.T.);
#15055=EDGE_CURVE('',#11300,#11560,#665,.T.);
#15056=EDGE_CURVE('',#11561,#11299,#666,.T.);
#15057=EDGE_CURVE('',#11562,#11561,#3505,.T.);
#15058=EDGE_CURVE('',#11304,#11562,#667,.T.);
#15059=EDGE_CURVE('',#11563,#11303,#668,.T.);
#15060=EDGE_CURVE('',#11564,#11563,#3506,.T.);
#15061=EDGE_CURVE('',#11565,#11564,#669,.T.);
#15062=EDGE_CURVE('',#11566,#11565,#1597,.T.);
#15063=EDGE_CURVE('',#11567,#11566,#670,.T.);
#15064=EDGE_CURVE('',#11568,#11567,#3507,.T.);
#15065=EDGE_CURVE('',#11569,#11568,#671,.T.);
#15066=EDGE_CURVE('',#11570,#11569,#1598,.T.);
#15067=EDGE_CURVE('',#11571,#11570,#672,.T.);
#15068=EDGE_CURVE('',#11572,#11571,#3508,.T.);
#15069=EDGE_CURVE('',#11573,#11572,#673,.T.);
#15070=EDGE_CURVE('',#11574,#11573,#1599,.T.);
#15071=EDGE_CURVE('',#11575,#11574,#674,.T.);
#15072=EDGE_CURVE('',#11576,#11575,#3509,.T.);
#15073=EDGE_CURVE('',#11577,#11576,#675,.T.);
#15074=EDGE_CURVE('',#11578,#11577,#1600,.T.);
#15075=EDGE_CURVE('',#11579,#11578,#676,.T.);
#15076=EDGE_CURVE('',#11580,#11579,#3510,.T.);
#15077=EDGE_CURVE('',#11581,#11580,#677,.T.);
#15078=EDGE_CURVE('',#11582,#11581,#1601,.T.);
#15079=EDGE_CURVE('',#11583,#11582,#678,.T.);
#15080=EDGE_CURVE('',#11584,#11583,#3511,.T.);
#15081=EDGE_CURVE('',#11585,#11584,#679,.T.);
#15082=EDGE_CURVE('',#11586,#11585,#1602,.T.);
#15083=EDGE_CURVE('',#11587,#11586,#680,.T.);
#15084=EDGE_CURVE('',#11588,#11587,#3512,.T.);
#15085=EDGE_CURVE('',#11589,#11588,#681,.T.);
#15086=EDGE_CURVE('',#11590,#11589,#1603,.T.);
#15087=EDGE_CURVE('',#11591,#11590,#682,.T.);
#15088=EDGE_CURVE('',#11592,#11591,#3513,.T.);
#15089=EDGE_CURVE('',#11593,#11592,#683,.T.);
#15090=EDGE_CURVE('',#11594,#11593,#1604,.T.);
#15091=EDGE_CURVE('',#11595,#11594,#684,.T.);
#15092=EDGE_CURVE('',#11596,#11595,#3514,.T.);
#15093=EDGE_CURVE('',#11597,#11596,#685,.T.);
#15094=EDGE_CURVE('',#11598,#11597,#1605,.T.);
#15095=EDGE_CURVE('',#11599,#11598,#686,.T.);
#15096=EDGE_CURVE('',#11600,#11599,#3515,.T.);
#15097=EDGE_CURVE('',#11601,#11600,#687,.T.);
#15098=EDGE_CURVE('',#11602,#11601,#1606,.T.);
#15099=EDGE_CURVE('',#11603,#11602,#688,.T.);
#15100=EDGE_CURVE('',#11604,#11603,#3516,.T.);
#15101=EDGE_CURVE('',#11605,#11604,#689,.T.);
#15102=EDGE_CURVE('',#11606,#11605,#1607,.T.);
#15103=EDGE_CURVE('',#11607,#11606,#690,.T.);
#15104=EDGE_CURVE('',#11608,#11607,#3517,.T.);
#15105=EDGE_CURVE('',#11609,#11608,#691,.T.);
#15106=EDGE_CURVE('',#11610,#11609,#1608,.T.);
#15107=EDGE_CURVE('',#11611,#11610,#692,.T.);
#15108=EDGE_CURVE('',#11612,#11611,#3518,.T.);
#15109=EDGE_CURVE('',#11613,#11612,#693,.T.);
#15110=EDGE_CURVE('',#11614,#11613,#1609,.T.);
#15111=EDGE_CURVE('',#11615,#11614,#694,.T.);
#15112=EDGE_CURVE('',#11616,#11615,#3519,.T.);
#15113=EDGE_CURVE('',#11617,#11616,#695,.T.);
#15114=EDGE_CURVE('',#11618,#11617,#1610,.T.);
#15115=EDGE_CURVE('',#11619,#11618,#696,.T.);
#15116=EDGE_CURVE('',#11620,#11619,#3520,.T.);
#15117=EDGE_CURVE('',#11621,#11620,#697,.T.);
#15118=EDGE_CURVE('',#11622,#11621,#1611,.T.);
#15119=EDGE_CURVE('',#11623,#11622,#698,.T.);
#15120=EDGE_CURVE('',#11624,#11623,#3521,.T.);
#15121=EDGE_CURVE('',#11625,#11624,#699,.T.);
#15122=EDGE_CURVE('',#11626,#11625,#1612,.T.);
#15123=EDGE_CURVE('',#11627,#11626,#700,.T.);
#15124=EDGE_CURVE('',#11628,#11627,#3522,.T.);
#15125=EDGE_CURVE('',#11629,#11628,#701,.T.);
#15126=EDGE_CURVE('',#11630,#11629,#1613,.T.);
#15127=EDGE_CURVE('',#11631,#11630,#702,.T.);
#15128=EDGE_CURVE('',#11632,#11631,#3523,.T.);
#15129=EDGE_CURVE('',#11633,#11632,#703,.T.);
#15130=EDGE_CURVE('',#11634,#11633,#1614,.T.);
#15131=EDGE_CURVE('',#11635,#11634,#704,.T.);
#15132=EDGE_CURVE('',#11636,#11635,#3524,.T.);
#15133=EDGE_CURVE('',#11637,#11636,#705,.T.);
#15134=EDGE_CURVE('',#11638,#11637,#1615,.T.);
#15135=EDGE_CURVE('',#11639,#11638,#706,.T.);
#15136=EDGE_CURVE('',#11640,#11639,#3525,.T.);
#15137=EDGE_CURVE('',#11641,#11640,#707,.T.);
#15138=EDGE_CURVE('',#11352,#11641,#3096,.T.);
#15139=EDGE_CURVE('',#11352,#11349,#8747,.T.);
#15140=EDGE_CURVE('',#11642,#11643,#3097,.T.);
#15141=EDGE_CURVE('',#11644,#11642,#708,.T.);
#15142=EDGE_CURVE('',#11644,#11645,#3526,.T.);
#15143=EDGE_CURVE('',#11646,#11645,#709,.T.);
#15144=EDGE_CURVE('',#11647,#11646,#1616,.T.);
#15145=EDGE_CURVE('',#11648,#11647,#710,.T.);
#15146=EDGE_CURVE('',#11648,#11649,#3527,.T.);
#15147=EDGE_CURVE('',#11650,#11649,#711,.T.);
#15148=EDGE_CURVE('',#11651,#11650,#1617,.T.);
#15149=EDGE_CURVE('',#11652,#11651,#712,.T.);
#15150=EDGE_CURVE('',#11652,#11653,#3528,.T.);
#15151=EDGE_CURVE('',#11654,#11653,#713,.T.);
#15152=EDGE_CURVE('',#11655,#11654,#1618,.T.);
#15153=EDGE_CURVE('',#11656,#11655,#714,.T.);
#15154=EDGE_CURVE('',#11656,#11657,#3529,.T.);
#15155=EDGE_CURVE('',#11658,#11657,#715,.T.);
#15156=EDGE_CURVE('',#11659,#11658,#1619,.T.);
#15157=EDGE_CURVE('',#11660,#11659,#716,.T.);
#15158=EDGE_CURVE('',#11660,#11661,#3530,.T.);
#15159=EDGE_CURVE('',#11662,#11661,#717,.T.);
#15160=EDGE_CURVE('',#11663,#11662,#1620,.T.);
#15161=EDGE_CURVE('',#11664,#11663,#718,.T.);
#15162=EDGE_CURVE('',#11664,#11665,#3531,.T.);
#15163=EDGE_CURVE('',#11666,#11665,#719,.T.);
#15164=EDGE_CURVE('',#11667,#11666,#1621,.T.);
#15165=EDGE_CURVE('',#11668,#11667,#720,.T.);
#15166=EDGE_CURVE('',#11668,#11669,#3532,.T.);
#15167=EDGE_CURVE('',#11670,#11669,#721,.T.);
#15168=EDGE_CURVE('',#11671,#11670,#1622,.T.);
#15169=EDGE_CURVE('',#11672,#11671,#722,.T.);
#15170=EDGE_CURVE('',#11672,#11673,#3533,.T.);
#15171=EDGE_CURVE('',#11674,#11673,#723,.T.);
#15172=EDGE_CURVE('',#11675,#11674,#1623,.T.);
#15173=EDGE_CURVE('',#11676,#11675,#724,.T.);
#15174=EDGE_CURVE('',#11676,#11677,#3534,.T.);
#15175=EDGE_CURVE('',#11678,#11677,#725,.T.);
#15176=EDGE_CURVE('',#11679,#11678,#1624,.T.);
#15177=EDGE_CURVE('',#11680,#11679,#726,.T.);
#15178=EDGE_CURVE('',#11680,#11681,#3535,.T.);
#15179=EDGE_CURVE('',#11682,#11681,#727,.T.);
#15180=EDGE_CURVE('',#11683,#11682,#1625,.T.);
#15181=EDGE_CURVE('',#11684,#11683,#728,.T.);
#15182=EDGE_CURVE('',#11684,#11685,#3536,.T.);
#15183=EDGE_CURVE('',#11686,#11685,#729,.T.);
#15184=EDGE_CURVE('',#11687,#11686,#1626,.T.);
#15185=EDGE_CURVE('',#11688,#11687,#730,.T.);
#15186=EDGE_CURVE('',#11688,#11689,#3537,.T.);
#15187=EDGE_CURVE('',#11690,#11689,#731,.T.);
#15188=EDGE_CURVE('',#11691,#11690,#1627,.T.);
#15189=EDGE_CURVE('',#11692,#11691,#732,.T.);
#15190=EDGE_CURVE('',#11692,#11693,#3538,.T.);
#15191=EDGE_CURVE('',#11694,#11693,#733,.T.);
#15192=EDGE_CURVE('',#11695,#11694,#1628,.T.);
#15193=EDGE_CURVE('',#11696,#11695,#734,.T.);
#15194=EDGE_CURVE('',#11696,#11697,#3539,.T.);
#15195=EDGE_CURVE('',#11698,#11697,#735,.T.);
#15196=EDGE_CURVE('',#11699,#11698,#1629,.T.);
#15197=EDGE_CURVE('',#11700,#11699,#736,.T.);
#15198=EDGE_CURVE('',#11700,#11701,#3540,.T.);
#15199=EDGE_CURVE('',#11702,#11701,#737,.T.);
#15200=EDGE_CURVE('',#11703,#11702,#1630,.T.);
#15201=EDGE_CURVE('',#11704,#11703,#738,.T.);
#15202=EDGE_CURVE('',#11704,#11705,#3541,.T.);
#15203=EDGE_CURVE('',#11706,#11705,#739,.T.);
#15204=EDGE_CURVE('',#11707,#11706,#1631,.T.);
#15205=EDGE_CURVE('',#11708,#11707,#740,.T.);
#15206=EDGE_CURVE('',#11708,#11709,#3542,.T.);
#15207=EDGE_CURVE('',#11710,#11709,#741,.T.);
#15208=EDGE_CURVE('',#11711,#11710,#1632,.T.);
#15209=EDGE_CURVE('',#11712,#11711,#742,.T.);
#15210=EDGE_CURVE('',#11712,#11713,#3543,.T.);
#15211=EDGE_CURVE('',#11714,#11713,#743,.T.);
#15212=EDGE_CURVE('',#11715,#11714,#1633,.T.);
#15213=EDGE_CURVE('',#11716,#11715,#744,.T.);
#15214=EDGE_CURVE('',#11716,#11717,#3544,.T.);
#15215=EDGE_CURVE('',#11718,#11717,#745,.T.);
#15216=EDGE_CURVE('',#11719,#11718,#1634,.T.);
#15217=EDGE_CURVE('',#11720,#11719,#746,.T.);
#15218=EDGE_CURVE('',#11720,#11721,#3545,.T.);
#15219=EDGE_CURVE('',#11722,#11721,#747,.T.);
#15220=EDGE_CURVE('',#11723,#11722,#1635,.T.);
#15221=EDGE_CURVE('',#11724,#11723,#748,.T.);
#15222=EDGE_CURVE('',#11724,#11725,#3546,.T.);
#15223=EDGE_CURVE('',#11726,#11725,#749,.T.);
#15224=EDGE_CURVE('',#11727,#11726,#1636,.T.);
#15225=EDGE_CURVE('',#11728,#11727,#750,.T.);
#15226=EDGE_CURVE('',#11728,#11729,#3547,.T.);
#15227=EDGE_CURVE('',#11730,#11729,#751,.T.);
#15228=EDGE_CURVE('',#11731,#11730,#1637,.T.);
#15229=EDGE_CURVE('',#11732,#11731,#752,.T.);
#15230=EDGE_CURVE('',#11732,#11733,#3548,.T.);
#15231=EDGE_CURVE('',#11734,#11733,#753,.T.);
#15232=EDGE_CURVE('',#11735,#11734,#1638,.T.);
#15233=EDGE_CURVE('',#11736,#11735,#754,.T.);
#15234=EDGE_CURVE('',#11736,#11737,#3549,.T.);
#15235=EDGE_CURVE('',#11738,#11737,#755,.T.);
#15236=EDGE_CURVE('',#11739,#11738,#1639,.T.);
#15237=EDGE_CURVE('',#11740,#11739,#756,.T.);
#15238=EDGE_CURVE('',#11740,#11741,#3550,.T.);
#15239=EDGE_CURVE('',#11742,#11741,#757,.T.);
#15240=EDGE_CURVE('',#11743,#11742,#1640,.T.);
#15241=EDGE_CURVE('',#11744,#11743,#758,.T.);
#15242=EDGE_CURVE('',#11744,#11745,#3551,.T.);
#15243=EDGE_CURVE('',#11746,#11745,#759,.T.);
#15244=EDGE_CURVE('',#11747,#11746,#1641,.T.);
#15245=EDGE_CURVE('',#11748,#11747,#760,.T.);
#15246=EDGE_CURVE('',#11748,#11749,#3552,.T.);
#15247=EDGE_CURVE('',#11750,#11749,#761,.T.);
#15248=EDGE_CURVE('',#11751,#11750,#1642,.T.);
#15249=EDGE_CURVE('',#11752,#11751,#762,.T.);
#15250=EDGE_CURVE('',#11752,#11753,#3553,.T.);
#15251=EDGE_CURVE('',#11754,#11753,#763,.T.);
#15252=EDGE_CURVE('',#11755,#11754,#1643,.T.);
#15253=EDGE_CURVE('',#11756,#11755,#764,.T.);
#15254=EDGE_CURVE('',#11756,#11757,#3554,.T.);
#15255=EDGE_CURVE('',#11758,#11757,#765,.T.);
#15256=EDGE_CURVE('',#11759,#11758,#1644,.T.);
#15257=EDGE_CURVE('',#11760,#11759,#766,.T.);
#15258=EDGE_CURVE('',#11760,#11761,#3555,.T.);
#15259=EDGE_CURVE('',#11762,#11761,#767,.T.);
#15260=EDGE_CURVE('',#11763,#11762,#1645,.T.);
#15261=EDGE_CURVE('',#11764,#11763,#768,.T.);
#15262=EDGE_CURVE('',#11764,#11765,#3556,.T.);
#15263=EDGE_CURVE('',#11766,#11765,#769,.T.);
#15264=EDGE_CURVE('',#11767,#11766,#1646,.T.);
#15265=EDGE_CURVE('',#11768,#11767,#770,.T.);
#15266=EDGE_CURVE('',#11768,#11769,#3557,.T.);
#15267=EDGE_CURVE('',#11770,#11769,#771,.T.);
#15268=EDGE_CURVE('',#11771,#11770,#1647,.T.);
#15269=EDGE_CURVE('',#11772,#11771,#772,.T.);
#15270=EDGE_CURVE('',#11772,#11773,#3558,.T.);
#15271=EDGE_CURVE('',#11774,#11773,#773,.T.);
#15272=EDGE_CURVE('',#11775,#11774,#1648,.T.);
#15273=EDGE_CURVE('',#11776,#11775,#774,.T.);
#15274=EDGE_CURVE('',#11776,#11777,#3559,.T.);
#15275=EDGE_CURVE('',#11778,#11777,#775,.T.);
#15276=EDGE_CURVE('',#11779,#11778,#1649,.T.);
#15277=EDGE_CURVE('',#11780,#11779,#776,.T.);
#15278=EDGE_CURVE('',#11780,#11781,#3560,.T.);
#15279=EDGE_CURVE('',#11782,#11781,#777,.T.);
#15280=EDGE_CURVE('',#11783,#11782,#1650,.T.);
#15281=EDGE_CURVE('',#11784,#11783,#778,.T.);
#15282=EDGE_CURVE('',#11784,#11785,#3561,.T.);
#15283=EDGE_CURVE('',#11786,#11785,#779,.T.);
#15284=EDGE_CURVE('',#11787,#11786,#1651,.T.);
#15285=EDGE_CURVE('',#11788,#11787,#780,.T.);
#15286=EDGE_CURVE('',#11788,#11789,#3562,.T.);
#15287=EDGE_CURVE('',#11790,#11789,#781,.T.);
#15288=EDGE_CURVE('',#11791,#11790,#1652,.T.);
#15289=EDGE_CURVE('',#11792,#11791,#782,.T.);
#15290=EDGE_CURVE('',#11792,#11793,#3563,.T.);
#15291=EDGE_CURVE('',#11794,#11793,#783,.T.);
#15292=EDGE_CURVE('',#11795,#11794,#1653,.T.);
#15293=EDGE_CURVE('',#11796,#11795,#784,.T.);
#15294=EDGE_CURVE('',#11796,#11797,#3564,.T.);
#15295=EDGE_CURVE('',#11798,#11797,#785,.T.);
#15296=EDGE_CURVE('',#11799,#11798,#1654,.T.);
#15297=EDGE_CURVE('',#11800,#11799,#786,.T.);
#15298=EDGE_CURVE('',#11800,#11801,#3565,.T.);
#15299=EDGE_CURVE('',#11802,#11801,#787,.T.);
#15300=EDGE_CURVE('',#11803,#11802,#1655,.T.);
#15301=EDGE_CURVE('',#11804,#11803,#788,.T.);
#15302=EDGE_CURVE('',#11804,#11805,#3566,.T.);
#15303=EDGE_CURVE('',#11806,#11805,#789,.T.);
#15304=EDGE_CURVE('',#11807,#11806,#1656,.T.);
#15305=EDGE_CURVE('',#11808,#11807,#790,.T.);
#15306=EDGE_CURVE('',#11808,#11809,#3567,.T.);
#15307=EDGE_CURVE('',#11810,#11809,#791,.T.);
#15308=EDGE_CURVE('',#11811,#11810,#1657,.T.);
#15309=EDGE_CURVE('',#11812,#11811,#792,.T.);
#15310=EDGE_CURVE('',#11812,#11813,#3568,.T.);
#15311=EDGE_CURVE('',#11814,#11813,#793,.T.);
#15312=EDGE_CURVE('',#11815,#11814,#1658,.T.);
#15313=EDGE_CURVE('',#11816,#11815,#794,.T.);
#15314=EDGE_CURVE('',#11816,#11817,#3569,.T.);
#15315=EDGE_CURVE('',#11818,#11817,#795,.T.);
#15316=EDGE_CURVE('',#11819,#11818,#1659,.T.);
#15317=EDGE_CURVE('',#11820,#11819,#796,.T.);
#15318=EDGE_CURVE('',#11820,#11821,#3570,.T.);
#15319=EDGE_CURVE('',#11822,#11821,#797,.T.);
#15320=EDGE_CURVE('',#11823,#11822,#1660,.T.);
#15321=EDGE_CURVE('',#11824,#11823,#798,.T.);
#15322=EDGE_CURVE('',#11824,#11825,#3571,.T.);
#15323=EDGE_CURVE('',#11826,#11825,#799,.T.);
#15324=EDGE_CURVE('',#11827,#11826,#1661,.T.);
#15325=EDGE_CURVE('',#11828,#11827,#800,.T.);
#15326=EDGE_CURVE('',#11828,#11829,#3572,.T.);
#15327=EDGE_CURVE('',#11830,#11829,#801,.T.);
#15328=EDGE_CURVE('',#11831,#11830,#1662,.T.);
#15329=EDGE_CURVE('',#11832,#11831,#802,.T.);
#15330=EDGE_CURVE('',#11832,#11833,#3573,.T.);
#15331=EDGE_CURVE('',#11834,#11833,#803,.T.);
#15332=EDGE_CURVE('',#11835,#11834,#1663,.T.);
#15333=EDGE_CURVE('',#11836,#11835,#804,.T.);
#15334=EDGE_CURVE('',#11836,#11837,#3574,.T.);
#15335=EDGE_CURVE('',#11838,#11837,#805,.T.);
#15336=EDGE_CURVE('',#11839,#11838,#1664,.T.);
#15337=EDGE_CURVE('',#11840,#11839,#806,.T.);
#15338=EDGE_CURVE('',#11840,#11841,#3575,.T.);
#15339=EDGE_CURVE('',#11842,#11841,#807,.T.);
#15340=EDGE_CURVE('',#11843,#11842,#1665,.T.);
#15341=EDGE_CURVE('',#11844,#11843,#808,.T.);
#15342=EDGE_CURVE('',#11844,#11845,#3576,.T.);
#15343=EDGE_CURVE('',#11846,#11845,#809,.T.);
#15344=EDGE_CURVE('',#11847,#11846,#1666,.T.);
#15345=EDGE_CURVE('',#11848,#11847,#810,.T.);
#15346=EDGE_CURVE('',#11848,#11849,#3577,.T.);
#15347=EDGE_CURVE('',#11850,#11849,#811,.T.);
#15348=EDGE_CURVE('',#11851,#11850,#1667,.T.);
#15349=EDGE_CURVE('',#11852,#11851,#812,.T.);
#15350=EDGE_CURVE('',#11852,#11853,#3578,.T.);
#15351=EDGE_CURVE('',#11854,#11853,#813,.T.);
#15352=EDGE_CURVE('',#11855,#11854,#1668,.T.);
#15353=EDGE_CURVE('',#11856,#11855,#814,.T.);
#15354=EDGE_CURVE('',#11856,#11857,#3579,.T.);
#15355=EDGE_CURVE('',#11858,#11857,#815,.T.);
#15356=EDGE_CURVE('',#11859,#11858,#1669,.T.);
#15357=EDGE_CURVE('',#11860,#11859,#816,.T.);
#15358=EDGE_CURVE('',#11860,#11861,#3580,.T.);
#15359=EDGE_CURVE('',#11862,#11861,#817,.T.);
#15360=EDGE_CURVE('',#11863,#11862,#1670,.T.);
#15361=EDGE_CURVE('',#11864,#11863,#818,.T.);
#15362=EDGE_CURVE('',#11864,#11865,#3581,.T.);
#15363=EDGE_CURVE('',#11866,#11865,#819,.T.);
#15364=EDGE_CURVE('',#11867,#11866,#1671,.T.);
#15365=EDGE_CURVE('',#11868,#11867,#820,.T.);
#15366=EDGE_CURVE('',#11868,#11869,#3582,.T.);
#15367=EDGE_CURVE('',#11870,#11869,#821,.T.);
#15368=EDGE_CURVE('',#11871,#11870,#1672,.T.);
#15369=EDGE_CURVE('',#11872,#11871,#822,.T.);
#15370=EDGE_CURVE('',#11872,#11873,#3583,.T.);
#15371=EDGE_CURVE('',#11874,#11873,#823,.T.);
#15372=EDGE_CURVE('',#11875,#11874,#1673,.T.);
#15373=EDGE_CURVE('',#11876,#11875,#824,.T.);
#15374=EDGE_CURVE('',#11876,#11877,#3584,.T.);
#15375=EDGE_CURVE('',#11878,#11877,#825,.T.);
#15376=EDGE_CURVE('',#11879,#11878,#1674,.T.);
#15377=EDGE_CURVE('',#11880,#11879,#826,.T.);
#15378=EDGE_CURVE('',#11880,#11881,#3585,.T.);
#15379=EDGE_CURVE('',#11302,#11881,#827,.T.);
#15380=EDGE_CURVE('',#11882,#11301,#828,.T.);
#15381=EDGE_CURVE('',#11882,#11883,#3586,.T.);
#15382=EDGE_CURVE('',#11298,#11883,#829,.T.);
#15383=EDGE_CURVE('',#11884,#11297,#830,.T.);
#15384=EDGE_CURVE('',#11884,#11885,#3587,.T.);
#15385=EDGE_CURVE('',#11294,#11885,#831,.T.);
#15386=EDGE_CURVE('',#11886,#11293,#832,.T.);
#15387=EDGE_CURVE('',#11886,#11887,#3588,.T.);
#15388=EDGE_CURVE('',#11290,#11887,#833,.T.);
#15389=EDGE_CURVE('',#11888,#11289,#834,.T.);
#15390=EDGE_CURVE('',#11888,#11889,#3589,.T.);
#15391=EDGE_CURVE('',#11286,#11889,#835,.T.);
#15392=EDGE_CURVE('',#11890,#11285,#836,.T.);
#15393=EDGE_CURVE('',#11890,#11891,#3590,.T.);
#15394=EDGE_CURVE('',#11282,#11891,#837,.T.);
#15395=EDGE_CURVE('',#11892,#11281,#838,.T.);
#15396=EDGE_CURVE('',#11892,#11893,#3591,.T.);
#15397=EDGE_CURVE('',#11306,#11893,#839,.T.);
#15398=EDGE_CURVE('',#11894,#11305,#840,.T.);
#15399=EDGE_CURVE('',#11894,#11895,#3592,.T.);
#15400=EDGE_CURVE('',#11310,#11895,#841,.T.);
#15401=EDGE_CURVE('',#11896,#11309,#842,.T.);
#15402=EDGE_CURVE('',#11896,#11897,#3593,.T.);
#15403=EDGE_CURVE('',#11314,#11897,#843,.T.);
#15404=EDGE_CURVE('',#11898,#11313,#844,.T.);
#15405=EDGE_CURVE('',#11898,#11899,#3594,.T.);
#15406=EDGE_CURVE('',#11318,#11899,#845,.T.);
#15407=EDGE_CURVE('',#11900,#11317,#846,.T.);
#15408=EDGE_CURVE('',#11900,#11901,#3595,.T.);
#15409=EDGE_CURVE('',#11322,#11901,#847,.T.);
#15410=EDGE_CURVE('',#11902,#11321,#848,.T.);
#15411=EDGE_CURVE('',#11902,#11903,#3596,.T.);
#15412=EDGE_CURVE('',#11326,#11903,#849,.T.);
#15413=EDGE_CURVE('',#11904,#11325,#850,.T.);
#15414=EDGE_CURVE('',#11904,#11905,#3597,.T.);
#15415=EDGE_CURVE('',#11330,#11905,#851,.T.);
#15416=EDGE_CURVE('',#11906,#11329,#852,.T.);
#15417=EDGE_CURVE('',#11906,#11907,#3598,.T.);
#15418=EDGE_CURVE('',#11334,#11907,#853,.T.);
#15419=EDGE_CURVE('',#11908,#11333,#854,.T.);
#15420=EDGE_CURVE('',#11908,#11909,#3599,.T.);
#15421=EDGE_CURVE('',#11338,#11909,#855,.T.);
#15422=EDGE_CURVE('',#11910,#11337,#856,.T.);
#15423=EDGE_CURVE('',#11910,#11911,#3600,.T.);
#15424=EDGE_CURVE('',#11912,#11911,#857,.T.);
#15425=EDGE_CURVE('',#11913,#11912,#1675,.T.);
#15426=EDGE_CURVE('',#11914,#11913,#858,.T.);
#15427=EDGE_CURVE('',#11914,#11915,#3601,.T.);
#15428=EDGE_CURVE('',#11916,#11915,#859,.T.);
#15429=EDGE_CURVE('',#11917,#11916,#1676,.T.);
#15430=EDGE_CURVE('',#11918,#11917,#860,.T.);
#15431=EDGE_CURVE('',#11918,#11919,#3602,.T.);
#15432=EDGE_CURVE('',#11920,#11919,#861,.T.);
#15433=EDGE_CURVE('',#11921,#11920,#1677,.T.);
#15434=EDGE_CURVE('',#11922,#11921,#862,.T.);
#15435=EDGE_CURVE('',#11922,#11923,#3603,.T.);
#15436=EDGE_CURVE('',#11924,#11923,#863,.T.);
#15437=EDGE_CURVE('',#11925,#11924,#1678,.T.);
#15438=EDGE_CURVE('',#11926,#11925,#864,.T.);
#15439=EDGE_CURVE('',#11926,#11927,#3604,.T.);
#15440=EDGE_CURVE('',#11928,#11927,#865,.T.);
#15441=EDGE_CURVE('',#11929,#11928,#1679,.T.);
#15442=EDGE_CURVE('',#11930,#11929,#866,.T.);
#15443=EDGE_CURVE('',#11930,#11931,#3605,.T.);
#15444=EDGE_CURVE('',#11932,#11931,#867,.T.);
#15445=EDGE_CURVE('',#11643,#11932,#3098,.T.);
#15446=EDGE_CURVE('',#11643,#11933,#8748,.T.);
#15447=EDGE_CURVE('',#11934,#11933,#3606,.T.);
#15448=EDGE_CURVE('',#11933,#11934,#3607,.T.);
#15449=EDGE_CURVE('',#11935,#11935,#3608,.T.);
#15450=EDGE_CURVE('',#11935,#11934,#3609,.T.);
#15451=EDGE_CURVE('',#11936,#11936,#3610,.T.);
#15452=EDGE_CURVE('',#11936,#11935,#8749,.T.);
#15453=EDGE_CURVE('',#11937,#11937,#3611,.T.);
#15454=EDGE_CURVE('',#11937,#11936,#3612,.T.);
#15455=EDGE_CURVE('',#11159,#11938,#3613,.T.);
#15456=EDGE_CURVE('',#11938,#11938,#3614,.T.);
#15457=EDGE_CURVE('',#11939,#11892,#1680,.T.);
#15458=EDGE_CURVE('',#11939,#11940,#3615,.T.);
#15459=EDGE_CURVE('',#11893,#11940,#1681,.T.);
#15460=EDGE_CURVE('',#11891,#11941,#1682,.T.);
#15461=EDGE_CURVE('',#11942,#11890,#1683,.T.);
#15462=EDGE_CURVE('',#11942,#11941,#3616,.T.);
#15463=EDGE_CURVE('',#11889,#11943,#1684,.T.);
#15464=EDGE_CURVE('',#11944,#11888,#1685,.T.);
#15465=EDGE_CURVE('',#11944,#11943,#3617,.T.);
#15466=EDGE_CURVE('',#11887,#11945,#1686,.T.);
#15467=EDGE_CURVE('',#11946,#11886,#1687,.T.);
#15468=EDGE_CURVE('',#11946,#11945,#3618,.T.);
#15469=EDGE_CURVE('',#11885,#11947,#1688,.T.);
#15470=EDGE_CURVE('',#11948,#11884,#1689,.T.);
#15471=EDGE_CURVE('',#11948,#11947,#3619,.T.);
#15472=EDGE_CURVE('',#11883,#11949,#1690,.T.);
#15473=EDGE_CURVE('',#11950,#11882,#1691,.T.);
#15474=EDGE_CURVE('',#11950,#11949,#3620,.T.);
#15475=EDGE_CURVE('',#11881,#11951,#1692,.T.);
#15476=EDGE_CURVE('',#11952,#11880,#1693,.T.);
#15477=EDGE_CURVE('',#11952,#11951,#3621,.T.);
#15478=EDGE_CURVE('',#11877,#11953,#1694,.T.);
#15479=EDGE_CURVE('',#11954,#11876,#1695,.T.);
#15480=EDGE_CURVE('',#11954,#11953,#3622,.T.);
#15481=EDGE_CURVE('',#11873,#11955,#1696,.T.);
#15482=EDGE_CURVE('',#11956,#11872,#1697,.T.);
#15483=EDGE_CURVE('',#11956,#11955,#3623,.T.);
#15484=EDGE_CURVE('',#11869,#11957,#1698,.T.);
#15485=EDGE_CURVE('',#11958,#11868,#1699,.T.);
#15486=EDGE_CURVE('',#11958,#11957,#3624,.T.);
#15487=EDGE_CURVE('',#11865,#11959,#1700,.T.);
#15488=EDGE_CURVE('',#11960,#11864,#1701,.T.);
#15489=EDGE_CURVE('',#11960,#11959,#3625,.T.);
#15490=EDGE_CURVE('',#11861,#11961,#1702,.T.);
#15491=EDGE_CURVE('',#11962,#11860,#1703,.T.);
#15492=EDGE_CURVE('',#11962,#11961,#3626,.T.);
#15493=EDGE_CURVE('',#11857,#11963,#1704,.T.);
#15494=EDGE_CURVE('',#11964,#11856,#1705,.T.);
#15495=EDGE_CURVE('',#11964,#11963,#3627,.T.);
#15496=EDGE_CURVE('',#11853,#11965,#1706,.T.);
#15497=EDGE_CURVE('',#11966,#11852,#1707,.T.);
#15498=EDGE_CURVE('',#11966,#11965,#3628,.T.);
#15499=EDGE_CURVE('',#11849,#11967,#1708,.T.);
#15500=EDGE_CURVE('',#11968,#11848,#1709,.T.);
#15501=EDGE_CURVE('',#11968,#11967,#3629,.T.);
#15502=EDGE_CURVE('',#11845,#11969,#1710,.T.);
#15503=EDGE_CURVE('',#11970,#11844,#1711,.T.);
#15504=EDGE_CURVE('',#11970,#11969,#3630,.T.);
#15505=EDGE_CURVE('',#11841,#11971,#1712,.T.);
#15506=EDGE_CURVE('',#11972,#11840,#1713,.T.);
#15507=EDGE_CURVE('',#11972,#11971,#3631,.T.);
#15508=EDGE_CURVE('',#11837,#11973,#1714,.T.);
#15509=EDGE_CURVE('',#11974,#11836,#1715,.T.);
#15510=EDGE_CURVE('',#11974,#11973,#3632,.T.);
#15511=EDGE_CURVE('',#11833,#11975,#1716,.T.);
#15512=EDGE_CURVE('',#11976,#11832,#1717,.T.);
#15513=EDGE_CURVE('',#11976,#11975,#3633,.T.);
#15514=EDGE_CURVE('',#11829,#11977,#1718,.T.);
#15515=EDGE_CURVE('',#11978,#11828,#1719,.T.);
#15516=EDGE_CURVE('',#11978,#11977,#3634,.T.);
#15517=EDGE_CURVE('',#11825,#11979,#1720,.T.);
#15518=EDGE_CURVE('',#11980,#11824,#1721,.T.);
#15519=EDGE_CURVE('',#11980,#11979,#3635,.T.);
#15520=EDGE_CURVE('',#11821,#11981,#1722,.T.);
#15521=EDGE_CURVE('',#11982,#11820,#1723,.T.);
#15522=EDGE_CURVE('',#11982,#11981,#3636,.T.);
#15523=EDGE_CURVE('',#11817,#11983,#1724,.T.);
#15524=EDGE_CURVE('',#11984,#11816,#1725,.T.);
#15525=EDGE_CURVE('',#11984,#11983,#3637,.T.);
#15526=EDGE_CURVE('',#11813,#11985,#1726,.T.);
#15527=EDGE_CURVE('',#11986,#11812,#1727,.T.);
#15528=EDGE_CURVE('',#11986,#11985,#3638,.T.);
#15529=EDGE_CURVE('',#11809,#11987,#1728,.T.);
#15530=EDGE_CURVE('',#11988,#11808,#1729,.T.);
#15531=EDGE_CURVE('',#11988,#11987,#3639,.T.);
#15532=EDGE_CURVE('',#11805,#11989,#1730,.T.);
#15533=EDGE_CURVE('',#11990,#11804,#1731,.T.);
#15534=EDGE_CURVE('',#11990,#11989,#3640,.T.);
#15535=EDGE_CURVE('',#11801,#11991,#1732,.T.);
#15536=EDGE_CURVE('',#11992,#11800,#1733,.T.);
#15537=EDGE_CURVE('',#11992,#11991,#3641,.T.);
#15538=EDGE_CURVE('',#11797,#11993,#1734,.T.);
#15539=EDGE_CURVE('',#11994,#11796,#1735,.T.);
#15540=EDGE_CURVE('',#11994,#11993,#3642,.T.);
#15541=EDGE_CURVE('',#11793,#11995,#1736,.T.);
#15542=EDGE_CURVE('',#11996,#11792,#1737,.T.);
#15543=EDGE_CURVE('',#11996,#11995,#3643,.T.);
#15544=EDGE_CURVE('',#11789,#11997,#1738,.T.);
#15545=EDGE_CURVE('',#11998,#11788,#1739,.T.);
#15546=EDGE_CURVE('',#11998,#11997,#3644,.T.);
#15547=EDGE_CURVE('',#11785,#11999,#1740,.T.);
#15548=EDGE_CURVE('',#12000,#11784,#1741,.T.);
#15549=EDGE_CURVE('',#12000,#11999,#3645,.T.);
#15550=EDGE_CURVE('',#11781,#12001,#1742,.T.);
#15551=EDGE_CURVE('',#12002,#11780,#1743,.T.);
#15552=EDGE_CURVE('',#12002,#12001,#3646,.T.);
#15553=EDGE_CURVE('',#11777,#12003,#1744,.T.);
#15554=EDGE_CURVE('',#12004,#11776,#1745,.T.);
#15555=EDGE_CURVE('',#12004,#12003,#3647,.T.);
#15556=EDGE_CURVE('',#11773,#12005,#1746,.T.);
#15557=EDGE_CURVE('',#12006,#11772,#1747,.T.);
#15558=EDGE_CURVE('',#12006,#12005,#3648,.T.);
#15559=EDGE_CURVE('',#11769,#12007,#1748,.T.);
#15560=EDGE_CURVE('',#12008,#11768,#1749,.T.);
#15561=EDGE_CURVE('',#12008,#12007,#3649,.T.);
#15562=EDGE_CURVE('',#11765,#12009,#1750,.T.);
#15563=EDGE_CURVE('',#12010,#11764,#1751,.T.);
#15564=EDGE_CURVE('',#12010,#12009,#3650,.T.);
#15565=EDGE_CURVE('',#11761,#12011,#1752,.T.);
#15566=EDGE_CURVE('',#12012,#11760,#1753,.T.);
#15567=EDGE_CURVE('',#12012,#12011,#3651,.T.);
#15568=EDGE_CURVE('',#11757,#12013,#1754,.T.);
#15569=EDGE_CURVE('',#12014,#11756,#1755,.T.);
#15570=EDGE_CURVE('',#12014,#12013,#3652,.T.);
#15571=EDGE_CURVE('',#11753,#12015,#1756,.T.);
#15572=EDGE_CURVE('',#12016,#11752,#1757,.T.);
#15573=EDGE_CURVE('',#12016,#12015,#3653,.T.);
#15574=EDGE_CURVE('',#11749,#12017,#1758,.T.);
#15575=EDGE_CURVE('',#12018,#11748,#1759,.T.);
#15576=EDGE_CURVE('',#12018,#12017,#3654,.T.);
#15577=EDGE_CURVE('',#11745,#12019,#1760,.T.);
#15578=EDGE_CURVE('',#12020,#11744,#1761,.T.);
#15579=EDGE_CURVE('',#12020,#12019,#3655,.T.);
#15580=EDGE_CURVE('',#11741,#12021,#1762,.T.);
#15581=EDGE_CURVE('',#12022,#11740,#1763,.T.);
#15582=EDGE_CURVE('',#12022,#12021,#3656,.T.);
#15583=EDGE_CURVE('',#11737,#12023,#1764,.T.);
#15584=EDGE_CURVE('',#12024,#11736,#1765,.T.);
#15585=EDGE_CURVE('',#12024,#12023,#3657,.T.);
#15586=EDGE_CURVE('',#11733,#12025,#1766,.T.);
#15587=EDGE_CURVE('',#12026,#11732,#1767,.T.);
#15588=EDGE_CURVE('',#12026,#12025,#3658,.T.);
#15589=EDGE_CURVE('',#11729,#12027,#1768,.T.);
#15590=EDGE_CURVE('',#12028,#11728,#1769,.T.);
#15591=EDGE_CURVE('',#12028,#12027,#3659,.T.);
#15592=EDGE_CURVE('',#11725,#12029,#1770,.T.);
#15593=EDGE_CURVE('',#12030,#11724,#1771,.T.);
#15594=EDGE_CURVE('',#12030,#12029,#3660,.T.);
#15595=EDGE_CURVE('',#11721,#12031,#1772,.T.);
#15596=EDGE_CURVE('',#12032,#11720,#1773,.T.);
#15597=EDGE_CURVE('',#12032,#12031,#3661,.T.);
#15598=EDGE_CURVE('',#11717,#12033,#1774,.T.);
#15599=EDGE_CURVE('',#12034,#11716,#1775,.T.);
#15600=EDGE_CURVE('',#12034,#12033,#3662,.T.);
#15601=EDGE_CURVE('',#11713,#12035,#1776,.T.);
#15602=EDGE_CURVE('',#12036,#11712,#1777,.T.);
#15603=EDGE_CURVE('',#12036,#12035,#3663,.T.);
#15604=EDGE_CURVE('',#11709,#12037,#1778,.T.);
#15605=EDGE_CURVE('',#12038,#11708,#1779,.T.);
#15606=EDGE_CURVE('',#12038,#12037,#3664,.T.);
#15607=EDGE_CURVE('',#11705,#12039,#1780,.T.);
#15608=EDGE_CURVE('',#12040,#11704,#1781,.T.);
#15609=EDGE_CURVE('',#12040,#12039,#3665,.T.);
#15610=EDGE_CURVE('',#11701,#12041,#1782,.T.);
#15611=EDGE_CURVE('',#12042,#11700,#1783,.T.);
#15612=EDGE_CURVE('',#12042,#12041,#3666,.T.);
#15613=EDGE_CURVE('',#11697,#12043,#1784,.T.);
#15614=EDGE_CURVE('',#12044,#11696,#1785,.T.);
#15615=EDGE_CURVE('',#12044,#12043,#3667,.T.);
#15616=EDGE_CURVE('',#11693,#12045,#1786,.T.);
#15617=EDGE_CURVE('',#12046,#11692,#1787,.T.);
#15618=EDGE_CURVE('',#12046,#12045,#3668,.T.);
#15619=EDGE_CURVE('',#11689,#12047,#1788,.T.);
#15620=EDGE_CURVE('',#12048,#11688,#1789,.T.);
#15621=EDGE_CURVE('',#12048,#12047,#3669,.T.);
#15622=EDGE_CURVE('',#11685,#12049,#1790,.T.);
#15623=EDGE_CURVE('',#12050,#11684,#1791,.T.);
#15624=EDGE_CURVE('',#12050,#12049,#3670,.T.);
#15625=EDGE_CURVE('',#11681,#12051,#1792,.T.);
#15626=EDGE_CURVE('',#12052,#11680,#1793,.T.);
#15627=EDGE_CURVE('',#12052,#12051,#3671,.T.);
#15628=EDGE_CURVE('',#11677,#12053,#1794,.T.);
#15629=EDGE_CURVE('',#12054,#11676,#1795,.T.);
#15630=EDGE_CURVE('',#12054,#12053,#3672,.T.);
#15631=EDGE_CURVE('',#11673,#12055,#1796,.T.);
#15632=EDGE_CURVE('',#12056,#11672,#1797,.T.);
#15633=EDGE_CURVE('',#12056,#12055,#3673,.T.);
#15634=EDGE_CURVE('',#11669,#12057,#1798,.T.);
#15635=EDGE_CURVE('',#12058,#11668,#1799,.T.);
#15636=EDGE_CURVE('',#12058,#12057,#3674,.T.);
#15637=EDGE_CURVE('',#11665,#12059,#1800,.T.);
#15638=EDGE_CURVE('',#12060,#11664,#1801,.T.);
#15639=EDGE_CURVE('',#12060,#12059,#3675,.T.);
#15640=EDGE_CURVE('',#11661,#12061,#1802,.T.);
#15641=EDGE_CURVE('',#12062,#11660,#1803,.T.);
#15642=EDGE_CURVE('',#12062,#12061,#3676,.T.);
#15643=EDGE_CURVE('',#11657,#12063,#1804,.T.);
#15644=EDGE_CURVE('',#12064,#11656,#1805,.T.);
#15645=EDGE_CURVE('',#12064,#12063,#3677,.T.);
#15646=EDGE_CURVE('',#11653,#12065,#1806,.T.);
#15647=EDGE_CURVE('',#12066,#11652,#1807,.T.);
#15648=EDGE_CURVE('',#12066,#12065,#3678,.T.);
#15649=EDGE_CURVE('',#12067,#11894,#1808,.T.);
#15650=EDGE_CURVE('',#12067,#12068,#3679,.T.);
#15651=EDGE_CURVE('',#11895,#12068,#1809,.T.);
#15652=EDGE_CURVE('',#12069,#11896,#1810,.T.);
#15653=EDGE_CURVE('',#12069,#12070,#3680,.T.);
#15654=EDGE_CURVE('',#11897,#12070,#1811,.T.);
#15655=EDGE_CURVE('',#12071,#11898,#1812,.T.);
#15656=EDGE_CURVE('',#12071,#12072,#3681,.T.);
#15657=EDGE_CURVE('',#11899,#12072,#1813,.T.);
#15658=EDGE_CURVE('',#12073,#11900,#1814,.T.);
#15659=EDGE_CURVE('',#12073,#12074,#3682,.T.);
#15660=EDGE_CURVE('',#11901,#12074,#1815,.T.);
#15661=EDGE_CURVE('',#12075,#11902,#1816,.T.);
#15662=EDGE_CURVE('',#12075,#12076,#3683,.T.);
#15663=EDGE_CURVE('',#11903,#12076,#1817,.T.);
#15664=EDGE_CURVE('',#12077,#11904,#1818,.T.);
#15665=EDGE_CURVE('',#12077,#12078,#3684,.T.);
#15666=EDGE_CURVE('',#11905,#12078,#1819,.T.);
#15667=EDGE_CURVE('',#12079,#11906,#1820,.T.);
#15668=EDGE_CURVE('',#12079,#12080,#3685,.T.);
#15669=EDGE_CURVE('',#11907,#12080,#1821,.T.);
#15670=EDGE_CURVE('',#12081,#11908,#1822,.T.);
#15671=EDGE_CURVE('',#12081,#12082,#3686,.T.);
#15672=EDGE_CURVE('',#11909,#12082,#1823,.T.);
#15673=EDGE_CURVE('',#12083,#11910,#1824,.T.);
#15674=EDGE_CURVE('',#12083,#12084,#3687,.T.);
#15675=EDGE_CURVE('',#11911,#12084,#1825,.T.);
#15676=EDGE_CURVE('',#12085,#11914,#1826,.T.);
#15677=EDGE_CURVE('',#12085,#12086,#3688,.T.);
#15678=EDGE_CURVE('',#11915,#12086,#1827,.T.);
#15679=EDGE_CURVE('',#12087,#11918,#1828,.T.);
#15680=EDGE_CURVE('',#12087,#12088,#3689,.T.);
#15681=EDGE_CURVE('',#11919,#12088,#1829,.T.);
#15682=EDGE_CURVE('',#12089,#11922,#1830,.T.);
#15683=EDGE_CURVE('',#12089,#12090,#3690,.T.);
#15684=EDGE_CURVE('',#11923,#12090,#1831,.T.);
#15685=EDGE_CURVE('',#12091,#11926,#1832,.T.);
#15686=EDGE_CURVE('',#12091,#12092,#3691,.T.);
#15687=EDGE_CURVE('',#11927,#12092,#1833,.T.);
#15688=EDGE_CURVE('',#12093,#11930,#1834,.T.);
#15689=EDGE_CURVE('',#12093,#12094,#3692,.T.);
#15690=EDGE_CURVE('',#11931,#12094,#1835,.T.);
#15691=EDGE_CURVE('',#11649,#12095,#1836,.T.);
#15692=EDGE_CURVE('',#12096,#11648,#1837,.T.);
#15693=EDGE_CURVE('',#12096,#12095,#3693,.T.);
#15694=EDGE_CURVE('',#12097,#11939,#8750,.T.);
#15695=EDGE_CURVE('',#12097,#12098,#3694,.T.);
#15696=EDGE_CURVE('',#11940,#12098,#8751,.T.);
#15697=EDGE_CURVE('',#11941,#12099,#8752,.T.);
#15698=EDGE_CURVE('',#12100,#11942,#8753,.T.);
#15699=EDGE_CURVE('',#12100,#12099,#3695,.T.);
#15700=EDGE_CURVE('',#11943,#12101,#8754,.T.);
#15701=EDGE_CURVE('',#12102,#11944,#8755,.T.);
#15702=EDGE_CURVE('',#12102,#12101,#3696,.T.);
#15703=EDGE_CURVE('',#11945,#12103,#8756,.T.);
#15704=EDGE_CURVE('',#12104,#11946,#8757,.T.);
#15705=EDGE_CURVE('',#12104,#12103,#3697,.T.);
#15706=EDGE_CURVE('',#11947,#12105,#8758,.T.);
#15707=EDGE_CURVE('',#12106,#11948,#8759,.T.);
#15708=EDGE_CURVE('',#12106,#12105,#3698,.T.);
#15709=EDGE_CURVE('',#11949,#12107,#8760,.T.);
#15710=EDGE_CURVE('',#12108,#11950,#8761,.T.);
#15711=EDGE_CURVE('',#12108,#12107,#3699,.T.);
#15712=EDGE_CURVE('',#11951,#12109,#8762,.T.);
#15713=EDGE_CURVE('',#12110,#11952,#8763,.T.);
#15714=EDGE_CURVE('',#12110,#12109,#3700,.T.);
#15715=EDGE_CURVE('',#11953,#12111,#8764,.T.);
#15716=EDGE_CURVE('',#12112,#11954,#8765,.T.);
#15717=EDGE_CURVE('',#12112,#12111,#3701,.T.);
#15718=EDGE_CURVE('',#11955,#12113,#8766,.T.);
#15719=EDGE_CURVE('',#12114,#11956,#8767,.T.);
#15720=EDGE_CURVE('',#12114,#12113,#3702,.T.);
#15721=EDGE_CURVE('',#11957,#12115,#8768,.T.);
#15722=EDGE_CURVE('',#12116,#11958,#8769,.T.);
#15723=EDGE_CURVE('',#12116,#12115,#3703,.T.);
#15724=EDGE_CURVE('',#11959,#12117,#8770,.T.);
#15725=EDGE_CURVE('',#12118,#11960,#8771,.T.);
#15726=EDGE_CURVE('',#12118,#12117,#3704,.T.);
#15727=EDGE_CURVE('',#11961,#12119,#8772,.T.);
#15728=EDGE_CURVE('',#12120,#11962,#8773,.T.);
#15729=EDGE_CURVE('',#12120,#12119,#3705,.T.);
#15730=EDGE_CURVE('',#11963,#12121,#8774,.T.);
#15731=EDGE_CURVE('',#12122,#11964,#8775,.T.);
#15732=EDGE_CURVE('',#12122,#12121,#3706,.T.);
#15733=EDGE_CURVE('',#11965,#12123,#8776,.T.);
#15734=EDGE_CURVE('',#12124,#11966,#8777,.T.);
#15735=EDGE_CURVE('',#12124,#12123,#3707,.T.);
#15736=EDGE_CURVE('',#11967,#12125,#8778,.T.);
#15737=EDGE_CURVE('',#12126,#11968,#8779,.T.);
#15738=EDGE_CURVE('',#12126,#12125,#3708,.T.);
#15739=EDGE_CURVE('',#11969,#12127,#8780,.T.);
#15740=EDGE_CURVE('',#12128,#11970,#8781,.T.);
#15741=EDGE_CURVE('',#12128,#12127,#3709,.T.);
#15742=EDGE_CURVE('',#11971,#12129,#8782,.T.);
#15743=EDGE_CURVE('',#12130,#11972,#8783,.T.);
#15744=EDGE_CURVE('',#12130,#12129,#3710,.T.);
#15745=EDGE_CURVE('',#11973,#12131,#8784,.T.);
#15746=EDGE_CURVE('',#12132,#11974,#8785,.T.);
#15747=EDGE_CURVE('',#12132,#12131,#3711,.T.);
#15748=EDGE_CURVE('',#11975,#12133,#8786,.T.);
#15749=EDGE_CURVE('',#12134,#11976,#8787,.T.);
#15750=EDGE_CURVE('',#12134,#12133,#3712,.T.);
#15751=EDGE_CURVE('',#11977,#12135,#8788,.T.);
#15752=EDGE_CURVE('',#12136,#11978,#8789,.T.);
#15753=EDGE_CURVE('',#12136,#12135,#3713,.T.);
#15754=EDGE_CURVE('',#11979,#12137,#8790,.T.);
#15755=EDGE_CURVE('',#12138,#11980,#8791,.T.);
#15756=EDGE_CURVE('',#12138,#12137,#3714,.T.);
#15757=EDGE_CURVE('',#11981,#12139,#8792,.T.);
#15758=EDGE_CURVE('',#12140,#11982,#8793,.T.);
#15759=EDGE_CURVE('',#12140,#12139,#3715,.T.);
#15760=EDGE_CURVE('',#11983,#12141,#8794,.T.);
#15761=EDGE_CURVE('',#12142,#11984,#8795,.T.);
#15762=EDGE_CURVE('',#12142,#12141,#3716,.T.);
#15763=EDGE_CURVE('',#11985,#12143,#8796,.T.);
#15764=EDGE_CURVE('',#12144,#11986,#8797,.T.);
#15765=EDGE_CURVE('',#12144,#12143,#3717,.T.);
#15766=EDGE_CURVE('',#11987,#12145,#8798,.T.);
#15767=EDGE_CURVE('',#12146,#11988,#8799,.T.);
#15768=EDGE_CURVE('',#12146,#12145,#3718,.T.);
#15769=EDGE_CURVE('',#11989,#12147,#8800,.T.);
#15770=EDGE_CURVE('',#12148,#11990,#8801,.T.);
#15771=EDGE_CURVE('',#12148,#12147,#3719,.T.);
#15772=EDGE_CURVE('',#11991,#12149,#8802,.T.);
#15773=EDGE_CURVE('',#12150,#11992,#8803,.T.);
#15774=EDGE_CURVE('',#12150,#12149,#3720,.T.);
#15775=EDGE_CURVE('',#11993,#12151,#8804,.T.);
#15776=EDGE_CURVE('',#12152,#11994,#8805,.T.);
#15777=EDGE_CURVE('',#12152,#12151,#3721,.T.);
#15778=EDGE_CURVE('',#11995,#12153,#8806,.T.);
#15779=EDGE_CURVE('',#12154,#11996,#8807,.T.);
#15780=EDGE_CURVE('',#12154,#12153,#3722,.T.);
#15781=EDGE_CURVE('',#11997,#12155,#8808,.T.);
#15782=EDGE_CURVE('',#12156,#11998,#8809,.T.);
#15783=EDGE_CURVE('',#12156,#12155,#3723,.T.);
#15784=EDGE_CURVE('',#11999,#12157,#8810,.T.);
#15785=EDGE_CURVE('',#12158,#12000,#8811,.T.);
#15786=EDGE_CURVE('',#12158,#12157,#3724,.T.);
#15787=EDGE_CURVE('',#12001,#12159,#8812,.T.);
#15788=EDGE_CURVE('',#12160,#12002,#8813,.T.);
#15789=EDGE_CURVE('',#12160,#12159,#3725,.T.);
#15790=EDGE_CURVE('',#12003,#12161,#8814,.T.);
#15791=EDGE_CURVE('',#12162,#12004,#8815,.T.);
#15792=EDGE_CURVE('',#12162,#12161,#3726,.T.);
#15793=EDGE_CURVE('',#12005,#12163,#8816,.T.);
#15794=EDGE_CURVE('',#12164,#12006,#8817,.T.);
#15795=EDGE_CURVE('',#12164,#12163,#3727,.T.);
#15796=EDGE_CURVE('',#12007,#12165,#8818,.T.);
#15797=EDGE_CURVE('',#12166,#12008,#8819,.T.);
#15798=EDGE_CURVE('',#12166,#12165,#3728,.T.);
#15799=EDGE_CURVE('',#12009,#12167,#8820,.T.);
#15800=EDGE_CURVE('',#12168,#12010,#8821,.T.);
#15801=EDGE_CURVE('',#12168,#12167,#3729,.T.);
#15802=EDGE_CURVE('',#12011,#12169,#8822,.T.);
#15803=EDGE_CURVE('',#12170,#12012,#8823,.T.);
#15804=EDGE_CURVE('',#12170,#12169,#3730,.T.);
#15805=EDGE_CURVE('',#12013,#12171,#8824,.T.);
#15806=EDGE_CURVE('',#12172,#12014,#8825,.T.);
#15807=EDGE_CURVE('',#12172,#12171,#3731,.T.);
#15808=EDGE_CURVE('',#12015,#12173,#8826,.T.);
#15809=EDGE_CURVE('',#12174,#12016,#8827,.T.);
#15810=EDGE_CURVE('',#12174,#12173,#3732,.T.);
#15811=EDGE_CURVE('',#12017,#12175,#8828,.T.);
#15812=EDGE_CURVE('',#12176,#12018,#8829,.T.);
#15813=EDGE_CURVE('',#12176,#12175,#3733,.T.);
#15814=EDGE_CURVE('',#12019,#12177,#8830,.T.);
#15815=EDGE_CURVE('',#12178,#12020,#8831,.T.);
#15816=EDGE_CURVE('',#12178,#12177,#3734,.T.);
#15817=EDGE_CURVE('',#12021,#12179,#8832,.T.);
#15818=EDGE_CURVE('',#12180,#12022,#8833,.T.);
#15819=EDGE_CURVE('',#12180,#12179,#3735,.T.);
#15820=EDGE_CURVE('',#12023,#12181,#8834,.T.);
#15821=EDGE_CURVE('',#12182,#12024,#8835,.T.);
#15822=EDGE_CURVE('',#12182,#12181,#3736,.T.);
#15823=EDGE_CURVE('',#12025,#12183,#8836,.T.);
#15824=EDGE_CURVE('',#12184,#12026,#8837,.T.);
#15825=EDGE_CURVE('',#12184,#12183,#3737,.T.);
#15826=EDGE_CURVE('',#12027,#12185,#8838,.T.);
#15827=EDGE_CURVE('',#12186,#12028,#8839,.T.);
#15828=EDGE_CURVE('',#12186,#12185,#3738,.T.);
#15829=EDGE_CURVE('',#12029,#12187,#8840,.T.);
#15830=EDGE_CURVE('',#12188,#12030,#8841,.T.);
#15831=EDGE_CURVE('',#12188,#12187,#3739,.T.);
#15832=EDGE_CURVE('',#12031,#12189,#8842,.T.);
#15833=EDGE_CURVE('',#12190,#12032,#8843,.T.);
#15834=EDGE_CURVE('',#12190,#12189,#3740,.T.);
#15835=EDGE_CURVE('',#12033,#12191,#8844,.T.);
#15836=EDGE_CURVE('',#12192,#12034,#8845,.T.);
#15837=EDGE_CURVE('',#12192,#12191,#3741,.T.);
#15838=EDGE_CURVE('',#12035,#12193,#8846,.T.);
#15839=EDGE_CURVE('',#12194,#12036,#8847,.T.);
#15840=EDGE_CURVE('',#12194,#12193,#3742,.T.);
#15841=EDGE_CURVE('',#12037,#12195,#8848,.T.);
#15842=EDGE_CURVE('',#12196,#12038,#8849,.T.);
#15843=EDGE_CURVE('',#12196,#12195,#3743,.T.);
#15844=EDGE_CURVE('',#12039,#12197,#8850,.T.);
#15845=EDGE_CURVE('',#12198,#12040,#8851,.T.);
#15846=EDGE_CURVE('',#12198,#12197,#3744,.T.);
#15847=EDGE_CURVE('',#12041,#12199,#8852,.T.);
#15848=EDGE_CURVE('',#12200,#12042,#8853,.T.);
#15849=EDGE_CURVE('',#12200,#12199,#3745,.T.);
#15850=EDGE_CURVE('',#12043,#12201,#8854,.T.);
#15851=EDGE_CURVE('',#12202,#12044,#8855,.T.);
#15852=EDGE_CURVE('',#12202,#12201,#3746,.T.);
#15853=EDGE_CURVE('',#12045,#12203,#8856,.T.);
#15854=EDGE_CURVE('',#12204,#12046,#8857,.T.);
#15855=EDGE_CURVE('',#12204,#12203,#3747,.T.);
#15856=EDGE_CURVE('',#12047,#12205,#8858,.T.);
#15857=EDGE_CURVE('',#12206,#12048,#8859,.T.);
#15858=EDGE_CURVE('',#12206,#12205,#3748,.T.);
#15859=EDGE_CURVE('',#12049,#12207,#8860,.T.);
#15860=EDGE_CURVE('',#12208,#12050,#8861,.T.);
#15861=EDGE_CURVE('',#12208,#12207,#3749,.T.);
#15862=EDGE_CURVE('',#12051,#12209,#8862,.T.);
#15863=EDGE_CURVE('',#12210,#12052,#8863,.T.);
#15864=EDGE_CURVE('',#12210,#12209,#3750,.T.);
#15865=EDGE_CURVE('',#12053,#12211,#8864,.T.);
#15866=EDGE_CURVE('',#12212,#12054,#8865,.T.);
#15867=EDGE_CURVE('',#12212,#12211,#3751,.T.);
#15868=EDGE_CURVE('',#12055,#12213,#8866,.T.);
#15869=EDGE_CURVE('',#12214,#12056,#8867,.T.);
#15870=EDGE_CURVE('',#12214,#12213,#3752,.T.);
#15871=EDGE_CURVE('',#12057,#12215,#8868,.T.);
#15872=EDGE_CURVE('',#12216,#12058,#8869,.T.);
#15873=EDGE_CURVE('',#12216,#12215,#3753,.T.);
#15874=EDGE_CURVE('',#12059,#12217,#8870,.T.);
#15875=EDGE_CURVE('',#12218,#12060,#8871,.T.);
#15876=EDGE_CURVE('',#12218,#12217,#3754,.T.);
#15877=EDGE_CURVE('',#12061,#12219,#8872,.T.);
#15878=EDGE_CURVE('',#12220,#12062,#8873,.T.);
#15879=EDGE_CURVE('',#12220,#12219,#3755,.T.);
#15880=EDGE_CURVE('',#12063,#12221,#8874,.T.);
#15881=EDGE_CURVE('',#12222,#12064,#8875,.T.);
#15882=EDGE_CURVE('',#12222,#12221,#3756,.T.);
#15883=EDGE_CURVE('',#12065,#12223,#8876,.T.);
#15884=EDGE_CURVE('',#12224,#12066,#8877,.T.);
#15885=EDGE_CURVE('',#12224,#12223,#3757,.T.);
#15886=EDGE_CURVE('',#12225,#12067,#8878,.T.);
#15887=EDGE_CURVE('',#12225,#12226,#3758,.T.);
#15888=EDGE_CURVE('',#12068,#12226,#8879,.T.);
#15889=EDGE_CURVE('',#12227,#12069,#8880,.T.);
#15890=EDGE_CURVE('',#12227,#12228,#3759,.T.);
#15891=EDGE_CURVE('',#12070,#12228,#8881,.T.);
#15892=EDGE_CURVE('',#12229,#12071,#8882,.T.);
#15893=EDGE_CURVE('',#12229,#12230,#3760,.T.);
#15894=EDGE_CURVE('',#12072,#12230,#8883,.T.);
#15895=EDGE_CURVE('',#12231,#12073,#8884,.T.);
#15896=EDGE_CURVE('',#12231,#12232,#3761,.T.);
#15897=EDGE_CURVE('',#12074,#12232,#8885,.T.);
#15898=EDGE_CURVE('',#12233,#12075,#8886,.T.);
#15899=EDGE_CURVE('',#12233,#12234,#3762,.T.);
#15900=EDGE_CURVE('',#12076,#12234,#8887,.T.);
#15901=EDGE_CURVE('',#12235,#12077,#8888,.T.);
#15902=EDGE_CURVE('',#12235,#12236,#3763,.T.);
#15903=EDGE_CURVE('',#12078,#12236,#8889,.T.);
#15904=EDGE_CURVE('',#12237,#12079,#8890,.T.);
#15905=EDGE_CURVE('',#12237,#12238,#3764,.T.);
#15906=EDGE_CURVE('',#12080,#12238,#8891,.T.);
#15907=EDGE_CURVE('',#12239,#12081,#8892,.T.);
#15908=EDGE_CURVE('',#12239,#12240,#3765,.T.);
#15909=EDGE_CURVE('',#12082,#12240,#8893,.T.);
#15910=EDGE_CURVE('',#12241,#12083,#8894,.T.);
#15911=EDGE_CURVE('',#12241,#12242,#3766,.T.);
#15912=EDGE_CURVE('',#12084,#12242,#8895,.T.);
#15913=EDGE_CURVE('',#12243,#12085,#8896,.T.);
#15914=EDGE_CURVE('',#12243,#12244,#3767,.T.);
#15915=EDGE_CURVE('',#12086,#12244,#8897,.T.);
#15916=EDGE_CURVE('',#12245,#12087,#8898,.T.);
#15917=EDGE_CURVE('',#12245,#12246,#3768,.T.);
#15918=EDGE_CURVE('',#12088,#12246,#8899,.T.);
#15919=EDGE_CURVE('',#12247,#12089,#8900,.T.);
#15920=EDGE_CURVE('',#12247,#12248,#3769,.T.);
#15921=EDGE_CURVE('',#12090,#12248,#8901,.T.);
#15922=EDGE_CURVE('',#12249,#12091,#8902,.T.);
#15923=EDGE_CURVE('',#12249,#12250,#3770,.T.);
#15924=EDGE_CURVE('',#12092,#12250,#8903,.T.);
#15925=EDGE_CURVE('',#12251,#12093,#8904,.T.);
#15926=EDGE_CURVE('',#12251,#12252,#3771,.T.);
#15927=EDGE_CURVE('',#12094,#12252,#8905,.T.);
#15928=EDGE_CURVE('',#12095,#12253,#8906,.T.);
#15929=EDGE_CURVE('',#12254,#12096,#8907,.T.);
#15930=EDGE_CURVE('',#12254,#12253,#3772,.T.);
#15931=EDGE_CURVE('',#11552,#12097,#1838,.T.);
#15932=EDGE_CURVE('',#12098,#11551,#1839,.T.);
#15933=EDGE_CURVE('',#12099,#11553,#1840,.T.);
#15934=EDGE_CURVE('',#11554,#12100,#1841,.T.);
#15935=EDGE_CURVE('',#12101,#11555,#1842,.T.);
#15936=EDGE_CURVE('',#11556,#12102,#1843,.T.);
#15937=EDGE_CURVE('',#12103,#11557,#1844,.T.);
#15938=EDGE_CURVE('',#11558,#12104,#1845,.T.);
#15939=EDGE_CURVE('',#12105,#11559,#1846,.T.);
#15940=EDGE_CURVE('',#11560,#12106,#1847,.T.);
#15941=EDGE_CURVE('',#12107,#11561,#1848,.T.);
#15942=EDGE_CURVE('',#11562,#12108,#1849,.T.);
#15943=EDGE_CURVE('',#12109,#11563,#1850,.T.);
#15944=EDGE_CURVE('',#11564,#12110,#1851,.T.);
#15945=EDGE_CURVE('',#12111,#11567,#1852,.T.);
#15946=EDGE_CURVE('',#11568,#12112,#1853,.T.);
#15947=EDGE_CURVE('',#12113,#11571,#1854,.T.);
#15948=EDGE_CURVE('',#11572,#12114,#1855,.T.);
#15949=EDGE_CURVE('',#12115,#11575,#1856,.T.);
#15950=EDGE_CURVE('',#11576,#12116,#1857,.T.);
#15951=EDGE_CURVE('',#12117,#11579,#1858,.T.);
#15952=EDGE_CURVE('',#11580,#12118,#1859,.T.);
#15953=EDGE_CURVE('',#12119,#11583,#1860,.T.);
#15954=EDGE_CURVE('',#11584,#12120,#1861,.T.);
#15955=EDGE_CURVE('',#12121,#11587,#1862,.T.);
#15956=EDGE_CURVE('',#11588,#12122,#1863,.T.);
#15957=EDGE_CURVE('',#12123,#11591,#1864,.T.);
#15958=EDGE_CURVE('',#11592,#12124,#1865,.T.);
#15959=EDGE_CURVE('',#12125,#11595,#1866,.T.);
#15960=EDGE_CURVE('',#11596,#12126,#1867,.T.);
#15961=EDGE_CURVE('',#12127,#11599,#1868,.T.);
#15962=EDGE_CURVE('',#11600,#12128,#1869,.T.);
#15963=EDGE_CURVE('',#12129,#11603,#1870,.T.);
#15964=EDGE_CURVE('',#11604,#12130,#1871,.T.);
#15965=EDGE_CURVE('',#12131,#11607,#1872,.T.);
#15966=EDGE_CURVE('',#11608,#12132,#1873,.T.);
#15967=EDGE_CURVE('',#12133,#11611,#1874,.T.);
#15968=EDGE_CURVE('',#11612,#12134,#1875,.T.);
#15969=EDGE_CURVE('',#12135,#11615,#1876,.T.);
#15970=EDGE_CURVE('',#11616,#12136,#1877,.T.);
#15971=EDGE_CURVE('',#12137,#11619,#1878,.T.);
#15972=EDGE_CURVE('',#11620,#12138,#1879,.T.);
#15973=EDGE_CURVE('',#12139,#11623,#1880,.T.);
#15974=EDGE_CURVE('',#11624,#12140,#1881,.T.);
#15975=EDGE_CURVE('',#12141,#11627,#1882,.T.);
#15976=EDGE_CURVE('',#11628,#12142,#1883,.T.);
#15977=EDGE_CURVE('',#12143,#11631,#1884,.T.);
#15978=EDGE_CURVE('',#11632,#12144,#1885,.T.);
#15979=EDGE_CURVE('',#12145,#11635,#1886,.T.);
#15980=EDGE_CURVE('',#11636,#12146,#1887,.T.);
#15981=EDGE_CURVE('',#12147,#11639,#1888,.T.);
#15982=EDGE_CURVE('',#11640,#12148,#1889,.T.);
#15983=EDGE_CURVE('',#12149,#11353,#1890,.T.);
#15984=EDGE_CURVE('',#11354,#12150,#1891,.T.);
#15985=EDGE_CURVE('',#12151,#11357,#1892,.T.);
#15986=EDGE_CURVE('',#11358,#12152,#1893,.T.);
#15987=EDGE_CURVE('',#12153,#11361,#1894,.T.);
#15988=EDGE_CURVE('',#11362,#12154,#1895,.T.);
#15989=EDGE_CURVE('',#12155,#11365,#1896,.T.);
#15990=EDGE_CURVE('',#11366,#12156,#1897,.T.);
#15991=EDGE_CURVE('',#12157,#11369,#1898,.T.);
#15992=EDGE_CURVE('',#11370,#12158,#1899,.T.);
#15993=EDGE_CURVE('',#12159,#11373,#1900,.T.);
#15994=EDGE_CURVE('',#11374,#12160,#1901,.T.);
#15995=EDGE_CURVE('',#12161,#11377,#1902,.T.);
#15996=EDGE_CURVE('',#11378,#12162,#1903,.T.);
#15997=EDGE_CURVE('',#12163,#11381,#1904,.T.);
#15998=EDGE_CURVE('',#11382,#12164,#1905,.T.);
#15999=EDGE_CURVE('',#12165,#11385,#1906,.T.);
#16000=EDGE_CURVE('',#11386,#12166,#1907,.T.);
#16001=EDGE_CURVE('',#12167,#11389,#1908,.T.);
#16002=EDGE_CURVE('',#11390,#12168,#1909,.T.);
#16003=EDGE_CURVE('',#12169,#11393,#1910,.T.);
#16004=EDGE_CURVE('',#11394,#12170,#1911,.T.);
#16005=EDGE_CURVE('',#12171,#11397,#1912,.T.);
#16006=EDGE_CURVE('',#11398,#12172,#1913,.T.);
#16007=EDGE_CURVE('',#12173,#11401,#1914,.T.);
#16008=EDGE_CURVE('',#11402,#12174,#1915,.T.);
#16009=EDGE_CURVE('',#12175,#11405,#1916,.T.);
#16010=EDGE_CURVE('',#11406,#12176,#1917,.T.);
#16011=EDGE_CURVE('',#12177,#11409,#1918,.T.);
#16012=EDGE_CURVE('',#11410,#12178,#1919,.T.);
#16013=EDGE_CURVE('',#12179,#11413,#1920,.T.);
#16014=EDGE_CURVE('',#11414,#12180,#1921,.T.);
#16015=EDGE_CURVE('',#12181,#11417,#1922,.T.);
#16016=EDGE_CURVE('',#11418,#12182,#1923,.T.);
#16017=EDGE_CURVE('',#12183,#11421,#1924,.T.);
#16018=EDGE_CURVE('',#11422,#12184,#1925,.T.);
#16019=EDGE_CURVE('',#12185,#11425,#1926,.T.);
#16020=EDGE_CURVE('',#11426,#12186,#1927,.T.);
#16021=EDGE_CURVE('',#12187,#11429,#1928,.T.);
#16022=EDGE_CURVE('',#11430,#12188,#1929,.T.);
#16023=EDGE_CURVE('',#12189,#11433,#1930,.T.);
#16024=EDGE_CURVE('',#11434,#12190,#1931,.T.);
#16025=EDGE_CURVE('',#12191,#11437,#1932,.T.);
#16026=EDGE_CURVE('',#11438,#12192,#1933,.T.);
#16027=EDGE_CURVE('',#12193,#11441,#1934,.T.);
#16028=EDGE_CURVE('',#11442,#12194,#1935,.T.);
#16029=EDGE_CURVE('',#12195,#11445,#1936,.T.);
#16030=EDGE_CURVE('',#11446,#12196,#1937,.T.);
#16031=EDGE_CURVE('',#12197,#11449,#1938,.T.);
#16032=EDGE_CURVE('',#11450,#12198,#1939,.T.);
#16033=EDGE_CURVE('',#12199,#11453,#1940,.T.);
#16034=EDGE_CURVE('',#11454,#12200,#1941,.T.);
#16035=EDGE_CURVE('',#12201,#11457,#1942,.T.);
#16036=EDGE_CURVE('',#11458,#12202,#1943,.T.);
#16037=EDGE_CURVE('',#12203,#11461,#1944,.T.);
#16038=EDGE_CURVE('',#11462,#12204,#1945,.T.);
#16039=EDGE_CURVE('',#12205,#11465,#1946,.T.);
#16040=EDGE_CURVE('',#11466,#12206,#1947,.T.);
#16041=EDGE_CURVE('',#12207,#11469,#1948,.T.);
#16042=EDGE_CURVE('',#11470,#12208,#1949,.T.);
#16043=EDGE_CURVE('',#12209,#11473,#1950,.T.);
#16044=EDGE_CURVE('',#11474,#12210,#1951,.T.);
#16045=EDGE_CURVE('',#12211,#11477,#1952,.T.);
#16046=EDGE_CURVE('',#11478,#12212,#1953,.T.);
#16047=EDGE_CURVE('',#12213,#11481,#1954,.T.);
#16048=EDGE_CURVE('',#11482,#12214,#1955,.T.);
#16049=EDGE_CURVE('',#12215,#11485,#1956,.T.);
#16050=EDGE_CURVE('',#11486,#12216,#1957,.T.);
#16051=EDGE_CURVE('',#12217,#11489,#1958,.T.);
#16052=EDGE_CURVE('',#11490,#12218,#1959,.T.);
#16053=EDGE_CURVE('',#12219,#11493,#1960,.T.);
#16054=EDGE_CURVE('',#11494,#12220,#1961,.T.);
#16055=EDGE_CURVE('',#12221,#11497,#1962,.T.);
#16056=EDGE_CURVE('',#11498,#12222,#1963,.T.);
#16057=EDGE_CURVE('',#12223,#11501,#1964,.T.);
#16058=EDGE_CURVE('',#11502,#12224,#1965,.T.);
#16059=EDGE_CURVE('',#11550,#12225,#1966,.T.);
#16060=EDGE_CURVE('',#12226,#11549,#1967,.T.);
#16061=EDGE_CURVE('',#11548,#12227,#1968,.T.);
#16062=EDGE_CURVE('',#12228,#11547,#1969,.T.);
#16063=EDGE_CURVE('',#11546,#12229,#1970,.T.);
#16064=EDGE_CURVE('',#12230,#11545,#1971,.T.);
#16065=EDGE_CURVE('',#11544,#12231,#1972,.T.);
#16066=EDGE_CURVE('',#12232,#11543,#1973,.T.);
#16067=EDGE_CURVE('',#11542,#12233,#1974,.T.);
#16068=EDGE_CURVE('',#12234,#11541,#1975,.T.);
#16069=EDGE_CURVE('',#11540,#12235,#1976,.T.);
#16070=EDGE_CURVE('',#12236,#11539,#1977,.T.);
#16071=EDGE_CURVE('',#11538,#12237,#1978,.T.);
#16072=EDGE_CURVE('',#12238,#11537,#1979,.T.);
#16073=EDGE_CURVE('',#11536,#12239,#1980,.T.);
#16074=EDGE_CURVE('',#12240,#11535,#1981,.T.);
#16075=EDGE_CURVE('',#11534,#12241,#1982,.T.);
#16076=EDGE_CURVE('',#12242,#11533,#1983,.T.);
#16077=EDGE_CURVE('',#11530,#12243,#1984,.T.);
#16078=EDGE_CURVE('',#12244,#11529,#1985,.T.);
#16079=EDGE_CURVE('',#11526,#12245,#1986,.T.);
#16080=EDGE_CURVE('',#12246,#11525,#1987,.T.);
#16081=EDGE_CURVE('',#11522,#12247,#1988,.T.);
#16082=EDGE_CURVE('',#12248,#11521,#1989,.T.);
#16083=EDGE_CURVE('',#11518,#12249,#1990,.T.);
#16084=EDGE_CURVE('',#12250,#11517,#1991,.T.);
#16085=EDGE_CURVE('',#11514,#12251,#1992,.T.);
#16086=EDGE_CURVE('',#12252,#11513,#1993,.T.);
#16087=EDGE_CURVE('',#12253,#11505,#1994,.T.);
#16088=EDGE_CURVE('',#11506,#12254,#1995,.T.);
#16089=EDGE_CURVE('',#11645,#12255,#1996,.T.);
#16090=EDGE_CURVE('',#12256,#11644,#1997,.T.);
#16091=EDGE_CURVE('',#12256,#12255,#3773,.T.);
#16092=EDGE_CURVE('',#12255,#12257,#8908,.T.);
#16093=EDGE_CURVE('',#12258,#12256,#8909,.T.);
#16094=EDGE_CURVE('',#12258,#12257,#3774,.T.);
#16095=EDGE_CURVE('',#12257,#11509,#1998,.T.);
#16096=EDGE_CURVE('',#11510,#12258,#1999,.T.);
#16097=EDGE_CURVE('',#12259,#12260,#8910,.T.);
#16098=EDGE_CURVE('',#12260,#12261,#8911,.T.);
#16099=EDGE_CURVE('',#12261,#12262,#8912,.T.);
#16100=EDGE_CURVE('',#12262,#12263,#8913,.T.);
#16101=EDGE_CURVE('',#12263,#12264,#8914,.T.);
#16102=EDGE_CURVE('',#12264,#12259,#8915,.T.);
#16103=EDGE_CURVE('',#12260,#11345,#8916,.T.);
#16104=EDGE_CURVE('',#12261,#11344,#8917,.T.);
#16105=EDGE_CURVE('',#12262,#11343,#8918,.T.);
#16106=EDGE_CURVE('',#12263,#11341,#8919,.T.);
#16107=EDGE_CURVE('',#12264,#11347,#8920,.T.);
#16108=EDGE_CURVE('',#12259,#11346,#8921,.T.);
#16109=EDGE_CURVE('',#11278,#11160,#3099,.T.);
#16110=EDGE_CURVE('',#11158,#11276,#8922,.T.);
#16111=EDGE_CURVE('',#11642,#11511,#8923,.T.);
#16112=EDGE_CURVE('',#11932,#11512,#8924,.T.);
#16113=EDGE_CURVE('',#11647,#11507,#8925,.T.);
#16114=EDGE_CURVE('',#11646,#11508,#8926,.T.);
#16115=EDGE_CURVE('',#11929,#11515,#8927,.T.);
#16116=EDGE_CURVE('',#11928,#11516,#8928,.T.);
#16117=EDGE_CURVE('',#11925,#11519,#8929,.T.);
#16118=EDGE_CURVE('',#11924,#11520,#8930,.T.);
#16119=EDGE_CURVE('',#11921,#11523,#8931,.T.);
#16120=EDGE_CURVE('',#11920,#11524,#8932,.T.);
#16121=EDGE_CURVE('',#11917,#11527,#8933,.T.);
#16122=EDGE_CURVE('',#11916,#11528,#8934,.T.);
#16123=EDGE_CURVE('',#11913,#11531,#8935,.T.);
#16124=EDGE_CURVE('',#11912,#11532,#8936,.T.);
#16125=EDGE_CURVE('',#11651,#11503,#8937,.T.);
#16126=EDGE_CURVE('',#11650,#11504,#8938,.T.);
#16127=EDGE_CURVE('',#11655,#11499,#8939,.T.);
#16128=EDGE_CURVE('',#11654,#11500,#8940,.T.);
#16129=EDGE_CURVE('',#11659,#11495,#8941,.T.);
#16130=EDGE_CURVE('',#11658,#11496,#8942,.T.);
#16131=EDGE_CURVE('',#11663,#11491,#8943,.T.);
#16132=EDGE_CURVE('',#11662,#11492,#8944,.T.);
#16133=EDGE_CURVE('',#11667,#11487,#8945,.T.);
#16134=EDGE_CURVE('',#11666,#11488,#8946,.T.);
#16135=EDGE_CURVE('',#11671,#11483,#8947,.T.);
#16136=EDGE_CURVE('',#11670,#11484,#8948,.T.);
#16137=EDGE_CURVE('',#11675,#11479,#8949,.T.);
#16138=EDGE_CURVE('',#11674,#11480,#8950,.T.);
#16139=EDGE_CURVE('',#11679,#11475,#8951,.T.);
#16140=EDGE_CURVE('',#11678,#11476,#8952,.T.);
#16141=EDGE_CURVE('',#11683,#11471,#8953,.T.);
#16142=EDGE_CURVE('',#11682,#11472,#8954,.T.);
#16143=EDGE_CURVE('',#11687,#11467,#8955,.T.);
#16144=EDGE_CURVE('',#11686,#11468,#8956,.T.);
#16145=EDGE_CURVE('',#11691,#11463,#8957,.T.);
#16146=EDGE_CURVE('',#11690,#11464,#8958,.T.);
#16147=EDGE_CURVE('',#11695,#11459,#8959,.T.);
#16148=EDGE_CURVE('',#11694,#11460,#8960,.T.);
#16149=EDGE_CURVE('',#11699,#11455,#8961,.T.);
#16150=EDGE_CURVE('',#11698,#11456,#8962,.T.);
#16151=EDGE_CURVE('',#11703,#11451,#8963,.T.);
#16152=EDGE_CURVE('',#11702,#11452,#8964,.T.);
#16153=EDGE_CURVE('',#11707,#11447,#8965,.T.);
#16154=EDGE_CURVE('',#11706,#11448,#8966,.T.);
#16155=EDGE_CURVE('',#11711,#11443,#8967,.T.);
#16156=EDGE_CURVE('',#11710,#11444,#8968,.T.);
#16157=EDGE_CURVE('',#11715,#11439,#8969,.T.);
#16158=EDGE_CURVE('',#11714,#11440,#8970,.T.);
#16159=EDGE_CURVE('',#11719,#11435,#8971,.T.);
#16160=EDGE_CURVE('',#11718,#11436,#8972,.T.);
#16161=EDGE_CURVE('',#11723,#11431,#8973,.T.);
#16162=EDGE_CURVE('',#11722,#11432,#8974,.T.);
#16163=EDGE_CURVE('',#11727,#11427,#8975,.T.);
#16164=EDGE_CURVE('',#11726,#11428,#8976,.T.);
#16165=EDGE_CURVE('',#11731,#11423,#8977,.T.);
#16166=EDGE_CURVE('',#11730,#11424,#8978,.T.);
#16167=EDGE_CURVE('',#11735,#11419,#8979,.T.);
#16168=EDGE_CURVE('',#11734,#11420,#8980,.T.);
#16169=EDGE_CURVE('',#11739,#11415,#8981,.T.);
#16170=EDGE_CURVE('',#11738,#11416,#8982,.T.);
#16171=EDGE_CURVE('',#11743,#11411,#8983,.T.);
#16172=EDGE_CURVE('',#11742,#11412,#8984,.T.);
#16173=EDGE_CURVE('',#11747,#11407,#8985,.T.);
#16174=EDGE_CURVE('',#11746,#11408,#8986,.T.);
#16175=EDGE_CURVE('',#11751,#11403,#8987,.T.);
#16176=EDGE_CURVE('',#11750,#11404,#8988,.T.);
#16177=EDGE_CURVE('',#11755,#11399,#8989,.T.);
#16178=EDGE_CURVE('',#11754,#11400,#8990,.T.);
#16179=EDGE_CURVE('',#11759,#11395,#8991,.T.);
#16180=EDGE_CURVE('',#11758,#11396,#8992,.T.);
#16181=EDGE_CURVE('',#11763,#11391,#8993,.T.);
#16182=EDGE_CURVE('',#11762,#11392,#8994,.T.);
#16183=EDGE_CURVE('',#11767,#11387,#8995,.T.);
#16184=EDGE_CURVE('',#11766,#11388,#8996,.T.);
#16185=EDGE_CURVE('',#11771,#11383,#8997,.T.);
#16186=EDGE_CURVE('',#11770,#11384,#8998,.T.);
#16187=EDGE_CURVE('',#11775,#11379,#8999,.T.);
#16188=EDGE_CURVE('',#11774,#11380,#9000,.T.);
#16189=EDGE_CURVE('',#11779,#11375,#9001,.T.);
#16190=EDGE_CURVE('',#11778,#11376,#9002,.T.);
#16191=EDGE_CURVE('',#11783,#11371,#9003,.T.);
#16192=EDGE_CURVE('',#11782,#11372,#9004,.T.);
#16193=EDGE_CURVE('',#11787,#11367,#9005,.T.);
#16194=EDGE_CURVE('',#11786,#11368,#9006,.T.);
#16195=EDGE_CURVE('',#11791,#11363,#9007,.T.);
#16196=EDGE_CURVE('',#11790,#11364,#9008,.T.);
#16197=EDGE_CURVE('',#11795,#11359,#9009,.T.);
#16198=EDGE_CURVE('',#11794,#11360,#9010,.T.);
#16199=EDGE_CURVE('',#11799,#11355,#9011,.T.);
#16200=EDGE_CURVE('',#11798,#11356,#9012,.T.);
#16201=EDGE_CURVE('',#11803,#11641,#9013,.T.);
#16202=EDGE_CURVE('',#11802,#11351,#9014,.T.);
#16203=EDGE_CURVE('',#11807,#11637,#9015,.T.);
#16204=EDGE_CURVE('',#11806,#11638,#9016,.T.);
#16205=EDGE_CURVE('',#11811,#11633,#9017,.T.);
#16206=EDGE_CURVE('',#11810,#11634,#9018,.T.);
#16207=EDGE_CURVE('',#11815,#11629,#9019,.T.);
#16208=EDGE_CURVE('',#11814,#11630,#9020,.T.);
#16209=EDGE_CURVE('',#11819,#11625,#9021,.T.);
#16210=EDGE_CURVE('',#11818,#11626,#9022,.T.);
#16211=EDGE_CURVE('',#11823,#11621,#9023,.T.);
#16212=EDGE_CURVE('',#11822,#11622,#9024,.T.);
#16213=EDGE_CURVE('',#11827,#11617,#9025,.T.);
#16214=EDGE_CURVE('',#11826,#11618,#9026,.T.);
#16215=EDGE_CURVE('',#11831,#11613,#9027,.T.);
#16216=EDGE_CURVE('',#11830,#11614,#9028,.T.);
#16217=EDGE_CURVE('',#11835,#11609,#9029,.T.);
#16218=EDGE_CURVE('',#11834,#11610,#9030,.T.);
#16219=EDGE_CURVE('',#11839,#11605,#9031,.T.);
#16220=EDGE_CURVE('',#11838,#11606,#9032,.T.);
#16221=EDGE_CURVE('',#11843,#11601,#9033,.T.);
#16222=EDGE_CURVE('',#11842,#11602,#9034,.T.);
#16223=EDGE_CURVE('',#11847,#11597,#9035,.T.);
#16224=EDGE_CURVE('',#11846,#11598,#9036,.T.);
#16225=EDGE_CURVE('',#11851,#11593,#9037,.T.);
#16226=EDGE_CURVE('',#11850,#11594,#9038,.T.);
#16227=EDGE_CURVE('',#11855,#11589,#9039,.T.);
#16228=EDGE_CURVE('',#11854,#11590,#9040,.T.);
#16229=EDGE_CURVE('',#11859,#11585,#9041,.T.);
#16230=EDGE_CURVE('',#11858,#11586,#9042,.T.);
#16231=EDGE_CURVE('',#11863,#11581,#9043,.T.);
#16232=EDGE_CURVE('',#11862,#11582,#9044,.T.);
#16233=EDGE_CURVE('',#11867,#11577,#9045,.T.);
#16234=EDGE_CURVE('',#11866,#11578,#9046,.T.);
#16235=EDGE_CURVE('',#11871,#11573,#9047,.T.);
#16236=EDGE_CURVE('',#11870,#11574,#9048,.T.);
#16237=EDGE_CURVE('',#11875,#11569,#9049,.T.);
#16238=EDGE_CURVE('',#11874,#11570,#9050,.T.);
#16239=EDGE_CURVE('',#11879,#11565,#9051,.T.);
#16240=EDGE_CURVE('',#11878,#11566,#9052,.T.);
#19757=ORIENTED_EDGE('',*,*,#14573,.F.);
#19758=ORIENTED_EDGE('',*,*,#14574,.F.);
#19759=ORIENTED_EDGE('',*,*,#14575,.T.);
#19760=ORIENTED_EDGE('',*,*,#14576,.T.);
#19761=ORIENTED_EDGE('',*,*,#14575,.F.);
#19762=ORIENTED_EDGE('',*,*,#14577,.F.);
#19763=ORIENTED_EDGE('',*,*,#14578,.F.);
#19764=ORIENTED_EDGE('',*,*,#14579,.F.);
#19765=ORIENTED_EDGE('',*,*,#14580,.F.);
#19766=ORIENTED_EDGE('',*,*,#14573,.T.);
#19767=ORIENTED_EDGE('',*,*,#14581,.F.);
#19768=ORIENTED_EDGE('',*,*,#14582,.F.);
#19769=ORIENTED_EDGE('',*,*,#14583,.F.);
#19770=ORIENTED_EDGE('',*,*,#14579,.T.);
#19771=ORIENTED_EDGE('',*,*,#14584,.F.);
#19772=ORIENTED_EDGE('',*,*,#14585,.F.);
#19773=ORIENTED_EDGE('',*,*,#14586,.F.);
#19774=ORIENTED_EDGE('',*,*,#14582,.T.);
#19775=ORIENTED_EDGE('',*,*,#14587,.F.);
#19776=ORIENTED_EDGE('',*,*,#14588,.F.);
#19777=ORIENTED_EDGE('',*,*,#14589,.F.);
#19778=ORIENTED_EDGE('',*,*,#14585,.T.);
#19779=ORIENTED_EDGE('',*,*,#14590,.F.);
#19780=ORIENTED_EDGE('',*,*,#14591,.F.);
#19781=ORIENTED_EDGE('',*,*,#14592,.F.);
#19782=ORIENTED_EDGE('',*,*,#14588,.T.);
#19783=ORIENTED_EDGE('',*,*,#14593,.F.);
#19784=ORIENTED_EDGE('',*,*,#14594,.F.);
#19785=ORIENTED_EDGE('',*,*,#14595,.F.);
#19786=ORIENTED_EDGE('',*,*,#14591,.T.);
#19787=ORIENTED_EDGE('',*,*,#14596,.F.);
#19788=ORIENTED_EDGE('',*,*,#14597,.F.);
#19789=ORIENTED_EDGE('',*,*,#14598,.F.);
#19790=ORIENTED_EDGE('',*,*,#14594,.T.);
#19791=ORIENTED_EDGE('',*,*,#14599,.F.);
#19792=ORIENTED_EDGE('',*,*,#14600,.F.);
#19793=ORIENTED_EDGE('',*,*,#14601,.F.);
#19794=ORIENTED_EDGE('',*,*,#14597,.T.);
#19795=ORIENTED_EDGE('',*,*,#14602,.F.);
#19796=ORIENTED_EDGE('',*,*,#14603,.F.);
#19797=ORIENTED_EDGE('',*,*,#14604,.F.);
#19798=ORIENTED_EDGE('',*,*,#14600,.T.);
#19799=ORIENTED_EDGE('',*,*,#14605,.F.);
#19800=ORIENTED_EDGE('',*,*,#14606,.F.);
#19801=ORIENTED_EDGE('',*,*,#14607,.F.);
#19802=ORIENTED_EDGE('',*,*,#14603,.T.);
#19803=ORIENTED_EDGE('',*,*,#14608,.F.);
#19804=ORIENTED_EDGE('',*,*,#14609,.F.);
#19805=ORIENTED_EDGE('',*,*,#14610,.F.);
#19806=ORIENTED_EDGE('',*,*,#14606,.T.);
#19807=ORIENTED_EDGE('',*,*,#14611,.F.);
#19808=ORIENTED_EDGE('',*,*,#14612,.F.);
#19809=ORIENTED_EDGE('',*,*,#14613,.F.);
#19810=ORIENTED_EDGE('',*,*,#14609,.T.);
#19811=ORIENTED_EDGE('',*,*,#14614,.F.);
#19812=ORIENTED_EDGE('',*,*,#14615,.F.);
#19813=ORIENTED_EDGE('',*,*,#14616,.F.);
#19814=ORIENTED_EDGE('',*,*,#14612,.T.);
#19815=ORIENTED_EDGE('',*,*,#14617,.F.);
#19816=ORIENTED_EDGE('',*,*,#14618,.F.);
#19817=ORIENTED_EDGE('',*,*,#14619,.F.);
#19818=ORIENTED_EDGE('',*,*,#14615,.T.);
#19819=ORIENTED_EDGE('',*,*,#14620,.F.);
#19820=ORIENTED_EDGE('',*,*,#14621,.F.);
#19821=ORIENTED_EDGE('',*,*,#14622,.F.);
#19822=ORIENTED_EDGE('',*,*,#14618,.T.);
#19823=ORIENTED_EDGE('',*,*,#14623,.F.);
#19824=ORIENTED_EDGE('',*,*,#14624,.F.);
#19825=ORIENTED_EDGE('',*,*,#14625,.F.);
#19826=ORIENTED_EDGE('',*,*,#14621,.T.);
#19827=ORIENTED_EDGE('',*,*,#14626,.F.);
#19828=ORIENTED_EDGE('',*,*,#14627,.F.);
#19829=ORIENTED_EDGE('',*,*,#14628,.F.);
#19830=ORIENTED_EDGE('',*,*,#14624,.T.);
#19831=ORIENTED_EDGE('',*,*,#14629,.F.);
#19832=ORIENTED_EDGE('',*,*,#14630,.F.);
#19833=ORIENTED_EDGE('',*,*,#14631,.F.);
#19834=ORIENTED_EDGE('',*,*,#14627,.T.);
#19835=ORIENTED_EDGE('',*,*,#14632,.F.);
#19836=ORIENTED_EDGE('',*,*,#14633,.F.);
#19837=ORIENTED_EDGE('',*,*,#14634,.F.);
#19838=ORIENTED_EDGE('',*,*,#14630,.T.);
#19839=ORIENTED_EDGE('',*,*,#14635,.F.);
#19840=ORIENTED_EDGE('',*,*,#14636,.F.);
#19841=ORIENTED_EDGE('',*,*,#14637,.F.);
#19842=ORIENTED_EDGE('',*,*,#14633,.T.);
#19843=ORIENTED_EDGE('',*,*,#14638,.F.);
#19844=ORIENTED_EDGE('',*,*,#14639,.F.);
#19845=ORIENTED_EDGE('',*,*,#14640,.F.);
#19846=ORIENTED_EDGE('',*,*,#14636,.T.);
#19847=ORIENTED_EDGE('',*,*,#14641,.F.);
#19848=ORIENTED_EDGE('',*,*,#14642,.F.);
#19849=ORIENTED_EDGE('',*,*,#14643,.F.);
#19850=ORIENTED_EDGE('',*,*,#14639,.T.);
#19851=ORIENTED_EDGE('',*,*,#14644,.F.);
#19852=ORIENTED_EDGE('',*,*,#14645,.F.);
#19853=ORIENTED_EDGE('',*,*,#14646,.F.);
#19854=ORIENTED_EDGE('',*,*,#14642,.T.);
#19855=ORIENTED_EDGE('',*,*,#14647,.F.);
#19856=ORIENTED_EDGE('',*,*,#14648,.F.);
#19857=ORIENTED_EDGE('',*,*,#14649,.F.);
#19858=ORIENTED_EDGE('',*,*,#14645,.T.);
#19859=ORIENTED_EDGE('',*,*,#14650,.F.);
#19860=ORIENTED_EDGE('',*,*,#14651,.F.);
#19861=ORIENTED_EDGE('',*,*,#14652,.F.);
#19862=ORIENTED_EDGE('',*,*,#14648,.T.);
#19863=ORIENTED_EDGE('',*,*,#14653,.F.);
#19864=ORIENTED_EDGE('',*,*,#14654,.F.);
#19865=ORIENTED_EDGE('',*,*,#14655,.F.);
#19866=ORIENTED_EDGE('',*,*,#14651,.T.);
#19867=ORIENTED_EDGE('',*,*,#14656,.F.);
#19868=ORIENTED_EDGE('',*,*,#14657,.F.);
#19869=ORIENTED_EDGE('',*,*,#14658,.F.);
#19870=ORIENTED_EDGE('',*,*,#14654,.T.);
#19871=ORIENTED_EDGE('',*,*,#14659,.F.);
#19872=ORIENTED_EDGE('',*,*,#14660,.F.);
#19873=ORIENTED_EDGE('',*,*,#14661,.T.);
#19874=ORIENTED_EDGE('',*,*,#14662,.F.);
#19875=ORIENTED_EDGE('',*,*,#14663,.F.);
#19876=ORIENTED_EDGE('',*,*,#14664,.F.);
#19877=ORIENTED_EDGE('',*,*,#14665,.F.);
#19878=ORIENTED_EDGE('',*,*,#14666,.F.);
#19879=ORIENTED_EDGE('',*,*,#14667,.F.);
#19880=ORIENTED_EDGE('',*,*,#14663,.T.);
#19881=ORIENTED_EDGE('',*,*,#14668,.T.);
#19882=ORIENTED_EDGE('',*,*,#14669,.F.);
#19883=ORIENTED_EDGE('',*,*,#14670,.F.);
#19884=ORIENTED_EDGE('',*,*,#14666,.T.);
#19885=ORIENTED_EDGE('',*,*,#14671,.T.);
#19886=ORIENTED_EDGE('',*,*,#14672,.F.);
#19887=ORIENTED_EDGE('',*,*,#14673,.F.);
#19888=ORIENTED_EDGE('',*,*,#14669,.T.);
#19889=ORIENTED_EDGE('',*,*,#14674,.T.);
#19890=ORIENTED_EDGE('',*,*,#14675,.F.);
#19891=ORIENTED_EDGE('',*,*,#14676,.F.);
#19892=ORIENTED_EDGE('',*,*,#14672,.T.);
#19893=ORIENTED_EDGE('',*,*,#14677,.T.);
#19894=ORIENTED_EDGE('',*,*,#14678,.F.);
#19895=ORIENTED_EDGE('',*,*,#14679,.F.);
#19896=ORIENTED_EDGE('',*,*,#14675,.T.);
#19897=ORIENTED_EDGE('',*,*,#14680,.T.);
#19898=ORIENTED_EDGE('',*,*,#14681,.F.);
#19899=ORIENTED_EDGE('',*,*,#14682,.F.);
#19900=ORIENTED_EDGE('',*,*,#14678,.T.);
#19901=ORIENTED_EDGE('',*,*,#14683,.T.);
#19902=ORIENTED_EDGE('',*,*,#14684,.F.);
#19903=ORIENTED_EDGE('',*,*,#14685,.F.);
#19904=ORIENTED_EDGE('',*,*,#14681,.T.);
#19905=ORIENTED_EDGE('',*,*,#14686,.T.);
#19906=ORIENTED_EDGE('',*,*,#14687,.F.);
#19907=ORIENTED_EDGE('',*,*,#14688,.F.);
#19908=ORIENTED_EDGE('',*,*,#14684,.T.);
#19909=ORIENTED_EDGE('',*,*,#14689,.T.);
#19910=ORIENTED_EDGE('',*,*,#14690,.F.);
#19911=ORIENTED_EDGE('',*,*,#14691,.F.);
#19912=ORIENTED_EDGE('',*,*,#14687,.T.);
#19913=ORIENTED_EDGE('',*,*,#14692,.T.);
#19914=ORIENTED_EDGE('',*,*,#14693,.F.);
#19915=ORIENTED_EDGE('',*,*,#14694,.F.);
#19916=ORIENTED_EDGE('',*,*,#14690,.T.);
#19917=ORIENTED_EDGE('',*,*,#14695,.T.);
#19918=ORIENTED_EDGE('',*,*,#14696,.F.);
#19919=ORIENTED_EDGE('',*,*,#14697,.F.);
#19920=ORIENTED_EDGE('',*,*,#14693,.T.);
#19921=ORIENTED_EDGE('',*,*,#14698,.T.);
#19922=ORIENTED_EDGE('',*,*,#14699,.F.);
#19923=ORIENTED_EDGE('',*,*,#14700,.F.);
#19924=ORIENTED_EDGE('',*,*,#14696,.T.);
#19925=ORIENTED_EDGE('',*,*,#14701,.T.);
#19926=ORIENTED_EDGE('',*,*,#14702,.F.);
#19927=ORIENTED_EDGE('',*,*,#14703,.F.);
#19928=ORIENTED_EDGE('',*,*,#14699,.T.);
#19929=ORIENTED_EDGE('',*,*,#14704,.T.);
#19930=ORIENTED_EDGE('',*,*,#14705,.F.);
#19931=ORIENTED_EDGE('',*,*,#14706,.F.);
#19932=ORIENTED_EDGE('',*,*,#14702,.T.);
#19933=ORIENTED_EDGE('',*,*,#14707,.T.);
#19934=ORIENTED_EDGE('',*,*,#14708,.F.);
#19935=ORIENTED_EDGE('',*,*,#14709,.F.);
#19936=ORIENTED_EDGE('',*,*,#14705,.T.);
#19937=ORIENTED_EDGE('',*,*,#14710,.T.);
#19938=ORIENTED_EDGE('',*,*,#14711,.F.);
#19939=ORIENTED_EDGE('',*,*,#14712,.F.);
#19940=ORIENTED_EDGE('',*,*,#14708,.T.);
#19941=ORIENTED_EDGE('',*,*,#14713,.T.);
#19942=ORIENTED_EDGE('',*,*,#14714,.F.);
#19943=ORIENTED_EDGE('',*,*,#14715,.F.);
#19944=ORIENTED_EDGE('',*,*,#14711,.T.);
#19945=ORIENTED_EDGE('',*,*,#14716,.T.);
#19946=ORIENTED_EDGE('',*,*,#14717,.F.);
#19947=ORIENTED_EDGE('',*,*,#14718,.F.);
#19948=ORIENTED_EDGE('',*,*,#14714,.T.);
#19949=ORIENTED_EDGE('',*,*,#14719,.T.);
#19950=ORIENTED_EDGE('',*,*,#14720,.F.);
#19951=ORIENTED_EDGE('',*,*,#14721,.F.);
#19952=ORIENTED_EDGE('',*,*,#14717,.T.);
#19953=ORIENTED_EDGE('',*,*,#14722,.T.);
#19954=ORIENTED_EDGE('',*,*,#14723,.F.);
#19955=ORIENTED_EDGE('',*,*,#14724,.F.);
#19956=ORIENTED_EDGE('',*,*,#14720,.T.);
#19957=ORIENTED_EDGE('',*,*,#14725,.T.);
#19958=ORIENTED_EDGE('',*,*,#14726,.F.);
#19959=ORIENTED_EDGE('',*,*,#14727,.F.);
#19960=ORIENTED_EDGE('',*,*,#14723,.T.);
#19961=ORIENTED_EDGE('',*,*,#14728,.T.);
#19962=ORIENTED_EDGE('',*,*,#14729,.F.);
#19963=ORIENTED_EDGE('',*,*,#14730,.F.);
#19964=ORIENTED_EDGE('',*,*,#14726,.T.);
#19965=ORIENTED_EDGE('',*,*,#14731,.T.);
#19966=ORIENTED_EDGE('',*,*,#14732,.F.);
#19967=ORIENTED_EDGE('',*,*,#14733,.F.);
#19968=ORIENTED_EDGE('',*,*,#14729,.T.);
#19969=ORIENTED_EDGE('',*,*,#14734,.T.);
#19970=ORIENTED_EDGE('',*,*,#14735,.F.);
#19971=ORIENTED_EDGE('',*,*,#14736,.F.);
#19972=ORIENTED_EDGE('',*,*,#14732,.T.);
#19973=ORIENTED_EDGE('',*,*,#14737,.T.);
#19974=ORIENTED_EDGE('',*,*,#14738,.F.);
#19975=ORIENTED_EDGE('',*,*,#14739,.F.);
#19976=ORIENTED_EDGE('',*,*,#14735,.T.);
#19977=ORIENTED_EDGE('',*,*,#14740,.T.);
#19978=ORIENTED_EDGE('',*,*,#14741,.F.);
#19979=ORIENTED_EDGE('',*,*,#14742,.F.);
#19980=ORIENTED_EDGE('',*,*,#14738,.T.);
#19981=ORIENTED_EDGE('',*,*,#14743,.T.);
#19982=ORIENTED_EDGE('',*,*,#14744,.F.);
#19983=ORIENTED_EDGE('',*,*,#14745,.F.);
#19984=ORIENTED_EDGE('',*,*,#14741,.T.);
#19985=ORIENTED_EDGE('',*,*,#14746,.T.);
#19986=ORIENTED_EDGE('',*,*,#14747,.F.);
#19987=ORIENTED_EDGE('',*,*,#14748,.F.);
#19988=ORIENTED_EDGE('',*,*,#14744,.T.);
#19989=ORIENTED_EDGE('',*,*,#14749,.T.);
#19990=ORIENTED_EDGE('',*,*,#14750,.F.);
#19991=ORIENTED_EDGE('',*,*,#14751,.F.);
#19992=ORIENTED_EDGE('',*,*,#14747,.T.);
#19993=ORIENTED_EDGE('',*,*,#14752,.T.);
#19994=ORIENTED_EDGE('',*,*,#14750,.T.);
#19995=ORIENTED_EDGE('',*,*,#14753,.T.);
#19996=ORIENTED_EDGE('',*,*,#14754,.F.);
#19997=ORIENTED_EDGE('',*,*,#14660,.T.);
#19998=ORIENTED_EDGE('',*,*,#14755,.F.);
#19999=ORIENTED_EDGE('',*,*,#14756,.T.);
#20000=ORIENTED_EDGE('',*,*,#14757,.T.);
#20001=ORIENTED_EDGE('',*,*,#14758,.T.);
#20002=ORIENTED_EDGE('',*,*,#14657,.T.);
#20003=ORIENTED_EDGE('',*,*,#14759,.F.);
#20004=ORIENTED_EDGE('',*,*,#14757,.F.);
#20005=ORIENTED_EDGE('',*,*,#14760,.F.);
#20006=ORIENTED_EDGE('',*,*,#14761,.T.);
#20007=ORIENTED_EDGE('',*,*,#14762,.T.);
#20008=ORIENTED_EDGE('',*,*,#14763,.T.);
#20009=ORIENTED_EDGE('',*,*,#14764,.F.);
#20010=ORIENTED_EDGE('',*,*,#14765,.T.);
#20011=ORIENTED_EDGE('',*,*,#14766,.T.);
#20012=ORIENTED_EDGE('',*,*,#14767,.T.);
#20013=ORIENTED_EDGE('',*,*,#14768,.F.);
#20014=ORIENTED_EDGE('',*,*,#14769,.T.);
#20015=ORIENTED_EDGE('',*,*,#14770,.T.);
#20016=ORIENTED_EDGE('',*,*,#14771,.T.);
#20017=ORIENTED_EDGE('',*,*,#14772,.F.);
#20018=ORIENTED_EDGE('',*,*,#14773,.T.);
#20019=ORIENTED_EDGE('',*,*,#14774,.T.);
#20020=ORIENTED_EDGE('',*,*,#14775,.T.);
#20021=ORIENTED_EDGE('',*,*,#14776,.F.);
#20022=ORIENTED_EDGE('',*,*,#14777,.T.);
#20023=ORIENTED_EDGE('',*,*,#14778,.T.);
#20024=ORIENTED_EDGE('',*,*,#14779,.T.);
#20025=ORIENTED_EDGE('',*,*,#14780,.F.);
#20026=ORIENTED_EDGE('',*,*,#14781,.T.);
#20027=ORIENTED_EDGE('',*,*,#14782,.T.);
#20028=ORIENTED_EDGE('',*,*,#14783,.T.);
#20029=ORIENTED_EDGE('',*,*,#14784,.F.);
#20030=ORIENTED_EDGE('',*,*,#14785,.T.);
#20031=ORIENTED_EDGE('',*,*,#14786,.T.);
#20032=ORIENTED_EDGE('',*,*,#14787,.T.);
#20033=ORIENTED_EDGE('',*,*,#14788,.F.);
#20034=ORIENTED_EDGE('',*,*,#14789,.T.);
#20035=ORIENTED_EDGE('',*,*,#14790,.T.);
#20036=ORIENTED_EDGE('',*,*,#14791,.T.);
#20037=ORIENTED_EDGE('',*,*,#14792,.F.);
#20038=ORIENTED_EDGE('',*,*,#14793,.T.);
#20039=ORIENTED_EDGE('',*,*,#14794,.T.);
#20040=ORIENTED_EDGE('',*,*,#14795,.T.);
#20041=ORIENTED_EDGE('',*,*,#14796,.F.);
#20042=ORIENTED_EDGE('',*,*,#14797,.T.);
#20043=ORIENTED_EDGE('',*,*,#14798,.T.);
#20044=ORIENTED_EDGE('',*,*,#14799,.T.);
#20045=ORIENTED_EDGE('',*,*,#14800,.F.);
#20046=ORIENTED_EDGE('',*,*,#14801,.T.);
#20047=ORIENTED_EDGE('',*,*,#14802,.T.);
#20048=ORIENTED_EDGE('',*,*,#14803,.T.);
#20049=ORIENTED_EDGE('',*,*,#14804,.F.);
#20050=ORIENTED_EDGE('',*,*,#14805,.T.);
#20051=ORIENTED_EDGE('',*,*,#14806,.T.);
#20052=ORIENTED_EDGE('',*,*,#14807,.T.);
#20053=ORIENTED_EDGE('',*,*,#14808,.F.);
#20054=ORIENTED_EDGE('',*,*,#14809,.T.);
#20055=ORIENTED_EDGE('',*,*,#14810,.T.);
#20056=ORIENTED_EDGE('',*,*,#14811,.T.);
#20057=ORIENTED_EDGE('',*,*,#14812,.F.);
#20058=ORIENTED_EDGE('',*,*,#14813,.T.);
#20059=ORIENTED_EDGE('',*,*,#14814,.T.);
#20060=ORIENTED_EDGE('',*,*,#14815,.T.);
#20061=ORIENTED_EDGE('',*,*,#14816,.F.);
#20062=ORIENTED_EDGE('',*,*,#14817,.T.);
#20063=ORIENTED_EDGE('',*,*,#14818,.T.);
#20064=ORIENTED_EDGE('',*,*,#14819,.T.);
#20065=ORIENTED_EDGE('',*,*,#14820,.F.);
#20066=ORIENTED_EDGE('',*,*,#14821,.F.);
#20067=ORIENTED_EDGE('',*,*,#14822,.F.);
#20068=ORIENTED_EDGE('',*,*,#14823,.F.);
#20069=ORIENTED_EDGE('',*,*,#14824,.F.);
#20070=ORIENTED_EDGE('',*,*,#14825,.F.);
#20071=ORIENTED_EDGE('',*,*,#14826,.F.);
#20072=ORIENTED_EDGE('',*,*,#14827,.F.);
#20073=ORIENTED_EDGE('',*,*,#14828,.T.);
#20074=ORIENTED_EDGE('',*,*,#14829,.T.);
#20075=ORIENTED_EDGE('',*,*,#14828,.F.);
#20076=ORIENTED_EDGE('',*,*,#14830,.F.);
#20077=ORIENTED_EDGE('',*,*,#14831,.T.);
#20078=ORIENTED_EDGE('',*,*,#14832,.T.);
#20079=ORIENTED_EDGE('',*,*,#14831,.F.);
#20080=ORIENTED_EDGE('',*,*,#14833,.F.);
#20081=ORIENTED_EDGE('',*,*,#14834,.F.);
#20082=ORIENTED_EDGE('',*,*,#14835,.F.);
#20083=ORIENTED_EDGE('',*,*,#14836,.F.);
#20084=ORIENTED_EDGE('',*,*,#14837,.F.);
#20085=ORIENTED_EDGE('',*,*,#14838,.F.);
#20086=ORIENTED_EDGE('',*,*,#14839,.F.);
#20087=ORIENTED_EDGE('',*,*,#14840,.F.);
#20088=ORIENTED_EDGE('',*,*,#14841,.F.);
#20089=ORIENTED_EDGE('',*,*,#14842,.F.);
#20090=ORIENTED_EDGE('',*,*,#14843,.F.);
#20091=ORIENTED_EDGE('',*,*,#14844,.F.);
#20092=ORIENTED_EDGE('',*,*,#14845,.F.);
#20093=ORIENTED_EDGE('',*,*,#14846,.F.);
#20094=ORIENTED_EDGE('',*,*,#14847,.F.);
#20095=ORIENTED_EDGE('',*,*,#14848,.F.);
#20096=ORIENTED_EDGE('',*,*,#14849,.F.);
#20097=ORIENTED_EDGE('',*,*,#14850,.F.);
#20098=ORIENTED_EDGE('',*,*,#14851,.F.);
#20099=ORIENTED_EDGE('',*,*,#14852,.F.);
#20100=ORIENTED_EDGE('',*,*,#14853,.F.);
#20101=ORIENTED_EDGE('',*,*,#14854,.F.);
#20102=ORIENTED_EDGE('',*,*,#14855,.F.);
#20103=ORIENTED_EDGE('',*,*,#14856,.F.);
#20104=ORIENTED_EDGE('',*,*,#14857,.F.);
#20105=ORIENTED_EDGE('',*,*,#14858,.F.);
#20106=ORIENTED_EDGE('',*,*,#14859,.F.);
#20107=ORIENTED_EDGE('',*,*,#14860,.F.);
#20108=ORIENTED_EDGE('',*,*,#14861,.F.);
#20109=ORIENTED_EDGE('',*,*,#14862,.F.);
#20110=ORIENTED_EDGE('',*,*,#14863,.F.);
#20111=ORIENTED_EDGE('',*,*,#14864,.F.);
#20112=ORIENTED_EDGE('',*,*,#14865,.F.);
#20113=ORIENTED_EDGE('',*,*,#14866,.F.);
#20114=ORIENTED_EDGE('',*,*,#14867,.F.);
#20115=ORIENTED_EDGE('',*,*,#14868,.F.);
#20116=ORIENTED_EDGE('',*,*,#14869,.F.);
#20117=ORIENTED_EDGE('',*,*,#14870,.F.);
#20118=ORIENTED_EDGE('',*,*,#14871,.F.);
#20119=ORIENTED_EDGE('',*,*,#14872,.F.);
#20120=ORIENTED_EDGE('',*,*,#14873,.F.);
#20121=ORIENTED_EDGE('',*,*,#14874,.F.);
#20122=ORIENTED_EDGE('',*,*,#14875,.F.);
#20123=ORIENTED_EDGE('',*,*,#14876,.F.);
#20124=ORIENTED_EDGE('',*,*,#14877,.F.);
#20125=ORIENTED_EDGE('',*,*,#14878,.F.);
#20126=ORIENTED_EDGE('',*,*,#14879,.F.);
#20127=ORIENTED_EDGE('',*,*,#14880,.F.);
#20128=ORIENTED_EDGE('',*,*,#14881,.F.);
#20129=ORIENTED_EDGE('',*,*,#14882,.F.);
#20130=ORIENTED_EDGE('',*,*,#14883,.F.);
#20131=ORIENTED_EDGE('',*,*,#14884,.F.);
#20132=ORIENTED_EDGE('',*,*,#14885,.F.);
#20133=ORIENTED_EDGE('',*,*,#14886,.F.);
#20134=ORIENTED_EDGE('',*,*,#14887,.F.);
#20135=ORIENTED_EDGE('',*,*,#14888,.F.);
#20136=ORIENTED_EDGE('',*,*,#14889,.F.);
#20137=ORIENTED_EDGE('',*,*,#14890,.F.);
#20138=ORIENTED_EDGE('',*,*,#14891,.F.);
#20139=ORIENTED_EDGE('',*,*,#14892,.F.);
#20140=ORIENTED_EDGE('',*,*,#14893,.F.);
#20141=ORIENTED_EDGE('',*,*,#14894,.F.);
#20142=ORIENTED_EDGE('',*,*,#14895,.F.);
#20143=ORIENTED_EDGE('',*,*,#14896,.F.);
#20144=ORIENTED_EDGE('',*,*,#14897,.F.);
#20145=ORIENTED_EDGE('',*,*,#14898,.F.);
#20146=ORIENTED_EDGE('',*,*,#14899,.F.);
#20147=ORIENTED_EDGE('',*,*,#14900,.F.);
#20148=ORIENTED_EDGE('',*,*,#14901,.F.);
#20149=ORIENTED_EDGE('',*,*,#14902,.F.);
#20150=ORIENTED_EDGE('',*,*,#14903,.F.);
#20151=ORIENTED_EDGE('',*,*,#14904,.F.);
#20152=ORIENTED_EDGE('',*,*,#14905,.F.);
#20153=ORIENTED_EDGE('',*,*,#14906,.F.);
#20154=ORIENTED_EDGE('',*,*,#14907,.F.);
#20155=ORIENTED_EDGE('',*,*,#14908,.F.);
#20156=ORIENTED_EDGE('',*,*,#14909,.F.);
#20157=ORIENTED_EDGE('',*,*,#14910,.F.);
#20158=ORIENTED_EDGE('',*,*,#14911,.F.);
#20159=ORIENTED_EDGE('',*,*,#14912,.F.);
#20160=ORIENTED_EDGE('',*,*,#14913,.F.);
#20161=ORIENTED_EDGE('',*,*,#14914,.F.);
#20162=ORIENTED_EDGE('',*,*,#14915,.F.);
#20163=ORIENTED_EDGE('',*,*,#14916,.F.);
#20164=ORIENTED_EDGE('',*,*,#14917,.F.);
#20165=ORIENTED_EDGE('',*,*,#14918,.F.);
#20166=ORIENTED_EDGE('',*,*,#14919,.F.);
#20167=ORIENTED_EDGE('',*,*,#14920,.F.);
#20168=ORIENTED_EDGE('',*,*,#14921,.F.);
#20169=ORIENTED_EDGE('',*,*,#14922,.F.);
#20170=ORIENTED_EDGE('',*,*,#14923,.F.);
#20171=ORIENTED_EDGE('',*,*,#14924,.F.);
#20172=ORIENTED_EDGE('',*,*,#14925,.F.);
#20173=ORIENTED_EDGE('',*,*,#14926,.F.);
#20174=ORIENTED_EDGE('',*,*,#14927,.F.);
#20175=ORIENTED_EDGE('',*,*,#14928,.F.);
#20176=ORIENTED_EDGE('',*,*,#14929,.F.);
#20177=ORIENTED_EDGE('',*,*,#14930,.F.);
#20178=ORIENTED_EDGE('',*,*,#14931,.F.);
#20179=ORIENTED_EDGE('',*,*,#14932,.F.);
#20180=ORIENTED_EDGE('',*,*,#14933,.F.);
#20181=ORIENTED_EDGE('',*,*,#14934,.F.);
#20182=ORIENTED_EDGE('',*,*,#14935,.F.);
#20183=ORIENTED_EDGE('',*,*,#14936,.F.);
#20184=ORIENTED_EDGE('',*,*,#14937,.F.);
#20185=ORIENTED_EDGE('',*,*,#14938,.F.);
#20186=ORIENTED_EDGE('',*,*,#14939,.F.);
#20187=ORIENTED_EDGE('',*,*,#14940,.F.);
#20188=ORIENTED_EDGE('',*,*,#14941,.F.);
#20189=ORIENTED_EDGE('',*,*,#14942,.F.);
#20190=ORIENTED_EDGE('',*,*,#14943,.F.);
#20191=ORIENTED_EDGE('',*,*,#14944,.F.);
#20192=ORIENTED_EDGE('',*,*,#14945,.F.);
#20193=ORIENTED_EDGE('',*,*,#14946,.F.);
#20194=ORIENTED_EDGE('',*,*,#14947,.F.);
#20195=ORIENTED_EDGE('',*,*,#14948,.F.);
#20196=ORIENTED_EDGE('',*,*,#14949,.F.);
#20197=ORIENTED_EDGE('',*,*,#14950,.F.);
#20198=ORIENTED_EDGE('',*,*,#14951,.F.);
#20199=ORIENTED_EDGE('',*,*,#14952,.F.);
#20200=ORIENTED_EDGE('',*,*,#14953,.F.);
#20201=ORIENTED_EDGE('',*,*,#14954,.F.);
#20202=ORIENTED_EDGE('',*,*,#14955,.F.);
#20203=ORIENTED_EDGE('',*,*,#14956,.F.);
#20204=ORIENTED_EDGE('',*,*,#14957,.F.);
#20205=ORIENTED_EDGE('',*,*,#14958,.F.);
#20206=ORIENTED_EDGE('',*,*,#14959,.F.);
#20207=ORIENTED_EDGE('',*,*,#14960,.F.);
#20208=ORIENTED_EDGE('',*,*,#14961,.F.);
#20209=ORIENTED_EDGE('',*,*,#14962,.F.);
#20210=ORIENTED_EDGE('',*,*,#14963,.F.);
#20211=ORIENTED_EDGE('',*,*,#14964,.F.);
#20212=ORIENTED_EDGE('',*,*,#14965,.F.);
#20213=ORIENTED_EDGE('',*,*,#14966,.F.);
#20214=ORIENTED_EDGE('',*,*,#14967,.F.);
#20215=ORIENTED_EDGE('',*,*,#14968,.F.);
#20216=ORIENTED_EDGE('',*,*,#14969,.F.);
#20217=ORIENTED_EDGE('',*,*,#14970,.F.);
#20218=ORIENTED_EDGE('',*,*,#14971,.F.);
#20219=ORIENTED_EDGE('',*,*,#14972,.F.);
#20220=ORIENTED_EDGE('',*,*,#14973,.F.);
#20221=ORIENTED_EDGE('',*,*,#14974,.F.);
#20222=ORIENTED_EDGE('',*,*,#14975,.F.);
#20223=ORIENTED_EDGE('',*,*,#14976,.F.);
#20224=ORIENTED_EDGE('',*,*,#14977,.F.);
#20225=ORIENTED_EDGE('',*,*,#14978,.F.);
#20226=ORIENTED_EDGE('',*,*,#14979,.F.);
#20227=ORIENTED_EDGE('',*,*,#14980,.F.);
#20228=ORIENTED_EDGE('',*,*,#14981,.F.);
#20229=ORIENTED_EDGE('',*,*,#14982,.F.);
#20230=ORIENTED_EDGE('',*,*,#14983,.F.);
#20231=ORIENTED_EDGE('',*,*,#14984,.F.);
#20232=ORIENTED_EDGE('',*,*,#14985,.F.);
#20233=ORIENTED_EDGE('',*,*,#14986,.F.);
#20234=ORIENTED_EDGE('',*,*,#14987,.F.);
#20235=ORIENTED_EDGE('',*,*,#14988,.F.);
#20236=ORIENTED_EDGE('',*,*,#14989,.F.);
#20237=ORIENTED_EDGE('',*,*,#14990,.F.);
#20238=ORIENTED_EDGE('',*,*,#14991,.F.);
#20239=ORIENTED_EDGE('',*,*,#14992,.F.);
#20240=ORIENTED_EDGE('',*,*,#14993,.F.);
#20241=ORIENTED_EDGE('',*,*,#14994,.F.);
#20242=ORIENTED_EDGE('',*,*,#14995,.F.);
#20243=ORIENTED_EDGE('',*,*,#14996,.F.);
#20244=ORIENTED_EDGE('',*,*,#14997,.F.);
#20245=ORIENTED_EDGE('',*,*,#14998,.F.);
#20246=ORIENTED_EDGE('',*,*,#14999,.F.);
#20247=ORIENTED_EDGE('',*,*,#15000,.F.);
#20248=ORIENTED_EDGE('',*,*,#15001,.F.);
#20249=ORIENTED_EDGE('',*,*,#15002,.F.);
#20250=ORIENTED_EDGE('',*,*,#15003,.F.);
#20251=ORIENTED_EDGE('',*,*,#15004,.F.);
#20252=ORIENTED_EDGE('',*,*,#15005,.F.);
#20253=ORIENTED_EDGE('',*,*,#15006,.F.);
#20254=ORIENTED_EDGE('',*,*,#15007,.F.);
#20255=ORIENTED_EDGE('',*,*,#15008,.F.);
#20256=ORIENTED_EDGE('',*,*,#15009,.F.);
#20257=ORIENTED_EDGE('',*,*,#15010,.F.);
#20258=ORIENTED_EDGE('',*,*,#15011,.F.);
#20259=ORIENTED_EDGE('',*,*,#15012,.F.);
#20260=ORIENTED_EDGE('',*,*,#15013,.F.);
#20261=ORIENTED_EDGE('',*,*,#15014,.F.);
#20262=ORIENTED_EDGE('',*,*,#15015,.F.);
#20263=ORIENTED_EDGE('',*,*,#15016,.F.);
#20264=ORIENTED_EDGE('',*,*,#14819,.F.);
#20265=ORIENTED_EDGE('',*,*,#15017,.F.);
#20266=ORIENTED_EDGE('',*,*,#15018,.F.);
#20267=ORIENTED_EDGE('',*,*,#15019,.F.);
#20268=ORIENTED_EDGE('',*,*,#14815,.F.);
#20269=ORIENTED_EDGE('',*,*,#15020,.F.);
#20270=ORIENTED_EDGE('',*,*,#15021,.F.);
#20271=ORIENTED_EDGE('',*,*,#15022,.F.);
#20272=ORIENTED_EDGE('',*,*,#14811,.F.);
#20273=ORIENTED_EDGE('',*,*,#15023,.F.);
#20274=ORIENTED_EDGE('',*,*,#15024,.F.);
#20275=ORIENTED_EDGE('',*,*,#15025,.F.);
#20276=ORIENTED_EDGE('',*,*,#14807,.F.);
#20277=ORIENTED_EDGE('',*,*,#15026,.F.);
#20278=ORIENTED_EDGE('',*,*,#15027,.F.);
#20279=ORIENTED_EDGE('',*,*,#15028,.F.);
#20280=ORIENTED_EDGE('',*,*,#14803,.F.);
#20281=ORIENTED_EDGE('',*,*,#15029,.F.);
#20282=ORIENTED_EDGE('',*,*,#15030,.F.);
#20283=ORIENTED_EDGE('',*,*,#15031,.F.);
#20284=ORIENTED_EDGE('',*,*,#14799,.F.);
#20285=ORIENTED_EDGE('',*,*,#15032,.F.);
#20286=ORIENTED_EDGE('',*,*,#15033,.F.);
#20287=ORIENTED_EDGE('',*,*,#15034,.F.);
#20288=ORIENTED_EDGE('',*,*,#14795,.F.);
#20289=ORIENTED_EDGE('',*,*,#15035,.F.);
#20290=ORIENTED_EDGE('',*,*,#15036,.F.);
#20291=ORIENTED_EDGE('',*,*,#15037,.F.);
#20292=ORIENTED_EDGE('',*,*,#14791,.F.);
#20293=ORIENTED_EDGE('',*,*,#15038,.F.);
#20294=ORIENTED_EDGE('',*,*,#15039,.F.);
#20295=ORIENTED_EDGE('',*,*,#15040,.F.);
#20296=ORIENTED_EDGE('',*,*,#14787,.F.);
#20297=ORIENTED_EDGE('',*,*,#15041,.F.);
#20298=ORIENTED_EDGE('',*,*,#15042,.F.);
#20299=ORIENTED_EDGE('',*,*,#15043,.F.);
#20300=ORIENTED_EDGE('',*,*,#14763,.F.);
#20301=ORIENTED_EDGE('',*,*,#15044,.F.);
#20302=ORIENTED_EDGE('',*,*,#15045,.F.);
#20303=ORIENTED_EDGE('',*,*,#15046,.F.);
#20304=ORIENTED_EDGE('',*,*,#14767,.F.);
#20305=ORIENTED_EDGE('',*,*,#15047,.F.);
#20306=ORIENTED_EDGE('',*,*,#15048,.F.);
#20307=ORIENTED_EDGE('',*,*,#15049,.F.);
#20308=ORIENTED_EDGE('',*,*,#14771,.F.);
#20309=ORIENTED_EDGE('',*,*,#15050,.F.);
#20310=ORIENTED_EDGE('',*,*,#15051,.F.);
#20311=ORIENTED_EDGE('',*,*,#15052,.F.);
#20312=ORIENTED_EDGE('',*,*,#14775,.F.);
#20313=ORIENTED_EDGE('',*,*,#15053,.F.);
#20314=ORIENTED_EDGE('',*,*,#15054,.F.);
#20315=ORIENTED_EDGE('',*,*,#15055,.F.);
#20316=ORIENTED_EDGE('',*,*,#14779,.F.);
#20317=ORIENTED_EDGE('',*,*,#15056,.F.);
#20318=ORIENTED_EDGE('',*,*,#15057,.F.);
#20319=ORIENTED_EDGE('',*,*,#15058,.F.);
#20320=ORIENTED_EDGE('',*,*,#14783,.F.);
#20321=ORIENTED_EDGE('',*,*,#15059,.F.);
#20322=ORIENTED_EDGE('',*,*,#15060,.F.);
#20323=ORIENTED_EDGE('',*,*,#15061,.F.);
#20324=ORIENTED_EDGE('',*,*,#15062,.F.);
#20325=ORIENTED_EDGE('',*,*,#15063,.F.);
#20326=ORIENTED_EDGE('',*,*,#15064,.F.);
#20327=ORIENTED_EDGE('',*,*,#15065,.F.);
#20328=ORIENTED_EDGE('',*,*,#15066,.F.);
#20329=ORIENTED_EDGE('',*,*,#15067,.F.);
#20330=ORIENTED_EDGE('',*,*,#15068,.F.);
#20331=ORIENTED_EDGE('',*,*,#15069,.F.);
#20332=ORIENTED_EDGE('',*,*,#15070,.F.);
#20333=ORIENTED_EDGE('',*,*,#15071,.F.);
#20334=ORIENTED_EDGE('',*,*,#15072,.F.);
#20335=ORIENTED_EDGE('',*,*,#15073,.F.);
#20336=ORIENTED_EDGE('',*,*,#15074,.F.);
#20337=ORIENTED_EDGE('',*,*,#15075,.F.);
#20338=ORIENTED_EDGE('',*,*,#15076,.F.);
#20339=ORIENTED_EDGE('',*,*,#15077,.F.);
#20340=ORIENTED_EDGE('',*,*,#15078,.F.);
#20341=ORIENTED_EDGE('',*,*,#15079,.F.);
#20342=ORIENTED_EDGE('',*,*,#15080,.F.);
#20343=ORIENTED_EDGE('',*,*,#15081,.F.);
#20344=ORIENTED_EDGE('',*,*,#15082,.F.);
#20345=ORIENTED_EDGE('',*,*,#15083,.F.);
#20346=ORIENTED_EDGE('',*,*,#15084,.F.);
#20347=ORIENTED_EDGE('',*,*,#15085,.F.);
#20348=ORIENTED_EDGE('',*,*,#15086,.F.);
#20349=ORIENTED_EDGE('',*,*,#15087,.F.);
#20350=ORIENTED_EDGE('',*,*,#15088,.F.);
#20351=ORIENTED_EDGE('',*,*,#15089,.F.);
#20352=ORIENTED_EDGE('',*,*,#15090,.F.);
#20353=ORIENTED_EDGE('',*,*,#15091,.F.);
#20354=ORIENTED_EDGE('',*,*,#15092,.F.);
#20355=ORIENTED_EDGE('',*,*,#15093,.F.);
#20356=ORIENTED_EDGE('',*,*,#15094,.F.);
#20357=ORIENTED_EDGE('',*,*,#15095,.F.);
#20358=ORIENTED_EDGE('',*,*,#15096,.F.);
#20359=ORIENTED_EDGE('',*,*,#15097,.F.);
#20360=ORIENTED_EDGE('',*,*,#15098,.F.);
#20361=ORIENTED_EDGE('',*,*,#15099,.F.);
#20362=ORIENTED_EDGE('',*,*,#15100,.F.);
#20363=ORIENTED_EDGE('',*,*,#15101,.F.);
#20364=ORIENTED_EDGE('',*,*,#15102,.F.);
#20365=ORIENTED_EDGE('',*,*,#15103,.F.);
#20366=ORIENTED_EDGE('',*,*,#15104,.F.);
#20367=ORIENTED_EDGE('',*,*,#15105,.F.);
#20368=ORIENTED_EDGE('',*,*,#15106,.F.);
#20369=ORIENTED_EDGE('',*,*,#15107,.F.);
#20370=ORIENTED_EDGE('',*,*,#15108,.F.);
#20371=ORIENTED_EDGE('',*,*,#15109,.F.);
#20372=ORIENTED_EDGE('',*,*,#15110,.F.);
#20373=ORIENTED_EDGE('',*,*,#15111,.F.);
#20374=ORIENTED_EDGE('',*,*,#15112,.F.);
#20375=ORIENTED_EDGE('',*,*,#15113,.F.);
#20376=ORIENTED_EDGE('',*,*,#15114,.F.);
#20377=ORIENTED_EDGE('',*,*,#15115,.F.);
#20378=ORIENTED_EDGE('',*,*,#15116,.F.);
#20379=ORIENTED_EDGE('',*,*,#15117,.F.);
#20380=ORIENTED_EDGE('',*,*,#15118,.F.);
#20381=ORIENTED_EDGE('',*,*,#15119,.F.);
#20382=ORIENTED_EDGE('',*,*,#15120,.F.);
#20383=ORIENTED_EDGE('',*,*,#15121,.F.);
#20384=ORIENTED_EDGE('',*,*,#15122,.F.);
#20385=ORIENTED_EDGE('',*,*,#15123,.F.);
#20386=ORIENTED_EDGE('',*,*,#15124,.F.);
#20387=ORIENTED_EDGE('',*,*,#15125,.F.);
#20388=ORIENTED_EDGE('',*,*,#15126,.F.);
#20389=ORIENTED_EDGE('',*,*,#15127,.F.);
#20390=ORIENTED_EDGE('',*,*,#15128,.F.);
#20391=ORIENTED_EDGE('',*,*,#15129,.F.);
#20392=ORIENTED_EDGE('',*,*,#15130,.F.);
#20393=ORIENTED_EDGE('',*,*,#15131,.F.);
#20394=ORIENTED_EDGE('',*,*,#15132,.F.);
#20395=ORIENTED_EDGE('',*,*,#15133,.F.);
#20396=ORIENTED_EDGE('',*,*,#15134,.F.);
#20397=ORIENTED_EDGE('',*,*,#15135,.F.);
#20398=ORIENTED_EDGE('',*,*,#15136,.F.);
#20399=ORIENTED_EDGE('',*,*,#15137,.F.);
#20400=ORIENTED_EDGE('',*,*,#15138,.F.);
#20401=ORIENTED_EDGE('',*,*,#15139,.T.);
#20402=ORIENTED_EDGE('',*,*,#14830,.T.);
#20403=ORIENTED_EDGE('',*,*,#15139,.F.);
#20404=ORIENTED_EDGE('',*,*,#15140,.F.);
#20405=ORIENTED_EDGE('',*,*,#15141,.F.);
#20406=ORIENTED_EDGE('',*,*,#15142,.T.);
#20407=ORIENTED_EDGE('',*,*,#15143,.F.);
#20408=ORIENTED_EDGE('',*,*,#15144,.F.);
#20409=ORIENTED_EDGE('',*,*,#15145,.F.);
#20410=ORIENTED_EDGE('',*,*,#15146,.T.);
#20411=ORIENTED_EDGE('',*,*,#15147,.F.);
#20412=ORIENTED_EDGE('',*,*,#15148,.F.);
#20413=ORIENTED_EDGE('',*,*,#15149,.F.);
#20414=ORIENTED_EDGE('',*,*,#15150,.T.);
#20415=ORIENTED_EDGE('',*,*,#15151,.F.);
#20416=ORIENTED_EDGE('',*,*,#15152,.F.);
#20417=ORIENTED_EDGE('',*,*,#15153,.F.);
#20418=ORIENTED_EDGE('',*,*,#15154,.T.);
#20419=ORIENTED_EDGE('',*,*,#15155,.F.);
#20420=ORIENTED_EDGE('',*,*,#15156,.F.);
#20421=ORIENTED_EDGE('',*,*,#15157,.F.);
#20422=ORIENTED_EDGE('',*,*,#15158,.T.);
#20423=ORIENTED_EDGE('',*,*,#15159,.F.);
#20424=ORIENTED_EDGE('',*,*,#15160,.F.);
#20425=ORIENTED_EDGE('',*,*,#15161,.F.);
#20426=ORIENTED_EDGE('',*,*,#15162,.T.);
#20427=ORIENTED_EDGE('',*,*,#15163,.F.);
#20428=ORIENTED_EDGE('',*,*,#15164,.F.);
#20429=ORIENTED_EDGE('',*,*,#15165,.F.);
#20430=ORIENTED_EDGE('',*,*,#15166,.T.);
#20431=ORIENTED_EDGE('',*,*,#15167,.F.);
#20432=ORIENTED_EDGE('',*,*,#15168,.F.);
#20433=ORIENTED_EDGE('',*,*,#15169,.F.);
#20434=ORIENTED_EDGE('',*,*,#15170,.T.);
#20435=ORIENTED_EDGE('',*,*,#15171,.F.);
#20436=ORIENTED_EDGE('',*,*,#15172,.F.);
#20437=ORIENTED_EDGE('',*,*,#15173,.F.);
#20438=ORIENTED_EDGE('',*,*,#15174,.T.);
#20439=ORIENTED_EDGE('',*,*,#15175,.F.);
#20440=ORIENTED_EDGE('',*,*,#15176,.F.);
#20441=ORIENTED_EDGE('',*,*,#15177,.F.);
#20442=ORIENTED_EDGE('',*,*,#15178,.T.);
#20443=ORIENTED_EDGE('',*,*,#15179,.F.);
#20444=ORIENTED_EDGE('',*,*,#15180,.F.);
#20445=ORIENTED_EDGE('',*,*,#15181,.F.);
#20446=ORIENTED_EDGE('',*,*,#15182,.T.);
#20447=ORIENTED_EDGE('',*,*,#15183,.F.);
#20448=ORIENTED_EDGE('',*,*,#15184,.F.);
#20449=ORIENTED_EDGE('',*,*,#15185,.F.);
#20450=ORIENTED_EDGE('',*,*,#15186,.T.);
#20451=ORIENTED_EDGE('',*,*,#15187,.F.);
#20452=ORIENTED_EDGE('',*,*,#15188,.F.);
#20453=ORIENTED_EDGE('',*,*,#15189,.F.);
#20454=ORIENTED_EDGE('',*,*,#15190,.T.);
#20455=ORIENTED_EDGE('',*,*,#15191,.F.);
#20456=ORIENTED_EDGE('',*,*,#15192,.F.);
#20457=ORIENTED_EDGE('',*,*,#15193,.F.);
#20458=ORIENTED_EDGE('',*,*,#15194,.T.);
#20459=ORIENTED_EDGE('',*,*,#15195,.F.);
#20460=ORIENTED_EDGE('',*,*,#15196,.F.);
#20461=ORIENTED_EDGE('',*,*,#15197,.F.);
#20462=ORIENTED_EDGE('',*,*,#15198,.T.);
#20463=ORIENTED_EDGE('',*,*,#15199,.F.);
#20464=ORIENTED_EDGE('',*,*,#15200,.F.);
#20465=ORIENTED_EDGE('',*,*,#15201,.F.);
#20466=ORIENTED_EDGE('',*,*,#15202,.T.);
#20467=ORIENTED_EDGE('',*,*,#15203,.F.);
#20468=ORIENTED_EDGE('',*,*,#15204,.F.);
#20469=ORIENTED_EDGE('',*,*,#15205,.F.);
#20470=ORIENTED_EDGE('',*,*,#15206,.T.);
#20471=ORIENTED_EDGE('',*,*,#15207,.F.);
#20472=ORIENTED_EDGE('',*,*,#15208,.F.);
#20473=ORIENTED_EDGE('',*,*,#15209,.F.);
#20474=ORIENTED_EDGE('',*,*,#15210,.T.);
#20475=ORIENTED_EDGE('',*,*,#15211,.F.);
#20476=ORIENTED_EDGE('',*,*,#15212,.F.);
#20477=ORIENTED_EDGE('',*,*,#15213,.F.);
#20478=ORIENTED_EDGE('',*,*,#15214,.T.);
#20479=ORIENTED_EDGE('',*,*,#15215,.F.);
#20480=ORIENTED_EDGE('',*,*,#15216,.F.);
#20481=ORIENTED_EDGE('',*,*,#15217,.F.);
#20482=ORIENTED_EDGE('',*,*,#15218,.T.);
#20483=ORIENTED_EDGE('',*,*,#15219,.F.);
#20484=ORIENTED_EDGE('',*,*,#15220,.F.);
#20485=ORIENTED_EDGE('',*,*,#15221,.F.);
#20486=ORIENTED_EDGE('',*,*,#15222,.T.);
#20487=ORIENTED_EDGE('',*,*,#15223,.F.);
#20488=ORIENTED_EDGE('',*,*,#15224,.F.);
#20489=ORIENTED_EDGE('',*,*,#15225,.F.);
#20490=ORIENTED_EDGE('',*,*,#15226,.T.);
#20491=ORIENTED_EDGE('',*,*,#15227,.F.);
#20492=ORIENTED_EDGE('',*,*,#15228,.F.);
#20493=ORIENTED_EDGE('',*,*,#15229,.F.);
#20494=ORIENTED_EDGE('',*,*,#15230,.T.);
#20495=ORIENTED_EDGE('',*,*,#15231,.F.);
#20496=ORIENTED_EDGE('',*,*,#15232,.F.);
#20497=ORIENTED_EDGE('',*,*,#15233,.F.);
#20498=ORIENTED_EDGE('',*,*,#15234,.T.);
#20499=ORIENTED_EDGE('',*,*,#15235,.F.);
#20500=ORIENTED_EDGE('',*,*,#15236,.F.);
#20501=ORIENTED_EDGE('',*,*,#15237,.F.);
#20502=ORIENTED_EDGE('',*,*,#15238,.T.);
#20503=ORIENTED_EDGE('',*,*,#15239,.F.);
#20504=ORIENTED_EDGE('',*,*,#15240,.F.);
#20505=ORIENTED_EDGE('',*,*,#15241,.F.);
#20506=ORIENTED_EDGE('',*,*,#15242,.T.);
#20507=ORIENTED_EDGE('',*,*,#15243,.F.);
#20508=ORIENTED_EDGE('',*,*,#15244,.F.);
#20509=ORIENTED_EDGE('',*,*,#15245,.F.);
#20510=ORIENTED_EDGE('',*,*,#15246,.T.);
#20511=ORIENTED_EDGE('',*,*,#15247,.F.);
#20512=ORIENTED_EDGE('',*,*,#15248,.F.);
#20513=ORIENTED_EDGE('',*,*,#15249,.F.);
#20514=ORIENTED_EDGE('',*,*,#15250,.T.);
#20515=ORIENTED_EDGE('',*,*,#15251,.F.);
#20516=ORIENTED_EDGE('',*,*,#15252,.F.);
#20517=ORIENTED_EDGE('',*,*,#15253,.F.);
#20518=ORIENTED_EDGE('',*,*,#15254,.T.);
#20519=ORIENTED_EDGE('',*,*,#15255,.F.);
#20520=ORIENTED_EDGE('',*,*,#15256,.F.);
#20521=ORIENTED_EDGE('',*,*,#15257,.F.);
#20522=ORIENTED_EDGE('',*,*,#15258,.T.);
#20523=ORIENTED_EDGE('',*,*,#15259,.F.);
#20524=ORIENTED_EDGE('',*,*,#15260,.F.);
#20525=ORIENTED_EDGE('',*,*,#15261,.F.);
#20526=ORIENTED_EDGE('',*,*,#15262,.T.);
#20527=ORIENTED_EDGE('',*,*,#15263,.F.);
#20528=ORIENTED_EDGE('',*,*,#15264,.F.);
#20529=ORIENTED_EDGE('',*,*,#15265,.F.);
#20530=ORIENTED_EDGE('',*,*,#15266,.T.);
#20531=ORIENTED_EDGE('',*,*,#15267,.F.);
#20532=ORIENTED_EDGE('',*,*,#15268,.F.);
#20533=ORIENTED_EDGE('',*,*,#15269,.F.);
#20534=ORIENTED_EDGE('',*,*,#15270,.T.);
#20535=ORIENTED_EDGE('',*,*,#15271,.F.);
#20536=ORIENTED_EDGE('',*,*,#15272,.F.);
#20537=ORIENTED_EDGE('',*,*,#15273,.F.);
#20538=ORIENTED_EDGE('',*,*,#15274,.T.);
#20539=ORIENTED_EDGE('',*,*,#15275,.F.);
#20540=ORIENTED_EDGE('',*,*,#15276,.F.);
#20541=ORIENTED_EDGE('',*,*,#15277,.F.);
#20542=ORIENTED_EDGE('',*,*,#15278,.T.);
#20543=ORIENTED_EDGE('',*,*,#15279,.F.);
#20544=ORIENTED_EDGE('',*,*,#15280,.F.);
#20545=ORIENTED_EDGE('',*,*,#15281,.F.);
#20546=ORIENTED_EDGE('',*,*,#15282,.T.);
#20547=ORIENTED_EDGE('',*,*,#15283,.F.);
#20548=ORIENTED_EDGE('',*,*,#15284,.F.);
#20549=ORIENTED_EDGE('',*,*,#15285,.F.);
#20550=ORIENTED_EDGE('',*,*,#15286,.T.);
#20551=ORIENTED_EDGE('',*,*,#15287,.F.);
#20552=ORIENTED_EDGE('',*,*,#15288,.F.);
#20553=ORIENTED_EDGE('',*,*,#15289,.F.);
#20554=ORIENTED_EDGE('',*,*,#15290,.T.);
#20555=ORIENTED_EDGE('',*,*,#15291,.F.);
#20556=ORIENTED_EDGE('',*,*,#15292,.F.);
#20557=ORIENTED_EDGE('',*,*,#15293,.F.);
#20558=ORIENTED_EDGE('',*,*,#15294,.T.);
#20559=ORIENTED_EDGE('',*,*,#15295,.F.);
#20560=ORIENTED_EDGE('',*,*,#15296,.F.);
#20561=ORIENTED_EDGE('',*,*,#15297,.F.);
#20562=ORIENTED_EDGE('',*,*,#15298,.T.);
#20563=ORIENTED_EDGE('',*,*,#15299,.F.);
#20564=ORIENTED_EDGE('',*,*,#15300,.F.);
#20565=ORIENTED_EDGE('',*,*,#15301,.F.);
#20566=ORIENTED_EDGE('',*,*,#15302,.T.);
#20567=ORIENTED_EDGE('',*,*,#15303,.F.);
#20568=ORIENTED_EDGE('',*,*,#15304,.F.);
#20569=ORIENTED_EDGE('',*,*,#15305,.F.);
#20570=ORIENTED_EDGE('',*,*,#15306,.T.);
#20571=ORIENTED_EDGE('',*,*,#15307,.F.);
#20572=ORIENTED_EDGE('',*,*,#15308,.F.);
#20573=ORIENTED_EDGE('',*,*,#15309,.F.);
#20574=ORIENTED_EDGE('',*,*,#15310,.T.);
#20575=ORIENTED_EDGE('',*,*,#15311,.F.);
#20576=ORIENTED_EDGE('',*,*,#15312,.F.);
#20577=ORIENTED_EDGE('',*,*,#15313,.F.);
#20578=ORIENTED_EDGE('',*,*,#15314,.T.);
#20579=ORIENTED_EDGE('',*,*,#15315,.F.);
#20580=ORIENTED_EDGE('',*,*,#15316,.F.);
#20581=ORIENTED_EDGE('',*,*,#15317,.F.);
#20582=ORIENTED_EDGE('',*,*,#15318,.T.);
#20583=ORIENTED_EDGE('',*,*,#15319,.F.);
#20584=ORIENTED_EDGE('',*,*,#15320,.F.);
#20585=ORIENTED_EDGE('',*,*,#15321,.F.);
#20586=ORIENTED_EDGE('',*,*,#15322,.T.);
#20587=ORIENTED_EDGE('',*,*,#15323,.F.);
#20588=ORIENTED_EDGE('',*,*,#15324,.F.);
#20589=ORIENTED_EDGE('',*,*,#15325,.F.);
#20590=ORIENTED_EDGE('',*,*,#15326,.T.);
#20591=ORIENTED_EDGE('',*,*,#15327,.F.);
#20592=ORIENTED_EDGE('',*,*,#15328,.F.);
#20593=ORIENTED_EDGE('',*,*,#15329,.F.);
#20594=ORIENTED_EDGE('',*,*,#15330,.T.);
#20595=ORIENTED_EDGE('',*,*,#15331,.F.);
#20596=ORIENTED_EDGE('',*,*,#15332,.F.);
#20597=ORIENTED_EDGE('',*,*,#15333,.F.);
#20598=ORIENTED_EDGE('',*,*,#15334,.T.);
#20599=ORIENTED_EDGE('',*,*,#15335,.F.);
#20600=ORIENTED_EDGE('',*,*,#15336,.F.);
#20601=ORIENTED_EDGE('',*,*,#15337,.F.);
#20602=ORIENTED_EDGE('',*,*,#15338,.T.);
#20603=ORIENTED_EDGE('',*,*,#15339,.F.);
#20604=ORIENTED_EDGE('',*,*,#15340,.F.);
#20605=ORIENTED_EDGE('',*,*,#15341,.F.);
#20606=ORIENTED_EDGE('',*,*,#15342,.T.);
#20607=ORIENTED_EDGE('',*,*,#15343,.F.);
#20608=ORIENTED_EDGE('',*,*,#15344,.F.);
#20609=ORIENTED_EDGE('',*,*,#15345,.F.);
#20610=ORIENTED_EDGE('',*,*,#15346,.T.);
#20611=ORIENTED_EDGE('',*,*,#15347,.F.);
#20612=ORIENTED_EDGE('',*,*,#15348,.F.);
#20613=ORIENTED_EDGE('',*,*,#15349,.F.);
#20614=ORIENTED_EDGE('',*,*,#15350,.T.);
#20615=ORIENTED_EDGE('',*,*,#15351,.F.);
#20616=ORIENTED_EDGE('',*,*,#15352,.F.);
#20617=ORIENTED_EDGE('',*,*,#15353,.F.);
#20618=ORIENTED_EDGE('',*,*,#15354,.T.);
#20619=ORIENTED_EDGE('',*,*,#15355,.F.);
#20620=ORIENTED_EDGE('',*,*,#15356,.F.);
#20621=ORIENTED_EDGE('',*,*,#15357,.F.);
#20622=ORIENTED_EDGE('',*,*,#15358,.T.);
#20623=ORIENTED_EDGE('',*,*,#15359,.F.);
#20624=ORIENTED_EDGE('',*,*,#15360,.F.);
#20625=ORIENTED_EDGE('',*,*,#15361,.F.);
#20626=ORIENTED_EDGE('',*,*,#15362,.T.);
#20627=ORIENTED_EDGE('',*,*,#15363,.F.);
#20628=ORIENTED_EDGE('',*,*,#15364,.F.);
#20629=ORIENTED_EDGE('',*,*,#15365,.F.);
#20630=ORIENTED_EDGE('',*,*,#15366,.T.);
#20631=ORIENTED_EDGE('',*,*,#15367,.F.);
#20632=ORIENTED_EDGE('',*,*,#15368,.F.);
#20633=ORIENTED_EDGE('',*,*,#15369,.F.);
#20634=ORIENTED_EDGE('',*,*,#15370,.T.);
#20635=ORIENTED_EDGE('',*,*,#15371,.F.);
#20636=ORIENTED_EDGE('',*,*,#15372,.F.);
#20637=ORIENTED_EDGE('',*,*,#15373,.F.);
#20638=ORIENTED_EDGE('',*,*,#15374,.T.);
#20639=ORIENTED_EDGE('',*,*,#15375,.F.);
#20640=ORIENTED_EDGE('',*,*,#15376,.F.);
#20641=ORIENTED_EDGE('',*,*,#15377,.F.);
#20642=ORIENTED_EDGE('',*,*,#15378,.T.);
#20643=ORIENTED_EDGE('',*,*,#15379,.F.);
#20644=ORIENTED_EDGE('',*,*,#14781,.F.);
#20645=ORIENTED_EDGE('',*,*,#15380,.F.);
#20646=ORIENTED_EDGE('',*,*,#15381,.T.);
#20647=ORIENTED_EDGE('',*,*,#15382,.F.);
#20648=ORIENTED_EDGE('',*,*,#14777,.F.);
#20649=ORIENTED_EDGE('',*,*,#15383,.F.);
#20650=ORIENTED_EDGE('',*,*,#15384,.T.);
#20651=ORIENTED_EDGE('',*,*,#15385,.F.);
#20652=ORIENTED_EDGE('',*,*,#14773,.F.);
#20653=ORIENTED_EDGE('',*,*,#15386,.F.);
#20654=ORIENTED_EDGE('',*,*,#15387,.T.);
#20655=ORIENTED_EDGE('',*,*,#15388,.F.);
#20656=ORIENTED_EDGE('',*,*,#14769,.F.);
#20657=ORIENTED_EDGE('',*,*,#15389,.F.);
#20658=ORIENTED_EDGE('',*,*,#15390,.T.);
#20659=ORIENTED_EDGE('',*,*,#15391,.F.);
#20660=ORIENTED_EDGE('',*,*,#14765,.F.);
#20661=ORIENTED_EDGE('',*,*,#15392,.F.);
#20662=ORIENTED_EDGE('',*,*,#15393,.T.);
#20663=ORIENTED_EDGE('',*,*,#15394,.F.);
#20664=ORIENTED_EDGE('',*,*,#14761,.F.);
#20665=ORIENTED_EDGE('',*,*,#15395,.F.);
#20666=ORIENTED_EDGE('',*,*,#15396,.T.);
#20667=ORIENTED_EDGE('',*,*,#15397,.F.);
#20668=ORIENTED_EDGE('',*,*,#14785,.F.);
#20669=ORIENTED_EDGE('',*,*,#15398,.F.);
#20670=ORIENTED_EDGE('',*,*,#15399,.T.);
#20671=ORIENTED_EDGE('',*,*,#15400,.F.);
#20672=ORIENTED_EDGE('',*,*,#14789,.F.);
#20673=ORIENTED_EDGE('',*,*,#15401,.F.);
#20674=ORIENTED_EDGE('',*,*,#15402,.T.);
#20675=ORIENTED_EDGE('',*,*,#15403,.F.);
#20676=ORIENTED_EDGE('',*,*,#14793,.F.);
#20677=ORIENTED_EDGE('',*,*,#15404,.F.);
#20678=ORIENTED_EDGE('',*,*,#15405,.T.);
#20679=ORIENTED_EDGE('',*,*,#15406,.F.);
#20680=ORIENTED_EDGE('',*,*,#14797,.F.);
#20681=ORIENTED_EDGE('',*,*,#15407,.F.);
#20682=ORIENTED_EDGE('',*,*,#15408,.T.);
#20683=ORIENTED_EDGE('',*,*,#15409,.F.);
#20684=ORIENTED_EDGE('',*,*,#14801,.F.);
#20685=ORIENTED_EDGE('',*,*,#15410,.F.);
#20686=ORIENTED_EDGE('',*,*,#15411,.T.);
#20687=ORIENTED_EDGE('',*,*,#15412,.F.);
#20688=ORIENTED_EDGE('',*,*,#14805,.F.);
#20689=ORIENTED_EDGE('',*,*,#15413,.F.);
#20690=ORIENTED_EDGE('',*,*,#15414,.T.);
#20691=ORIENTED_EDGE('',*,*,#15415,.F.);
#20692=ORIENTED_EDGE('',*,*,#14809,.F.);
#20693=ORIENTED_EDGE('',*,*,#15416,.F.);
#20694=ORIENTED_EDGE('',*,*,#15417,.T.);
#20695=ORIENTED_EDGE('',*,*,#15418,.F.);
#20696=ORIENTED_EDGE('',*,*,#14813,.F.);
#20697=ORIENTED_EDGE('',*,*,#15419,.F.);
#20698=ORIENTED_EDGE('',*,*,#15420,.T.);
#20699=ORIENTED_EDGE('',*,*,#15421,.F.);
#20700=ORIENTED_EDGE('',*,*,#14817,.F.);
#20701=ORIENTED_EDGE('',*,*,#15422,.F.);
#20702=ORIENTED_EDGE('',*,*,#15423,.T.);
#20703=ORIENTED_EDGE('',*,*,#15424,.F.);
#20704=ORIENTED_EDGE('',*,*,#15425,.F.);
#20705=ORIENTED_EDGE('',*,*,#15426,.F.);
#20706=ORIENTED_EDGE('',*,*,#15427,.T.);
#20707=ORIENTED_EDGE('',*,*,#15428,.F.);
#20708=ORIENTED_EDGE('',*,*,#15429,.F.);
#20709=ORIENTED_EDGE('',*,*,#15430,.F.);
#20710=ORIENTED_EDGE('',*,*,#15431,.T.);
#20711=ORIENTED_EDGE('',*,*,#15432,.F.);
#20712=ORIENTED_EDGE('',*,*,#15433,.F.);
#20713=ORIENTED_EDGE('',*,*,#15434,.F.);
#20714=ORIENTED_EDGE('',*,*,#15435,.T.);
#20715=ORIENTED_EDGE('',*,*,#15436,.F.);
#20716=ORIENTED_EDGE('',*,*,#15437,.F.);
#20717=ORIENTED_EDGE('',*,*,#15438,.F.);
#20718=ORIENTED_EDGE('',*,*,#15439,.T.);
#20719=ORIENTED_EDGE('',*,*,#15440,.F.);
#20720=ORIENTED_EDGE('',*,*,#15441,.F.);
#20721=ORIENTED_EDGE('',*,*,#15442,.F.);
#20722=ORIENTED_EDGE('',*,*,#15443,.T.);
#20723=ORIENTED_EDGE('',*,*,#15444,.F.);
#20724=ORIENTED_EDGE('',*,*,#15445,.F.);
#20725=ORIENTED_EDGE('',*,*,#15446,.T.);
#20726=ORIENTED_EDGE('',*,*,#15447,.F.);
#20727=ORIENTED_EDGE('',*,*,#15448,.F.);
#20728=ORIENTED_EDGE('',*,*,#15446,.F.);
#20729=ORIENTED_EDGE('',*,*,#15449,.F.);
#20730=ORIENTED_EDGE('',*,*,#15450,.T.);
#20731=ORIENTED_EDGE('',*,*,#15447,.T.);
#20732=ORIENTED_EDGE('',*,*,#15448,.T.);
#20733=ORIENTED_EDGE('',*,*,#15450,.F.);
#20734=ORIENTED_EDGE('',*,*,#15451,.F.);
#20735=ORIENTED_EDGE('',*,*,#15452,.T.);
#20736=ORIENTED_EDGE('',*,*,#15449,.T.);
#20737=ORIENTED_EDGE('',*,*,#15452,.F.);
#20738=ORIENTED_EDGE('',*,*,#15453,.F.);
#20739=ORIENTED_EDGE('',*,*,#15454,.T.);
#20740=ORIENTED_EDGE('',*,*,#15451,.T.);
#20741=ORIENTED_EDGE('',*,*,#15454,.F.);
#20742=ORIENTED_EDGE('',*,*,#14576,.F.);
#20743=ORIENTED_EDGE('',*,*,#15455,.T.);
#20744=ORIENTED_EDGE('',*,*,#15456,.T.);
#20745=ORIENTED_EDGE('',*,*,#15455,.F.);
#20746=ORIENTED_EDGE('',*,*,#15457,.F.);
#20747=ORIENTED_EDGE('',*,*,#15458,.T.);
#20748=ORIENTED_EDGE('',*,*,#15459,.F.);
#20749=ORIENTED_EDGE('',*,*,#15396,.F.);
#20750=ORIENTED_EDGE('',*,*,#15460,.F.);
#20751=ORIENTED_EDGE('',*,*,#15393,.F.);
#20752=ORIENTED_EDGE('',*,*,#15461,.F.);
#20753=ORIENTED_EDGE('',*,*,#15462,.T.);
#20754=ORIENTED_EDGE('',*,*,#15463,.F.);
#20755=ORIENTED_EDGE('',*,*,#15390,.F.);
#20756=ORIENTED_EDGE('',*,*,#15464,.F.);
#20757=ORIENTED_EDGE('',*,*,#15465,.T.);
#20758=ORIENTED_EDGE('',*,*,#15466,.F.);
#20759=ORIENTED_EDGE('',*,*,#15387,.F.);
#20760=ORIENTED_EDGE('',*,*,#15467,.F.);
#20761=ORIENTED_EDGE('',*,*,#15468,.T.);
#20762=ORIENTED_EDGE('',*,*,#15469,.F.);
#20763=ORIENTED_EDGE('',*,*,#15384,.F.);
#20764=ORIENTED_EDGE('',*,*,#15470,.F.);
#20765=ORIENTED_EDGE('',*,*,#15471,.T.);
#20766=ORIENTED_EDGE('',*,*,#15472,.F.);
#20767=ORIENTED_EDGE('',*,*,#15381,.F.);
#20768=ORIENTED_EDGE('',*,*,#15473,.F.);
#20769=ORIENTED_EDGE('',*,*,#15474,.T.);
#20770=ORIENTED_EDGE('',*,*,#15475,.F.);
#20771=ORIENTED_EDGE('',*,*,#15378,.F.);
#20772=ORIENTED_EDGE('',*,*,#15476,.F.);
#20773=ORIENTED_EDGE('',*,*,#15477,.T.);
#20774=ORIENTED_EDGE('',*,*,#15478,.F.);
#20775=ORIENTED_EDGE('',*,*,#15374,.F.);
#20776=ORIENTED_EDGE('',*,*,#15479,.F.);
#20777=ORIENTED_EDGE('',*,*,#15480,.T.);
#20778=ORIENTED_EDGE('',*,*,#15481,.F.);
#20779=ORIENTED_EDGE('',*,*,#15370,.F.);
#20780=ORIENTED_EDGE('',*,*,#15482,.F.);
#20781=ORIENTED_EDGE('',*,*,#15483,.T.);
#20782=ORIENTED_EDGE('',*,*,#15484,.F.);
#20783=ORIENTED_EDGE('',*,*,#15366,.F.);
#20784=ORIENTED_EDGE('',*,*,#15485,.F.);
#20785=ORIENTED_EDGE('',*,*,#15486,.T.);
#20786=ORIENTED_EDGE('',*,*,#15487,.F.);
#20787=ORIENTED_EDGE('',*,*,#15362,.F.);
#20788=ORIENTED_EDGE('',*,*,#15488,.F.);
#20789=ORIENTED_EDGE('',*,*,#15489,.T.);
#20790=ORIENTED_EDGE('',*,*,#15490,.F.);
#20791=ORIENTED_EDGE('',*,*,#15358,.F.);
#20792=ORIENTED_EDGE('',*,*,#15491,.F.);
#20793=ORIENTED_EDGE('',*,*,#15492,.T.);
#20794=ORIENTED_EDGE('',*,*,#15493,.F.);
#20795=ORIENTED_EDGE('',*,*,#15354,.F.);
#20796=ORIENTED_EDGE('',*,*,#15494,.F.);
#20797=ORIENTED_EDGE('',*,*,#15495,.T.);
#20798=ORIENTED_EDGE('',*,*,#15496,.F.);
#20799=ORIENTED_EDGE('',*,*,#15350,.F.);
#20800=ORIENTED_EDGE('',*,*,#15497,.F.);
#20801=ORIENTED_EDGE('',*,*,#15498,.T.);
#20802=ORIENTED_EDGE('',*,*,#15499,.F.);
#20803=ORIENTED_EDGE('',*,*,#15346,.F.);
#20804=ORIENTED_EDGE('',*,*,#15500,.F.);
#20805=ORIENTED_EDGE('',*,*,#15501,.T.);
#20806=ORIENTED_EDGE('',*,*,#15502,.F.);
#20807=ORIENTED_EDGE('',*,*,#15342,.F.);
#20808=ORIENTED_EDGE('',*,*,#15503,.F.);
#20809=ORIENTED_EDGE('',*,*,#15504,.T.);
#20810=ORIENTED_EDGE('',*,*,#15505,.F.);
#20811=ORIENTED_EDGE('',*,*,#15338,.F.);
#20812=ORIENTED_EDGE('',*,*,#15506,.F.);
#20813=ORIENTED_EDGE('',*,*,#15507,.T.);
#20814=ORIENTED_EDGE('',*,*,#15508,.F.);
#20815=ORIENTED_EDGE('',*,*,#15334,.F.);
#20816=ORIENTED_EDGE('',*,*,#15509,.F.);
#20817=ORIENTED_EDGE('',*,*,#15510,.T.);
#20818=ORIENTED_EDGE('',*,*,#15511,.F.);
#20819=ORIENTED_EDGE('',*,*,#15330,.F.);
#20820=ORIENTED_EDGE('',*,*,#15512,.F.);
#20821=ORIENTED_EDGE('',*,*,#15513,.T.);
#20822=ORIENTED_EDGE('',*,*,#15514,.F.);
#20823=ORIENTED_EDGE('',*,*,#15326,.F.);
#20824=ORIENTED_EDGE('',*,*,#15515,.F.);
#20825=ORIENTED_EDGE('',*,*,#15516,.T.);
#20826=ORIENTED_EDGE('',*,*,#15517,.F.);
#20827=ORIENTED_EDGE('',*,*,#15322,.F.);
#20828=ORIENTED_EDGE('',*,*,#15518,.F.);
#20829=ORIENTED_EDGE('',*,*,#15519,.T.);
#20830=ORIENTED_EDGE('',*,*,#15520,.F.);
#20831=ORIENTED_EDGE('',*,*,#15318,.F.);
#20832=ORIENTED_EDGE('',*,*,#15521,.F.);
#20833=ORIENTED_EDGE('',*,*,#15522,.T.);
#20834=ORIENTED_EDGE('',*,*,#15523,.F.);
#20835=ORIENTED_EDGE('',*,*,#15314,.F.);
#20836=ORIENTED_EDGE('',*,*,#15524,.F.);
#20837=ORIENTED_EDGE('',*,*,#15525,.T.);
#20838=ORIENTED_EDGE('',*,*,#15526,.F.);
#20839=ORIENTED_EDGE('',*,*,#15310,.F.);
#20840=ORIENTED_EDGE('',*,*,#15527,.F.);
#20841=ORIENTED_EDGE('',*,*,#15528,.T.);
#20842=ORIENTED_EDGE('',*,*,#15529,.F.);
#20843=ORIENTED_EDGE('',*,*,#15306,.F.);
#20844=ORIENTED_EDGE('',*,*,#15530,.F.);
#20845=ORIENTED_EDGE('',*,*,#15531,.T.);
#20846=ORIENTED_EDGE('',*,*,#15532,.F.);
#20847=ORIENTED_EDGE('',*,*,#15302,.F.);
#20848=ORIENTED_EDGE('',*,*,#15533,.F.);
#20849=ORIENTED_EDGE('',*,*,#15534,.T.);
#20850=ORIENTED_EDGE('',*,*,#15535,.F.);
#20851=ORIENTED_EDGE('',*,*,#15298,.F.);
#20852=ORIENTED_EDGE('',*,*,#15536,.F.);
#20853=ORIENTED_EDGE('',*,*,#15537,.T.);
#20854=ORIENTED_EDGE('',*,*,#15538,.F.);
#20855=ORIENTED_EDGE('',*,*,#15294,.F.);
#20856=ORIENTED_EDGE('',*,*,#15539,.F.);
#20857=ORIENTED_EDGE('',*,*,#15540,.T.);
#20858=ORIENTED_EDGE('',*,*,#15541,.F.);
#20859=ORIENTED_EDGE('',*,*,#15290,.F.);
#20860=ORIENTED_EDGE('',*,*,#15542,.F.);
#20861=ORIENTED_EDGE('',*,*,#15543,.T.);
#20862=ORIENTED_EDGE('',*,*,#15544,.F.);
#20863=ORIENTED_EDGE('',*,*,#15286,.F.);
#20864=ORIENTED_EDGE('',*,*,#15545,.F.);
#20865=ORIENTED_EDGE('',*,*,#15546,.T.);
#20866=ORIENTED_EDGE('',*,*,#15547,.F.);
#20867=ORIENTED_EDGE('',*,*,#15282,.F.);
#20868=ORIENTED_EDGE('',*,*,#15548,.F.);
#20869=ORIENTED_EDGE('',*,*,#15549,.T.);
#20870=ORIENTED_EDGE('',*,*,#15550,.F.);
#20871=ORIENTED_EDGE('',*,*,#15278,.F.);
#20872=ORIENTED_EDGE('',*,*,#15551,.F.);
#20873=ORIENTED_EDGE('',*,*,#15552,.T.);
#20874=ORIENTED_EDGE('',*,*,#15553,.F.);
#20875=ORIENTED_EDGE('',*,*,#15274,.F.);
#20876=ORIENTED_EDGE('',*,*,#15554,.F.);
#20877=ORIENTED_EDGE('',*,*,#15555,.T.);
#20878=ORIENTED_EDGE('',*,*,#15556,.F.);
#20879=ORIENTED_EDGE('',*,*,#15270,.F.);
#20880=ORIENTED_EDGE('',*,*,#15557,.F.);
#20881=ORIENTED_EDGE('',*,*,#15558,.T.);
#20882=ORIENTED_EDGE('',*,*,#15559,.F.);
#20883=ORIENTED_EDGE('',*,*,#15266,.F.);
#20884=ORIENTED_EDGE('',*,*,#15560,.F.);
#20885=ORIENTED_EDGE('',*,*,#15561,.T.);
#20886=ORIENTED_EDGE('',*,*,#15562,.F.);
#20887=ORIENTED_EDGE('',*,*,#15262,.F.);
#20888=ORIENTED_EDGE('',*,*,#15563,.F.);
#20889=ORIENTED_EDGE('',*,*,#15564,.T.);
#20890=ORIENTED_EDGE('',*,*,#15565,.F.);
#20891=ORIENTED_EDGE('',*,*,#15258,.F.);
#20892=ORIENTED_EDGE('',*,*,#15566,.F.);
#20893=ORIENTED_EDGE('',*,*,#15567,.T.);
#20894=ORIENTED_EDGE('',*,*,#15568,.F.);
#20895=ORIENTED_EDGE('',*,*,#15254,.F.);
#20896=ORIENTED_EDGE('',*,*,#15569,.F.);
#20897=ORIENTED_EDGE('',*,*,#15570,.T.);
#20898=ORIENTED_EDGE('',*,*,#15571,.F.);
#20899=ORIENTED_EDGE('',*,*,#15250,.F.);
#20900=ORIENTED_EDGE('',*,*,#15572,.F.);
#20901=ORIENTED_EDGE('',*,*,#15573,.T.);
#20902=ORIENTED_EDGE('',*,*,#15574,.F.);
#20903=ORIENTED_EDGE('',*,*,#15246,.F.);
#20904=ORIENTED_EDGE('',*,*,#15575,.F.);
#20905=ORIENTED_EDGE('',*,*,#15576,.T.);
#20906=ORIENTED_EDGE('',*,*,#15577,.F.);
#20907=ORIENTED_EDGE('',*,*,#15242,.F.);
#20908=ORIENTED_EDGE('',*,*,#15578,.F.);
#20909=ORIENTED_EDGE('',*,*,#15579,.T.);
#20910=ORIENTED_EDGE('',*,*,#15580,.F.);
#20911=ORIENTED_EDGE('',*,*,#15238,.F.);
#20912=ORIENTED_EDGE('',*,*,#15581,.F.);
#20913=ORIENTED_EDGE('',*,*,#15582,.T.);
#20914=ORIENTED_EDGE('',*,*,#15583,.F.);
#20915=ORIENTED_EDGE('',*,*,#15234,.F.);
#20916=ORIENTED_EDGE('',*,*,#15584,.F.);
#20917=ORIENTED_EDGE('',*,*,#15585,.T.);
#20918=ORIENTED_EDGE('',*,*,#15586,.F.);
#20919=ORIENTED_EDGE('',*,*,#15230,.F.);
#20920=ORIENTED_EDGE('',*,*,#15587,.F.);
#20921=ORIENTED_EDGE('',*,*,#15588,.T.);
#20922=ORIENTED_EDGE('',*,*,#15589,.F.);
#20923=ORIENTED_EDGE('',*,*,#15226,.F.);
#20924=ORIENTED_EDGE('',*,*,#15590,.F.);
#20925=ORIENTED_EDGE('',*,*,#15591,.T.);
#20926=ORIENTED_EDGE('',*,*,#15592,.F.);
#20927=ORIENTED_EDGE('',*,*,#15222,.F.);
#20928=ORIENTED_EDGE('',*,*,#15593,.F.);
#20929=ORIENTED_EDGE('',*,*,#15594,.T.);
#20930=ORIENTED_EDGE('',*,*,#15595,.F.);
#20931=ORIENTED_EDGE('',*,*,#15218,.F.);
#20932=ORIENTED_EDGE('',*,*,#15596,.F.);
#20933=ORIENTED_EDGE('',*,*,#15597,.T.);
#20934=ORIENTED_EDGE('',*,*,#15598,.F.);
#20935=ORIENTED_EDGE('',*,*,#15214,.F.);
#20936=ORIENTED_EDGE('',*,*,#15599,.F.);
#20937=ORIENTED_EDGE('',*,*,#15600,.T.);
#20938=ORIENTED_EDGE('',*,*,#15601,.F.);
#20939=ORIENTED_EDGE('',*,*,#15210,.F.);
#20940=ORIENTED_EDGE('',*,*,#15602,.F.);
#20941=ORIENTED_EDGE('',*,*,#15603,.T.);
#20942=ORIENTED_EDGE('',*,*,#15604,.F.);
#20943=ORIENTED_EDGE('',*,*,#15206,.F.);
#20944=ORIENTED_EDGE('',*,*,#15605,.F.);
#20945=ORIENTED_EDGE('',*,*,#15606,.T.);
#20946=ORIENTED_EDGE('',*,*,#15607,.F.);
#20947=ORIENTED_EDGE('',*,*,#15202,.F.);
#20948=ORIENTED_EDGE('',*,*,#15608,.F.);
#20949=ORIENTED_EDGE('',*,*,#15609,.T.);
#20950=ORIENTED_EDGE('',*,*,#15610,.F.);
#20951=ORIENTED_EDGE('',*,*,#15198,.F.);
#20952=ORIENTED_EDGE('',*,*,#15611,.F.);
#20953=ORIENTED_EDGE('',*,*,#15612,.T.);
#20954=ORIENTED_EDGE('',*,*,#15613,.F.);
#20955=ORIENTED_EDGE('',*,*,#15194,.F.);
#20956=ORIENTED_EDGE('',*,*,#15614,.F.);
#20957=ORIENTED_EDGE('',*,*,#15615,.T.);
#20958=ORIENTED_EDGE('',*,*,#15616,.F.);
#20959=ORIENTED_EDGE('',*,*,#15190,.F.);
#20960=ORIENTED_EDGE('',*,*,#15617,.F.);
#20961=ORIENTED_EDGE('',*,*,#15618,.T.);
#20962=ORIENTED_EDGE('',*,*,#15619,.F.);
#20963=ORIENTED_EDGE('',*,*,#15186,.F.);
#20964=ORIENTED_EDGE('',*,*,#15620,.F.);
#20965=ORIENTED_EDGE('',*,*,#15621,.T.);
#20966=ORIENTED_EDGE('',*,*,#15622,.F.);
#20967=ORIENTED_EDGE('',*,*,#15182,.F.);
#20968=ORIENTED_EDGE('',*,*,#15623,.F.);
#20969=ORIENTED_EDGE('',*,*,#15624,.T.);
#20970=ORIENTED_EDGE('',*,*,#15625,.F.);
#20971=ORIENTED_EDGE('',*,*,#15178,.F.);
#20972=ORIENTED_EDGE('',*,*,#15626,.F.);
#20973=ORIENTED_EDGE('',*,*,#15627,.T.);
#20974=ORIENTED_EDGE('',*,*,#15628,.F.);
#20975=ORIENTED_EDGE('',*,*,#15174,.F.);
#20976=ORIENTED_EDGE('',*,*,#15629,.F.);
#20977=ORIENTED_EDGE('',*,*,#15630,.T.);
#20978=ORIENTED_EDGE('',*,*,#15631,.F.);
#20979=ORIENTED_EDGE('',*,*,#15170,.F.);
#20980=ORIENTED_EDGE('',*,*,#15632,.F.);
#20981=ORIENTED_EDGE('',*,*,#15633,.T.);
#20982=ORIENTED_EDGE('',*,*,#15634,.F.);
#20983=ORIENTED_EDGE('',*,*,#15166,.F.);
#20984=ORIENTED_EDGE('',*,*,#15635,.F.);
#20985=ORIENTED_EDGE('',*,*,#15636,.T.);
#20986=ORIENTED_EDGE('',*,*,#15637,.F.);
#20987=ORIENTED_EDGE('',*,*,#15162,.F.);
#20988=ORIENTED_EDGE('',*,*,#15638,.F.);
#20989=ORIENTED_EDGE('',*,*,#15639,.T.);
#20990=ORIENTED_EDGE('',*,*,#15640,.F.);
#20991=ORIENTED_EDGE('',*,*,#15158,.F.);
#20992=ORIENTED_EDGE('',*,*,#15641,.F.);
#20993=ORIENTED_EDGE('',*,*,#15642,.T.);
#20994=ORIENTED_EDGE('',*,*,#15643,.F.);
#20995=ORIENTED_EDGE('',*,*,#15154,.F.);
#20996=ORIENTED_EDGE('',*,*,#15644,.F.);
#20997=ORIENTED_EDGE('',*,*,#15645,.T.);
#20998=ORIENTED_EDGE('',*,*,#15646,.F.);
#20999=ORIENTED_EDGE('',*,*,#15150,.F.);
#21000=ORIENTED_EDGE('',*,*,#15647,.F.);
#21001=ORIENTED_EDGE('',*,*,#15648,.T.);
#21002=ORIENTED_EDGE('',*,*,#15649,.F.);
#21003=ORIENTED_EDGE('',*,*,#15650,.T.);
#21004=ORIENTED_EDGE('',*,*,#15651,.F.);
#21005=ORIENTED_EDGE('',*,*,#15399,.F.);
#21006=ORIENTED_EDGE('',*,*,#15652,.F.);
#21007=ORIENTED_EDGE('',*,*,#15653,.T.);
#21008=ORIENTED_EDGE('',*,*,#15654,.F.);
#21009=ORIENTED_EDGE('',*,*,#15402,.F.);
#21010=ORIENTED_EDGE('',*,*,#15655,.F.);
#21011=ORIENTED_EDGE('',*,*,#15656,.T.);
#21012=ORIENTED_EDGE('',*,*,#15657,.F.);
#21013=ORIENTED_EDGE('',*,*,#15405,.F.);
#21014=ORIENTED_EDGE('',*,*,#15658,.F.);
#21015=ORIENTED_EDGE('',*,*,#15659,.T.);
#21016=ORIENTED_EDGE('',*,*,#15660,.F.);
#21017=ORIENTED_EDGE('',*,*,#15408,.F.);
#21018=ORIENTED_EDGE('',*,*,#15661,.F.);
#21019=ORIENTED_EDGE('',*,*,#15662,.T.);
#21020=ORIENTED_EDGE('',*,*,#15663,.F.);
#21021=ORIENTED_EDGE('',*,*,#15411,.F.);
#21022=ORIENTED_EDGE('',*,*,#15664,.F.);
#21023=ORIENTED_EDGE('',*,*,#15665,.T.);
#21024=ORIENTED_EDGE('',*,*,#15666,.F.);
#21025=ORIENTED_EDGE('',*,*,#15414,.F.);
#21026=ORIENTED_EDGE('',*,*,#15667,.F.);
#21027=ORIENTED_EDGE('',*,*,#15668,.T.);
#21028=ORIENTED_EDGE('',*,*,#15669,.F.);
#21029=ORIENTED_EDGE('',*,*,#15417,.F.);
#21030=ORIENTED_EDGE('',*,*,#15670,.F.);
#21031=ORIENTED_EDGE('',*,*,#15671,.T.);
#21032=ORIENTED_EDGE('',*,*,#15672,.F.);
#21033=ORIENTED_EDGE('',*,*,#15420,.F.);
#21034=ORIENTED_EDGE('',*,*,#15673,.F.);
#21035=ORIENTED_EDGE('',*,*,#15674,.T.);
#21036=ORIENTED_EDGE('',*,*,#15675,.F.);
#21037=ORIENTED_EDGE('',*,*,#15423,.F.);
#21038=ORIENTED_EDGE('',*,*,#15676,.F.);
#21039=ORIENTED_EDGE('',*,*,#15677,.T.);
#21040=ORIENTED_EDGE('',*,*,#15678,.F.);
#21041=ORIENTED_EDGE('',*,*,#15427,.F.);
#21042=ORIENTED_EDGE('',*,*,#15679,.F.);
#21043=ORIENTED_EDGE('',*,*,#15680,.T.);
#21044=ORIENTED_EDGE('',*,*,#15681,.F.);
#21045=ORIENTED_EDGE('',*,*,#15431,.F.);
#21046=ORIENTED_EDGE('',*,*,#15682,.F.);
#21047=ORIENTED_EDGE('',*,*,#15683,.T.);
#21048=ORIENTED_EDGE('',*,*,#15684,.F.);
#21049=ORIENTED_EDGE('',*,*,#15435,.F.);
#21050=ORIENTED_EDGE('',*,*,#15685,.F.);
#21051=ORIENTED_EDGE('',*,*,#15686,.T.);
#21052=ORIENTED_EDGE('',*,*,#15687,.F.);
#21053=ORIENTED_EDGE('',*,*,#15439,.F.);
#21054=ORIENTED_EDGE('',*,*,#15688,.F.);
#21055=ORIENTED_EDGE('',*,*,#15689,.T.);
#21056=ORIENTED_EDGE('',*,*,#15690,.F.);
#21057=ORIENTED_EDGE('',*,*,#15443,.F.);
#21058=ORIENTED_EDGE('',*,*,#15691,.F.);
#21059=ORIENTED_EDGE('',*,*,#15146,.F.);
#21060=ORIENTED_EDGE('',*,*,#15692,.F.);
#21061=ORIENTED_EDGE('',*,*,#15693,.T.);
#21062=ORIENTED_EDGE('',*,*,#15694,.F.);
#21063=ORIENTED_EDGE('',*,*,#15695,.T.);
#21064=ORIENTED_EDGE('',*,*,#15696,.F.);
#21065=ORIENTED_EDGE('',*,*,#15458,.F.);
#21066=ORIENTED_EDGE('',*,*,#15697,.F.);
#21067=ORIENTED_EDGE('',*,*,#15462,.F.);
#21068=ORIENTED_EDGE('',*,*,#15698,.F.);
#21069=ORIENTED_EDGE('',*,*,#15699,.T.);
#21070=ORIENTED_EDGE('',*,*,#15700,.F.);
#21071=ORIENTED_EDGE('',*,*,#15465,.F.);
#21072=ORIENTED_EDGE('',*,*,#15701,.F.);
#21073=ORIENTED_EDGE('',*,*,#15702,.T.);
#21074=ORIENTED_EDGE('',*,*,#15703,.F.);
#21075=ORIENTED_EDGE('',*,*,#15468,.F.);
#21076=ORIENTED_EDGE('',*,*,#15704,.F.);
#21077=ORIENTED_EDGE('',*,*,#15705,.T.);
#21078=ORIENTED_EDGE('',*,*,#15706,.F.);
#21079=ORIENTED_EDGE('',*,*,#15471,.F.);
#21080=ORIENTED_EDGE('',*,*,#15707,.F.);
#21081=ORIENTED_EDGE('',*,*,#15708,.T.);
#21082=ORIENTED_EDGE('',*,*,#15709,.F.);
#21083=ORIENTED_EDGE('',*,*,#15474,.F.);
#21084=ORIENTED_EDGE('',*,*,#15710,.F.);
#21085=ORIENTED_EDGE('',*,*,#15711,.T.);
#21086=ORIENTED_EDGE('',*,*,#15712,.F.);
#21087=ORIENTED_EDGE('',*,*,#15477,.F.);
#21088=ORIENTED_EDGE('',*,*,#15713,.F.);
#21089=ORIENTED_EDGE('',*,*,#15714,.T.);
#21090=ORIENTED_EDGE('',*,*,#15715,.F.);
#21091=ORIENTED_EDGE('',*,*,#15480,.F.);
#21092=ORIENTED_EDGE('',*,*,#15716,.F.);
#21093=ORIENTED_EDGE('',*,*,#15717,.T.);
#21094=ORIENTED_EDGE('',*,*,#15718,.F.);
#21095=ORIENTED_EDGE('',*,*,#15483,.F.);
#21096=ORIENTED_EDGE('',*,*,#15719,.F.);
#21097=ORIENTED_EDGE('',*,*,#15720,.T.);
#21098=ORIENTED_EDGE('',*,*,#15721,.F.);
#21099=ORIENTED_EDGE('',*,*,#15486,.F.);
#21100=ORIENTED_EDGE('',*,*,#15722,.F.);
#21101=ORIENTED_EDGE('',*,*,#15723,.T.);
#21102=ORIENTED_EDGE('',*,*,#15724,.F.);
#21103=ORIENTED_EDGE('',*,*,#15489,.F.);
#21104=ORIENTED_EDGE('',*,*,#15725,.F.);
#21105=ORIENTED_EDGE('',*,*,#15726,.T.);
#21106=ORIENTED_EDGE('',*,*,#15727,.F.);
#21107=ORIENTED_EDGE('',*,*,#15492,.F.);
#21108=ORIENTED_EDGE('',*,*,#15728,.F.);
#21109=ORIENTED_EDGE('',*,*,#15729,.T.);
#21110=ORIENTED_EDGE('',*,*,#15730,.F.);
#21111=ORIENTED_EDGE('',*,*,#15495,.F.);
#21112=ORIENTED_EDGE('',*,*,#15731,.F.);
#21113=ORIENTED_EDGE('',*,*,#15732,.T.);
#21114=ORIENTED_EDGE('',*,*,#15733,.F.);
#21115=ORIENTED_EDGE('',*,*,#15498,.F.);
#21116=ORIENTED_EDGE('',*,*,#15734,.F.);
#21117=ORIENTED_EDGE('',*,*,#15735,.T.);
#21118=ORIENTED_EDGE('',*,*,#15736,.F.);
#21119=ORIENTED_EDGE('',*,*,#15501,.F.);
#21120=ORIENTED_EDGE('',*,*,#15737,.F.);
#21121=ORIENTED_EDGE('',*,*,#15738,.T.);
#21122=ORIENTED_EDGE('',*,*,#15739,.F.);
#21123=ORIENTED_EDGE('',*,*,#15504,.F.);
#21124=ORIENTED_EDGE('',*,*,#15740,.F.);
#21125=ORIENTED_EDGE('',*,*,#15741,.T.);
#21126=ORIENTED_EDGE('',*,*,#15742,.F.);
#21127=ORIENTED_EDGE('',*,*,#15507,.F.);
#21128=ORIENTED_EDGE('',*,*,#15743,.F.);
#21129=ORIENTED_EDGE('',*,*,#15744,.T.);
#21130=ORIENTED_EDGE('',*,*,#15745,.F.);
#21131=ORIENTED_EDGE('',*,*,#15510,.F.);
#21132=ORIENTED_EDGE('',*,*,#15746,.F.);
#21133=ORIENTED_EDGE('',*,*,#15747,.T.);
#21134=ORIENTED_EDGE('',*,*,#15748,.F.);
#21135=ORIENTED_EDGE('',*,*,#15513,.F.);
#21136=ORIENTED_EDGE('',*,*,#15749,.F.);
#21137=ORIENTED_EDGE('',*,*,#15750,.T.);
#21138=ORIENTED_EDGE('',*,*,#15751,.F.);
#21139=ORIENTED_EDGE('',*,*,#15516,.F.);
#21140=ORIENTED_EDGE('',*,*,#15752,.F.);
#21141=ORIENTED_EDGE('',*,*,#15753,.T.);
#21142=ORIENTED_EDGE('',*,*,#15754,.F.);
#21143=ORIENTED_EDGE('',*,*,#15519,.F.);
#21144=ORIENTED_EDGE('',*,*,#15755,.F.);
#21145=ORIENTED_EDGE('',*,*,#15756,.T.);
#21146=ORIENTED_EDGE('',*,*,#15757,.F.);
#21147=ORIENTED_EDGE('',*,*,#15522,.F.);
#21148=ORIENTED_EDGE('',*,*,#15758,.F.);
#21149=ORIENTED_EDGE('',*,*,#15759,.T.);
#21150=ORIENTED_EDGE('',*,*,#15760,.F.);
#21151=ORIENTED_EDGE('',*,*,#15525,.F.);
#21152=ORIENTED_EDGE('',*,*,#15761,.F.);
#21153=ORIENTED_EDGE('',*,*,#15762,.T.);
#21154=ORIENTED_EDGE('',*,*,#15763,.F.);
#21155=ORIENTED_EDGE('',*,*,#15528,.F.);
#21156=ORIENTED_EDGE('',*,*,#15764,.F.);
#21157=ORIENTED_EDGE('',*,*,#15765,.T.);
#21158=ORIENTED_EDGE('',*,*,#15766,.F.);
#21159=ORIENTED_EDGE('',*,*,#15531,.F.);
#21160=ORIENTED_EDGE('',*,*,#15767,.F.);
#21161=ORIENTED_EDGE('',*,*,#15768,.T.);
#21162=ORIENTED_EDGE('',*,*,#15769,.F.);
#21163=ORIENTED_EDGE('',*,*,#15534,.F.);
#21164=ORIENTED_EDGE('',*,*,#15770,.F.);
#21165=ORIENTED_EDGE('',*,*,#15771,.T.);
#21166=ORIENTED_EDGE('',*,*,#15772,.F.);
#21167=ORIENTED_EDGE('',*,*,#15537,.F.);
#21168=ORIENTED_EDGE('',*,*,#15773,.F.);
#21169=ORIENTED_EDGE('',*,*,#15774,.T.);
#21170=ORIENTED_EDGE('',*,*,#15775,.F.);
#21171=ORIENTED_EDGE('',*,*,#15540,.F.);
#21172=ORIENTED_EDGE('',*,*,#15776,.F.);
#21173=ORIENTED_EDGE('',*,*,#15777,.T.);
#21174=ORIENTED_EDGE('',*,*,#15778,.F.);
#21175=ORIENTED_EDGE('',*,*,#15543,.F.);
#21176=ORIENTED_EDGE('',*,*,#15779,.F.);
#21177=ORIENTED_EDGE('',*,*,#15780,.T.);
#21178=ORIENTED_EDGE('',*,*,#15781,.F.);
#21179=ORIENTED_EDGE('',*,*,#15546,.F.);
#21180=ORIENTED_EDGE('',*,*,#15782,.F.);
#21181=ORIENTED_EDGE('',*,*,#15783,.T.);
#21182=ORIENTED_EDGE('',*,*,#15784,.F.);
#21183=ORIENTED_EDGE('',*,*,#15549,.F.);
#21184=ORIENTED_EDGE('',*,*,#15785,.F.);
#21185=ORIENTED_EDGE('',*,*,#15786,.T.);
#21186=ORIENTED_EDGE('',*,*,#15787,.F.);
#21187=ORIENTED_EDGE('',*,*,#15552,.F.);
#21188=ORIENTED_EDGE('',*,*,#15788,.F.);
#21189=ORIENTED_EDGE('',*,*,#15789,.T.);
#21190=ORIENTED_EDGE('',*,*,#15790,.F.);
#21191=ORIENTED_EDGE('',*,*,#15555,.F.);
#21192=ORIENTED_EDGE('',*,*,#15791,.F.);
#21193=ORIENTED_EDGE('',*,*,#15792,.T.);
#21194=ORIENTED_EDGE('',*,*,#15793,.F.);
#21195=ORIENTED_EDGE('',*,*,#15558,.F.);
#21196=ORIENTED_EDGE('',*,*,#15794,.F.);
#21197=ORIENTED_EDGE('',*,*,#15795,.T.);
#21198=ORIENTED_EDGE('',*,*,#15796,.F.);
#21199=ORIENTED_EDGE('',*,*,#15561,.F.);
#21200=ORIENTED_EDGE('',*,*,#15797,.F.);
#21201=ORIENTED_EDGE('',*,*,#15798,.T.);
#21202=ORIENTED_EDGE('',*,*,#15799,.F.);
#21203=ORIENTED_EDGE('',*,*,#15564,.F.);
#21204=ORIENTED_EDGE('',*,*,#15800,.F.);
#21205=ORIENTED_EDGE('',*,*,#15801,.T.);
#21206=ORIENTED_EDGE('',*,*,#15802,.F.);
#21207=ORIENTED_EDGE('',*,*,#15567,.F.);
#21208=ORIENTED_EDGE('',*,*,#15803,.F.);
#21209=ORIENTED_EDGE('',*,*,#15804,.T.);
#21210=ORIENTED_EDGE('',*,*,#15805,.F.);
#21211=ORIENTED_EDGE('',*,*,#15570,.F.);
#21212=ORIENTED_EDGE('',*,*,#15806,.F.);
#21213=ORIENTED_EDGE('',*,*,#15807,.T.);
#21214=ORIENTED_EDGE('',*,*,#15808,.F.);
#21215=ORIENTED_EDGE('',*,*,#15573,.F.);
#21216=ORIENTED_EDGE('',*,*,#15809,.F.);
#21217=ORIENTED_EDGE('',*,*,#15810,.T.);
#21218=ORIENTED_EDGE('',*,*,#15811,.F.);
#21219=ORIENTED_EDGE('',*,*,#15576,.F.);
#21220=ORIENTED_EDGE('',*,*,#15812,.F.);
#21221=ORIENTED_EDGE('',*,*,#15813,.T.);
#21222=ORIENTED_EDGE('',*,*,#15814,.F.);
#21223=ORIENTED_EDGE('',*,*,#15579,.F.);
#21224=ORIENTED_EDGE('',*,*,#15815,.F.);
#21225=ORIENTED_EDGE('',*,*,#15816,.T.);
#21226=ORIENTED_EDGE('',*,*,#15817,.F.);
#21227=ORIENTED_EDGE('',*,*,#15582,.F.);
#21228=ORIENTED_EDGE('',*,*,#15818,.F.);
#21229=ORIENTED_EDGE('',*,*,#15819,.T.);
#21230=ORIENTED_EDGE('',*,*,#15820,.F.);
#21231=ORIENTED_EDGE('',*,*,#15585,.F.);
#21232=ORIENTED_EDGE('',*,*,#15821,.F.);
#21233=ORIENTED_EDGE('',*,*,#15822,.T.);
#21234=ORIENTED_EDGE('',*,*,#15823,.F.);
#21235=ORIENTED_EDGE('',*,*,#15588,.F.);
#21236=ORIENTED_EDGE('',*,*,#15824,.F.);
#21237=ORIENTED_EDGE('',*,*,#15825,.T.);
#21238=ORIENTED_EDGE('',*,*,#15826,.F.);
#21239=ORIENTED_EDGE('',*,*,#15591,.F.);
#21240=ORIENTED_EDGE('',*,*,#15827,.F.);
#21241=ORIENTED_EDGE('',*,*,#15828,.T.);
#21242=ORIENTED_EDGE('',*,*,#15829,.F.);
#21243=ORIENTED_EDGE('',*,*,#15594,.F.);
#21244=ORIENTED_EDGE('',*,*,#15830,.F.);
#21245=ORIENTED_EDGE('',*,*,#15831,.T.);
#21246=ORIENTED_EDGE('',*,*,#15832,.F.);
#21247=ORIENTED_EDGE('',*,*,#15597,.F.);
#21248=ORIENTED_EDGE('',*,*,#15833,.F.);
#21249=ORIENTED_EDGE('',*,*,#15834,.T.);
#21250=ORIENTED_EDGE('',*,*,#15835,.F.);
#21251=ORIENTED_EDGE('',*,*,#15600,.F.);
#21252=ORIENTED_EDGE('',*,*,#15836,.F.);
#21253=ORIENTED_EDGE('',*,*,#15837,.T.);
#21254=ORIENTED_EDGE('',*,*,#15838,.F.);
#21255=ORIENTED_EDGE('',*,*,#15603,.F.);
#21256=ORIENTED_EDGE('',*,*,#15839,.F.);
#21257=ORIENTED_EDGE('',*,*,#15840,.T.);
#21258=ORIENTED_EDGE('',*,*,#15841,.F.);
#21259=ORIENTED_EDGE('',*,*,#15606,.F.);
#21260=ORIENTED_EDGE('',*,*,#15842,.F.);
#21261=ORIENTED_EDGE('',*,*,#15843,.T.);
#21262=ORIENTED_EDGE('',*,*,#15844,.F.);
#21263=ORIENTED_EDGE('',*,*,#15609,.F.);
#21264=ORIENTED_EDGE('',*,*,#15845,.F.);
#21265=ORIENTED_EDGE('',*,*,#15846,.T.);
#21266=ORIENTED_EDGE('',*,*,#15847,.F.);
#21267=ORIENTED_EDGE('',*,*,#15612,.F.);
#21268=ORIENTED_EDGE('',*,*,#15848,.F.);
#21269=ORIENTED_EDGE('',*,*,#15849,.T.);
#21270=ORIENTED_EDGE('',*,*,#15850,.F.);
#21271=ORIENTED_EDGE('',*,*,#15615,.F.);
#21272=ORIENTED_EDGE('',*,*,#15851,.F.);
#21273=ORIENTED_EDGE('',*,*,#15852,.T.);
#21274=ORIENTED_EDGE('',*,*,#15853,.F.);
#21275=ORIENTED_EDGE('',*,*,#15618,.F.);
#21276=ORIENTED_EDGE('',*,*,#15854,.F.);
#21277=ORIENTED_EDGE('',*,*,#15855,.T.);
#21278=ORIENTED_EDGE('',*,*,#15856,.F.);
#21279=ORIENTED_EDGE('',*,*,#15621,.F.);
#21280=ORIENTED_EDGE('',*,*,#15857,.F.);
#21281=ORIENTED_EDGE('',*,*,#15858,.T.);
#21282=ORIENTED_EDGE('',*,*,#15859,.F.);
#21283=ORIENTED_EDGE('',*,*,#15624,.F.);
#21284=ORIENTED_EDGE('',*,*,#15860,.F.);
#21285=ORIENTED_EDGE('',*,*,#15861,.T.);
#21286=ORIENTED_EDGE('',*,*,#15862,.F.);
#21287=ORIENTED_EDGE('',*,*,#15627,.F.);
#21288=ORIENTED_EDGE('',*,*,#15863,.F.);
#21289=ORIENTED_EDGE('',*,*,#15864,.T.);
#21290=ORIENTED_EDGE('',*,*,#15865,.F.);
#21291=ORIENTED_EDGE('',*,*,#15630,.F.);
#21292=ORIENTED_EDGE('',*,*,#15866,.F.);
#21293=ORIENTED_EDGE('',*,*,#15867,.T.);
#21294=ORIENTED_EDGE('',*,*,#15868,.F.);
#21295=ORIENTED_EDGE('',*,*,#15633,.F.);
#21296=ORIENTED_EDGE('',*,*,#15869,.F.);
#21297=ORIENTED_EDGE('',*,*,#15870,.T.);
#21298=ORIENTED_EDGE('',*,*,#15871,.F.);
#21299=ORIENTED_EDGE('',*,*,#15636,.F.);
#21300=ORIENTED_EDGE('',*,*,#15872,.F.);
#21301=ORIENTED_EDGE('',*,*,#15873,.T.);
#21302=ORIENTED_EDGE('',*,*,#15874,.F.);
#21303=ORIENTED_EDGE('',*,*,#15639,.F.);
#21304=ORIENTED_EDGE('',*,*,#15875,.F.);
#21305=ORIENTED_EDGE('',*,*,#15876,.T.);
#21306=ORIENTED_EDGE('',*,*,#15877,.F.);
#21307=ORIENTED_EDGE('',*,*,#15642,.F.);
#21308=ORIENTED_EDGE('',*,*,#15878,.F.);
#21309=ORIENTED_EDGE('',*,*,#15879,.T.);
#21310=ORIENTED_EDGE('',*,*,#15880,.F.);
#21311=ORIENTED_EDGE('',*,*,#15645,.F.);
#21312=ORIENTED_EDGE('',*,*,#15881,.F.);
#21313=ORIENTED_EDGE('',*,*,#15882,.T.);
#21314=ORIENTED_EDGE('',*,*,#15883,.F.);
#21315=ORIENTED_EDGE('',*,*,#15648,.F.);
#21316=ORIENTED_EDGE('',*,*,#15884,.F.);
#21317=ORIENTED_EDGE('',*,*,#15885,.T.);
#21318=ORIENTED_EDGE('',*,*,#15886,.F.);
#21319=ORIENTED_EDGE('',*,*,#15887,.T.);
#21320=ORIENTED_EDGE('',*,*,#15888,.F.);
#21321=ORIENTED_EDGE('',*,*,#15650,.F.);
#21322=ORIENTED_EDGE('',*,*,#15889,.F.);
#21323=ORIENTED_EDGE('',*,*,#15890,.T.);
#21324=ORIENTED_EDGE('',*,*,#15891,.F.);
#21325=ORIENTED_EDGE('',*,*,#15653,.F.);
#21326=ORIENTED_EDGE('',*,*,#15892,.F.);
#21327=ORIENTED_EDGE('',*,*,#15893,.T.);
#21328=ORIENTED_EDGE('',*,*,#15894,.F.);
#21329=ORIENTED_EDGE('',*,*,#15656,.F.);
#21330=ORIENTED_EDGE('',*,*,#15895,.F.);
#21331=ORIENTED_EDGE('',*,*,#15896,.T.);
#21332=ORIENTED_EDGE('',*,*,#15897,.F.);
#21333=ORIENTED_EDGE('',*,*,#15659,.F.);
#21334=ORIENTED_EDGE('',*,*,#15898,.F.);
#21335=ORIENTED_EDGE('',*,*,#15899,.T.);
#21336=ORIENTED_EDGE('',*,*,#15900,.F.);
#21337=ORIENTED_EDGE('',*,*,#15662,.F.);
#21338=ORIENTED_EDGE('',*,*,#15901,.F.);
#21339=ORIENTED_EDGE('',*,*,#15902,.T.);
#21340=ORIENTED_EDGE('',*,*,#15903,.F.);
#21341=ORIENTED_EDGE('',*,*,#15665,.F.);
#21342=ORIENTED_EDGE('',*,*,#15904,.F.);
#21343=ORIENTED_EDGE('',*,*,#15905,.T.);
#21344=ORIENTED_EDGE('',*,*,#15906,.F.);
#21345=ORIENTED_EDGE('',*,*,#15668,.F.);
#21346=ORIENTED_EDGE('',*,*,#15907,.F.);
#21347=ORIENTED_EDGE('',*,*,#15908,.T.);
#21348=ORIENTED_EDGE('',*,*,#15909,.F.);
#21349=ORIENTED_EDGE('',*,*,#15671,.F.);
#21350=ORIENTED_EDGE('',*,*,#15910,.F.);
#21351=ORIENTED_EDGE('',*,*,#15911,.T.);
#21352=ORIENTED_EDGE('',*,*,#15912,.F.);
#21353=ORIENTED_EDGE('',*,*,#15674,.F.);
#21354=ORIENTED_EDGE('',*,*,#15913,.F.);
#21355=ORIENTED_EDGE('',*,*,#15914,.T.);
#21356=ORIENTED_EDGE('',*,*,#15915,.F.);
#21357=ORIENTED_EDGE('',*,*,#15677,.F.);
#21358=ORIENTED_EDGE('',*,*,#15916,.F.);
#21359=ORIENTED_EDGE('',*,*,#15917,.T.);
#21360=ORIENTED_EDGE('',*,*,#15918,.F.);
#21361=ORIENTED_EDGE('',*,*,#15680,.F.);
#21362=ORIENTED_EDGE('',*,*,#15919,.F.);
#21363=ORIENTED_EDGE('',*,*,#15920,.T.);
#21364=ORIENTED_EDGE('',*,*,#15921,.F.);
#21365=ORIENTED_EDGE('',*,*,#15683,.F.);
#21366=ORIENTED_EDGE('',*,*,#15922,.F.);
#21367=ORIENTED_EDGE('',*,*,#15923,.T.);
#21368=ORIENTED_EDGE('',*,*,#15924,.F.);
#21369=ORIENTED_EDGE('',*,*,#15686,.F.);
#21370=ORIENTED_EDGE('',*,*,#15925,.F.);
#21371=ORIENTED_EDGE('',*,*,#15926,.T.);
#21372=ORIENTED_EDGE('',*,*,#15927,.F.);
#21373=ORIENTED_EDGE('',*,*,#15689,.F.);
#21374=ORIENTED_EDGE('',*,*,#15928,.F.);
#21375=ORIENTED_EDGE('',*,*,#15693,.F.);
#21376=ORIENTED_EDGE('',*,*,#15929,.F.);
#21377=ORIENTED_EDGE('',*,*,#15930,.T.);
#21378=ORIENTED_EDGE('',*,*,#15931,.F.);
#21379=ORIENTED_EDGE('',*,*,#15042,.T.);
#21380=ORIENTED_EDGE('',*,*,#15932,.F.);
#21381=ORIENTED_EDGE('',*,*,#15695,.F.);
#21382=ORIENTED_EDGE('',*,*,#15933,.F.);
#21383=ORIENTED_EDGE('',*,*,#15699,.F.);
#21384=ORIENTED_EDGE('',*,*,#15934,.F.);
#21385=ORIENTED_EDGE('',*,*,#15045,.T.);
#21386=ORIENTED_EDGE('',*,*,#15935,.F.);
#21387=ORIENTED_EDGE('',*,*,#15702,.F.);
#21388=ORIENTED_EDGE('',*,*,#15936,.F.);
#21389=ORIENTED_EDGE('',*,*,#15048,.T.);
#21390=ORIENTED_EDGE('',*,*,#15937,.F.);
#21391=ORIENTED_EDGE('',*,*,#15705,.F.);
#21392=ORIENTED_EDGE('',*,*,#15938,.F.);
#21393=ORIENTED_EDGE('',*,*,#15051,.T.);
#21394=ORIENTED_EDGE('',*,*,#15939,.F.);
#21395=ORIENTED_EDGE('',*,*,#15708,.F.);
#21396=ORIENTED_EDGE('',*,*,#15940,.F.);
#21397=ORIENTED_EDGE('',*,*,#15054,.T.);
#21398=ORIENTED_EDGE('',*,*,#15941,.F.);
#21399=ORIENTED_EDGE('',*,*,#15711,.F.);
#21400=ORIENTED_EDGE('',*,*,#15942,.F.);
#21401=ORIENTED_EDGE('',*,*,#15057,.T.);
#21402=ORIENTED_EDGE('',*,*,#15943,.F.);
#21403=ORIENTED_EDGE('',*,*,#15714,.F.);
#21404=ORIENTED_EDGE('',*,*,#15944,.F.);
#21405=ORIENTED_EDGE('',*,*,#15060,.T.);
#21406=ORIENTED_EDGE('',*,*,#15945,.F.);
#21407=ORIENTED_EDGE('',*,*,#15717,.F.);
#21408=ORIENTED_EDGE('',*,*,#15946,.F.);
#21409=ORIENTED_EDGE('',*,*,#15064,.T.);
#21410=ORIENTED_EDGE('',*,*,#15947,.F.);
#21411=ORIENTED_EDGE('',*,*,#15720,.F.);
#21412=ORIENTED_EDGE('',*,*,#15948,.F.);
#21413=ORIENTED_EDGE('',*,*,#15068,.T.);
#21414=ORIENTED_EDGE('',*,*,#15949,.F.);
#21415=ORIENTED_EDGE('',*,*,#15723,.F.);
#21416=ORIENTED_EDGE('',*,*,#15950,.F.);
#21417=ORIENTED_EDGE('',*,*,#15072,.T.);
#21418=ORIENTED_EDGE('',*,*,#15951,.F.);
#21419=ORIENTED_EDGE('',*,*,#15726,.F.);
#21420=ORIENTED_EDGE('',*,*,#15952,.F.);
#21421=ORIENTED_EDGE('',*,*,#15076,.T.);
#21422=ORIENTED_EDGE('',*,*,#15953,.F.);
#21423=ORIENTED_EDGE('',*,*,#15729,.F.);
#21424=ORIENTED_EDGE('',*,*,#15954,.F.);
#21425=ORIENTED_EDGE('',*,*,#15080,.T.);
#21426=ORIENTED_EDGE('',*,*,#15955,.F.);
#21427=ORIENTED_EDGE('',*,*,#15732,.F.);
#21428=ORIENTED_EDGE('',*,*,#15956,.F.);
#21429=ORIENTED_EDGE('',*,*,#15084,.T.);
#21430=ORIENTED_EDGE('',*,*,#15957,.F.);
#21431=ORIENTED_EDGE('',*,*,#15735,.F.);
#21432=ORIENTED_EDGE('',*,*,#15958,.F.);
#21433=ORIENTED_EDGE('',*,*,#15088,.T.);
#21434=ORIENTED_EDGE('',*,*,#15959,.F.);
#21435=ORIENTED_EDGE('',*,*,#15738,.F.);
#21436=ORIENTED_EDGE('',*,*,#15960,.F.);
#21437=ORIENTED_EDGE('',*,*,#15092,.T.);
#21438=ORIENTED_EDGE('',*,*,#15961,.F.);
#21439=ORIENTED_EDGE('',*,*,#15741,.F.);
#21440=ORIENTED_EDGE('',*,*,#15962,.F.);
#21441=ORIENTED_EDGE('',*,*,#15096,.T.);
#21442=ORIENTED_EDGE('',*,*,#15963,.F.);
#21443=ORIENTED_EDGE('',*,*,#15744,.F.);
#21444=ORIENTED_EDGE('',*,*,#15964,.F.);
#21445=ORIENTED_EDGE('',*,*,#15100,.T.);
#21446=ORIENTED_EDGE('',*,*,#15965,.F.);
#21447=ORIENTED_EDGE('',*,*,#15747,.F.);
#21448=ORIENTED_EDGE('',*,*,#15966,.F.);
#21449=ORIENTED_EDGE('',*,*,#15104,.T.);
#21450=ORIENTED_EDGE('',*,*,#15967,.F.);
#21451=ORIENTED_EDGE('',*,*,#15750,.F.);
#21452=ORIENTED_EDGE('',*,*,#15968,.F.);
#21453=ORIENTED_EDGE('',*,*,#15108,.T.);
#21454=ORIENTED_EDGE('',*,*,#15969,.F.);
#21455=ORIENTED_EDGE('',*,*,#15753,.F.);
#21456=ORIENTED_EDGE('',*,*,#15970,.F.);
#21457=ORIENTED_EDGE('',*,*,#15112,.T.);
#21458=ORIENTED_EDGE('',*,*,#15971,.F.);
#21459=ORIENTED_EDGE('',*,*,#15756,.F.);
#21460=ORIENTED_EDGE('',*,*,#15972,.F.);
#21461=ORIENTED_EDGE('',*,*,#15116,.T.);
#21462=ORIENTED_EDGE('',*,*,#15973,.F.);
#21463=ORIENTED_EDGE('',*,*,#15759,.F.);
#21464=ORIENTED_EDGE('',*,*,#15974,.F.);
#21465=ORIENTED_EDGE('',*,*,#15120,.T.);
#21466=ORIENTED_EDGE('',*,*,#15975,.F.);
#21467=ORIENTED_EDGE('',*,*,#15762,.F.);
#21468=ORIENTED_EDGE('',*,*,#15976,.F.);
#21469=ORIENTED_EDGE('',*,*,#15124,.T.);
#21470=ORIENTED_EDGE('',*,*,#15977,.F.);
#21471=ORIENTED_EDGE('',*,*,#15765,.F.);
#21472=ORIENTED_EDGE('',*,*,#15978,.F.);
#21473=ORIENTED_EDGE('',*,*,#15128,.T.);
#21474=ORIENTED_EDGE('',*,*,#15979,.F.);
#21475=ORIENTED_EDGE('',*,*,#15768,.F.);
#21476=ORIENTED_EDGE('',*,*,#15980,.F.);
#21477=ORIENTED_EDGE('',*,*,#15132,.T.);
#21478=ORIENTED_EDGE('',*,*,#15981,.F.);
#21479=ORIENTED_EDGE('',*,*,#15771,.F.);
#21480=ORIENTED_EDGE('',*,*,#15982,.F.);
#21481=ORIENTED_EDGE('',*,*,#15136,.T.);
#21482=ORIENTED_EDGE('',*,*,#15983,.F.);
#21483=ORIENTED_EDGE('',*,*,#15774,.F.);
#21484=ORIENTED_EDGE('',*,*,#15984,.F.);
#21485=ORIENTED_EDGE('',*,*,#14835,.T.);
#21486=ORIENTED_EDGE('',*,*,#15985,.F.);
#21487=ORIENTED_EDGE('',*,*,#15777,.F.);
#21488=ORIENTED_EDGE('',*,*,#15986,.F.);
#21489=ORIENTED_EDGE('',*,*,#14839,.T.);
#21490=ORIENTED_EDGE('',*,*,#15987,.F.);
#21491=ORIENTED_EDGE('',*,*,#15780,.F.);
#21492=ORIENTED_EDGE('',*,*,#15988,.F.);
#21493=ORIENTED_EDGE('',*,*,#14843,.T.);
#21494=ORIENTED_EDGE('',*,*,#15989,.F.);
#21495=ORIENTED_EDGE('',*,*,#15783,.F.);
#21496=ORIENTED_EDGE('',*,*,#15990,.F.);
#21497=ORIENTED_EDGE('',*,*,#14847,.T.);
#21498=ORIENTED_EDGE('',*,*,#15991,.F.);
#21499=ORIENTED_EDGE('',*,*,#15786,.F.);
#21500=ORIENTED_EDGE('',*,*,#15992,.F.);
#21501=ORIENTED_EDGE('',*,*,#14851,.T.);
#21502=ORIENTED_EDGE('',*,*,#15993,.F.);
#21503=ORIENTED_EDGE('',*,*,#15789,.F.);
#21504=ORIENTED_EDGE('',*,*,#15994,.F.);
#21505=ORIENTED_EDGE('',*,*,#14855,.T.);
#21506=ORIENTED_EDGE('',*,*,#15995,.F.);
#21507=ORIENTED_EDGE('',*,*,#15792,.F.);
#21508=ORIENTED_EDGE('',*,*,#15996,.F.);
#21509=ORIENTED_EDGE('',*,*,#14859,.T.);
#21510=ORIENTED_EDGE('',*,*,#15997,.F.);
#21511=ORIENTED_EDGE('',*,*,#15795,.F.);
#21512=ORIENTED_EDGE('',*,*,#15998,.F.);
#21513=ORIENTED_EDGE('',*,*,#14863,.T.);
#21514=ORIENTED_EDGE('',*,*,#15999,.F.);
#21515=ORIENTED_EDGE('',*,*,#15798,.F.);
#21516=ORIENTED_EDGE('',*,*,#16000,.F.);
#21517=ORIENTED_EDGE('',*,*,#14867,.T.);
#21518=ORIENTED_EDGE('',*,*,#16001,.F.);
#21519=ORIENTED_EDGE('',*,*,#15801,.F.);
#21520=ORIENTED_EDGE('',*,*,#16002,.F.);
#21521=ORIENTED_EDGE('',*,*,#14871,.T.);
#21522=ORIENTED_EDGE('',*,*,#16003,.F.);
#21523=ORIENTED_EDGE('',*,*,#15804,.F.);
#21524=ORIENTED_EDGE('',*,*,#16004,.F.);
#21525=ORIENTED_EDGE('',*,*,#14875,.T.);
#21526=ORIENTED_EDGE('',*,*,#16005,.F.);
#21527=ORIENTED_EDGE('',*,*,#15807,.F.);
#21528=ORIENTED_EDGE('',*,*,#16006,.F.);
#21529=ORIENTED_EDGE('',*,*,#14879,.T.);
#21530=ORIENTED_EDGE('',*,*,#16007,.F.);
#21531=ORIENTED_EDGE('',*,*,#15810,.F.);
#21532=ORIENTED_EDGE('',*,*,#16008,.F.);
#21533=ORIENTED_EDGE('',*,*,#14883,.T.);
#21534=ORIENTED_EDGE('',*,*,#16009,.F.);
#21535=ORIENTED_EDGE('',*,*,#15813,.F.);
#21536=ORIENTED_EDGE('',*,*,#16010,.F.);
#21537=ORIENTED_EDGE('',*,*,#14887,.T.);
#21538=ORIENTED_EDGE('',*,*,#16011,.F.);
#21539=ORIENTED_EDGE('',*,*,#15816,.F.);
#21540=ORIENTED_EDGE('',*,*,#16012,.F.);
#21541=ORIENTED_EDGE('',*,*,#14891,.T.);
#21542=ORIENTED_EDGE('',*,*,#16013,.F.);
#21543=ORIENTED_EDGE('',*,*,#15819,.F.);
#21544=ORIENTED_EDGE('',*,*,#16014,.F.);
#21545=ORIENTED_EDGE('',*,*,#14895,.T.);
#21546=ORIENTED_EDGE('',*,*,#16015,.F.);
#21547=ORIENTED_EDGE('',*,*,#15822,.F.);
#21548=ORIENTED_EDGE('',*,*,#16016,.F.);
#21549=ORIENTED_EDGE('',*,*,#14899,.T.);
#21550=ORIENTED_EDGE('',*,*,#16017,.F.);
#21551=ORIENTED_EDGE('',*,*,#15825,.F.);
#21552=ORIENTED_EDGE('',*,*,#16018,.F.);
#21553=ORIENTED_EDGE('',*,*,#14903,.T.);
#21554=ORIENTED_EDGE('',*,*,#16019,.F.);
#21555=ORIENTED_EDGE('',*,*,#15828,.F.);
#21556=ORIENTED_EDGE('',*,*,#16020,.F.);
#21557=ORIENTED_EDGE('',*,*,#14907,.T.);
#21558=ORIENTED_EDGE('',*,*,#16021,.F.);
#21559=ORIENTED_EDGE('',*,*,#15831,.F.);
#21560=ORIENTED_EDGE('',*,*,#16022,.F.);
#21561=ORIENTED_EDGE('',*,*,#14911,.T.);
#21562=ORIENTED_EDGE('',*,*,#16023,.F.);
#21563=ORIENTED_EDGE('',*,*,#15834,.F.);
#21564=ORIENTED_EDGE('',*,*,#16024,.F.);
#21565=ORIENTED_EDGE('',*,*,#14915,.T.);
#21566=ORIENTED_EDGE('',*,*,#16025,.F.);
#21567=ORIENTED_EDGE('',*,*,#15837,.F.);
#21568=ORIENTED_EDGE('',*,*,#16026,.F.);
#21569=ORIENTED_EDGE('',*,*,#14919,.T.);
#21570=ORIENTED_EDGE('',*,*,#16027,.F.);
#21571=ORIENTED_EDGE('',*,*,#15840,.F.);
#21572=ORIENTED_EDGE('',*,*,#16028,.F.);
#21573=ORIENTED_EDGE('',*,*,#14923,.T.);
#21574=ORIENTED_EDGE('',*,*,#16029,.F.);
#21575=ORIENTED_EDGE('',*,*,#15843,.F.);
#21576=ORIENTED_EDGE('',*,*,#16030,.F.);
#21577=ORIENTED_EDGE('',*,*,#14927,.T.);
#21578=ORIENTED_EDGE('',*,*,#16031,.F.);
#21579=ORIENTED_EDGE('',*,*,#15846,.F.);
#21580=ORIENTED_EDGE('',*,*,#16032,.F.);
#21581=ORIENTED_EDGE('',*,*,#14931,.T.);
#21582=ORIENTED_EDGE('',*,*,#16033,.F.);
#21583=ORIENTED_EDGE('',*,*,#15849,.F.);
#21584=ORIENTED_EDGE('',*,*,#16034,.F.);
#21585=ORIENTED_EDGE('',*,*,#14935,.T.);
#21586=ORIENTED_EDGE('',*,*,#16035,.F.);
#21587=ORIENTED_EDGE('',*,*,#15852,.F.);
#21588=ORIENTED_EDGE('',*,*,#16036,.F.);
#21589=ORIENTED_EDGE('',*,*,#14939,.T.);
#21590=ORIENTED_EDGE('',*,*,#16037,.F.);
#21591=ORIENTED_EDGE('',*,*,#15855,.F.);
#21592=ORIENTED_EDGE('',*,*,#16038,.F.);
#21593=ORIENTED_EDGE('',*,*,#14943,.T.);
#21594=ORIENTED_EDGE('',*,*,#16039,.F.);
#21595=ORIENTED_EDGE('',*,*,#15858,.F.);
#21596=ORIENTED_EDGE('',*,*,#16040,.F.);
#21597=ORIENTED_EDGE('',*,*,#14947,.T.);
#21598=ORIENTED_EDGE('',*,*,#16041,.F.);
#21599=ORIENTED_EDGE('',*,*,#15861,.F.);
#21600=ORIENTED_EDGE('',*,*,#16042,.F.);
#21601=ORIENTED_EDGE('',*,*,#14951,.T.);
#21602=ORIENTED_EDGE('',*,*,#16043,.F.);
#21603=ORIENTED_EDGE('',*,*,#15864,.F.);
#21604=ORIENTED_EDGE('',*,*,#16044,.F.);
#21605=ORIENTED_EDGE('',*,*,#14955,.T.);
#21606=ORIENTED_EDGE('',*,*,#16045,.F.);
#21607=ORIENTED_EDGE('',*,*,#15867,.F.);
#21608=ORIENTED_EDGE('',*,*,#16046,.F.);
#21609=ORIENTED_EDGE('',*,*,#14959,.T.);
#21610=ORIENTED_EDGE('',*,*,#16047,.F.);
#21611=ORIENTED_EDGE('',*,*,#15870,.F.);
#21612=ORIENTED_EDGE('',*,*,#16048,.F.);
#21613=ORIENTED_EDGE('',*,*,#14963,.T.);
#21614=ORIENTED_EDGE('',*,*,#16049,.F.);
#21615=ORIENTED_EDGE('',*,*,#15873,.F.);
#21616=ORIENTED_EDGE('',*,*,#16050,.F.);
#21617=ORIENTED_EDGE('',*,*,#14967,.T.);
#21618=ORIENTED_EDGE('',*,*,#16051,.F.);
#21619=ORIENTED_EDGE('',*,*,#15876,.F.);
#21620=ORIENTED_EDGE('',*,*,#16052,.F.);
#21621=ORIENTED_EDGE('',*,*,#14971,.T.);
#21622=ORIENTED_EDGE('',*,*,#16053,.F.);
#21623=ORIENTED_EDGE('',*,*,#15879,.F.);
#21624=ORIENTED_EDGE('',*,*,#16054,.F.);
#21625=ORIENTED_EDGE('',*,*,#14975,.T.);
#21626=ORIENTED_EDGE('',*,*,#16055,.F.);
#21627=ORIENTED_EDGE('',*,*,#15882,.F.);
#21628=ORIENTED_EDGE('',*,*,#16056,.F.);
#21629=ORIENTED_EDGE('',*,*,#14979,.T.);
#21630=ORIENTED_EDGE('',*,*,#16057,.F.);
#21631=ORIENTED_EDGE('',*,*,#15885,.F.);
#21632=ORIENTED_EDGE('',*,*,#16058,.F.);
#21633=ORIENTED_EDGE('',*,*,#14983,.T.);
#21634=ORIENTED_EDGE('',*,*,#16059,.F.);
#21635=ORIENTED_EDGE('',*,*,#15039,.T.);
#21636=ORIENTED_EDGE('',*,*,#16060,.F.);
#21637=ORIENTED_EDGE('',*,*,#15887,.F.);
#21638=ORIENTED_EDGE('',*,*,#16061,.F.);
#21639=ORIENTED_EDGE('',*,*,#15036,.T.);
#21640=ORIENTED_EDGE('',*,*,#16062,.F.);
#21641=ORIENTED_EDGE('',*,*,#15890,.F.);
#21642=ORIENTED_EDGE('',*,*,#16063,.F.);
#21643=ORIENTED_EDGE('',*,*,#15033,.T.);
#21644=ORIENTED_EDGE('',*,*,#16064,.F.);
#21645=ORIENTED_EDGE('',*,*,#15893,.F.);
#21646=ORIENTED_EDGE('',*,*,#16065,.F.);
#21647=ORIENTED_EDGE('',*,*,#15030,.T.);
#21648=ORIENTED_EDGE('',*,*,#16066,.F.);
#21649=ORIENTED_EDGE('',*,*,#15896,.F.);
#21650=ORIENTED_EDGE('',*,*,#16067,.F.);
#21651=ORIENTED_EDGE('',*,*,#15027,.T.);
#21652=ORIENTED_EDGE('',*,*,#16068,.F.);
#21653=ORIENTED_EDGE('',*,*,#15899,.F.);
#21654=ORIENTED_EDGE('',*,*,#16069,.F.);
#21655=ORIENTED_EDGE('',*,*,#15024,.T.);
#21656=ORIENTED_EDGE('',*,*,#16070,.F.);
#21657=ORIENTED_EDGE('',*,*,#15902,.F.);
#21658=ORIENTED_EDGE('',*,*,#16071,.F.);
#21659=ORIENTED_EDGE('',*,*,#15021,.T.);
#21660=ORIENTED_EDGE('',*,*,#16072,.F.);
#21661=ORIENTED_EDGE('',*,*,#15905,.F.);
#21662=ORIENTED_EDGE('',*,*,#16073,.F.);
#21663=ORIENTED_EDGE('',*,*,#15018,.T.);
#21664=ORIENTED_EDGE('',*,*,#16074,.F.);
#21665=ORIENTED_EDGE('',*,*,#15908,.F.);
#21666=ORIENTED_EDGE('',*,*,#16075,.F.);
#21667=ORIENTED_EDGE('',*,*,#15015,.T.);
#21668=ORIENTED_EDGE('',*,*,#16076,.F.);
#21669=ORIENTED_EDGE('',*,*,#15911,.F.);
#21670=ORIENTED_EDGE('',*,*,#16077,.F.);
#21671=ORIENTED_EDGE('',*,*,#15011,.T.);
#21672=ORIENTED_EDGE('',*,*,#16078,.F.);
#21673=ORIENTED_EDGE('',*,*,#15914,.F.);
#21674=ORIENTED_EDGE('',*,*,#16079,.F.);
#21675=ORIENTED_EDGE('',*,*,#15007,.T.);
#21676=ORIENTED_EDGE('',*,*,#16080,.F.);
#21677=ORIENTED_EDGE('',*,*,#15917,.F.);
#21678=ORIENTED_EDGE('',*,*,#16081,.F.);
#21679=ORIENTED_EDGE('',*,*,#15003,.T.);
#21680=ORIENTED_EDGE('',*,*,#16082,.F.);
#21681=ORIENTED_EDGE('',*,*,#15920,.F.);
#21682=ORIENTED_EDGE('',*,*,#16083,.F.);
#21683=ORIENTED_EDGE('',*,*,#14999,.T.);
#21684=ORIENTED_EDGE('',*,*,#16084,.F.);
#21685=ORIENTED_EDGE('',*,*,#15923,.F.);
#21686=ORIENTED_EDGE('',*,*,#16085,.F.);
#21687=ORIENTED_EDGE('',*,*,#14995,.T.);
#21688=ORIENTED_EDGE('',*,*,#16086,.F.);
#21689=ORIENTED_EDGE('',*,*,#15926,.F.);
#21690=ORIENTED_EDGE('',*,*,#16087,.F.);
#21691=ORIENTED_EDGE('',*,*,#15930,.F.);
#21692=ORIENTED_EDGE('',*,*,#16088,.F.);
#21693=ORIENTED_EDGE('',*,*,#14987,.T.);
#21694=ORIENTED_EDGE('',*,*,#14665,.T.);
#21695=ORIENTED_EDGE('',*,*,#14755,.T.);
#21696=ORIENTED_EDGE('',*,*,#14662,.T.);
#21697=ORIENTED_EDGE('',*,*,#15453,.T.);
#21698=ORIENTED_EDGE('',*,*,#15456,.F.);
#21699=ORIENTED_EDGE('',*,*,#16089,.F.);
#21700=ORIENTED_EDGE('',*,*,#15142,.F.);
#21701=ORIENTED_EDGE('',*,*,#16090,.F.);
#21702=ORIENTED_EDGE('',*,*,#16091,.T.);
#21703=ORIENTED_EDGE('',*,*,#16092,.F.);
#21704=ORIENTED_EDGE('',*,*,#16091,.F.);
#21705=ORIENTED_EDGE('',*,*,#16093,.F.);
#21706=ORIENTED_EDGE('',*,*,#16094,.T.);
#21707=ORIENTED_EDGE('',*,*,#16095,.F.);
#21708=ORIENTED_EDGE('',*,*,#16094,.F.);
#21709=ORIENTED_EDGE('',*,*,#16096,.F.);
#21710=ORIENTED_EDGE('',*,*,#14991,.T.);
#21711=ORIENTED_EDGE('',*,*,#14832,.F.);
#21712=ORIENTED_EDGE('',*,*,#14829,.F.);
#21713=ORIENTED_EDGE('',*,*,#16097,.T.);
#21714=ORIENTED_EDGE('',*,*,#16098,.T.);
#21715=ORIENTED_EDGE('',*,*,#16099,.T.);
#21716=ORIENTED_EDGE('',*,*,#16100,.T.);
#21717=ORIENTED_EDGE('',*,*,#16101,.T.);
#21718=ORIENTED_EDGE('',*,*,#16102,.T.);
#21719=ORIENTED_EDGE('',*,*,#16103,.T.);
#21720=ORIENTED_EDGE('',*,*,#14824,.T.);
#21721=ORIENTED_EDGE('',*,*,#16104,.F.);
#21722=ORIENTED_EDGE('',*,*,#16098,.F.);
#21723=ORIENTED_EDGE('',*,*,#16104,.T.);
#21724=ORIENTED_EDGE('',*,*,#14823,.T.);
#21725=ORIENTED_EDGE('',*,*,#16105,.F.);
#21726=ORIENTED_EDGE('',*,*,#16099,.F.);
#21727=ORIENTED_EDGE('',*,*,#16105,.T.);
#21728=ORIENTED_EDGE('',*,*,#14822,.T.);
#21729=ORIENTED_EDGE('',*,*,#16106,.F.);
#21730=ORIENTED_EDGE('',*,*,#16100,.F.);
#21731=ORIENTED_EDGE('',*,*,#16106,.T.);
#21732=ORIENTED_EDGE('',*,*,#14821,.T.);
#21733=ORIENTED_EDGE('',*,*,#14827,.T.);
#21734=ORIENTED_EDGE('',*,*,#16107,.F.);
#21735=ORIENTED_EDGE('',*,*,#16101,.F.);
#21736=ORIENTED_EDGE('',*,*,#16107,.T.);
#21737=ORIENTED_EDGE('',*,*,#14826,.T.);
#21738=ORIENTED_EDGE('',*,*,#16108,.F.);
#21739=ORIENTED_EDGE('',*,*,#16102,.F.);
#21740=ORIENTED_EDGE('',*,*,#16108,.T.);
#21741=ORIENTED_EDGE('',*,*,#14825,.T.);
#21742=ORIENTED_EDGE('',*,*,#16103,.F.);
#21743=ORIENTED_EDGE('',*,*,#16097,.F.);
#21744=ORIENTED_EDGE('',*,*,#16109,.F.);
#21745=ORIENTED_EDGE('',*,*,#14753,.F.);
#21746=ORIENTED_EDGE('',*,*,#14752,.F.);
#21747=ORIENTED_EDGE('',*,*,#14749,.F.);
#21748=ORIENTED_EDGE('',*,*,#14746,.F.);
#21749=ORIENTED_EDGE('',*,*,#14743,.F.);
#21750=ORIENTED_EDGE('',*,*,#14740,.F.);
#21751=ORIENTED_EDGE('',*,*,#14737,.F.);
#21752=ORIENTED_EDGE('',*,*,#14734,.F.);
#21753=ORIENTED_EDGE('',*,*,#14731,.F.);
#21754=ORIENTED_EDGE('',*,*,#14728,.F.);
#21755=ORIENTED_EDGE('',*,*,#14725,.F.);
#21756=ORIENTED_EDGE('',*,*,#14722,.F.);
#21757=ORIENTED_EDGE('',*,*,#14719,.F.);
#21758=ORIENTED_EDGE('',*,*,#14716,.F.);
#21759=ORIENTED_EDGE('',*,*,#14713,.F.);
#21760=ORIENTED_EDGE('',*,*,#14710,.F.);
#21761=ORIENTED_EDGE('',*,*,#14707,.F.);
#21762=ORIENTED_EDGE('',*,*,#14704,.F.);
#21763=ORIENTED_EDGE('',*,*,#14701,.F.);
#21764=ORIENTED_EDGE('',*,*,#14698,.F.);
#21765=ORIENTED_EDGE('',*,*,#14695,.F.);
#21766=ORIENTED_EDGE('',*,*,#14692,.F.);
#21767=ORIENTED_EDGE('',*,*,#14689,.F.);
#21768=ORIENTED_EDGE('',*,*,#14686,.F.);
#21769=ORIENTED_EDGE('',*,*,#14683,.F.);
#21770=ORIENTED_EDGE('',*,*,#14680,.F.);
#21771=ORIENTED_EDGE('',*,*,#14677,.F.);
#21772=ORIENTED_EDGE('',*,*,#14674,.F.);
#21773=ORIENTED_EDGE('',*,*,#14671,.F.);
#21774=ORIENTED_EDGE('',*,*,#14668,.F.);
#21775=ORIENTED_EDGE('',*,*,#14661,.F.);
#21776=ORIENTED_EDGE('',*,*,#14758,.F.);
#21777=ORIENTED_EDGE('',*,*,#14759,.T.);
#21778=ORIENTED_EDGE('',*,*,#14659,.T.);
#21779=ORIENTED_EDGE('',*,*,#14656,.T.);
#21780=ORIENTED_EDGE('',*,*,#14653,.T.);
#21781=ORIENTED_EDGE('',*,*,#14650,.T.);
#21782=ORIENTED_EDGE('',*,*,#14647,.T.);
#21783=ORIENTED_EDGE('',*,*,#14644,.T.);
#21784=ORIENTED_EDGE('',*,*,#14641,.T.);
#21785=ORIENTED_EDGE('',*,*,#14638,.T.);
#21786=ORIENTED_EDGE('',*,*,#14635,.T.);
#21787=ORIENTED_EDGE('',*,*,#14632,.T.);
#21788=ORIENTED_EDGE('',*,*,#14629,.T.);
#21789=ORIENTED_EDGE('',*,*,#14626,.T.);
#21790=ORIENTED_EDGE('',*,*,#14623,.T.);
#21791=ORIENTED_EDGE('',*,*,#14620,.T.);
#21792=ORIENTED_EDGE('',*,*,#14617,.T.);
#21793=ORIENTED_EDGE('',*,*,#14614,.T.);
#21794=ORIENTED_EDGE('',*,*,#14611,.T.);
#21795=ORIENTED_EDGE('',*,*,#14608,.T.);
#21796=ORIENTED_EDGE('',*,*,#14605,.T.);
#21797=ORIENTED_EDGE('',*,*,#14602,.T.);
#21798=ORIENTED_EDGE('',*,*,#14599,.T.);
#21799=ORIENTED_EDGE('',*,*,#14596,.T.);
#21800=ORIENTED_EDGE('',*,*,#14593,.T.);
#21801=ORIENTED_EDGE('',*,*,#14590,.T.);
#21802=ORIENTED_EDGE('',*,*,#14587,.T.);
#21803=ORIENTED_EDGE('',*,*,#14584,.T.);
#21804=ORIENTED_EDGE('',*,*,#14581,.T.);
#21805=ORIENTED_EDGE('',*,*,#14578,.T.);
#21806=ORIENTED_EDGE('',*,*,#16110,.F.);
#21807=ORIENTED_EDGE('',*,*,#14574,.T.);
#21808=ORIENTED_EDGE('',*,*,#14580,.T.);
#21809=ORIENTED_EDGE('',*,*,#14583,.T.);
#21810=ORIENTED_EDGE('',*,*,#14586,.T.);
#21811=ORIENTED_EDGE('',*,*,#14589,.T.);
#21812=ORIENTED_EDGE('',*,*,#14592,.T.);
#21813=ORIENTED_EDGE('',*,*,#14595,.T.);
#21814=ORIENTED_EDGE('',*,*,#14598,.T.);
#21815=ORIENTED_EDGE('',*,*,#14601,.T.);
#21816=ORIENTED_EDGE('',*,*,#14604,.T.);
#21817=ORIENTED_EDGE('',*,*,#14607,.T.);
#21818=ORIENTED_EDGE('',*,*,#14610,.T.);
#21819=ORIENTED_EDGE('',*,*,#14613,.T.);
#21820=ORIENTED_EDGE('',*,*,#14616,.T.);
#21821=ORIENTED_EDGE('',*,*,#14619,.T.);
#21822=ORIENTED_EDGE('',*,*,#14622,.T.);
#21823=ORIENTED_EDGE('',*,*,#14625,.T.);
#21824=ORIENTED_EDGE('',*,*,#14628,.T.);
#21825=ORIENTED_EDGE('',*,*,#14631,.T.);
#21826=ORIENTED_EDGE('',*,*,#14634,.T.);
#21827=ORIENTED_EDGE('',*,*,#14637,.T.);
#21828=ORIENTED_EDGE('',*,*,#14640,.T.);
#21829=ORIENTED_EDGE('',*,*,#14643,.T.);
#21830=ORIENTED_EDGE('',*,*,#14646,.T.);
#21831=ORIENTED_EDGE('',*,*,#14649,.T.);
#21832=ORIENTED_EDGE('',*,*,#14652,.T.);
#21833=ORIENTED_EDGE('',*,*,#14655,.T.);
#21834=ORIENTED_EDGE('',*,*,#14658,.T.);
#21835=ORIENTED_EDGE('',*,*,#14760,.T.);
#21836=ORIENTED_EDGE('',*,*,#14756,.F.);
#21837=ORIENTED_EDGE('',*,*,#14664,.T.);
#21838=ORIENTED_EDGE('',*,*,#14667,.T.);
#21839=ORIENTED_EDGE('',*,*,#14670,.T.);
#21840=ORIENTED_EDGE('',*,*,#14673,.T.);
#21841=ORIENTED_EDGE('',*,*,#14676,.T.);
#21842=ORIENTED_EDGE('',*,*,#14679,.T.);
#21843=ORIENTED_EDGE('',*,*,#14682,.T.);
#21844=ORIENTED_EDGE('',*,*,#14685,.T.);
#21845=ORIENTED_EDGE('',*,*,#14688,.T.);
#21846=ORIENTED_EDGE('',*,*,#14691,.T.);
#21847=ORIENTED_EDGE('',*,*,#14694,.T.);
#21848=ORIENTED_EDGE('',*,*,#14697,.T.);
#21849=ORIENTED_EDGE('',*,*,#14700,.T.);
#21850=ORIENTED_EDGE('',*,*,#14703,.T.);
#21851=ORIENTED_EDGE('',*,*,#14706,.T.);
#21852=ORIENTED_EDGE('',*,*,#14709,.T.);
#21853=ORIENTED_EDGE('',*,*,#14712,.T.);
#21854=ORIENTED_EDGE('',*,*,#14715,.T.);
#21855=ORIENTED_EDGE('',*,*,#14718,.T.);
#21856=ORIENTED_EDGE('',*,*,#14721,.T.);
#21857=ORIENTED_EDGE('',*,*,#14724,.T.);
#21858=ORIENTED_EDGE('',*,*,#14727,.T.);
#21859=ORIENTED_EDGE('',*,*,#14730,.T.);
#21860=ORIENTED_EDGE('',*,*,#14733,.T.);
#21861=ORIENTED_EDGE('',*,*,#14736,.T.);
#21862=ORIENTED_EDGE('',*,*,#14739,.T.);
#21863=ORIENTED_EDGE('',*,*,#14742,.T.);
#21864=ORIENTED_EDGE('',*,*,#14745,.T.);
#21865=ORIENTED_EDGE('',*,*,#14748,.T.);
#21866=ORIENTED_EDGE('',*,*,#14751,.T.);
#21867=ORIENTED_EDGE('',*,*,#14754,.T.);
#21868=ORIENTED_EDGE('',*,*,#16109,.T.);
#21869=ORIENTED_EDGE('',*,*,#14577,.T.);
#21870=ORIENTED_EDGE('',*,*,#16110,.T.);
#21871=ORIENTED_EDGE('',*,*,#15141,.T.);
#21872=ORIENTED_EDGE('',*,*,#16111,.T.);
#21873=ORIENTED_EDGE('',*,*,#14992,.T.);
#21874=ORIENTED_EDGE('',*,*,#16096,.T.);
#21875=ORIENTED_EDGE('',*,*,#16093,.T.);
#21876=ORIENTED_EDGE('',*,*,#16090,.T.);
#21877=ORIENTED_EDGE('',*,*,#15140,.T.);
#21878=ORIENTED_EDGE('',*,*,#15445,.T.);
#21879=ORIENTED_EDGE('',*,*,#16112,.T.);
#21880=ORIENTED_EDGE('',*,*,#14993,.T.);
#21881=ORIENTED_EDGE('',*,*,#16111,.F.);
#21882=ORIENTED_EDGE('',*,*,#15444,.T.);
#21883=ORIENTED_EDGE('',*,*,#15690,.T.);
#21884=ORIENTED_EDGE('',*,*,#15927,.T.);
#21885=ORIENTED_EDGE('',*,*,#16086,.T.);
#21886=ORIENTED_EDGE('',*,*,#14994,.T.);
#21887=ORIENTED_EDGE('',*,*,#16112,.F.);
#21888=ORIENTED_EDGE('',*,*,#15145,.T.);
#21889=ORIENTED_EDGE('',*,*,#16113,.T.);
#21890=ORIENTED_EDGE('',*,*,#14988,.T.);
#21891=ORIENTED_EDGE('',*,*,#16088,.T.);
#21892=ORIENTED_EDGE('',*,*,#15929,.T.);
#21893=ORIENTED_EDGE('',*,*,#15692,.T.);
#21894=ORIENTED_EDGE('',*,*,#15144,.T.);
#21895=ORIENTED_EDGE('',*,*,#16114,.T.);
#21896=ORIENTED_EDGE('',*,*,#14989,.T.);
#21897=ORIENTED_EDGE('',*,*,#16113,.F.);
#21898=ORIENTED_EDGE('',*,*,#15143,.T.);
#21899=ORIENTED_EDGE('',*,*,#16089,.T.);
#21900=ORIENTED_EDGE('',*,*,#16092,.T.);
#21901=ORIENTED_EDGE('',*,*,#16095,.T.);
#21902=ORIENTED_EDGE('',*,*,#14990,.T.);
#21903=ORIENTED_EDGE('',*,*,#16114,.F.);
#21904=ORIENTED_EDGE('',*,*,#15442,.T.);
#21905=ORIENTED_EDGE('',*,*,#16115,.T.);
#21906=ORIENTED_EDGE('',*,*,#14996,.T.);
#21907=ORIENTED_EDGE('',*,*,#16085,.T.);
#21908=ORIENTED_EDGE('',*,*,#15925,.T.);
#21909=ORIENTED_EDGE('',*,*,#15688,.T.);
#21910=ORIENTED_EDGE('',*,*,#15441,.T.);
#21911=ORIENTED_EDGE('',*,*,#16116,.T.);
#21912=ORIENTED_EDGE('',*,*,#14997,.T.);
#21913=ORIENTED_EDGE('',*,*,#16115,.F.);
#21914=ORIENTED_EDGE('',*,*,#15440,.T.);
#21915=ORIENTED_EDGE('',*,*,#15687,.T.);
#21916=ORIENTED_EDGE('',*,*,#15924,.T.);
#21917=ORIENTED_EDGE('',*,*,#16084,.T.);
#21918=ORIENTED_EDGE('',*,*,#14998,.T.);
#21919=ORIENTED_EDGE('',*,*,#16116,.F.);
#21920=ORIENTED_EDGE('',*,*,#15438,.T.);
#21921=ORIENTED_EDGE('',*,*,#16117,.T.);
#21922=ORIENTED_EDGE('',*,*,#15000,.T.);
#21923=ORIENTED_EDGE('',*,*,#16083,.T.);
#21924=ORIENTED_EDGE('',*,*,#15922,.T.);
#21925=ORIENTED_EDGE('',*,*,#15685,.T.);
#21926=ORIENTED_EDGE('',*,*,#15437,.T.);
#21927=ORIENTED_EDGE('',*,*,#16118,.T.);
#21928=ORIENTED_EDGE('',*,*,#15001,.T.);
#21929=ORIENTED_EDGE('',*,*,#16117,.F.);
#21930=ORIENTED_EDGE('',*,*,#15436,.T.);
#21931=ORIENTED_EDGE('',*,*,#15684,.T.);
#21932=ORIENTED_EDGE('',*,*,#15921,.T.);
#21933=ORIENTED_EDGE('',*,*,#16082,.T.);
#21934=ORIENTED_EDGE('',*,*,#15002,.T.);
#21935=ORIENTED_EDGE('',*,*,#16118,.F.);
#21936=ORIENTED_EDGE('',*,*,#15434,.T.);
#21937=ORIENTED_EDGE('',*,*,#16119,.T.);
#21938=ORIENTED_EDGE('',*,*,#15004,.T.);
#21939=ORIENTED_EDGE('',*,*,#16081,.T.);
#21940=ORIENTED_EDGE('',*,*,#15919,.T.);
#21941=ORIENTED_EDGE('',*,*,#15682,.T.);
#21942=ORIENTED_EDGE('',*,*,#15433,.T.);
#21943=ORIENTED_EDGE('',*,*,#16120,.T.);
#21944=ORIENTED_EDGE('',*,*,#15005,.T.);
#21945=ORIENTED_EDGE('',*,*,#16119,.F.);
#21946=ORIENTED_EDGE('',*,*,#15432,.T.);
#21947=ORIENTED_EDGE('',*,*,#15681,.T.);
#21948=ORIENTED_EDGE('',*,*,#15918,.T.);
#21949=ORIENTED_EDGE('',*,*,#16080,.T.);
#21950=ORIENTED_EDGE('',*,*,#15006,.T.);
#21951=ORIENTED_EDGE('',*,*,#16120,.F.);
#21952=ORIENTED_EDGE('',*,*,#15430,.T.);
#21953=ORIENTED_EDGE('',*,*,#16121,.T.);
#21954=ORIENTED_EDGE('',*,*,#15008,.T.);
#21955=ORIENTED_EDGE('',*,*,#16079,.T.);
#21956=ORIENTED_EDGE('',*,*,#15916,.T.);
#21957=ORIENTED_EDGE('',*,*,#15679,.T.);
#21958=ORIENTED_EDGE('',*,*,#15429,.T.);
#21959=ORIENTED_EDGE('',*,*,#16122,.T.);
#21960=ORIENTED_EDGE('',*,*,#15009,.T.);
#21961=ORIENTED_EDGE('',*,*,#16121,.F.);
#21962=ORIENTED_EDGE('',*,*,#15428,.T.);
#21963=ORIENTED_EDGE('',*,*,#15678,.T.);
#21964=ORIENTED_EDGE('',*,*,#15915,.T.);
#21965=ORIENTED_EDGE('',*,*,#16078,.T.);
#21966=ORIENTED_EDGE('',*,*,#15010,.T.);
#21967=ORIENTED_EDGE('',*,*,#16122,.F.);
#21968=ORIENTED_EDGE('',*,*,#15426,.T.);
#21969=ORIENTED_EDGE('',*,*,#16123,.T.);
#21970=ORIENTED_EDGE('',*,*,#15012,.T.);
#21971=ORIENTED_EDGE('',*,*,#16077,.T.);
#21972=ORIENTED_EDGE('',*,*,#15913,.T.);
#21973=ORIENTED_EDGE('',*,*,#15676,.T.);
#21974=ORIENTED_EDGE('',*,*,#15425,.T.);
#21975=ORIENTED_EDGE('',*,*,#16124,.T.);
#21976=ORIENTED_EDGE('',*,*,#15013,.T.);
#21977=ORIENTED_EDGE('',*,*,#16123,.F.);
#21978=ORIENTED_EDGE('',*,*,#15424,.T.);
#21979=ORIENTED_EDGE('',*,*,#15675,.T.);
#21980=ORIENTED_EDGE('',*,*,#15912,.T.);
#21981=ORIENTED_EDGE('',*,*,#16076,.T.);
#21982=ORIENTED_EDGE('',*,*,#15014,.T.);
#21983=ORIENTED_EDGE('',*,*,#16124,.F.);
#21984=ORIENTED_EDGE('',*,*,#15422,.T.);
#21985=ORIENTED_EDGE('',*,*,#14820,.T.);
#21986=ORIENTED_EDGE('',*,*,#15016,.T.);
#21987=ORIENTED_EDGE('',*,*,#16075,.T.);
#21988=ORIENTED_EDGE('',*,*,#15910,.T.);
#21989=ORIENTED_EDGE('',*,*,#15673,.T.);
#21990=ORIENTED_EDGE('',*,*,#15421,.T.);
#21991=ORIENTED_EDGE('',*,*,#15672,.T.);
#21992=ORIENTED_EDGE('',*,*,#15909,.T.);
#21993=ORIENTED_EDGE('',*,*,#16074,.T.);
#21994=ORIENTED_EDGE('',*,*,#15017,.T.);
#21995=ORIENTED_EDGE('',*,*,#14818,.F.);
#21996=ORIENTED_EDGE('',*,*,#15419,.T.);
#21997=ORIENTED_EDGE('',*,*,#14816,.T.);
#21998=ORIENTED_EDGE('',*,*,#15019,.T.);
#21999=ORIENTED_EDGE('',*,*,#16073,.T.);
#22000=ORIENTED_EDGE('',*,*,#15907,.T.);
#22001=ORIENTED_EDGE('',*,*,#15670,.T.);
#22002=ORIENTED_EDGE('',*,*,#15418,.T.);
#22003=ORIENTED_EDGE('',*,*,#15669,.T.);
#22004=ORIENTED_EDGE('',*,*,#15906,.T.);
#22005=ORIENTED_EDGE('',*,*,#16072,.T.);
#22006=ORIENTED_EDGE('',*,*,#15020,.T.);
#22007=ORIENTED_EDGE('',*,*,#14814,.F.);
#22008=ORIENTED_EDGE('',*,*,#15416,.T.);
#22009=ORIENTED_EDGE('',*,*,#14812,.T.);
#22010=ORIENTED_EDGE('',*,*,#15022,.T.);
#22011=ORIENTED_EDGE('',*,*,#16071,.T.);
#22012=ORIENTED_EDGE('',*,*,#15904,.T.);
#22013=ORIENTED_EDGE('',*,*,#15667,.T.);
#22014=ORIENTED_EDGE('',*,*,#15415,.T.);
#22015=ORIENTED_EDGE('',*,*,#15666,.T.);
#22016=ORIENTED_EDGE('',*,*,#15903,.T.);
#22017=ORIENTED_EDGE('',*,*,#16070,.T.);
#22018=ORIENTED_EDGE('',*,*,#15023,.T.);
#22019=ORIENTED_EDGE('',*,*,#14810,.F.);
#22020=ORIENTED_EDGE('',*,*,#15413,.T.);
#22021=ORIENTED_EDGE('',*,*,#14808,.T.);
#22022=ORIENTED_EDGE('',*,*,#15025,.T.);
#22023=ORIENTED_EDGE('',*,*,#16069,.T.);
#22024=ORIENTED_EDGE('',*,*,#15901,.T.);
#22025=ORIENTED_EDGE('',*,*,#15664,.T.);
#22026=ORIENTED_EDGE('',*,*,#15412,.T.);
#22027=ORIENTED_EDGE('',*,*,#15663,.T.);
#22028=ORIENTED_EDGE('',*,*,#15900,.T.);
#22029=ORIENTED_EDGE('',*,*,#16068,.T.);
#22030=ORIENTED_EDGE('',*,*,#15026,.T.);
#22031=ORIENTED_EDGE('',*,*,#14806,.F.);
#22032=ORIENTED_EDGE('',*,*,#15410,.T.);
#22033=ORIENTED_EDGE('',*,*,#14804,.T.);
#22034=ORIENTED_EDGE('',*,*,#15028,.T.);
#22035=ORIENTED_EDGE('',*,*,#16067,.T.);
#22036=ORIENTED_EDGE('',*,*,#15898,.T.);
#22037=ORIENTED_EDGE('',*,*,#15661,.T.);
#22038=ORIENTED_EDGE('',*,*,#15409,.T.);
#22039=ORIENTED_EDGE('',*,*,#15660,.T.);
#22040=ORIENTED_EDGE('',*,*,#15897,.T.);
#22041=ORIENTED_EDGE('',*,*,#16066,.T.);
#22042=ORIENTED_EDGE('',*,*,#15029,.T.);
#22043=ORIENTED_EDGE('',*,*,#14802,.F.);
#22044=ORIENTED_EDGE('',*,*,#15407,.T.);
#22045=ORIENTED_EDGE('',*,*,#14800,.T.);
#22046=ORIENTED_EDGE('',*,*,#15031,.T.);
#22047=ORIENTED_EDGE('',*,*,#16065,.T.);
#22048=ORIENTED_EDGE('',*,*,#15895,.T.);
#22049=ORIENTED_EDGE('',*,*,#15658,.T.);
#22050=ORIENTED_EDGE('',*,*,#15406,.T.);
#22051=ORIENTED_EDGE('',*,*,#15657,.T.);
#22052=ORIENTED_EDGE('',*,*,#15894,.T.);
#22053=ORIENTED_EDGE('',*,*,#16064,.T.);
#22054=ORIENTED_EDGE('',*,*,#15032,.T.);
#22055=ORIENTED_EDGE('',*,*,#14798,.F.);
#22056=ORIENTED_EDGE('',*,*,#15404,.T.);
#22057=ORIENTED_EDGE('',*,*,#14796,.T.);
#22058=ORIENTED_EDGE('',*,*,#15034,.T.);
#22059=ORIENTED_EDGE('',*,*,#16063,.T.);
#22060=ORIENTED_EDGE('',*,*,#15892,.T.);
#22061=ORIENTED_EDGE('',*,*,#15655,.T.);
#22062=ORIENTED_EDGE('',*,*,#15403,.T.);
#22063=ORIENTED_EDGE('',*,*,#15654,.T.);
#22064=ORIENTED_EDGE('',*,*,#15891,.T.);
#22065=ORIENTED_EDGE('',*,*,#16062,.T.);
#22066=ORIENTED_EDGE('',*,*,#15035,.T.);
#22067=ORIENTED_EDGE('',*,*,#14794,.F.);
#22068=ORIENTED_EDGE('',*,*,#15401,.T.);
#22069=ORIENTED_EDGE('',*,*,#14792,.T.);
#22070=ORIENTED_EDGE('',*,*,#15037,.T.);
#22071=ORIENTED_EDGE('',*,*,#16061,.T.);
#22072=ORIENTED_EDGE('',*,*,#15889,.T.);
#22073=ORIENTED_EDGE('',*,*,#15652,.T.);
#22074=ORIENTED_EDGE('',*,*,#15400,.T.);
#22075=ORIENTED_EDGE('',*,*,#15651,.T.);
#22076=ORIENTED_EDGE('',*,*,#15888,.T.);
#22077=ORIENTED_EDGE('',*,*,#16060,.T.);
#22078=ORIENTED_EDGE('',*,*,#15038,.T.);
#22079=ORIENTED_EDGE('',*,*,#14790,.F.);
#22080=ORIENTED_EDGE('',*,*,#15398,.T.);
#22081=ORIENTED_EDGE('',*,*,#14788,.T.);
#22082=ORIENTED_EDGE('',*,*,#15040,.T.);
#22083=ORIENTED_EDGE('',*,*,#16059,.T.);
#22084=ORIENTED_EDGE('',*,*,#15886,.T.);
#22085=ORIENTED_EDGE('',*,*,#15649,.T.);
#22086=ORIENTED_EDGE('',*,*,#15397,.T.);
#22087=ORIENTED_EDGE('',*,*,#15459,.T.);
#22088=ORIENTED_EDGE('',*,*,#15696,.T.);
#22089=ORIENTED_EDGE('',*,*,#15932,.T.);
#22090=ORIENTED_EDGE('',*,*,#15041,.T.);
#22091=ORIENTED_EDGE('',*,*,#14786,.F.);
#22092=ORIENTED_EDGE('',*,*,#15149,.T.);
#22093=ORIENTED_EDGE('',*,*,#16125,.T.);
#22094=ORIENTED_EDGE('',*,*,#14984,.T.);
#22095=ORIENTED_EDGE('',*,*,#16058,.T.);
#22096=ORIENTED_EDGE('',*,*,#15884,.T.);
#22097=ORIENTED_EDGE('',*,*,#15647,.T.);
#22098=ORIENTED_EDGE('',*,*,#15148,.T.);
#22099=ORIENTED_EDGE('',*,*,#16126,.T.);
#22100=ORIENTED_EDGE('',*,*,#14985,.T.);
#22101=ORIENTED_EDGE('',*,*,#16125,.F.);
#22102=ORIENTED_EDGE('',*,*,#15147,.T.);
#22103=ORIENTED_EDGE('',*,*,#15691,.T.);
#22104=ORIENTED_EDGE('',*,*,#15928,.T.);
#22105=ORIENTED_EDGE('',*,*,#16087,.T.);
#22106=ORIENTED_EDGE('',*,*,#14986,.T.);
#22107=ORIENTED_EDGE('',*,*,#16126,.F.);
#22108=ORIENTED_EDGE('',*,*,#15153,.T.);
#22109=ORIENTED_EDGE('',*,*,#16127,.T.);
#22110=ORIENTED_EDGE('',*,*,#14980,.T.);
#22111=ORIENTED_EDGE('',*,*,#16056,.T.);
#22112=ORIENTED_EDGE('',*,*,#15881,.T.);
#22113=ORIENTED_EDGE('',*,*,#15644,.T.);
#22114=ORIENTED_EDGE('',*,*,#15152,.T.);
#22115=ORIENTED_EDGE('',*,*,#16128,.T.);
#22116=ORIENTED_EDGE('',*,*,#14981,.T.);
#22117=ORIENTED_EDGE('',*,*,#16127,.F.);
#22118=ORIENTED_EDGE('',*,*,#15151,.T.);
#22119=ORIENTED_EDGE('',*,*,#15646,.T.);
#22120=ORIENTED_EDGE('',*,*,#15883,.T.);
#22121=ORIENTED_EDGE('',*,*,#16057,.T.);
#22122=ORIENTED_EDGE('',*,*,#14982,.T.);
#22123=ORIENTED_EDGE('',*,*,#16128,.F.);
#22124=ORIENTED_EDGE('',*,*,#15157,.T.);
#22125=ORIENTED_EDGE('',*,*,#16129,.T.);
#22126=ORIENTED_EDGE('',*,*,#14976,.T.);
#22127=ORIENTED_EDGE('',*,*,#16054,.T.);
#22128=ORIENTED_EDGE('',*,*,#15878,.T.);
#22129=ORIENTED_EDGE('',*,*,#15641,.T.);
#22130=ORIENTED_EDGE('',*,*,#15156,.T.);
#22131=ORIENTED_EDGE('',*,*,#16130,.T.);
#22132=ORIENTED_EDGE('',*,*,#14977,.T.);
#22133=ORIENTED_EDGE('',*,*,#16129,.F.);
#22134=ORIENTED_EDGE('',*,*,#15155,.T.);
#22135=ORIENTED_EDGE('',*,*,#15643,.T.);
#22136=ORIENTED_EDGE('',*,*,#15880,.T.);
#22137=ORIENTED_EDGE('',*,*,#16055,.T.);
#22138=ORIENTED_EDGE('',*,*,#14978,.T.);
#22139=ORIENTED_EDGE('',*,*,#16130,.F.);
#22140=ORIENTED_EDGE('',*,*,#15161,.T.);
#22141=ORIENTED_EDGE('',*,*,#16131,.T.);
#22142=ORIENTED_EDGE('',*,*,#14972,.T.);
#22143=ORIENTED_EDGE('',*,*,#16052,.T.);
#22144=ORIENTED_EDGE('',*,*,#15875,.T.);
#22145=ORIENTED_EDGE('',*,*,#15638,.T.);
#22146=ORIENTED_EDGE('',*,*,#15160,.T.);
#22147=ORIENTED_EDGE('',*,*,#16132,.T.);
#22148=ORIENTED_EDGE('',*,*,#14973,.T.);
#22149=ORIENTED_EDGE('',*,*,#16131,.F.);
#22150=ORIENTED_EDGE('',*,*,#15159,.T.);
#22151=ORIENTED_EDGE('',*,*,#15640,.T.);
#22152=ORIENTED_EDGE('',*,*,#15877,.T.);
#22153=ORIENTED_EDGE('',*,*,#16053,.T.);
#22154=ORIENTED_EDGE('',*,*,#14974,.T.);
#22155=ORIENTED_EDGE('',*,*,#16132,.F.);
#22156=ORIENTED_EDGE('',*,*,#15165,.T.);
#22157=ORIENTED_EDGE('',*,*,#16133,.T.);
#22158=ORIENTED_EDGE('',*,*,#14968,.T.);
#22159=ORIENTED_EDGE('',*,*,#16050,.T.);
#22160=ORIENTED_EDGE('',*,*,#15872,.T.);
#22161=ORIENTED_EDGE('',*,*,#15635,.T.);
#22162=ORIENTED_EDGE('',*,*,#15164,.T.);
#22163=ORIENTED_EDGE('',*,*,#16134,.T.);
#22164=ORIENTED_EDGE('',*,*,#14969,.T.);
#22165=ORIENTED_EDGE('',*,*,#16133,.F.);
#22166=ORIENTED_EDGE('',*,*,#15163,.T.);
#22167=ORIENTED_EDGE('',*,*,#15637,.T.);
#22168=ORIENTED_EDGE('',*,*,#15874,.T.);
#22169=ORIENTED_EDGE('',*,*,#16051,.T.);
#22170=ORIENTED_EDGE('',*,*,#14970,.T.);
#22171=ORIENTED_EDGE('',*,*,#16134,.F.);
#22172=ORIENTED_EDGE('',*,*,#15169,.T.);
#22173=ORIENTED_EDGE('',*,*,#16135,.T.);
#22174=ORIENTED_EDGE('',*,*,#14964,.T.);
#22175=ORIENTED_EDGE('',*,*,#16048,.T.);
#22176=ORIENTED_EDGE('',*,*,#15869,.T.);
#22177=ORIENTED_EDGE('',*,*,#15632,.T.);
#22178=ORIENTED_EDGE('',*,*,#15168,.T.);
#22179=ORIENTED_EDGE('',*,*,#16136,.T.);
#22180=ORIENTED_EDGE('',*,*,#14965,.T.);
#22181=ORIENTED_EDGE('',*,*,#16135,.F.);
#22182=ORIENTED_EDGE('',*,*,#15167,.T.);
#22183=ORIENTED_EDGE('',*,*,#15634,.T.);
#22184=ORIENTED_EDGE('',*,*,#15871,.T.);
#22185=ORIENTED_EDGE('',*,*,#16049,.T.);
#22186=ORIENTED_EDGE('',*,*,#14966,.T.);
#22187=ORIENTED_EDGE('',*,*,#16136,.F.);
#22188=ORIENTED_EDGE('',*,*,#15173,.T.);
#22189=ORIENTED_EDGE('',*,*,#16137,.T.);
#22190=ORIENTED_EDGE('',*,*,#14960,.T.);
#22191=ORIENTED_EDGE('',*,*,#16046,.T.);
#22192=ORIENTED_EDGE('',*,*,#15866,.T.);
#22193=ORIENTED_EDGE('',*,*,#15629,.T.);
#22194=ORIENTED_EDGE('',*,*,#15172,.T.);
#22195=ORIENTED_EDGE('',*,*,#16138,.T.);
#22196=ORIENTED_EDGE('',*,*,#14961,.T.);
#22197=ORIENTED_EDGE('',*,*,#16137,.F.);
#22198=ORIENTED_EDGE('',*,*,#15171,.T.);
#22199=ORIENTED_EDGE('',*,*,#15631,.T.);
#22200=ORIENTED_EDGE('',*,*,#15868,.T.);
#22201=ORIENTED_EDGE('',*,*,#16047,.T.);
#22202=ORIENTED_EDGE('',*,*,#14962,.T.);
#22203=ORIENTED_EDGE('',*,*,#16138,.F.);
#22204=ORIENTED_EDGE('',*,*,#15177,.T.);
#22205=ORIENTED_EDGE('',*,*,#16139,.T.);
#22206=ORIENTED_EDGE('',*,*,#14956,.T.);
#22207=ORIENTED_EDGE('',*,*,#16044,.T.);
#22208=ORIENTED_EDGE('',*,*,#15863,.T.);
#22209=ORIENTED_EDGE('',*,*,#15626,.T.);
#22210=ORIENTED_EDGE('',*,*,#15176,.T.);
#22211=ORIENTED_EDGE('',*,*,#16140,.T.);
#22212=ORIENTED_EDGE('',*,*,#14957,.T.);
#22213=ORIENTED_EDGE('',*,*,#16139,.F.);
#22214=ORIENTED_EDGE('',*,*,#15175,.T.);
#22215=ORIENTED_EDGE('',*,*,#15628,.T.);
#22216=ORIENTED_EDGE('',*,*,#15865,.T.);
#22217=ORIENTED_EDGE('',*,*,#16045,.T.);
#22218=ORIENTED_EDGE('',*,*,#14958,.T.);
#22219=ORIENTED_EDGE('',*,*,#16140,.F.);
#22220=ORIENTED_EDGE('',*,*,#15181,.T.);
#22221=ORIENTED_EDGE('',*,*,#16141,.T.);
#22222=ORIENTED_EDGE('',*,*,#14952,.T.);
#22223=ORIENTED_EDGE('',*,*,#16042,.T.);
#22224=ORIENTED_EDGE('',*,*,#15860,.T.);
#22225=ORIENTED_EDGE('',*,*,#15623,.T.);
#22226=ORIENTED_EDGE('',*,*,#15180,.T.);
#22227=ORIENTED_EDGE('',*,*,#16142,.T.);
#22228=ORIENTED_EDGE('',*,*,#14953,.T.);
#22229=ORIENTED_EDGE('',*,*,#16141,.F.);
#22230=ORIENTED_EDGE('',*,*,#15179,.T.);
#22231=ORIENTED_EDGE('',*,*,#15625,.T.);
#22232=ORIENTED_EDGE('',*,*,#15862,.T.);
#22233=ORIENTED_EDGE('',*,*,#16043,.T.);
#22234=ORIENTED_EDGE('',*,*,#14954,.T.);
#22235=ORIENTED_EDGE('',*,*,#16142,.F.);
#22236=ORIENTED_EDGE('',*,*,#15185,.T.);
#22237=ORIENTED_EDGE('',*,*,#16143,.T.);
#22238=ORIENTED_EDGE('',*,*,#14948,.T.);
#22239=ORIENTED_EDGE('',*,*,#16040,.T.);
#22240=ORIENTED_EDGE('',*,*,#15857,.T.);
#22241=ORIENTED_EDGE('',*,*,#15620,.T.);
#22242=ORIENTED_EDGE('',*,*,#15184,.T.);
#22243=ORIENTED_EDGE('',*,*,#16144,.T.);
#22244=ORIENTED_EDGE('',*,*,#14949,.T.);
#22245=ORIENTED_EDGE('',*,*,#16143,.F.);
#22246=ORIENTED_EDGE('',*,*,#15183,.T.);
#22247=ORIENTED_EDGE('',*,*,#15622,.T.);
#22248=ORIENTED_EDGE('',*,*,#15859,.T.);
#22249=ORIENTED_EDGE('',*,*,#16041,.T.);
#22250=ORIENTED_EDGE('',*,*,#14950,.T.);
#22251=ORIENTED_EDGE('',*,*,#16144,.F.);
#22252=ORIENTED_EDGE('',*,*,#15189,.T.);
#22253=ORIENTED_EDGE('',*,*,#16145,.T.);
#22254=ORIENTED_EDGE('',*,*,#14944,.T.);
#22255=ORIENTED_EDGE('',*,*,#16038,.T.);
#22256=ORIENTED_EDGE('',*,*,#15854,.T.);
#22257=ORIENTED_EDGE('',*,*,#15617,.T.);
#22258=ORIENTED_EDGE('',*,*,#15188,.T.);
#22259=ORIENTED_EDGE('',*,*,#16146,.T.);
#22260=ORIENTED_EDGE('',*,*,#14945,.T.);
#22261=ORIENTED_EDGE('',*,*,#16145,.F.);
#22262=ORIENTED_EDGE('',*,*,#15187,.T.);
#22263=ORIENTED_EDGE('',*,*,#15619,.T.);
#22264=ORIENTED_EDGE('',*,*,#15856,.T.);
#22265=ORIENTED_EDGE('',*,*,#16039,.T.);
#22266=ORIENTED_EDGE('',*,*,#14946,.T.);
#22267=ORIENTED_EDGE('',*,*,#16146,.F.);
#22268=ORIENTED_EDGE('',*,*,#15193,.T.);
#22269=ORIENTED_EDGE('',*,*,#16147,.T.);
#22270=ORIENTED_EDGE('',*,*,#14940,.T.);
#22271=ORIENTED_EDGE('',*,*,#16036,.T.);
#22272=ORIENTED_EDGE('',*,*,#15851,.T.);
#22273=ORIENTED_EDGE('',*,*,#15614,.T.);
#22274=ORIENTED_EDGE('',*,*,#15192,.T.);
#22275=ORIENTED_EDGE('',*,*,#16148,.T.);
#22276=ORIENTED_EDGE('',*,*,#14941,.T.);
#22277=ORIENTED_EDGE('',*,*,#16147,.F.);
#22278=ORIENTED_EDGE('',*,*,#15191,.T.);
#22279=ORIENTED_EDGE('',*,*,#15616,.T.);
#22280=ORIENTED_EDGE('',*,*,#15853,.T.);
#22281=ORIENTED_EDGE('',*,*,#16037,.T.);
#22282=ORIENTED_EDGE('',*,*,#14942,.T.);
#22283=ORIENTED_EDGE('',*,*,#16148,.F.);
#22284=ORIENTED_EDGE('',*,*,#15197,.T.);
#22285=ORIENTED_EDGE('',*,*,#16149,.T.);
#22286=ORIENTED_EDGE('',*,*,#14936,.T.);
#22287=ORIENTED_EDGE('',*,*,#16034,.T.);
#22288=ORIENTED_EDGE('',*,*,#15848,.T.);
#22289=ORIENTED_EDGE('',*,*,#15611,.T.);
#22290=ORIENTED_EDGE('',*,*,#15196,.T.);
#22291=ORIENTED_EDGE('',*,*,#16150,.T.);
#22292=ORIENTED_EDGE('',*,*,#14937,.T.);
#22293=ORIENTED_EDGE('',*,*,#16149,.F.);
#22294=ORIENTED_EDGE('',*,*,#15195,.T.);
#22295=ORIENTED_EDGE('',*,*,#15613,.T.);
#22296=ORIENTED_EDGE('',*,*,#15850,.T.);
#22297=ORIENTED_EDGE('',*,*,#16035,.T.);
#22298=ORIENTED_EDGE('',*,*,#14938,.T.);
#22299=ORIENTED_EDGE('',*,*,#16150,.F.);
#22300=ORIENTED_EDGE('',*,*,#15201,.T.);
#22301=ORIENTED_EDGE('',*,*,#16151,.T.);
#22302=ORIENTED_EDGE('',*,*,#14932,.T.);
#22303=ORIENTED_EDGE('',*,*,#16032,.T.);
#22304=ORIENTED_EDGE('',*,*,#15845,.T.);
#22305=ORIENTED_EDGE('',*,*,#15608,.T.);
#22306=ORIENTED_EDGE('',*,*,#15200,.T.);
#22307=ORIENTED_EDGE('',*,*,#16152,.T.);
#22308=ORIENTED_EDGE('',*,*,#14933,.T.);
#22309=ORIENTED_EDGE('',*,*,#16151,.F.);
#22310=ORIENTED_EDGE('',*,*,#15199,.T.);
#22311=ORIENTED_EDGE('',*,*,#15610,.T.);
#22312=ORIENTED_EDGE('',*,*,#15847,.T.);
#22313=ORIENTED_EDGE('',*,*,#16033,.T.);
#22314=ORIENTED_EDGE('',*,*,#14934,.T.);
#22315=ORIENTED_EDGE('',*,*,#16152,.F.);
#22316=ORIENTED_EDGE('',*,*,#15205,.T.);
#22317=ORIENTED_EDGE('',*,*,#16153,.T.);
#22318=ORIENTED_EDGE('',*,*,#14928,.T.);
#22319=ORIENTED_EDGE('',*,*,#16030,.T.);
#22320=ORIENTED_EDGE('',*,*,#15842,.T.);
#22321=ORIENTED_EDGE('',*,*,#15605,.T.);
#22322=ORIENTED_EDGE('',*,*,#15204,.T.);
#22323=ORIENTED_EDGE('',*,*,#16154,.T.);
#22324=ORIENTED_EDGE('',*,*,#14929,.T.);
#22325=ORIENTED_EDGE('',*,*,#16153,.F.);
#22326=ORIENTED_EDGE('',*,*,#15203,.T.);
#22327=ORIENTED_EDGE('',*,*,#15607,.T.);
#22328=ORIENTED_EDGE('',*,*,#15844,.T.);
#22329=ORIENTED_EDGE('',*,*,#16031,.T.);
#22330=ORIENTED_EDGE('',*,*,#14930,.T.);
#22331=ORIENTED_EDGE('',*,*,#16154,.F.);
#22332=ORIENTED_EDGE('',*,*,#15209,.T.);
#22333=ORIENTED_EDGE('',*,*,#16155,.T.);
#22334=ORIENTED_EDGE('',*,*,#14924,.T.);
#22335=ORIENTED_EDGE('',*,*,#16028,.T.);
#22336=ORIENTED_EDGE('',*,*,#15839,.T.);
#22337=ORIENTED_EDGE('',*,*,#15602,.T.);
#22338=ORIENTED_EDGE('',*,*,#15208,.T.);
#22339=ORIENTED_EDGE('',*,*,#16156,.T.);
#22340=ORIENTED_EDGE('',*,*,#14925,.T.);
#22341=ORIENTED_EDGE('',*,*,#16155,.F.);
#22342=ORIENTED_EDGE('',*,*,#15207,.T.);
#22343=ORIENTED_EDGE('',*,*,#15604,.T.);
#22344=ORIENTED_EDGE('',*,*,#15841,.T.);
#22345=ORIENTED_EDGE('',*,*,#16029,.T.);
#22346=ORIENTED_EDGE('',*,*,#14926,.T.);
#22347=ORIENTED_EDGE('',*,*,#16156,.F.);
#22348=ORIENTED_EDGE('',*,*,#15213,.T.);
#22349=ORIENTED_EDGE('',*,*,#16157,.T.);
#22350=ORIENTED_EDGE('',*,*,#14920,.T.);
#22351=ORIENTED_EDGE('',*,*,#16026,.T.);
#22352=ORIENTED_EDGE('',*,*,#15836,.T.);
#22353=ORIENTED_EDGE('',*,*,#15599,.T.);
#22354=ORIENTED_EDGE('',*,*,#15212,.T.);
#22355=ORIENTED_EDGE('',*,*,#16158,.T.);
#22356=ORIENTED_EDGE('',*,*,#14921,.T.);
#22357=ORIENTED_EDGE('',*,*,#16157,.F.);
#22358=ORIENTED_EDGE('',*,*,#15211,.T.);
#22359=ORIENTED_EDGE('',*,*,#15601,.T.);
#22360=ORIENTED_EDGE('',*,*,#15838,.T.);
#22361=ORIENTED_EDGE('',*,*,#16027,.T.);
#22362=ORIENTED_EDGE('',*,*,#14922,.T.);
#22363=ORIENTED_EDGE('',*,*,#16158,.F.);
#22364=ORIENTED_EDGE('',*,*,#15217,.T.);
#22365=ORIENTED_EDGE('',*,*,#16159,.T.);
#22366=ORIENTED_EDGE('',*,*,#14916,.T.);
#22367=ORIENTED_EDGE('',*,*,#16024,.T.);
#22368=ORIENTED_EDGE('',*,*,#15833,.T.);
#22369=ORIENTED_EDGE('',*,*,#15596,.T.);
#22370=ORIENTED_EDGE('',*,*,#15216,.T.);
#22371=ORIENTED_EDGE('',*,*,#16160,.T.);
#22372=ORIENTED_EDGE('',*,*,#14917,.T.);
#22373=ORIENTED_EDGE('',*,*,#16159,.F.);
#22374=ORIENTED_EDGE('',*,*,#15215,.T.);
#22375=ORIENTED_EDGE('',*,*,#15598,.T.);
#22376=ORIENTED_EDGE('',*,*,#15835,.T.);
#22377=ORIENTED_EDGE('',*,*,#16025,.T.);
#22378=ORIENTED_EDGE('',*,*,#14918,.T.);
#22379=ORIENTED_EDGE('',*,*,#16160,.F.);
#22380=ORIENTED_EDGE('',*,*,#15221,.T.);
#22381=ORIENTED_EDGE('',*,*,#16161,.T.);
#22382=ORIENTED_EDGE('',*,*,#14912,.T.);
#22383=ORIENTED_EDGE('',*,*,#16022,.T.);
#22384=ORIENTED_EDGE('',*,*,#15830,.T.);
#22385=ORIENTED_EDGE('',*,*,#15593,.T.);
#22386=ORIENTED_EDGE('',*,*,#15220,.T.);
#22387=ORIENTED_EDGE('',*,*,#16162,.T.);
#22388=ORIENTED_EDGE('',*,*,#14913,.T.);
#22389=ORIENTED_EDGE('',*,*,#16161,.F.);
#22390=ORIENTED_EDGE('',*,*,#15219,.T.);
#22391=ORIENTED_EDGE('',*,*,#15595,.T.);
#22392=ORIENTED_EDGE('',*,*,#15832,.T.);
#22393=ORIENTED_EDGE('',*,*,#16023,.T.);
#22394=ORIENTED_EDGE('',*,*,#14914,.T.);
#22395=ORIENTED_EDGE('',*,*,#16162,.F.);
#22396=ORIENTED_EDGE('',*,*,#15225,.T.);
#22397=ORIENTED_EDGE('',*,*,#16163,.T.);
#22398=ORIENTED_EDGE('',*,*,#14908,.T.);
#22399=ORIENTED_EDGE('',*,*,#16020,.T.);
#22400=ORIENTED_EDGE('',*,*,#15827,.T.);
#22401=ORIENTED_EDGE('',*,*,#15590,.T.);
#22402=ORIENTED_EDGE('',*,*,#15224,.T.);
#22403=ORIENTED_EDGE('',*,*,#16164,.T.);
#22404=ORIENTED_EDGE('',*,*,#14909,.T.);
#22405=ORIENTED_EDGE('',*,*,#16163,.F.);
#22406=ORIENTED_EDGE('',*,*,#15223,.T.);
#22407=ORIENTED_EDGE('',*,*,#15592,.T.);
#22408=ORIENTED_EDGE('',*,*,#15829,.T.);
#22409=ORIENTED_EDGE('',*,*,#16021,.T.);
#22410=ORIENTED_EDGE('',*,*,#14910,.T.);
#22411=ORIENTED_EDGE('',*,*,#16164,.F.);
#22412=ORIENTED_EDGE('',*,*,#15229,.T.);
#22413=ORIENTED_EDGE('',*,*,#16165,.T.);
#22414=ORIENTED_EDGE('',*,*,#14904,.T.);
#22415=ORIENTED_EDGE('',*,*,#16018,.T.);
#22416=ORIENTED_EDGE('',*,*,#15824,.T.);
#22417=ORIENTED_EDGE('',*,*,#15587,.T.);
#22418=ORIENTED_EDGE('',*,*,#15228,.T.);
#22419=ORIENTED_EDGE('',*,*,#16166,.T.);
#22420=ORIENTED_EDGE('',*,*,#14905,.T.);
#22421=ORIENTED_EDGE('',*,*,#16165,.F.);
#22422=ORIENTED_EDGE('',*,*,#15227,.T.);
#22423=ORIENTED_EDGE('',*,*,#15589,.T.);
#22424=ORIENTED_EDGE('',*,*,#15826,.T.);
#22425=ORIENTED_EDGE('',*,*,#16019,.T.);
#22426=ORIENTED_EDGE('',*,*,#14906,.T.);
#22427=ORIENTED_EDGE('',*,*,#16166,.F.);
#22428=ORIENTED_EDGE('',*,*,#15233,.T.);
#22429=ORIENTED_EDGE('',*,*,#16167,.T.);
#22430=ORIENTED_EDGE('',*,*,#14900,.T.);
#22431=ORIENTED_EDGE('',*,*,#16016,.T.);
#22432=ORIENTED_EDGE('',*,*,#15821,.T.);
#22433=ORIENTED_EDGE('',*,*,#15584,.T.);
#22434=ORIENTED_EDGE('',*,*,#15232,.T.);
#22435=ORIENTED_EDGE('',*,*,#16168,.T.);
#22436=ORIENTED_EDGE('',*,*,#14901,.T.);
#22437=ORIENTED_EDGE('',*,*,#16167,.F.);
#22438=ORIENTED_EDGE('',*,*,#15231,.T.);
#22439=ORIENTED_EDGE('',*,*,#15586,.T.);
#22440=ORIENTED_EDGE('',*,*,#15823,.T.);
#22441=ORIENTED_EDGE('',*,*,#16017,.T.);
#22442=ORIENTED_EDGE('',*,*,#14902,.T.);
#22443=ORIENTED_EDGE('',*,*,#16168,.F.);
#22444=ORIENTED_EDGE('',*,*,#15237,.T.);
#22445=ORIENTED_EDGE('',*,*,#16169,.T.);
#22446=ORIENTED_EDGE('',*,*,#14896,.T.);
#22447=ORIENTED_EDGE('',*,*,#16014,.T.);
#22448=ORIENTED_EDGE('',*,*,#15818,.T.);
#22449=ORIENTED_EDGE('',*,*,#15581,.T.);
#22450=ORIENTED_EDGE('',*,*,#15236,.T.);
#22451=ORIENTED_EDGE('',*,*,#16170,.T.);
#22452=ORIENTED_EDGE('',*,*,#14897,.T.);
#22453=ORIENTED_EDGE('',*,*,#16169,.F.);
#22454=ORIENTED_EDGE('',*,*,#15235,.T.);
#22455=ORIENTED_EDGE('',*,*,#15583,.T.);
#22456=ORIENTED_EDGE('',*,*,#15820,.T.);
#22457=ORIENTED_EDGE('',*,*,#16015,.T.);
#22458=ORIENTED_EDGE('',*,*,#14898,.T.);
#22459=ORIENTED_EDGE('',*,*,#16170,.F.);
#22460=ORIENTED_EDGE('',*,*,#15241,.T.);
#22461=ORIENTED_EDGE('',*,*,#16171,.T.);
#22462=ORIENTED_EDGE('',*,*,#14892,.T.);
#22463=ORIENTED_EDGE('',*,*,#16012,.T.);
#22464=ORIENTED_EDGE('',*,*,#15815,.T.);
#22465=ORIENTED_EDGE('',*,*,#15578,.T.);
#22466=ORIENTED_EDGE('',*,*,#15240,.T.);
#22467=ORIENTED_EDGE('',*,*,#16172,.T.);
#22468=ORIENTED_EDGE('',*,*,#14893,.T.);
#22469=ORIENTED_EDGE('',*,*,#16171,.F.);
#22470=ORIENTED_EDGE('',*,*,#15239,.T.);
#22471=ORIENTED_EDGE('',*,*,#15580,.T.);
#22472=ORIENTED_EDGE('',*,*,#15817,.T.);
#22473=ORIENTED_EDGE('',*,*,#16013,.T.);
#22474=ORIENTED_EDGE('',*,*,#14894,.T.);
#22475=ORIENTED_EDGE('',*,*,#16172,.F.);
#22476=ORIENTED_EDGE('',*,*,#15245,.T.);
#22477=ORIENTED_EDGE('',*,*,#16173,.T.);
#22478=ORIENTED_EDGE('',*,*,#14888,.T.);
#22479=ORIENTED_EDGE('',*,*,#16010,.T.);
#22480=ORIENTED_EDGE('',*,*,#15812,.T.);
#22481=ORIENTED_EDGE('',*,*,#15575,.T.);
#22482=ORIENTED_EDGE('',*,*,#15244,.T.);
#22483=ORIENTED_EDGE('',*,*,#16174,.T.);
#22484=ORIENTED_EDGE('',*,*,#14889,.T.);
#22485=ORIENTED_EDGE('',*,*,#16173,.F.);
#22486=ORIENTED_EDGE('',*,*,#15243,.T.);
#22487=ORIENTED_EDGE('',*,*,#15577,.T.);
#22488=ORIENTED_EDGE('',*,*,#15814,.T.);
#22489=ORIENTED_EDGE('',*,*,#16011,.T.);
#22490=ORIENTED_EDGE('',*,*,#14890,.T.);
#22491=ORIENTED_EDGE('',*,*,#16174,.F.);
#22492=ORIENTED_EDGE('',*,*,#15249,.T.);
#22493=ORIENTED_EDGE('',*,*,#16175,.T.);
#22494=ORIENTED_EDGE('',*,*,#14884,.T.);
#22495=ORIENTED_EDGE('',*,*,#16008,.T.);
#22496=ORIENTED_EDGE('',*,*,#15809,.T.);
#22497=ORIENTED_EDGE('',*,*,#15572,.T.);
#22498=ORIENTED_EDGE('',*,*,#15248,.T.);
#22499=ORIENTED_EDGE('',*,*,#16176,.T.);
#22500=ORIENTED_EDGE('',*,*,#14885,.T.);
#22501=ORIENTED_EDGE('',*,*,#16175,.F.);
#22502=ORIENTED_EDGE('',*,*,#15247,.T.);
#22503=ORIENTED_EDGE('',*,*,#15574,.T.);
#22504=ORIENTED_EDGE('',*,*,#15811,.T.);
#22505=ORIENTED_EDGE('',*,*,#16009,.T.);
#22506=ORIENTED_EDGE('',*,*,#14886,.T.);
#22507=ORIENTED_EDGE('',*,*,#16176,.F.);
#22508=ORIENTED_EDGE('',*,*,#15253,.T.);
#22509=ORIENTED_EDGE('',*,*,#16177,.T.);
#22510=ORIENTED_EDGE('',*,*,#14880,.T.);
#22511=ORIENTED_EDGE('',*,*,#16006,.T.);
#22512=ORIENTED_EDGE('',*,*,#15806,.T.);
#22513=ORIENTED_EDGE('',*,*,#15569,.T.);
#22514=ORIENTED_EDGE('',*,*,#15252,.T.);
#22515=ORIENTED_EDGE('',*,*,#16178,.T.);
#22516=ORIENTED_EDGE('',*,*,#14881,.T.);
#22517=ORIENTED_EDGE('',*,*,#16177,.F.);
#22518=ORIENTED_EDGE('',*,*,#15251,.T.);
#22519=ORIENTED_EDGE('',*,*,#15571,.T.);
#22520=ORIENTED_EDGE('',*,*,#15808,.T.);
#22521=ORIENTED_EDGE('',*,*,#16007,.T.);
#22522=ORIENTED_EDGE('',*,*,#14882,.T.);
#22523=ORIENTED_EDGE('',*,*,#16178,.F.);
#22524=ORIENTED_EDGE('',*,*,#15257,.T.);
#22525=ORIENTED_EDGE('',*,*,#16179,.T.);
#22526=ORIENTED_EDGE('',*,*,#14876,.T.);
#22527=ORIENTED_EDGE('',*,*,#16004,.T.);
#22528=ORIENTED_EDGE('',*,*,#15803,.T.);
#22529=ORIENTED_EDGE('',*,*,#15566,.T.);
#22530=ORIENTED_EDGE('',*,*,#15256,.T.);
#22531=ORIENTED_EDGE('',*,*,#16180,.T.);
#22532=ORIENTED_EDGE('',*,*,#14877,.T.);
#22533=ORIENTED_EDGE('',*,*,#16179,.F.);
#22534=ORIENTED_EDGE('',*,*,#15255,.T.);
#22535=ORIENTED_EDGE('',*,*,#15568,.T.);
#22536=ORIENTED_EDGE('',*,*,#15805,.T.);
#22537=ORIENTED_EDGE('',*,*,#16005,.T.);
#22538=ORIENTED_EDGE('',*,*,#14878,.T.);
#22539=ORIENTED_EDGE('',*,*,#16180,.F.);
#22540=ORIENTED_EDGE('',*,*,#15261,.T.);
#22541=ORIENTED_EDGE('',*,*,#16181,.T.);
#22542=ORIENTED_EDGE('',*,*,#14872,.T.);
#22543=ORIENTED_EDGE('',*,*,#16002,.T.);
#22544=ORIENTED_EDGE('',*,*,#15800,.T.);
#22545=ORIENTED_EDGE('',*,*,#15563,.T.);
#22546=ORIENTED_EDGE('',*,*,#15260,.T.);
#22547=ORIENTED_EDGE('',*,*,#16182,.T.);
#22548=ORIENTED_EDGE('',*,*,#14873,.T.);
#22549=ORIENTED_EDGE('',*,*,#16181,.F.);
#22550=ORIENTED_EDGE('',*,*,#15259,.T.);
#22551=ORIENTED_EDGE('',*,*,#15565,.T.);
#22552=ORIENTED_EDGE('',*,*,#15802,.T.);
#22553=ORIENTED_EDGE('',*,*,#16003,.T.);
#22554=ORIENTED_EDGE('',*,*,#14874,.T.);
#22555=ORIENTED_EDGE('',*,*,#16182,.F.);
#22556=ORIENTED_EDGE('',*,*,#15265,.T.);
#22557=ORIENTED_EDGE('',*,*,#16183,.T.);
#22558=ORIENTED_EDGE('',*,*,#14868,.T.);
#22559=ORIENTED_EDGE('',*,*,#16000,.T.);
#22560=ORIENTED_EDGE('',*,*,#15797,.T.);
#22561=ORIENTED_EDGE('',*,*,#15560,.T.);
#22562=ORIENTED_EDGE('',*,*,#15264,.T.);
#22563=ORIENTED_EDGE('',*,*,#16184,.T.);
#22564=ORIENTED_EDGE('',*,*,#14869,.T.);
#22565=ORIENTED_EDGE('',*,*,#16183,.F.);
#22566=ORIENTED_EDGE('',*,*,#15263,.T.);
#22567=ORIENTED_EDGE('',*,*,#15562,.T.);
#22568=ORIENTED_EDGE('',*,*,#15799,.T.);
#22569=ORIENTED_EDGE('',*,*,#16001,.T.);
#22570=ORIENTED_EDGE('',*,*,#14870,.T.);
#22571=ORIENTED_EDGE('',*,*,#16184,.F.);
#22572=ORIENTED_EDGE('',*,*,#15269,.T.);
#22573=ORIENTED_EDGE('',*,*,#16185,.T.);
#22574=ORIENTED_EDGE('',*,*,#14864,.T.);
#22575=ORIENTED_EDGE('',*,*,#15998,.T.);
#22576=ORIENTED_EDGE('',*,*,#15794,.T.);
#22577=ORIENTED_EDGE('',*,*,#15557,.T.);
#22578=ORIENTED_EDGE('',*,*,#15268,.T.);
#22579=ORIENTED_EDGE('',*,*,#16186,.T.);
#22580=ORIENTED_EDGE('',*,*,#14865,.T.);
#22581=ORIENTED_EDGE('',*,*,#16185,.F.);
#22582=ORIENTED_EDGE('',*,*,#15267,.T.);
#22583=ORIENTED_EDGE('',*,*,#15559,.T.);
#22584=ORIENTED_EDGE('',*,*,#15796,.T.);
#22585=ORIENTED_EDGE('',*,*,#15999,.T.);
#22586=ORIENTED_EDGE('',*,*,#14866,.T.);
#22587=ORIENTED_EDGE('',*,*,#16186,.F.);
#22588=ORIENTED_EDGE('',*,*,#15273,.T.);
#22589=ORIENTED_EDGE('',*,*,#16187,.T.);
#22590=ORIENTED_EDGE('',*,*,#14860,.T.);
#22591=ORIENTED_EDGE('',*,*,#15996,.T.);
#22592=ORIENTED_EDGE('',*,*,#15791,.T.);
#22593=ORIENTED_EDGE('',*,*,#15554,.T.);
#22594=ORIENTED_EDGE('',*,*,#15272,.T.);
#22595=ORIENTED_EDGE('',*,*,#16188,.T.);
#22596=ORIENTED_EDGE('',*,*,#14861,.T.);
#22597=ORIENTED_EDGE('',*,*,#16187,.F.);
#22598=ORIENTED_EDGE('',*,*,#15271,.T.);
#22599=ORIENTED_EDGE('',*,*,#15556,.T.);
#22600=ORIENTED_EDGE('',*,*,#15793,.T.);
#22601=ORIENTED_EDGE('',*,*,#15997,.T.);
#22602=ORIENTED_EDGE('',*,*,#14862,.T.);
#22603=ORIENTED_EDGE('',*,*,#16188,.F.);
#22604=ORIENTED_EDGE('',*,*,#15277,.T.);
#22605=ORIENTED_EDGE('',*,*,#16189,.T.);
#22606=ORIENTED_EDGE('',*,*,#14856,.T.);
#22607=ORIENTED_EDGE('',*,*,#15994,.T.);
#22608=ORIENTED_EDGE('',*,*,#15788,.T.);
#22609=ORIENTED_EDGE('',*,*,#15551,.T.);
#22610=ORIENTED_EDGE('',*,*,#15276,.T.);
#22611=ORIENTED_EDGE('',*,*,#16190,.T.);
#22612=ORIENTED_EDGE('',*,*,#14857,.T.);
#22613=ORIENTED_EDGE('',*,*,#16189,.F.);
#22614=ORIENTED_EDGE('',*,*,#15275,.T.);
#22615=ORIENTED_EDGE('',*,*,#15553,.T.);
#22616=ORIENTED_EDGE('',*,*,#15790,.T.);
#22617=ORIENTED_EDGE('',*,*,#15995,.T.);
#22618=ORIENTED_EDGE('',*,*,#14858,.T.);
#22619=ORIENTED_EDGE('',*,*,#16190,.F.);
#22620=ORIENTED_EDGE('',*,*,#15281,.T.);
#22621=ORIENTED_EDGE('',*,*,#16191,.T.);
#22622=ORIENTED_EDGE('',*,*,#14852,.T.);
#22623=ORIENTED_EDGE('',*,*,#15992,.T.);
#22624=ORIENTED_EDGE('',*,*,#15785,.T.);
#22625=ORIENTED_EDGE('',*,*,#15548,.T.);
#22626=ORIENTED_EDGE('',*,*,#15280,.T.);
#22627=ORIENTED_EDGE('',*,*,#16192,.T.);
#22628=ORIENTED_EDGE('',*,*,#14853,.T.);
#22629=ORIENTED_EDGE('',*,*,#16191,.F.);
#22630=ORIENTED_EDGE('',*,*,#15279,.T.);
#22631=ORIENTED_EDGE('',*,*,#15550,.T.);
#22632=ORIENTED_EDGE('',*,*,#15787,.T.);
#22633=ORIENTED_EDGE('',*,*,#15993,.T.);
#22634=ORIENTED_EDGE('',*,*,#14854,.T.);
#22635=ORIENTED_EDGE('',*,*,#16192,.F.);
#22636=ORIENTED_EDGE('',*,*,#15285,.T.);
#22637=ORIENTED_EDGE('',*,*,#16193,.T.);
#22638=ORIENTED_EDGE('',*,*,#14848,.T.);
#22639=ORIENTED_EDGE('',*,*,#15990,.T.);
#22640=ORIENTED_EDGE('',*,*,#15782,.T.);
#22641=ORIENTED_EDGE('',*,*,#15545,.T.);
#22642=ORIENTED_EDGE('',*,*,#15284,.T.);
#22643=ORIENTED_EDGE('',*,*,#16194,.T.);
#22644=ORIENTED_EDGE('',*,*,#14849,.T.);
#22645=ORIENTED_EDGE('',*,*,#16193,.F.);
#22646=ORIENTED_EDGE('',*,*,#15283,.T.);
#22647=ORIENTED_EDGE('',*,*,#15547,.T.);
#22648=ORIENTED_EDGE('',*,*,#15784,.T.);
#22649=ORIENTED_EDGE('',*,*,#15991,.T.);
#22650=ORIENTED_EDGE('',*,*,#14850,.T.);
#22651=ORIENTED_EDGE('',*,*,#16194,.F.);
#22652=ORIENTED_EDGE('',*,*,#15289,.T.);
#22653=ORIENTED_EDGE('',*,*,#16195,.T.);
#22654=ORIENTED_EDGE('',*,*,#14844,.T.);
#22655=ORIENTED_EDGE('',*,*,#15988,.T.);
#22656=ORIENTED_EDGE('',*,*,#15779,.T.);
#22657=ORIENTED_EDGE('',*,*,#15542,.T.);
#22658=ORIENTED_EDGE('',*,*,#15288,.T.);
#22659=ORIENTED_EDGE('',*,*,#16196,.T.);
#22660=ORIENTED_EDGE('',*,*,#14845,.T.);
#22661=ORIENTED_EDGE('',*,*,#16195,.F.);
#22662=ORIENTED_EDGE('',*,*,#15287,.T.);
#22663=ORIENTED_EDGE('',*,*,#15544,.T.);
#22664=ORIENTED_EDGE('',*,*,#15781,.T.);
#22665=ORIENTED_EDGE('',*,*,#15989,.T.);
#22666=ORIENTED_EDGE('',*,*,#14846,.T.);
#22667=ORIENTED_EDGE('',*,*,#16196,.F.);
#22668=ORIENTED_EDGE('',*,*,#15293,.T.);
#22669=ORIENTED_EDGE('',*,*,#16197,.T.);
#22670=ORIENTED_EDGE('',*,*,#14840,.T.);
#22671=ORIENTED_EDGE('',*,*,#15986,.T.);
#22672=ORIENTED_EDGE('',*,*,#15776,.T.);
#22673=ORIENTED_EDGE('',*,*,#15539,.T.);
#22674=ORIENTED_EDGE('',*,*,#15292,.T.);
#22675=ORIENTED_EDGE('',*,*,#16198,.T.);
#22676=ORIENTED_EDGE('',*,*,#14841,.T.);
#22677=ORIENTED_EDGE('',*,*,#16197,.F.);
#22678=ORIENTED_EDGE('',*,*,#15291,.T.);
#22679=ORIENTED_EDGE('',*,*,#15541,.T.);
#22680=ORIENTED_EDGE('',*,*,#15778,.T.);
#22681=ORIENTED_EDGE('',*,*,#15987,.T.);
#22682=ORIENTED_EDGE('',*,*,#14842,.T.);
#22683=ORIENTED_EDGE('',*,*,#16198,.F.);
#22684=ORIENTED_EDGE('',*,*,#15297,.T.);
#22685=ORIENTED_EDGE('',*,*,#16199,.T.);
#22686=ORIENTED_EDGE('',*,*,#14836,.T.);
#22687=ORIENTED_EDGE('',*,*,#15984,.T.);
#22688=ORIENTED_EDGE('',*,*,#15773,.T.);
#22689=ORIENTED_EDGE('',*,*,#15536,.T.);
#22690=ORIENTED_EDGE('',*,*,#15296,.T.);
#22691=ORIENTED_EDGE('',*,*,#16200,.T.);
#22692=ORIENTED_EDGE('',*,*,#14837,.T.);
#22693=ORIENTED_EDGE('',*,*,#16199,.F.);
#22694=ORIENTED_EDGE('',*,*,#15295,.T.);
#22695=ORIENTED_EDGE('',*,*,#15538,.T.);
#22696=ORIENTED_EDGE('',*,*,#15775,.T.);
#22697=ORIENTED_EDGE('',*,*,#15985,.T.);
#22698=ORIENTED_EDGE('',*,*,#14838,.T.);
#22699=ORIENTED_EDGE('',*,*,#16200,.F.);
#22700=ORIENTED_EDGE('',*,*,#15301,.T.);
#22701=ORIENTED_EDGE('',*,*,#16201,.T.);
#22702=ORIENTED_EDGE('',*,*,#15137,.T.);
#22703=ORIENTED_EDGE('',*,*,#15982,.T.);
#22704=ORIENTED_EDGE('',*,*,#15770,.T.);
#22705=ORIENTED_EDGE('',*,*,#15533,.T.);
#22706=ORIENTED_EDGE('',*,*,#15300,.T.);
#22707=ORIENTED_EDGE('',*,*,#16202,.T.);
#22708=ORIENTED_EDGE('',*,*,#14833,.T.);
#22709=ORIENTED_EDGE('',*,*,#15138,.T.);
#22710=ORIENTED_EDGE('',*,*,#16201,.F.);
#22711=ORIENTED_EDGE('',*,*,#15299,.T.);
#22712=ORIENTED_EDGE('',*,*,#15535,.T.);
#22713=ORIENTED_EDGE('',*,*,#15772,.T.);
#22714=ORIENTED_EDGE('',*,*,#15983,.T.);
#22715=ORIENTED_EDGE('',*,*,#14834,.T.);
#22716=ORIENTED_EDGE('',*,*,#16202,.F.);
#22717=ORIENTED_EDGE('',*,*,#15305,.T.);
#22718=ORIENTED_EDGE('',*,*,#16203,.T.);
#22719=ORIENTED_EDGE('',*,*,#15133,.T.);
#22720=ORIENTED_EDGE('',*,*,#15980,.T.);
#22721=ORIENTED_EDGE('',*,*,#15767,.T.);
#22722=ORIENTED_EDGE('',*,*,#15530,.T.);
#22723=ORIENTED_EDGE('',*,*,#15304,.T.);
#22724=ORIENTED_EDGE('',*,*,#16204,.T.);
#22725=ORIENTED_EDGE('',*,*,#15134,.T.);
#22726=ORIENTED_EDGE('',*,*,#16203,.F.);
#22727=ORIENTED_EDGE('',*,*,#15303,.T.);
#22728=ORIENTED_EDGE('',*,*,#15532,.T.);
#22729=ORIENTED_EDGE('',*,*,#15769,.T.);
#22730=ORIENTED_EDGE('',*,*,#15981,.T.);
#22731=ORIENTED_EDGE('',*,*,#15135,.T.);
#22732=ORIENTED_EDGE('',*,*,#16204,.F.);
#22733=ORIENTED_EDGE('',*,*,#15309,.T.);
#22734=ORIENTED_EDGE('',*,*,#16205,.T.);
#22735=ORIENTED_EDGE('',*,*,#15129,.T.);
#22736=ORIENTED_EDGE('',*,*,#15978,.T.);
#22737=ORIENTED_EDGE('',*,*,#15764,.T.);
#22738=ORIENTED_EDGE('',*,*,#15527,.T.);
#22739=ORIENTED_EDGE('',*,*,#15308,.T.);
#22740=ORIENTED_EDGE('',*,*,#16206,.T.);
#22741=ORIENTED_EDGE('',*,*,#15130,.T.);
#22742=ORIENTED_EDGE('',*,*,#16205,.F.);
#22743=ORIENTED_EDGE('',*,*,#15307,.T.);
#22744=ORIENTED_EDGE('',*,*,#15529,.T.);
#22745=ORIENTED_EDGE('',*,*,#15766,.T.);
#22746=ORIENTED_EDGE('',*,*,#15979,.T.);
#22747=ORIENTED_EDGE('',*,*,#15131,.T.);
#22748=ORIENTED_EDGE('',*,*,#16206,.F.);
#22749=ORIENTED_EDGE('',*,*,#15313,.T.);
#22750=ORIENTED_EDGE('',*,*,#16207,.T.);
#22751=ORIENTED_EDGE('',*,*,#15125,.T.);
#22752=ORIENTED_EDGE('',*,*,#15976,.T.);
#22753=ORIENTED_EDGE('',*,*,#15761,.T.);
#22754=ORIENTED_EDGE('',*,*,#15524,.T.);
#22755=ORIENTED_EDGE('',*,*,#15312,.T.);
#22756=ORIENTED_EDGE('',*,*,#16208,.T.);
#22757=ORIENTED_EDGE('',*,*,#15126,.T.);
#22758=ORIENTED_EDGE('',*,*,#16207,.F.);
#22759=ORIENTED_EDGE('',*,*,#15311,.T.);
#22760=ORIENTED_EDGE('',*,*,#15526,.T.);
#22761=ORIENTED_EDGE('',*,*,#15763,.T.);
#22762=ORIENTED_EDGE('',*,*,#15977,.T.);
#22763=ORIENTED_EDGE('',*,*,#15127,.T.);
#22764=ORIENTED_EDGE('',*,*,#16208,.F.);
#22765=ORIENTED_EDGE('',*,*,#15317,.T.);
#22766=ORIENTED_EDGE('',*,*,#16209,.T.);
#22767=ORIENTED_EDGE('',*,*,#15121,.T.);
#22768=ORIENTED_EDGE('',*,*,#15974,.T.);
#22769=ORIENTED_EDGE('',*,*,#15758,.T.);
#22770=ORIENTED_EDGE('',*,*,#15521,.T.);
#22771=ORIENTED_EDGE('',*,*,#15316,.T.);
#22772=ORIENTED_EDGE('',*,*,#16210,.T.);
#22773=ORIENTED_EDGE('',*,*,#15122,.T.);
#22774=ORIENTED_EDGE('',*,*,#16209,.F.);
#22775=ORIENTED_EDGE('',*,*,#15315,.T.);
#22776=ORIENTED_EDGE('',*,*,#15523,.T.);
#22777=ORIENTED_EDGE('',*,*,#15760,.T.);
#22778=ORIENTED_EDGE('',*,*,#15975,.T.);
#22779=ORIENTED_EDGE('',*,*,#15123,.T.);
#22780=ORIENTED_EDGE('',*,*,#16210,.F.);
#22781=ORIENTED_EDGE('',*,*,#15321,.T.);
#22782=ORIENTED_EDGE('',*,*,#16211,.T.);
#22783=ORIENTED_EDGE('',*,*,#15117,.T.);
#22784=ORIENTED_EDGE('',*,*,#15972,.T.);
#22785=ORIENTED_EDGE('',*,*,#15755,.T.);
#22786=ORIENTED_EDGE('',*,*,#15518,.T.);
#22787=ORIENTED_EDGE('',*,*,#15320,.T.);
#22788=ORIENTED_EDGE('',*,*,#16212,.T.);
#22789=ORIENTED_EDGE('',*,*,#15118,.T.);
#22790=ORIENTED_EDGE('',*,*,#16211,.F.);
#22791=ORIENTED_EDGE('',*,*,#15319,.T.);
#22792=ORIENTED_EDGE('',*,*,#15520,.T.);
#22793=ORIENTED_EDGE('',*,*,#15757,.T.);
#22794=ORIENTED_EDGE('',*,*,#15973,.T.);
#22795=ORIENTED_EDGE('',*,*,#15119,.T.);
#22796=ORIENTED_EDGE('',*,*,#16212,.F.);
#22797=ORIENTED_EDGE('',*,*,#15325,.T.);
#22798=ORIENTED_EDGE('',*,*,#16213,.T.);
#22799=ORIENTED_EDGE('',*,*,#15113,.T.);
#22800=ORIENTED_EDGE('',*,*,#15970,.T.);
#22801=ORIENTED_EDGE('',*,*,#15752,.T.);
#22802=ORIENTED_EDGE('',*,*,#15515,.T.);
#22803=ORIENTED_EDGE('',*,*,#15324,.T.);
#22804=ORIENTED_EDGE('',*,*,#16214,.T.);
#22805=ORIENTED_EDGE('',*,*,#15114,.T.);
#22806=ORIENTED_EDGE('',*,*,#16213,.F.);
#22807=ORIENTED_EDGE('',*,*,#15323,.T.);
#22808=ORIENTED_EDGE('',*,*,#15517,.T.);
#22809=ORIENTED_EDGE('',*,*,#15754,.T.);
#22810=ORIENTED_EDGE('',*,*,#15971,.T.);
#22811=ORIENTED_EDGE('',*,*,#15115,.T.);
#22812=ORIENTED_EDGE('',*,*,#16214,.F.);
#22813=ORIENTED_EDGE('',*,*,#15329,.T.);
#22814=ORIENTED_EDGE('',*,*,#16215,.T.);
#22815=ORIENTED_EDGE('',*,*,#15109,.T.);
#22816=ORIENTED_EDGE('',*,*,#15968,.T.);
#22817=ORIENTED_EDGE('',*,*,#15749,.T.);
#22818=ORIENTED_EDGE('',*,*,#15512,.T.);
#22819=ORIENTED_EDGE('',*,*,#15328,.T.);
#22820=ORIENTED_EDGE('',*,*,#16216,.T.);
#22821=ORIENTED_EDGE('',*,*,#15110,.T.);
#22822=ORIENTED_EDGE('',*,*,#16215,.F.);
#22823=ORIENTED_EDGE('',*,*,#15327,.T.);
#22824=ORIENTED_EDGE('',*,*,#15514,.T.);
#22825=ORIENTED_EDGE('',*,*,#15751,.T.);
#22826=ORIENTED_EDGE('',*,*,#15969,.T.);
#22827=ORIENTED_EDGE('',*,*,#15111,.T.);
#22828=ORIENTED_EDGE('',*,*,#16216,.F.);
#22829=ORIENTED_EDGE('',*,*,#15333,.T.);
#22830=ORIENTED_EDGE('',*,*,#16217,.T.);
#22831=ORIENTED_EDGE('',*,*,#15105,.T.);
#22832=ORIENTED_EDGE('',*,*,#15966,.T.);
#22833=ORIENTED_EDGE('',*,*,#15746,.T.);
#22834=ORIENTED_EDGE('',*,*,#15509,.T.);
#22835=ORIENTED_EDGE('',*,*,#15332,.T.);
#22836=ORIENTED_EDGE('',*,*,#16218,.T.);
#22837=ORIENTED_EDGE('',*,*,#15106,.T.);
#22838=ORIENTED_EDGE('',*,*,#16217,.F.);
#22839=ORIENTED_EDGE('',*,*,#15331,.T.);
#22840=ORIENTED_EDGE('',*,*,#15511,.T.);
#22841=ORIENTED_EDGE('',*,*,#15748,.T.);
#22842=ORIENTED_EDGE('',*,*,#15967,.T.);
#22843=ORIENTED_EDGE('',*,*,#15107,.T.);
#22844=ORIENTED_EDGE('',*,*,#16218,.F.);
#22845=ORIENTED_EDGE('',*,*,#15337,.T.);
#22846=ORIENTED_EDGE('',*,*,#16219,.T.);
#22847=ORIENTED_EDGE('',*,*,#15101,.T.);
#22848=ORIENTED_EDGE('',*,*,#15964,.T.);
#22849=ORIENTED_EDGE('',*,*,#15743,.T.);
#22850=ORIENTED_EDGE('',*,*,#15506,.T.);
#22851=ORIENTED_EDGE('',*,*,#15336,.T.);
#22852=ORIENTED_EDGE('',*,*,#16220,.T.);
#22853=ORIENTED_EDGE('',*,*,#15102,.T.);
#22854=ORIENTED_EDGE('',*,*,#16219,.F.);
#22855=ORIENTED_EDGE('',*,*,#15335,.T.);
#22856=ORIENTED_EDGE('',*,*,#15508,.T.);
#22857=ORIENTED_EDGE('',*,*,#15745,.T.);
#22858=ORIENTED_EDGE('',*,*,#15965,.T.);
#22859=ORIENTED_EDGE('',*,*,#15103,.T.);
#22860=ORIENTED_EDGE('',*,*,#16220,.F.);
#22861=ORIENTED_EDGE('',*,*,#15341,.T.);
#22862=ORIENTED_EDGE('',*,*,#16221,.T.);
#22863=ORIENTED_EDGE('',*,*,#15097,.T.);
#22864=ORIENTED_EDGE('',*,*,#15962,.T.);
#22865=ORIENTED_EDGE('',*,*,#15740,.T.);
#22866=ORIENTED_EDGE('',*,*,#15503,.T.);
#22867=ORIENTED_EDGE('',*,*,#15340,.T.);
#22868=ORIENTED_EDGE('',*,*,#16222,.T.);
#22869=ORIENTED_EDGE('',*,*,#15098,.T.);
#22870=ORIENTED_EDGE('',*,*,#16221,.F.);
#22871=ORIENTED_EDGE('',*,*,#15339,.T.);
#22872=ORIENTED_EDGE('',*,*,#15505,.T.);
#22873=ORIENTED_EDGE('',*,*,#15742,.T.);
#22874=ORIENTED_EDGE('',*,*,#15963,.T.);
#22875=ORIENTED_EDGE('',*,*,#15099,.T.);
#22876=ORIENTED_EDGE('',*,*,#16222,.F.);
#22877=ORIENTED_EDGE('',*,*,#15345,.T.);
#22878=ORIENTED_EDGE('',*,*,#16223,.T.);
#22879=ORIENTED_EDGE('',*,*,#15093,.T.);
#22880=ORIENTED_EDGE('',*,*,#15960,.T.);
#22881=ORIENTED_EDGE('',*,*,#15737,.T.);
#22882=ORIENTED_EDGE('',*,*,#15500,.T.);
#22883=ORIENTED_EDGE('',*,*,#15344,.T.);
#22884=ORIENTED_EDGE('',*,*,#16224,.T.);
#22885=ORIENTED_EDGE('',*,*,#15094,.T.);
#22886=ORIENTED_EDGE('',*,*,#16223,.F.);
#22887=ORIENTED_EDGE('',*,*,#15343,.T.);
#22888=ORIENTED_EDGE('',*,*,#15502,.T.);
#22889=ORIENTED_EDGE('',*,*,#15739,.T.);
#22890=ORIENTED_EDGE('',*,*,#15961,.T.);
#22891=ORIENTED_EDGE('',*,*,#15095,.T.);
#22892=ORIENTED_EDGE('',*,*,#16224,.F.);
#22893=ORIENTED_EDGE('',*,*,#15349,.T.);
#22894=ORIENTED_EDGE('',*,*,#16225,.T.);
#22895=ORIENTED_EDGE('',*,*,#15089,.T.);
#22896=ORIENTED_EDGE('',*,*,#15958,.T.);
#22897=ORIENTED_EDGE('',*,*,#15734,.T.);
#22898=ORIENTED_EDGE('',*,*,#15497,.T.);
#22899=ORIENTED_EDGE('',*,*,#15348,.T.);
#22900=ORIENTED_EDGE('',*,*,#16226,.T.);
#22901=ORIENTED_EDGE('',*,*,#15090,.T.);
#22902=ORIENTED_EDGE('',*,*,#16225,.F.);
#22903=ORIENTED_EDGE('',*,*,#15347,.T.);
#22904=ORIENTED_EDGE('',*,*,#15499,.T.);
#22905=ORIENTED_EDGE('',*,*,#15736,.T.);
#22906=ORIENTED_EDGE('',*,*,#15959,.T.);
#22907=ORIENTED_EDGE('',*,*,#15091,.T.);
#22908=ORIENTED_EDGE('',*,*,#16226,.F.);
#22909=ORIENTED_EDGE('',*,*,#15353,.T.);
#22910=ORIENTED_EDGE('',*,*,#16227,.T.);
#22911=ORIENTED_EDGE('',*,*,#15085,.T.);
#22912=ORIENTED_EDGE('',*,*,#15956,.T.);
#22913=ORIENTED_EDGE('',*,*,#15731,.T.);
#22914=ORIENTED_EDGE('',*,*,#15494,.T.);
#22915=ORIENTED_EDGE('',*,*,#15352,.T.);
#22916=ORIENTED_EDGE('',*,*,#16228,.T.);
#22917=ORIENTED_EDGE('',*,*,#15086,.T.);
#22918=ORIENTED_EDGE('',*,*,#16227,.F.);
#22919=ORIENTED_EDGE('',*,*,#15351,.T.);
#22920=ORIENTED_EDGE('',*,*,#15496,.T.);
#22921=ORIENTED_EDGE('',*,*,#15733,.T.);
#22922=ORIENTED_EDGE('',*,*,#15957,.T.);
#22923=ORIENTED_EDGE('',*,*,#15087,.T.);
#22924=ORIENTED_EDGE('',*,*,#16228,.F.);
#22925=ORIENTED_EDGE('',*,*,#15357,.T.);
#22926=ORIENTED_EDGE('',*,*,#16229,.T.);
#22927=ORIENTED_EDGE('',*,*,#15081,.T.);
#22928=ORIENTED_EDGE('',*,*,#15954,.T.);
#22929=ORIENTED_EDGE('',*,*,#15728,.T.);
#22930=ORIENTED_EDGE('',*,*,#15491,.T.);
#22931=ORIENTED_EDGE('',*,*,#15356,.T.);
#22932=ORIENTED_EDGE('',*,*,#16230,.T.);
#22933=ORIENTED_EDGE('',*,*,#15082,.T.);
#22934=ORIENTED_EDGE('',*,*,#16229,.F.);
#22935=ORIENTED_EDGE('',*,*,#15355,.T.);
#22936=ORIENTED_EDGE('',*,*,#15493,.T.);
#22937=ORIENTED_EDGE('',*,*,#15730,.T.);
#22938=ORIENTED_EDGE('',*,*,#15955,.T.);
#22939=ORIENTED_EDGE('',*,*,#15083,.T.);
#22940=ORIENTED_EDGE('',*,*,#16230,.F.);
#22941=ORIENTED_EDGE('',*,*,#15361,.T.);
#22942=ORIENTED_EDGE('',*,*,#16231,.T.);
#22943=ORIENTED_EDGE('',*,*,#15077,.T.);
#22944=ORIENTED_EDGE('',*,*,#15952,.T.);
#22945=ORIENTED_EDGE('',*,*,#15725,.T.);
#22946=ORIENTED_EDGE('',*,*,#15488,.T.);
#22947=ORIENTED_EDGE('',*,*,#15360,.T.);
#22948=ORIENTED_EDGE('',*,*,#16232,.T.);
#22949=ORIENTED_EDGE('',*,*,#15078,.T.);
#22950=ORIENTED_EDGE('',*,*,#16231,.F.);
#22951=ORIENTED_EDGE('',*,*,#15359,.T.);
#22952=ORIENTED_EDGE('',*,*,#15490,.T.);
#22953=ORIENTED_EDGE('',*,*,#15727,.T.);
#22954=ORIENTED_EDGE('',*,*,#15953,.T.);
#22955=ORIENTED_EDGE('',*,*,#15079,.T.);
#22956=ORIENTED_EDGE('',*,*,#16232,.F.);
#22957=ORIENTED_EDGE('',*,*,#15365,.T.);
#22958=ORIENTED_EDGE('',*,*,#16233,.T.);
#22959=ORIENTED_EDGE('',*,*,#15073,.T.);
#22960=ORIENTED_EDGE('',*,*,#15950,.T.);
#22961=ORIENTED_EDGE('',*,*,#15722,.T.);
#22962=ORIENTED_EDGE('',*,*,#15485,.T.);
#22963=ORIENTED_EDGE('',*,*,#15364,.T.);
#22964=ORIENTED_EDGE('',*,*,#16234,.T.);
#22965=ORIENTED_EDGE('',*,*,#15074,.T.);
#22966=ORIENTED_EDGE('',*,*,#16233,.F.);
#22967=ORIENTED_EDGE('',*,*,#15363,.T.);
#22968=ORIENTED_EDGE('',*,*,#15487,.T.);
#22969=ORIENTED_EDGE('',*,*,#15724,.T.);
#22970=ORIENTED_EDGE('',*,*,#15951,.T.);
#22971=ORIENTED_EDGE('',*,*,#15075,.T.);
#22972=ORIENTED_EDGE('',*,*,#16234,.F.);
#22973=ORIENTED_EDGE('',*,*,#15369,.T.);
#22974=ORIENTED_EDGE('',*,*,#16235,.T.);
#22975=ORIENTED_EDGE('',*,*,#15069,.T.);
#22976=ORIENTED_EDGE('',*,*,#15948,.T.);
#22977=ORIENTED_EDGE('',*,*,#15719,.T.);
#22978=ORIENTED_EDGE('',*,*,#15482,.T.);
#22979=ORIENTED_EDGE('',*,*,#15368,.T.);
#22980=ORIENTED_EDGE('',*,*,#16236,.T.);
#22981=ORIENTED_EDGE('',*,*,#15070,.T.);
#22982=ORIENTED_EDGE('',*,*,#16235,.F.);
#22983=ORIENTED_EDGE('',*,*,#15367,.T.);
#22984=ORIENTED_EDGE('',*,*,#15484,.T.);
#22985=ORIENTED_EDGE('',*,*,#15721,.T.);
#22986=ORIENTED_EDGE('',*,*,#15949,.T.);
#22987=ORIENTED_EDGE('',*,*,#15071,.T.);
#22988=ORIENTED_EDGE('',*,*,#16236,.F.);
#22989=ORIENTED_EDGE('',*,*,#15373,.T.);
#22990=ORIENTED_EDGE('',*,*,#16237,.T.);
#22991=ORIENTED_EDGE('',*,*,#15065,.T.);
#22992=ORIENTED_EDGE('',*,*,#15946,.T.);
#22993=ORIENTED_EDGE('',*,*,#15716,.T.);
#22994=ORIENTED_EDGE('',*,*,#15479,.T.);
#22995=ORIENTED_EDGE('',*,*,#15372,.T.);
#22996=ORIENTED_EDGE('',*,*,#16238,.T.);
#22997=ORIENTED_EDGE('',*,*,#15066,.T.);
#22998=ORIENTED_EDGE('',*,*,#16237,.F.);
#22999=ORIENTED_EDGE('',*,*,#15371,.T.);
#23000=ORIENTED_EDGE('',*,*,#15481,.T.);
#23001=ORIENTED_EDGE('',*,*,#15718,.T.);
#23002=ORIENTED_EDGE('',*,*,#15947,.T.);
#23003=ORIENTED_EDGE('',*,*,#15067,.T.);
#23004=ORIENTED_EDGE('',*,*,#16238,.F.);
#23005=ORIENTED_EDGE('',*,*,#15377,.T.);
#23006=ORIENTED_EDGE('',*,*,#16239,.T.);
#23007=ORIENTED_EDGE('',*,*,#15061,.T.);
#23008=ORIENTED_EDGE('',*,*,#15944,.T.);
#23009=ORIENTED_EDGE('',*,*,#15713,.T.);
#23010=ORIENTED_EDGE('',*,*,#15476,.T.);
#23011=ORIENTED_EDGE('',*,*,#15376,.T.);
#23012=ORIENTED_EDGE('',*,*,#16240,.T.);
#23013=ORIENTED_EDGE('',*,*,#15062,.T.);
#23014=ORIENTED_EDGE('',*,*,#16239,.F.);
#23015=ORIENTED_EDGE('',*,*,#15375,.T.);
#23016=ORIENTED_EDGE('',*,*,#15478,.T.);
#23017=ORIENTED_EDGE('',*,*,#15715,.T.);
#23018=ORIENTED_EDGE('',*,*,#15945,.T.);
#23019=ORIENTED_EDGE('',*,*,#15063,.T.);
#23020=ORIENTED_EDGE('',*,*,#16240,.F.);
#23021=ORIENTED_EDGE('',*,*,#15380,.T.);
#23022=ORIENTED_EDGE('',*,*,#14784,.T.);
#23023=ORIENTED_EDGE('',*,*,#15058,.T.);
#23024=ORIENTED_EDGE('',*,*,#15942,.T.);
#23025=ORIENTED_EDGE('',*,*,#15710,.T.);
#23026=ORIENTED_EDGE('',*,*,#15473,.T.);
#23027=ORIENTED_EDGE('',*,*,#15379,.T.);
#23028=ORIENTED_EDGE('',*,*,#15475,.T.);
#23029=ORIENTED_EDGE('',*,*,#15712,.T.);
#23030=ORIENTED_EDGE('',*,*,#15943,.T.);
#23031=ORIENTED_EDGE('',*,*,#15059,.T.);
#23032=ORIENTED_EDGE('',*,*,#14782,.F.);
#23033=ORIENTED_EDGE('',*,*,#15383,.T.);
#23034=ORIENTED_EDGE('',*,*,#14780,.T.);
#23035=ORIENTED_EDGE('',*,*,#15055,.T.);
#23036=ORIENTED_EDGE('',*,*,#15940,.T.);
#23037=ORIENTED_EDGE('',*,*,#15707,.T.);
#23038=ORIENTED_EDGE('',*,*,#15470,.T.);
#23039=ORIENTED_EDGE('',*,*,#15382,.T.);
#23040=ORIENTED_EDGE('',*,*,#15472,.T.);
#23041=ORIENTED_EDGE('',*,*,#15709,.T.);
#23042=ORIENTED_EDGE('',*,*,#15941,.T.);
#23043=ORIENTED_EDGE('',*,*,#15056,.T.);
#23044=ORIENTED_EDGE('',*,*,#14778,.F.);
#23045=ORIENTED_EDGE('',*,*,#15386,.T.);
#23046=ORIENTED_EDGE('',*,*,#14776,.T.);
#23047=ORIENTED_EDGE('',*,*,#15052,.T.);
#23048=ORIENTED_EDGE('',*,*,#15938,.T.);
#23049=ORIENTED_EDGE('',*,*,#15704,.T.);
#23050=ORIENTED_EDGE('',*,*,#15467,.T.);
#23051=ORIENTED_EDGE('',*,*,#15385,.T.);
#23052=ORIENTED_EDGE('',*,*,#15469,.T.);
#23053=ORIENTED_EDGE('',*,*,#15706,.T.);
#23054=ORIENTED_EDGE('',*,*,#15939,.T.);
#23055=ORIENTED_EDGE('',*,*,#15053,.T.);
#23056=ORIENTED_EDGE('',*,*,#14774,.F.);
#23057=ORIENTED_EDGE('',*,*,#15389,.T.);
#23058=ORIENTED_EDGE('',*,*,#14772,.T.);
#23059=ORIENTED_EDGE('',*,*,#15049,.T.);
#23060=ORIENTED_EDGE('',*,*,#15936,.T.);
#23061=ORIENTED_EDGE('',*,*,#15701,.T.);
#23062=ORIENTED_EDGE('',*,*,#15464,.T.);
#23063=ORIENTED_EDGE('',*,*,#15388,.T.);
#23064=ORIENTED_EDGE('',*,*,#15466,.T.);
#23065=ORIENTED_EDGE('',*,*,#15703,.T.);
#23066=ORIENTED_EDGE('',*,*,#15937,.T.);
#23067=ORIENTED_EDGE('',*,*,#15050,.T.);
#23068=ORIENTED_EDGE('',*,*,#14770,.F.);
#23069=ORIENTED_EDGE('',*,*,#15392,.T.);
#23070=ORIENTED_EDGE('',*,*,#14768,.T.);
#23071=ORIENTED_EDGE('',*,*,#15046,.T.);
#23072=ORIENTED_EDGE('',*,*,#15934,.T.);
#23073=ORIENTED_EDGE('',*,*,#15698,.T.);
#23074=ORIENTED_EDGE('',*,*,#15461,.T.);
#23075=ORIENTED_EDGE('',*,*,#15391,.T.);
#23076=ORIENTED_EDGE('',*,*,#15463,.T.);
#23077=ORIENTED_EDGE('',*,*,#15700,.T.);
#23078=ORIENTED_EDGE('',*,*,#15935,.T.);
#23079=ORIENTED_EDGE('',*,*,#15047,.T.);
#23080=ORIENTED_EDGE('',*,*,#14766,.F.);
#23081=ORIENTED_EDGE('',*,*,#15395,.T.);
#23082=ORIENTED_EDGE('',*,*,#14764,.T.);
#23083=ORIENTED_EDGE('',*,*,#15043,.T.);
#23084=ORIENTED_EDGE('',*,*,#15931,.T.);
#23085=ORIENTED_EDGE('',*,*,#15694,.T.);
#23086=ORIENTED_EDGE('',*,*,#15457,.T.);
#23087=ORIENTED_EDGE('',*,*,#15394,.T.);
#23088=ORIENTED_EDGE('',*,*,#15460,.T.);
#23089=ORIENTED_EDGE('',*,*,#15697,.T.);
#23090=ORIENTED_EDGE('',*,*,#15933,.T.);
#23091=ORIENTED_EDGE('',*,*,#15044,.T.);
#23092=ORIENTED_EDGE('',*,*,#14762,.F.);
#29784=PLANE('',#33332);
#29785=PLANE('',#33333);
#29786=PLANE('',#33343);
#29787=PLANE('',#33344);
#29788=PLANE('',#33345);
#29789=PLANE('',#33346);
#29790=PLANE('',#33347);
#29791=PLANE('',#33348);
#29792=PLANE('',#33349);
#29793=PLANE('',#33350);
#29794=PLANE('',#33352);
#29795=PLANE('',#33354);
#29796=PLANE('',#33355);
#29797=PLANE('',#33357);
#29798=PLANE('',#33358);
#29799=PLANE('',#33360);
#29800=PLANE('',#33361);
#29801=PLANE('',#33363);
#29802=PLANE('',#33364);
#29803=PLANE('',#33366);
#29804=PLANE('',#33367);
#29805=PLANE('',#33369);
#29806=PLANE('',#33370);
#29807=PLANE('',#33372);
#29808=PLANE('',#33373);
#29809=PLANE('',#33374);
#29810=PLANE('',#33375);
#29811=PLANE('',#33376);
#29812=PLANE('',#33377);
#29813=PLANE('',#33378);
#29814=PLANE('',#33379);
#29815=PLANE('',#33380);
#29816=PLANE('',#33381);
#29817=PLANE('',#33382);
#29818=PLANE('',#33383);
#29819=PLANE('',#33384);
#29820=PLANE('',#33385);
#29821=PLANE('',#33386);
#29822=PLANE('',#33387);
#29823=PLANE('',#33388);
#29824=PLANE('',#33389);
#29825=PLANE('',#33390);
#29826=PLANE('',#33391);
#29827=PLANE('',#33393);
#29828=PLANE('',#33394);
#29829=PLANE('',#33396);
#29830=PLANE('',#33397);
#29831=PLANE('',#33399);
#29832=PLANE('',#33400);
#29833=PLANE('',#33402);
#29834=PLANE('',#33403);
#29835=PLANE('',#33405);
#29836=PLANE('',#33406);
#29837=PLANE('',#33408);
#29838=PLANE('',#33409);
#29839=PLANE('',#33411);
#29840=PLANE('',#33412);
#29841=PLANE('',#33414);
#29842=PLANE('',#33415);
#29843=PLANE('',#33417);
#29844=PLANE('',#33418);
#29845=PLANE('',#33420);
#29846=PLANE('',#33421);
#29847=PLANE('',#33423);
#29848=PLANE('',#33424);
#29849=PLANE('',#33426);
#29850=PLANE('',#33427);
#29851=PLANE('',#33429);
#29852=PLANE('',#33430);
#29853=PLANE('',#33432);
#29854=PLANE('',#33433);
#29855=PLANE('',#33435);
#29856=PLANE('',#33436);
#29857=PLANE('',#33438);
#29858=PLANE('',#33439);
#29859=PLANE('',#33441);
#29860=PLANE('',#33442);
#29861=PLANE('',#33444);
#29862=PLANE('',#33445);
#29863=PLANE('',#33447);
#29864=PLANE('',#33448);
#29865=PLANE('',#33450);
#29866=PLANE('',#33451);
#29867=PLANE('',#33453);
#29868=PLANE('',#33454);
#29869=PLANE('',#33456);
#29870=PLANE('',#33457);
#29871=PLANE('',#33459);
#29872=PLANE('',#33460);
#29873=PLANE('',#33462);
#29874=PLANE('',#33463);
#29875=PLANE('',#33465);
#29876=PLANE('',#33466);
#29877=PLANE('',#33468);
#29878=PLANE('',#33469);
#29879=PLANE('',#33471);
#29880=PLANE('',#33472);
#29881=PLANE('',#33474);
#29882=PLANE('',#33475);
#29883=PLANE('',#33477);
#29884=PLANE('',#33478);
#29885=PLANE('',#33480);
#29886=PLANE('',#33481);
#29887=PLANE('',#33483);
#29888=PLANE('',#33484);
#29889=PLANE('',#33486);
#29890=PLANE('',#33487);
#29891=PLANE('',#33489);
#29892=PLANE('',#33490);
#29893=PLANE('',#33492);
#29894=PLANE('',#33493);
#29895=PLANE('',#33495);
#29896=PLANE('',#33496);
#29897=PLANE('',#33498);
#29898=PLANE('',#33499);
#29899=PLANE('',#33501);
#29900=PLANE('',#33502);
#29901=PLANE('',#33504);
#29902=PLANE('',#33505);
#29903=PLANE('',#33507);
#29904=PLANE('',#33508);
#29905=PLANE('',#33510);
#29906=PLANE('',#33511);
#29907=PLANE('',#33513);
#29908=PLANE('',#33514);
#29909=PLANE('',#33516);
#29910=PLANE('',#33517);
#29911=PLANE('',#33519);
#29912=PLANE('',#33520);
#29913=PLANE('',#33522);
#29914=PLANE('',#33523);
#29915=PLANE('',#33525);
#29916=PLANE('',#33526);
#29917=PLANE('',#33528);
#29918=PLANE('',#33529);
#29919=PLANE('',#33531);
#29920=PLANE('',#33532);
#29921=PLANE('',#33534);
#29922=PLANE('',#33535);
#29923=PLANE('',#33537);
#29924=PLANE('',#33538);
#29925=PLANE('',#33540);
#29926=PLANE('',#33541);
#29927=PLANE('',#33543);
#29928=PLANE('',#33544);
#29929=PLANE('',#33546);
#29930=PLANE('',#33547);
#29931=PLANE('',#33549);
#29932=PLANE('',#33550);
#29933=PLANE('',#33552);
#29934=PLANE('',#33553);
#29935=PLANE('',#33555);
#29936=PLANE('',#33556);
#29937=PLANE('',#33558);
#29938=PLANE('',#33559);
#29939=PLANE('',#33561);
#29940=PLANE('',#33562);
#29941=PLANE('',#33564);
#29942=PLANE('',#33565);
#29943=PLANE('',#33566);
#29944=PLANE('',#33567);
#29945=PLANE('',#33568);
#29946=PLANE('',#33569);
#29947=PLANE('',#33570);
#29948=PLANE('',#33571);
#29949=PLANE('',#33572);
#29950=PLANE('',#33573);
#29951=PLANE('',#33574);
#29952=PLANE('',#33575);
#29953=PLANE('',#33576);
#30332=ADVANCED_FACE('',(#5172),#4471,.T.);
#30333=ADVANCED_FACE('',(#5173),#4472,.T.);
#30334=ADVANCED_FACE('',(#5174),#4473,.T.);
#30335=ADVANCED_FACE('',(#5175),#4474,.T.);
#30336=ADVANCED_FACE('',(#5176),#4475,.T.);
#30337=ADVANCED_FACE('',(#5177),#4476,.T.);
#30338=ADVANCED_FACE('',(#5178),#4477,.T.);
#30339=ADVANCED_FACE('',(#5179),#4478,.T.);
#30340=ADVANCED_FACE('',(#5180),#4479,.T.);
#30341=ADVANCED_FACE('',(#5181),#4480,.T.);
#30342=ADVANCED_FACE('',(#5182),#4481,.T.);
#30343=ADVANCED_FACE('',(#5183),#4482,.T.);
#30344=ADVANCED_FACE('',(#5184),#4483,.T.);
#30345=ADVANCED_FACE('',(#5185),#4484,.T.);
#30346=ADVANCED_FACE('',(#5186),#4485,.T.);
#30347=ADVANCED_FACE('',(#5187),#4486,.T.);
#30348=ADVANCED_FACE('',(#5188),#4487,.T.);
#30349=ADVANCED_FACE('',(#5189),#4488,.T.);
#30350=ADVANCED_FACE('',(#5190),#4489,.T.);
#30351=ADVANCED_FACE('',(#5191),#4490,.T.);
#30352=ADVANCED_FACE('',(#5192),#4491,.T.);
#30353=ADVANCED_FACE('',(#5193),#4492,.T.);
#30354=ADVANCED_FACE('',(#5194),#4493,.T.);
#30355=ADVANCED_FACE('',(#5195),#4494,.T.);
#30356=ADVANCED_FACE('',(#5196),#4495,.T.);
#30357=ADVANCED_FACE('',(#5197),#4496,.T.);
#30358=ADVANCED_FACE('',(#5198),#4497,.T.);
#30359=ADVANCED_FACE('',(#5199),#4498,.T.);
#30360=ADVANCED_FACE('',(#5200),#2956,.T.);
#30361=ADVANCED_FACE('',(#5201),#4499,.T.);
#30362=ADVANCED_FACE('',(#5202),#4500,.T.);
#30363=ADVANCED_FACE('',(#5203),#4501,.T.);
#30364=ADVANCED_FACE('',(#5204),#4502,.T.);
#30365=ADVANCED_FACE('',(#5205),#4503,.T.);
#30366=ADVANCED_FACE('',(#5206),#4504,.T.);
#30367=ADVANCED_FACE('',(#5207),#4505,.T.);
#30368=ADVANCED_FACE('',(#5208),#4506,.T.);
#30369=ADVANCED_FACE('',(#5209),#4507,.T.);
#30370=ADVANCED_FACE('',(#5210),#4508,.T.);
#30371=ADVANCED_FACE('',(#5211),#4509,.T.);
#30372=ADVANCED_FACE('',(#5212),#4510,.T.);
#30373=ADVANCED_FACE('',(#5213),#4511,.T.);
#30374=ADVANCED_FACE('',(#5214),#4512,.T.);
#30375=ADVANCED_FACE('',(#5215),#4513,.T.);
#30376=ADVANCED_FACE('',(#5216),#4514,.T.);
#30377=ADVANCED_FACE('',(#5217),#4515,.T.);
#30378=ADVANCED_FACE('',(#5218),#4516,.T.);
#30379=ADVANCED_FACE('',(#5219),#4517,.T.);
#30380=ADVANCED_FACE('',(#5220),#4518,.T.);
#30381=ADVANCED_FACE('',(#5221),#4519,.T.);
#30382=ADVANCED_FACE('',(#5222),#4520,.T.);
#30383=ADVANCED_FACE('',(#5223),#4521,.T.);
#30384=ADVANCED_FACE('',(#5224),#4522,.T.);
#30385=ADVANCED_FACE('',(#5225),#4523,.T.);
#30386=ADVANCED_FACE('',(#5226),#4524,.T.);
#30387=ADVANCED_FACE('',(#5227),#4525,.T.);
#30388=ADVANCED_FACE('',(#5228),#4526,.T.);
#30389=ADVANCED_FACE('',(#5229),#4527,.T.);
#30390=ADVANCED_FACE('',(#5230),#4528,.T.);
#30391=ADVANCED_FACE('',(#5231),#4529,.T.);
#30392=ADVANCED_FACE('',(#5232),#2957,.T.);
#30393=ADVANCED_FACE('',(#5233),#4530,.T.);
#30394=ADVANCED_FACE('',(#5234),#4531,.F.);
#30395=ADVANCED_FACE('',(#5235),#4532,.F.);
#30396=ADVANCED_FACE('',(#5236),#4533,.F.);
#30397=ADVANCED_FACE('',(#5237),#4534,.F.);
#30398=ADVANCED_FACE('',(#5238),#4535,.F.);
#30399=ADVANCED_FACE('',(#5239),#4536,.F.);
#30400=ADVANCED_FACE('',(#5240),#4537,.F.);
#30401=ADVANCED_FACE('',(#5241),#4538,.F.);
#30402=ADVANCED_FACE('',(#5242),#4539,.F.);
#30403=ADVANCED_FACE('',(#5243),#4540,.F.);
#30404=ADVANCED_FACE('',(#5244),#4541,.F.);
#30405=ADVANCED_FACE('',(#5245),#4542,.F.);
#30406=ADVANCED_FACE('',(#5246),#4543,.F.);
#30407=ADVANCED_FACE('',(#5247),#4544,.F.);
#30408=ADVANCED_FACE('',(#5248),#4545,.F.);
#30409=ADVANCED_FACE('',(#5249),#2958,.F.);
#30410=ADVANCED_FACE('',(#5250),#49,.T.);
#30411=ADVANCED_FACE('',(#5251),#2959,.T.);
#30412=ADVANCED_FACE('',(#5252),#2960,.T.);
#30413=ADVANCED_FACE('',(#5253),#50,.F.);
#30414=ADVANCED_FACE('',(#5254),#4546,.T.);
#30415=ADVANCED_FACE('',(#5255),#51,.T.);
#30416=ADVANCED_FACE('',(#5256),#52,.F.);
#30417=ADVANCED_FACE('',(#5257),#53,.T.);
#30418=ADVANCED_FACE('',(#5258),#54,.T.);
#30419=ADVANCED_FACE('',(#5259),#55,.T.);
#30420=ADVANCED_FACE('',(#5260),#56,.T.);
#30421=ADVANCED_FACE('',(#5261),#57,.T.);
#30422=ADVANCED_FACE('',(#5262),#58,.T.);
#30423=ADVANCED_FACE('',(#5263),#59,.T.);
#30424=ADVANCED_FACE('',(#5264),#60,.T.);
#30425=ADVANCED_FACE('',(#5265),#61,.T.);
#30426=ADVANCED_FACE('',(#5266),#62,.T.);
#30427=ADVANCED_FACE('',(#5267),#63,.T.);
#30428=ADVANCED_FACE('',(#5268),#64,.T.);
#30429=ADVANCED_FACE('',(#5269),#65,.T.);
#30430=ADVANCED_FACE('',(#5270),#66,.T.);
#30431=ADVANCED_FACE('',(#5271),#67,.T.);
#30432=ADVANCED_FACE('',(#5272),#68,.T.);
#30433=ADVANCED_FACE('',(#5273),#69,.T.);
#30434=ADVANCED_FACE('',(#5274),#70,.T.);
#30435=ADVANCED_FACE('',(#5275),#71,.T.);
#30436=ADVANCED_FACE('',(#5276),#72,.T.);
#30437=ADVANCED_FACE('',(#5277),#73,.T.);
#30438=ADVANCED_FACE('',(#5278),#74,.T.);
#30439=ADVANCED_FACE('',(#5279),#75,.T.);
#30440=ADVANCED_FACE('',(#5280),#76,.T.);
#30441=ADVANCED_FACE('',(#5281),#77,.T.);
#30442=ADVANCED_FACE('',(#5282),#78,.T.);
#30443=ADVANCED_FACE('',(#5283),#79,.T.);
#30444=ADVANCED_FACE('',(#5284),#80,.T.);
#30445=ADVANCED_FACE('',(#5285),#81,.T.);
#30446=ADVANCED_FACE('',(#5286),#82,.T.);
#30447=ADVANCED_FACE('',(#5287),#83,.T.);
#30448=ADVANCED_FACE('',(#5288),#84,.T.);
#30449=ADVANCED_FACE('',(#5289),#85,.T.);
#30450=ADVANCED_FACE('',(#5290),#86,.T.);
#30451=ADVANCED_FACE('',(#5291),#87,.T.);
#30452=ADVANCED_FACE('',(#5292),#88,.T.);
#30453=ADVANCED_FACE('',(#5293),#89,.T.);
#30454=ADVANCED_FACE('',(#5294),#90,.T.);
#30455=ADVANCED_FACE('',(#5295),#91,.T.);
#30456=ADVANCED_FACE('',(#5296),#92,.T.);
#30457=ADVANCED_FACE('',(#5297),#93,.T.);
#30458=ADVANCED_FACE('',(#5298),#94,.T.);
#30459=ADVANCED_FACE('',(#5299),#95,.T.);
#30460=ADVANCED_FACE('',(#5300),#96,.T.);
#30461=ADVANCED_FACE('',(#5301),#97,.T.);
#30462=ADVANCED_FACE('',(#5302),#98,.T.);
#30463=ADVANCED_FACE('',(#5303),#99,.T.);
#30464=ADVANCED_FACE('',(#5304),#100,.T.);
#30465=ADVANCED_FACE('',(#5305),#101,.T.);
#30466=ADVANCED_FACE('',(#5306),#102,.T.);
#30467=ADVANCED_FACE('',(#5307),#103,.T.);
#30468=ADVANCED_FACE('',(#5308),#104,.T.);
#30469=ADVANCED_FACE('',(#5309),#105,.T.);
#30470=ADVANCED_FACE('',(#5310),#106,.T.);
#30471=ADVANCED_FACE('',(#5311),#107,.T.);
#30472=ADVANCED_FACE('',(#5312),#108,.T.);
#30473=ADVANCED_FACE('',(#5313),#109,.T.);
#30474=ADVANCED_FACE('',(#5314),#110,.T.);
#30475=ADVANCED_FACE('',(#5315),#111,.T.);
#30476=ADVANCED_FACE('',(#5316),#112,.T.);
#30477=ADVANCED_FACE('',(#5317),#113,.T.);
#30478=ADVANCED_FACE('',(#5318),#114,.T.);
#30479=ADVANCED_FACE('',(#5319),#115,.T.);
#30480=ADVANCED_FACE('',(#5320),#116,.T.);
#30481=ADVANCED_FACE('',(#5321),#117,.T.);
#30482=ADVANCED_FACE('',(#5322),#118,.T.);
#30483=ADVANCED_FACE('',(#5323),#119,.T.);
#30484=ADVANCED_FACE('',(#5324),#120,.T.);
#30485=ADVANCED_FACE('',(#5325),#121,.T.);
#30486=ADVANCED_FACE('',(#5326),#122,.T.);
#30487=ADVANCED_FACE('',(#5327),#123,.T.);
#30488=ADVANCED_FACE('',(#5328),#124,.T.);
#30489=ADVANCED_FACE('',(#5329),#125,.T.);
#30490=ADVANCED_FACE('',(#5330),#126,.T.);
#30491=ADVANCED_FACE('',(#5331),#127,.T.);
#30492=ADVANCED_FACE('',(#5332),#128,.T.);
#30493=ADVANCED_FACE('',(#5333),#129,.T.);
#30494=ADVANCED_FACE('',(#5334),#130,.T.);
#30495=ADVANCED_FACE('',(#5335),#131,.T.);
#30496=ADVANCED_FACE('',(#5336),#4547,.T.);
#30497=ADVANCED_FACE('',(#5337),#4548,.T.);
#30498=ADVANCED_FACE('',(#5338),#4549,.T.);
#30499=ADVANCED_FACE('',(#5339),#4550,.T.);
#30500=ADVANCED_FACE('',(#5340),#4551,.T.);
#30501=ADVANCED_FACE('',(#5341),#4552,.T.);
#30502=ADVANCED_FACE('',(#5342),#4553,.T.);
#30503=ADVANCED_FACE('',(#5343),#4554,.T.);
#30504=ADVANCED_FACE('',(#5344),#4555,.T.);
#30505=ADVANCED_FACE('',(#5345),#4556,.T.);
#30506=ADVANCED_FACE('',(#5346),#4557,.T.);
#30507=ADVANCED_FACE('',(#5347),#4558,.T.);
#30508=ADVANCED_FACE('',(#5348),#4559,.T.);
#30509=ADVANCED_FACE('',(#5349),#4560,.T.);
#30510=ADVANCED_FACE('',(#5350),#4561,.T.);
#30511=ADVANCED_FACE('',(#5351),#4562,.T.);
#30512=ADVANCED_FACE('',(#5352),#4563,.T.);
#30513=ADVANCED_FACE('',(#5353),#4564,.T.);
#30514=ADVANCED_FACE('',(#5354),#4565,.T.);
#30515=ADVANCED_FACE('',(#5355),#4566,.T.);
#30516=ADVANCED_FACE('',(#5356),#4567,.T.);
#30517=ADVANCED_FACE('',(#5357),#4568,.T.);
#30518=ADVANCED_FACE('',(#5358),#4569,.T.);
#30519=ADVANCED_FACE('',(#5359),#4570,.T.);
#30520=ADVANCED_FACE('',(#5360),#4571,.T.);
#30521=ADVANCED_FACE('',(#5361),#4572,.T.);
#30522=ADVANCED_FACE('',(#5362),#4573,.T.);
#30523=ADVANCED_FACE('',(#5363),#4574,.T.);
#30524=ADVANCED_FACE('',(#5364),#4575,.T.);
#30525=ADVANCED_FACE('',(#5365),#4576,.T.);
#30526=ADVANCED_FACE('',(#5366),#4577,.T.);
#30527=ADVANCED_FACE('',(#5367),#4578,.T.);
#30528=ADVANCED_FACE('',(#5368),#4579,.T.);
#30529=ADVANCED_FACE('',(#5369),#4580,.T.);
#30530=ADVANCED_FACE('',(#5370),#4581,.T.);
#30531=ADVANCED_FACE('',(#5371),#4582,.T.);
#30532=ADVANCED_FACE('',(#5372),#4583,.T.);
#30533=ADVANCED_FACE('',(#5373),#4584,.T.);
#30534=ADVANCED_FACE('',(#5374),#4585,.T.);
#30535=ADVANCED_FACE('',(#5375),#4586,.T.);
#30536=ADVANCED_FACE('',(#5376),#4587,.T.);
#30537=ADVANCED_FACE('',(#5377),#4588,.T.);
#30538=ADVANCED_FACE('',(#5378),#4589,.T.);
#30539=ADVANCED_FACE('',(#5379),#4590,.T.);
#30540=ADVANCED_FACE('',(#5380),#4591,.T.);
#30541=ADVANCED_FACE('',(#5381),#4592,.T.);
#30542=ADVANCED_FACE('',(#5382),#4593,.T.);
#30543=ADVANCED_FACE('',(#5383),#4594,.T.);
#30544=ADVANCED_FACE('',(#5384),#4595,.T.);
#30545=ADVANCED_FACE('',(#5385),#4596,.T.);
#30546=ADVANCED_FACE('',(#5386),#4597,.T.);
#30547=ADVANCED_FACE('',(#5387),#4598,.T.);
#30548=ADVANCED_FACE('',(#5388),#4599,.T.);
#30549=ADVANCED_FACE('',(#5389),#4600,.T.);
#30550=ADVANCED_FACE('',(#5390),#4601,.T.);
#30551=ADVANCED_FACE('',(#5391),#4602,.T.);
#30552=ADVANCED_FACE('',(#5392),#4603,.T.);
#30553=ADVANCED_FACE('',(#5393),#4604,.T.);
#30554=ADVANCED_FACE('',(#5394),#4605,.T.);
#30555=ADVANCED_FACE('',(#5395),#4606,.T.);
#30556=ADVANCED_FACE('',(#5396),#4607,.T.);
#30557=ADVANCED_FACE('',(#5397),#4608,.T.);
#30558=ADVANCED_FACE('',(#5398),#4609,.T.);
#30559=ADVANCED_FACE('',(#5399),#4610,.T.);
#30560=ADVANCED_FACE('',(#5400),#4611,.T.);
#30561=ADVANCED_FACE('',(#5401),#4612,.T.);
#30562=ADVANCED_FACE('',(#5402),#4613,.T.);
#30563=ADVANCED_FACE('',(#5403),#4614,.T.);
#30564=ADVANCED_FACE('',(#5404),#4615,.T.);
#30565=ADVANCED_FACE('',(#5405),#4616,.T.);
#30566=ADVANCED_FACE('',(#5406),#4617,.T.);
#30567=ADVANCED_FACE('',(#5407),#4618,.T.);
#30568=ADVANCED_FACE('',(#5408),#4619,.T.);
#30569=ADVANCED_FACE('',(#5409),#4620,.T.);
#30570=ADVANCED_FACE('',(#5410),#4621,.T.);
#30571=ADVANCED_FACE('',(#5411),#4622,.T.);
#30572=ADVANCED_FACE('',(#5412),#4623,.T.);
#30573=ADVANCED_FACE('',(#5413),#4624,.T.);
#30574=ADVANCED_FACE('',(#5414),#4625,.T.);
#30575=ADVANCED_FACE('',(#5415),#132,.T.);
#30576=ADVANCED_FACE('',(#5416),#133,.T.);
#30577=ADVANCED_FACE('',(#5417),#134,.T.);
#30578=ADVANCED_FACE('',(#5418),#135,.T.);
#30579=ADVANCED_FACE('',(#5419),#136,.T.);
#30580=ADVANCED_FACE('',(#5420),#137,.T.);
#30581=ADVANCED_FACE('',(#5421),#138,.T.);
#30582=ADVANCED_FACE('',(#5422),#139,.T.);
#30583=ADVANCED_FACE('',(#5423),#140,.T.);
#30584=ADVANCED_FACE('',(#5424),#141,.T.);
#30585=ADVANCED_FACE('',(#5425),#142,.T.);
#30586=ADVANCED_FACE('',(#5426),#143,.T.);
#30587=ADVANCED_FACE('',(#5427),#144,.T.);
#30588=ADVANCED_FACE('',(#5428),#145,.T.);
#30589=ADVANCED_FACE('',(#5429),#146,.T.);
#30590=ADVANCED_FACE('',(#5430),#147,.T.);
#30591=ADVANCED_FACE('',(#5431),#148,.T.);
#30592=ADVANCED_FACE('',(#5432),#149,.T.);
#30593=ADVANCED_FACE('',(#5433),#150,.T.);
#30594=ADVANCED_FACE('',(#5434),#151,.T.);
#30595=ADVANCED_FACE('',(#5435),#152,.T.);
#30596=ADVANCED_FACE('',(#5436),#153,.T.);
#30597=ADVANCED_FACE('',(#5437),#154,.T.);
#30598=ADVANCED_FACE('',(#5438),#155,.T.);
#30599=ADVANCED_FACE('',(#5439),#156,.T.);
#30600=ADVANCED_FACE('',(#5440),#157,.T.);
#30601=ADVANCED_FACE('',(#5441),#158,.T.);
#30602=ADVANCED_FACE('',(#5442),#159,.T.);
#30603=ADVANCED_FACE('',(#5443),#160,.T.);
#30604=ADVANCED_FACE('',(#5444),#161,.T.);
#30605=ADVANCED_FACE('',(#5445),#162,.T.);
#30606=ADVANCED_FACE('',(#5446),#163,.T.);
#30607=ADVANCED_FACE('',(#5447),#164,.T.);
#30608=ADVANCED_FACE('',(#5448),#165,.T.);
#30609=ADVANCED_FACE('',(#5449),#166,.T.);
#30610=ADVANCED_FACE('',(#5450),#167,.T.);
#30611=ADVANCED_FACE('',(#5451),#168,.T.);
#30612=ADVANCED_FACE('',(#5452),#169,.T.);
#30613=ADVANCED_FACE('',(#5453),#170,.T.);
#30614=ADVANCED_FACE('',(#5454),#171,.T.);
#30615=ADVANCED_FACE('',(#5455),#172,.T.);
#30616=ADVANCED_FACE('',(#5456),#173,.T.);
#30617=ADVANCED_FACE('',(#5457),#174,.T.);
#30618=ADVANCED_FACE('',(#5458),#175,.T.);
#30619=ADVANCED_FACE('',(#5459),#176,.T.);
#30620=ADVANCED_FACE('',(#5460),#177,.T.);
#30621=ADVANCED_FACE('',(#5461),#178,.T.);
#30622=ADVANCED_FACE('',(#5462),#179,.T.);
#30623=ADVANCED_FACE('',(#5463),#180,.T.);
#30624=ADVANCED_FACE('',(#5464),#181,.T.);
#30625=ADVANCED_FACE('',(#5465),#182,.T.);
#30626=ADVANCED_FACE('',(#5466),#183,.T.);
#30627=ADVANCED_FACE('',(#5467),#184,.T.);
#30628=ADVANCED_FACE('',(#5468),#185,.T.);
#30629=ADVANCED_FACE('',(#5469),#186,.T.);
#30630=ADVANCED_FACE('',(#5470),#187,.T.);
#30631=ADVANCED_FACE('',(#5471),#188,.T.);
#30632=ADVANCED_FACE('',(#5472),#189,.T.);
#30633=ADVANCED_FACE('',(#5473),#190,.T.);
#30634=ADVANCED_FACE('',(#5474),#191,.T.);
#30635=ADVANCED_FACE('',(#5475),#192,.T.);
#30636=ADVANCED_FACE('',(#5476),#193,.T.);
#30637=ADVANCED_FACE('',(#5477),#194,.T.);
#30638=ADVANCED_FACE('',(#5478),#195,.T.);
#30639=ADVANCED_FACE('',(#5479),#196,.T.);
#30640=ADVANCED_FACE('',(#5480),#197,.T.);
#30641=ADVANCED_FACE('',(#5481),#198,.T.);
#30642=ADVANCED_FACE('',(#5482),#199,.T.);
#30643=ADVANCED_FACE('',(#5483),#200,.T.);
#30644=ADVANCED_FACE('',(#5484),#201,.T.);
#30645=ADVANCED_FACE('',(#5485),#202,.T.);
#30646=ADVANCED_FACE('',(#5486),#203,.T.);
#30647=ADVANCED_FACE('',(#5487),#204,.T.);
#30648=ADVANCED_FACE('',(#5488),#205,.T.);
#30649=ADVANCED_FACE('',(#5489),#206,.T.);
#30650=ADVANCED_FACE('',(#5490),#207,.T.);
#30651=ADVANCED_FACE('',(#5491),#208,.T.);
#30652=ADVANCED_FACE('',(#5492),#209,.T.);
#30653=ADVANCED_FACE('',(#5493),#210,.T.);
#30654=ADVANCED_FACE('',(#5494),#29784,.T.);
#30655=ADVANCED_FACE('',(#5495,#3394),#29785,.T.);
#30656=ADVANCED_FACE('',(#5496),#211,.T.);
#30657=ADVANCED_FACE('',(#5497),#4626,.T.);
#30658=ADVANCED_FACE('',(#5498),#212,.T.);
#30659=ADVANCED_FACE('',(#5499,#3395),#29786,.T.);
#30660=ADVANCED_FACE('',(#5500),#29787,.T.);
#30661=ADVANCED_FACE('',(#5501),#29788,.F.);
#30662=ADVANCED_FACE('',(#5502),#29789,.F.);
#30663=ADVANCED_FACE('',(#5503),#29790,.F.);
#30664=ADVANCED_FACE('',(#5504),#29791,.F.);
#30665=ADVANCED_FACE('',(#5505),#29792,.F.);
#30666=ADVANCED_FACE('',(#5506),#29793,.F.);
#30667=ADVANCED_FACE('',(#5507),#43,.T.);
#30668=ADVANCED_FACE('',(#5508),#44,.T.);
#30669=ADVANCED_FACE('',(#5509),#2961,.T.);
#30670=ADVANCED_FACE('',(#5510),#29794,.F.);
#30671=ADVANCED_FACE('',(#5511),#4627,.F.);
#30672=ADVANCED_FACE('',(#5512),#29795,.F.);
#30673=ADVANCED_FACE('',(#5513),#29796,.F.);
#30674=ADVANCED_FACE('',(#5514),#4628,.F.);
#30675=ADVANCED_FACE('',(#5515),#29797,.F.);
#30676=ADVANCED_FACE('',(#5516),#29798,.F.);
#30677=ADVANCED_FACE('',(#5517),#4629,.F.);
#30678=ADVANCED_FACE('',(#5518),#29799,.F.);
#30679=ADVANCED_FACE('',(#5519),#29800,.F.);
#30680=ADVANCED_FACE('',(#5520),#4630,.F.);
#30681=ADVANCED_FACE('',(#5521),#29801,.F.);
#30682=ADVANCED_FACE('',(#5522),#29802,.F.);
#30683=ADVANCED_FACE('',(#5523),#4631,.F.);
#30684=ADVANCED_FACE('',(#5524),#29803,.F.);
#30685=ADVANCED_FACE('',(#5525),#29804,.F.);
#30686=ADVANCED_FACE('',(#5526),#4632,.F.);
#30687=ADVANCED_FACE('',(#5527),#29805,.F.);
#30688=ADVANCED_FACE('',(#5528),#29806,.F.);
#30689=ADVANCED_FACE('',(#5529),#4633,.F.);
#30690=ADVANCED_FACE('',(#5530),#29807,.F.);
#30691=ADVANCED_FACE('',(#5531),#29808,.F.);
#30692=ADVANCED_FACE('',(#5532),#29809,.F.);
#30693=ADVANCED_FACE('',(#5533),#29810,.F.);
#30694=ADVANCED_FACE('',(#5534),#29811,.F.);
#30695=ADVANCED_FACE('',(#5535),#29812,.F.);
#30696=ADVANCED_FACE('',(#5536),#29813,.F.);
#30697=ADVANCED_FACE('',(#5537),#29814,.F.);
#30698=ADVANCED_FACE('',(#5538),#29815,.F.);
#30699=ADVANCED_FACE('',(#5539),#29816,.F.);
#30700=ADVANCED_FACE('',(#5540),#29817,.F.);
#30701=ADVANCED_FACE('',(#5541),#29818,.F.);
#30702=ADVANCED_FACE('',(#5542),#29819,.F.);
#30703=ADVANCED_FACE('',(#5543),#29820,.F.);
#30704=ADVANCED_FACE('',(#5544),#29821,.F.);
#30705=ADVANCED_FACE('',(#5545),#29822,.F.);
#30706=ADVANCED_FACE('',(#5546),#29823,.F.);
#30707=ADVANCED_FACE('',(#5547),#29824,.F.);
#30708=ADVANCED_FACE('',(#5548),#29825,.F.);
#30709=ADVANCED_FACE('',(#5549),#29826,.F.);
#30710=ADVANCED_FACE('',(#5550),#4634,.F.);
#30711=ADVANCED_FACE('',(#5551),#29827,.F.);
#30712=ADVANCED_FACE('',(#5552),#29828,.F.);
#30713=ADVANCED_FACE('',(#5553),#4635,.F.);
#30714=ADVANCED_FACE('',(#5554),#29829,.F.);
#30715=ADVANCED_FACE('',(#5555),#29830,.F.);
#30716=ADVANCED_FACE('',(#5556),#4636,.F.);
#30717=ADVANCED_FACE('',(#5557),#29831,.F.);
#30718=ADVANCED_FACE('',(#5558),#29832,.F.);
#30719=ADVANCED_FACE('',(#5559),#4637,.F.);
#30720=ADVANCED_FACE('',(#5560),#29833,.F.);
#30721=ADVANCED_FACE('',(#5561),#29834,.F.);
#30722=ADVANCED_FACE('',(#5562),#4638,.F.);
#30723=ADVANCED_FACE('',(#5563),#29835,.F.);
#30724=ADVANCED_FACE('',(#5564),#29836,.F.);
#30725=ADVANCED_FACE('',(#5565),#4639,.F.);
#30726=ADVANCED_FACE('',(#5566),#29837,.F.);
#30727=ADVANCED_FACE('',(#5567),#29838,.F.);
#30728=ADVANCED_FACE('',(#5568),#4640,.F.);
#30729=ADVANCED_FACE('',(#5569),#29839,.F.);
#30730=ADVANCED_FACE('',(#5570),#29840,.F.);
#30731=ADVANCED_FACE('',(#5571),#4641,.F.);
#30732=ADVANCED_FACE('',(#5572),#29841,.F.);
#30733=ADVANCED_FACE('',(#5573),#29842,.F.);
#30734=ADVANCED_FACE('',(#5574),#4642,.F.);
#30735=ADVANCED_FACE('',(#5575),#29843,.F.);
#30736=ADVANCED_FACE('',(#5576),#29844,.F.);
#30737=ADVANCED_FACE('',(#5577),#4643,.F.);
#30738=ADVANCED_FACE('',(#5578),#29845,.F.);
#30739=ADVANCED_FACE('',(#5579),#29846,.F.);
#30740=ADVANCED_FACE('',(#5580),#4644,.F.);
#30741=ADVANCED_FACE('',(#5581),#29847,.F.);
#30742=ADVANCED_FACE('',(#5582),#29848,.F.);
#30743=ADVANCED_FACE('',(#5583),#4645,.F.);
#30744=ADVANCED_FACE('',(#5584),#29849,.F.);
#30745=ADVANCED_FACE('',(#5585),#29850,.F.);
#30746=ADVANCED_FACE('',(#5586),#4646,.F.);
#30747=ADVANCED_FACE('',(#5587),#29851,.F.);
#30748=ADVANCED_FACE('',(#5588),#29852,.F.);
#30749=ADVANCED_FACE('',(#5589),#4647,.F.);
#30750=ADVANCED_FACE('',(#5590),#29853,.F.);
#30751=ADVANCED_FACE('',(#5591),#29854,.F.);
#30752=ADVANCED_FACE('',(#5592),#4648,.F.);
#30753=ADVANCED_FACE('',(#5593),#29855,.F.);
#30754=ADVANCED_FACE('',(#5594),#29856,.F.);
#30755=ADVANCED_FACE('',(#5595),#4649,.F.);
#30756=ADVANCED_FACE('',(#5596),#29857,.F.);
#30757=ADVANCED_FACE('',(#5597),#29858,.F.);
#30758=ADVANCED_FACE('',(#5598),#4650,.F.);
#30759=ADVANCED_FACE('',(#5599),#29859,.F.);
#30760=ADVANCED_FACE('',(#5600),#29860,.F.);
#30761=ADVANCED_FACE('',(#5601),#4651,.F.);
#30762=ADVANCED_FACE('',(#5602),#29861,.F.);
#30763=ADVANCED_FACE('',(#5603),#29862,.F.);
#30764=ADVANCED_FACE('',(#5604),#4652,.F.);
#30765=ADVANCED_FACE('',(#5605),#29863,.F.);
#30766=ADVANCED_FACE('',(#5606),#29864,.F.);
#30767=ADVANCED_FACE('',(#5607),#4653,.F.);
#30768=ADVANCED_FACE('',(#5608),#29865,.F.);
#30769=ADVANCED_FACE('',(#5609),#29866,.F.);
#30770=ADVANCED_FACE('',(#5610),#4654,.F.);
#30771=ADVANCED_FACE('',(#5611),#29867,.F.);
#30772=ADVANCED_FACE('',(#5612),#29868,.F.);
#30773=ADVANCED_FACE('',(#5613),#4655,.F.);
#30774=ADVANCED_FACE('',(#5614),#29869,.F.);
#30775=ADVANCED_FACE('',(#5615),#29870,.F.);
#30776=ADVANCED_FACE('',(#5616),#4656,.F.);
#30777=ADVANCED_FACE('',(#5617),#29871,.F.);
#30778=ADVANCED_FACE('',(#5618),#29872,.F.);
#30779=ADVANCED_FACE('',(#5619),#4657,.F.);
#30780=ADVANCED_FACE('',(#5620),#29873,.F.);
#30781=ADVANCED_FACE('',(#5621),#29874,.F.);
#30782=ADVANCED_FACE('',(#5622),#4658,.F.);
#30783=ADVANCED_FACE('',(#5623),#29875,.F.);
#30784=ADVANCED_FACE('',(#5624),#29876,.F.);
#30785=ADVANCED_FACE('',(#5625),#4659,.F.);
#30786=ADVANCED_FACE('',(#5626),#29877,.F.);
#30787=ADVANCED_FACE('',(#5627),#29878,.F.);
#30788=ADVANCED_FACE('',(#5628),#4660,.F.);
#30789=ADVANCED_FACE('',(#5629),#29879,.F.);
#30790=ADVANCED_FACE('',(#5630),#29880,.F.);
#30791=ADVANCED_FACE('',(#5631),#4661,.F.);
#30792=ADVANCED_FACE('',(#5632),#29881,.F.);
#30793=ADVANCED_FACE('',(#5633),#29882,.F.);
#30794=ADVANCED_FACE('',(#5634),#4662,.F.);
#30795=ADVANCED_FACE('',(#5635),#29883,.F.);
#30796=ADVANCED_FACE('',(#5636),#29884,.F.);
#30797=ADVANCED_FACE('',(#5637),#4663,.F.);
#30798=ADVANCED_FACE('',(#5638),#29885,.F.);
#30799=ADVANCED_FACE('',(#5639),#29886,.F.);
#30800=ADVANCED_FACE('',(#5640),#4664,.F.);
#30801=ADVANCED_FACE('',(#5641),#29887,.F.);
#30802=ADVANCED_FACE('',(#5642),#29888,.F.);
#30803=ADVANCED_FACE('',(#5643),#4665,.F.);
#30804=ADVANCED_FACE('',(#5644),#29889,.F.);
#30805=ADVANCED_FACE('',(#5645),#29890,.F.);
#30806=ADVANCED_FACE('',(#5646),#4666,.F.);
#30807=ADVANCED_FACE('',(#5647),#29891,.F.);
#30808=ADVANCED_FACE('',(#5648),#29892,.F.);
#30809=ADVANCED_FACE('',(#5649),#4667,.F.);
#30810=ADVANCED_FACE('',(#5650),#29893,.F.);
#30811=ADVANCED_FACE('',(#5651),#29894,.F.);
#30812=ADVANCED_FACE('',(#5652),#4668,.F.);
#30813=ADVANCED_FACE('',(#5653),#29895,.F.);
#30814=ADVANCED_FACE('',(#5654),#29896,.F.);
#30815=ADVANCED_FACE('',(#5655),#4669,.F.);
#30816=ADVANCED_FACE('',(#5656),#29897,.F.);
#30817=ADVANCED_FACE('',(#5657),#29898,.F.);
#30818=ADVANCED_FACE('',(#5658),#4670,.F.);
#30819=ADVANCED_FACE('',(#5659),#29899,.F.);
#30820=ADVANCED_FACE('',(#5660),#29900,.F.);
#30821=ADVANCED_FACE('',(#5661),#4671,.F.);
#30822=ADVANCED_FACE('',(#5662),#29901,.F.);
#30823=ADVANCED_FACE('',(#5663),#29902,.F.);
#30824=ADVANCED_FACE('',(#5664),#4672,.F.);
#30825=ADVANCED_FACE('',(#5665),#29903,.F.);
#30826=ADVANCED_FACE('',(#5666),#29904,.F.);
#30827=ADVANCED_FACE('',(#5667),#4673,.F.);
#30828=ADVANCED_FACE('',(#5668),#29905,.F.);
#30829=ADVANCED_FACE('',(#5669),#29906,.F.);
#30830=ADVANCED_FACE('',(#5670),#4674,.F.);
#30831=ADVANCED_FACE('',(#5671),#29907,.F.);
#30832=ADVANCED_FACE('',(#5672),#29908,.F.);
#30833=ADVANCED_FACE('',(#5673),#4675,.F.);
#30834=ADVANCED_FACE('',(#5674),#29909,.F.);
#30835=ADVANCED_FACE('',(#5675),#29910,.F.);
#30836=ADVANCED_FACE('',(#5676),#4676,.F.);
#30837=ADVANCED_FACE('',(#5677),#29911,.F.);
#30838=ADVANCED_FACE('',(#5678),#29912,.F.);
#30839=ADVANCED_FACE('',(#5679),#4677,.F.);
#30840=ADVANCED_FACE('',(#5680),#29913,.F.);
#30841=ADVANCED_FACE('',(#5681),#29914,.F.);
#30842=ADVANCED_FACE('',(#5682),#4678,.F.);
#30843=ADVANCED_FACE('',(#5683),#29915,.F.);
#30844=ADVANCED_FACE('',(#5684),#29916,.F.);
#30845=ADVANCED_FACE('',(#5685),#4679,.F.);
#30846=ADVANCED_FACE('',(#5686),#29917,.F.);
#30847=ADVANCED_FACE('',(#5687),#29918,.F.);
#30848=ADVANCED_FACE('',(#5688),#4680,.F.);
#30849=ADVANCED_FACE('',(#5689),#29919,.F.);
#30850=ADVANCED_FACE('',(#5690),#29920,.F.);
#30851=ADVANCED_FACE('',(#5691),#4681,.F.);
#30852=ADVANCED_FACE('',(#5692),#29921,.F.);
#30853=ADVANCED_FACE('',(#5693),#29922,.F.);
#30854=ADVANCED_FACE('',(#5694),#4682,.F.);
#30855=ADVANCED_FACE('',(#5695),#29923,.F.);
#30856=ADVANCED_FACE('',(#5696),#29924,.F.);
#30857=ADVANCED_FACE('',(#5697),#4683,.F.);
#30858=ADVANCED_FACE('',(#5698),#29925,.F.);
#30859=ADVANCED_FACE('',(#5699),#29926,.F.);
#30860=ADVANCED_FACE('',(#5700),#4684,.F.);
#30861=ADVANCED_FACE('',(#5701),#29927,.F.);
#30862=ADVANCED_FACE('',(#5702),#29928,.F.);
#30863=ADVANCED_FACE('',(#5703),#4685,.F.);
#30864=ADVANCED_FACE('',(#5704),#29929,.F.);
#30865=ADVANCED_FACE('',(#5705),#29930,.F.);
#30866=ADVANCED_FACE('',(#5706),#4686,.F.);
#30867=ADVANCED_FACE('',(#5707),#29931,.F.);
#30868=ADVANCED_FACE('',(#5708),#29932,.F.);
#30869=ADVANCED_FACE('',(#5709),#4687,.F.);
#30870=ADVANCED_FACE('',(#5710),#29933,.F.);
#30871=ADVANCED_FACE('',(#5711),#29934,.F.);
#30872=ADVANCED_FACE('',(#5712),#4688,.F.);
#30873=ADVANCED_FACE('',(#5713),#29935,.F.);
#30874=ADVANCED_FACE('',(#5714),#29936,.F.);
#30875=ADVANCED_FACE('',(#5715),#4689,.F.);
#30876=ADVANCED_FACE('',(#5716),#29937,.F.);
#30877=ADVANCED_FACE('',(#5717),#29938,.F.);
#30878=ADVANCED_FACE('',(#5718),#4690,.F.);
#30879=ADVANCED_FACE('',(#5719),#29939,.F.);
#30880=ADVANCED_FACE('',(#5720),#29940,.F.);
#30881=ADVANCED_FACE('',(#5721),#4691,.F.);
#30882=ADVANCED_FACE('',(#5722),#29941,.F.);
#30883=ADVANCED_FACE('',(#5723),#29942,.F.);
#30884=ADVANCED_FACE('',(#5724),#29943,.F.);
#30885=ADVANCED_FACE('',(#5725),#29944,.F.);
#30886=ADVANCED_FACE('',(#5726),#29945,.F.);
#30887=ADVANCED_FACE('',(#5727),#29946,.F.);
#30888=ADVANCED_FACE('',(#5728),#29947,.F.);
#30889=ADVANCED_FACE('',(#5729),#29948,.F.);
#30890=ADVANCED_FACE('',(#5730),#29949,.F.);
#30891=ADVANCED_FACE('',(#5731),#29950,.F.);
#30892=ADVANCED_FACE('',(#5732),#29951,.F.);
#30893=ADVANCED_FACE('',(#5733),#29952,.F.);
#30894=ADVANCED_FACE('',(#5734),#29953,.F.);
#32026=CLOSED_SHELL('',(#30332,#30333,#30334,#30335,#30336,#30337,#30338,
#30339,#30340,#30341,#30342,#30343,#30344,#30345,#30346,#30347,#30348,#30349,
#30350,#30351,#30352,#30353,#30354,#30355,#30356,#30357,#30358,#30359,#30360,
#30361,#30362,#30363,#30364,#30365,#30366,#30367,#30368,#30369,#30370,#30371,
#30372,#30373,#30374,#30375,#30376,#30377,#30378,#30379,#30380,#30381,#30382,
#30383,#30384,#30385,#30386,#30387,#30388,#30389,#30390,#30391,#30392,#30393,
#30394,#30395,#30396,#30397,#30398,#30399,#30400,#30401,#30402,#30403,#30404,
#30405,#30406,#30407,#30408,#30409,#30410,#30411,#30412,#30413,#30414,#30415,
#30416,#30417,#30418,#30419,#30420,#30421,#30422,#30423,#30424,#30425,#30426,
#30427,#30428,#30429,#30430,#30431,#30432,#30433,#30434,#30435,#30436,#30437,
#30438,#30439,#30440,#30441,#30442,#30443,#30444,#30445,#30446,#30447,#30448,
#30449,#30450,#30451,#30452,#30453,#30454,#30455,#30456,#30457,#30458,#30459,
#30460,#30461,#30462,#30463,#30464,#30465,#30466,#30467,#30468,#30469,#30470,
#30471,#30472,#30473,#30474,#30475,#30476,#30477,#30478,#30479,#30480,#30481,
#30482,#30483,#30484,#30485,#30486,#30487,#30488,#30489,#30490,#30491,#30492,
#30493,#30494,#30495,#30496,#30497,#30498,#30499,#30500,#30501,#30502,#30503,
#30504,#30505,#30506,#30507,#30508,#30509,#30510,#30511,#30512,#30513,#30514,
#30515,#30516,#30517,#30518,#30519,#30520,#30521,#30522,#30523,#30524,#30525,
#30526,#30527,#30528,#30529,#30530,#30531,#30532,#30533,#30534,#30535,#30536,
#30537,#30538,#30539,#30540,#30541,#30542,#30543,#30544,#30545,#30546,#30547,
#30548,#30549,#30550,#30551,#30552,#30553,#30554,#30555,#30556,#30557,#30558,
#30559,#30560,#30561,#30562,#30563,#30564,#30565,#30566,#30567,#30568,#30569,
#30570,#30571,#30572,#30573,#30574,#30575,#30576,#30577,#30578,#30579,#30580,
#30581,#30582,#30583,#30584,#30585,#30586,#30587,#30588,#30589,#30590,#30591,
#30592,#30593,#30594,#30595,#30596,#30597,#30598,#30599,#30600,#30601,#30602,
#30603,#30604,#30605,#30606,#30607,#30608,#30609,#30610,#30611,#30612,#30613,
#30614,#30615,#30616,#30617,#30618,#30619,#30620,#30621,#30622,#30623,#30624,
#30625,#30626,#30627,#30628,#30629,#30630,#30631,#30632,#30633,#30634,#30635,
#30636,#30637,#30638,#30639,#30640,#30641,#30642,#30643,#30644,#30645,#30646,
#30647,#30648,#30649,#30650,#30651,#30652,#30653,#30654,#30655,#30656,#30657,
#30658,#30659,#30660,#30661,#30662,#30663,#30664,#30665,#30666,#30667,#30668,
#30669,#30670,#30671,#30672,#30673,#30674,#30675,#30676,#30677,#30678,#30679,
#30680,#30681,#30682,#30683,#30684,#30685,#30686,#30687,#30688,#30689,#30690,
#30691,#30692,#30693,#30694,#30695,#30696,#30697,#30698,#30699,#30700,#30701,
#30702,#30703,#30704,#30705,#30706,#30707,#30708,#30709,#30710,#30711,#30712,
#30713,#30714,#30715,#30716,#30717,#30718,#30719,#30720,#30721,#30722,#30723,
#30724,#30725,#30726,#30727,#30728,#30729,#30730,#30731,#30732,#30733,#30734,
#30735,#30736,#30737,#30738,#30739,#30740,#30741,#30742,#30743,#30744,#30745,
#30746,#30747,#30748,#30749,#30750,#30751,#30752,#30753,#30754,#30755,#30756,
#30757,#30758,#30759,#30760,#30761,#30762,#30763,#30764,#30765,#30766,#30767,
#30768,#30769,#30770,#30771,#30772,#30773,#30774,#30775,#30776,#30777,#30778,
#30779,#30780,#30781,#30782,#30783,#30784,#30785,#30786,#30787,#30788,#30789,
#30790,#30791,#30792,#30793,#30794,#30795,#30796,#30797,#30798,#30799,#30800,
#30801,#30802,#30803,#30804,#30805,#30806,#30807,#30808,#30809,#30810,#30811,
#30812,#30813,#30814,#30815,#30816,#30817,#30818,#30819,#30820,#30821,#30822,
#30823,#30824,#30825,#30826,#30827,#30828,#30829,#30830,#30831,#30832,#30833,
#30834,#30835,#30836,#30837,#30838,#30839,#30840,#30841,#30842,#30843,#30844,
#30845,#30846,#30847,#30848,#30849,#30850,#30851,#30852,#30853,#30854,#30855,
#30856,#30857,#30858,#30859,#30860,#30861,#30862,#30863,#30864,#30865,#30866,
#30867,#30868,#30869,#30870,#30871,#30872,#30873,#30874,#30875,#30876,#30877,
#30878,#30879,#30880,#30881,#30882,#30883,#30884,#30885,#30886,#30887,#30888,
#30889,#30890,#30891,#30892,#30893,#30894));
#32197=AXIS2_PLACEMENT_3D('',#46242,#36558,#36559);
#32198=AXIS2_PLACEMENT_3D('',#46243,#36560,#36561);
#32199=AXIS2_PLACEMENT_3D('',#46286,#36564,#36565);
#32200=AXIS2_PLACEMENT_3D('',#46288,#36566,#36567);
#32201=AXIS2_PLACEMENT_3D('',#46323,#36568,#36569);
#32202=AXIS2_PLACEMENT_3D('',#46399,#36571,#36572);
#32203=AXIS2_PLACEMENT_3D('',#46477,#36574,#36575);
#32204=AXIS2_PLACEMENT_3D('',#46553,#36577,#36578);
#32205=AXIS2_PLACEMENT_3D('',#46629,#36580,#36581);
#32206=AXIS2_PLACEMENT_3D('',#46705,#36583,#36584);
#32207=AXIS2_PLACEMENT_3D('',#46781,#36586,#36587);
#32208=AXIS2_PLACEMENT_3D('',#46859,#36589,#36590);
#32209=AXIS2_PLACEMENT_3D('',#46937,#36592,#36593);
#32210=AXIS2_PLACEMENT_3D('',#47013,#36595,#36596);
#32211=AXIS2_PLACEMENT_3D('',#47089,#36598,#36599);
#32212=AXIS2_PLACEMENT_3D('',#47165,#36601,#36602);
#32213=AXIS2_PLACEMENT_3D('',#47241,#36604,#36605);
#32214=AXIS2_PLACEMENT_3D('',#47319,#36607,#36608);
#32215=AXIS2_PLACEMENT_3D('',#47395,#36610,#36611);
#32216=AXIS2_PLACEMENT_3D('',#47473,#36613,#36614);
#32217=AXIS2_PLACEMENT_3D('',#47549,#36616,#36617);
#32218=AXIS2_PLACEMENT_3D('',#47625,#36619,#36620);
#32219=AXIS2_PLACEMENT_3D('',#47701,#36622,#36623);
#32220=AXIS2_PLACEMENT_3D('',#47777,#36625,#36626);
#32221=AXIS2_PLACEMENT_3D('',#47855,#36628,#36629);
#32222=AXIS2_PLACEMENT_3D('',#47933,#36631,#36632);
#32223=AXIS2_PLACEMENT_3D('',#48009,#36634,#36635);
#32224=AXIS2_PLACEMENT_3D('',#48085,#36637,#36638);
#32225=AXIS2_PLACEMENT_3D('',#48161,#36640,#36641);
#32226=AXIS2_PLACEMENT_3D('',#48237,#36643,#36644);
#32227=AXIS2_PLACEMENT_3D('',#48315,#36646,#36647);
#32228=AXIS2_PLACEMENT_3D('',#48391,#36649,#36650);
#32229=AXIS2_PLACEMENT_3D('',#48416,#36652,#36653);
#32230=AXIS2_PLACEMENT_3D('',#48417,#36654,#36655);
#32231=AXIS2_PLACEMENT_3D('',#48429,#36657,#36658);
#32232=AXIS2_PLACEMENT_3D('',#48430,#36659,#36660);
#32233=AXIS2_PLACEMENT_3D('',#48506,#36662,#36663);
#32234=AXIS2_PLACEMENT_3D('',#48582,#36665,#36666);
#32235=AXIS2_PLACEMENT_3D('',#48660,#36668,#36669);
#32236=AXIS2_PLACEMENT_3D('',#48736,#36671,#36672);
#32237=AXIS2_PLACEMENT_3D('',#48814,#36674,#36675);
#32238=AXIS2_PLACEMENT_3D('',#48890,#36677,#36678);
#32239=AXIS2_PLACEMENT_3D('',#48966,#36680,#36681);
#32240=AXIS2_PLACEMENT_3D('',#49042,#36683,#36684);
#32241=AXIS2_PLACEMENT_3D('',#49118,#36686,#36687);
#32242=AXIS2_PLACEMENT_3D('',#49196,#36689,#36690);
#32243=AXIS2_PLACEMENT_3D('',#49272,#36692,#36693);
#32244=AXIS2_PLACEMENT_3D('',#49350,#36695,#36696);
#32245=AXIS2_PLACEMENT_3D('',#49426,#36698,#36699);
#32246=AXIS2_PLACEMENT_3D('',#49502,#36701,#36702);
#32247=AXIS2_PLACEMENT_3D('',#49578,#36704,#36705);
#32248=AXIS2_PLACEMENT_3D('',#49654,#36707,#36708);
#32249=AXIS2_PLACEMENT_3D('',#49730,#36710,#36711);
#32250=AXIS2_PLACEMENT_3D('',#49808,#36713,#36714);
#32251=AXIS2_PLACEMENT_3D('',#49884,#36716,#36717);
#32252=AXIS2_PLACEMENT_3D('',#49962,#36719,#36720);
#32253=AXIS2_PLACEMENT_3D('',#50038,#36722,#36723);
#32254=AXIS2_PLACEMENT_3D('',#50114,#36725,#36726);
#32255=AXIS2_PLACEMENT_3D('',#50190,#36728,#36729);
#32256=AXIS2_PLACEMENT_3D('',#50266,#36731,#36732);
#32257=AXIS2_PLACEMENT_3D('',#50344,#36734,#36735);
#32258=AXIS2_PLACEMENT_3D('',#50420,#36737,#36738);
#32259=AXIS2_PLACEMENT_3D('',#50498,#36740,#36741);
#32260=AXIS2_PLACEMENT_3D('',#50574,#36743,#36744);
#32261=AXIS2_PLACEMENT_3D('',#50650,#36746,#36747);
#32262=AXIS2_PLACEMENT_3D('',#50660,#36748,#36749);
#32263=AXIS2_PLACEMENT_3D('',#50661,#36750,#36751);
#32264=AXIS2_PLACEMENT_3D('',#50662,#36752,#36753);
#32265=AXIS2_PLACEMENT_3D('',#50677,#36754,#36755);
#32266=AXIS2_PLACEMENT_3D('',#50700,#36756,#36757);
#32267=AXIS2_PLACEMENT_3D('',#50767,#36758,#36759);
#32268=AXIS2_PLACEMENT_3D('',#50770,#36760,#36761);
#32269=AXIS2_PLACEMENT_3D('',#50774,#36763,#36764);
#32270=AXIS2_PLACEMENT_3D('',#50776,#36766,#36767);
#32271=AXIS2_PLACEMENT_3D('',#50779,#36768,#36769);
#32272=AXIS2_PLACEMENT_3D('',#50783,#36771,#36772);
#32273=AXIS2_PLACEMENT_3D('',#50785,#36774,#36775);
#32274=AXIS2_PLACEMENT_3D('',#50788,#36776,#36777);
#32275=AXIS2_PLACEMENT_3D('',#50792,#36779,#36780);
#32276=AXIS2_PLACEMENT_3D('',#50794,#36782,#36783);
#32277=AXIS2_PLACEMENT_3D('',#50797,#36784,#36785);
#32278=AXIS2_PLACEMENT_3D('',#50801,#36787,#36788);
#32279=AXIS2_PLACEMENT_3D('',#50803,#36790,#36791);
#32280=AXIS2_PLACEMENT_3D('',#50806,#36792,#36793);
#32281=AXIS2_PLACEMENT_3D('',#50810,#36795,#36796);
#32282=AXIS2_PLACEMENT_3D('',#50812,#36798,#36799);
#32283=AXIS2_PLACEMENT_3D('',#50815,#36800,#36801);
#32284=AXIS2_PLACEMENT_3D('',#50819,#36803,#36804);
#32285=AXIS2_PLACEMENT_3D('',#50821,#36806,#36807);
#32286=AXIS2_PLACEMENT_3D('',#50824,#36808,#36809);
#32287=AXIS2_PLACEMENT_3D('',#50828,#36811,#36812);
#32288=AXIS2_PLACEMENT_3D('',#50830,#36814,#36815);
#32289=AXIS2_PLACEMENT_3D('',#50833,#36816,#36817);
#32290=AXIS2_PLACEMENT_3D('',#50837,#36819,#36820);
#32291=AXIS2_PLACEMENT_3D('',#50839,#36822,#36823);
#32292=AXIS2_PLACEMENT_3D('',#50842,#36824,#36825);
#32293=AXIS2_PLACEMENT_3D('',#50846,#36827,#36828);
#32294=AXIS2_PLACEMENT_3D('',#50848,#36830,#36831);
#32295=AXIS2_PLACEMENT_3D('',#50851,#36832,#36833);
#32296=AXIS2_PLACEMENT_3D('',#50855,#36835,#36836);
#32297=AXIS2_PLACEMENT_3D('',#50857,#36838,#36839);
#32298=AXIS2_PLACEMENT_3D('',#50860,#36840,#36841);
#32299=AXIS2_PLACEMENT_3D('',#50864,#36843,#36844);
#32300=AXIS2_PLACEMENT_3D('',#50866,#36846,#36847);
#32301=AXIS2_PLACEMENT_3D('',#50869,#36848,#36849);
#32302=AXIS2_PLACEMENT_3D('',#50873,#36851,#36852);
#32303=AXIS2_PLACEMENT_3D('',#50875,#36854,#36855);
#32304=AXIS2_PLACEMENT_3D('',#50878,#36856,#36857);
#32305=AXIS2_PLACEMENT_3D('',#50882,#36859,#36860);
#32306=AXIS2_PLACEMENT_3D('',#50884,#36862,#36863);
#32307=AXIS2_PLACEMENT_3D('',#50887,#36864,#36865);
#32308=AXIS2_PLACEMENT_3D('',#50891,#36867,#36868);
#32309=AXIS2_PLACEMENT_3D('',#50893,#36870,#36871);
#32310=AXIS2_PLACEMENT_3D('',#50896,#36872,#36873);
#32311=AXIS2_PLACEMENT_3D('',#50900,#36875,#36876);
#32312=AXIS2_PLACEMENT_3D('',#50902,#36878,#36879);
#32313=AXIS2_PLACEMENT_3D('',#50933,#36881,#36882);
#32314=AXIS2_PLACEMENT_3D('',#50934,#36883,#36884);
#32315=AXIS2_PLACEMENT_3D('',#50936,#36885,#36886);
#32316=AXIS2_PLACEMENT_3D('',#50938,#36887,#36888);
#32317=AXIS2_PLACEMENT_3D('',#50939,#36889,#36890);
#32318=AXIS2_PLACEMENT_3D('',#50940,#36891,#36892);
#32319=AXIS2_PLACEMENT_3D('',#50956,#36893,#36894);
#32320=AXIS2_PLACEMENT_3D('',#50962,#36895,#36896);
#32321=AXIS2_PLACEMENT_3D('',#50968,#36897,#36898);
#32322=AXIS2_PLACEMENT_3D('',#50974,#36899,#36900);
#32323=AXIS2_PLACEMENT_3D('',#50980,#36901,#36902);
#32324=AXIS2_PLACEMENT_3D('',#50986,#36903,#36904);
#32325=AXIS2_PLACEMENT_3D('',#50992,#36905,#36906);
#32326=AXIS2_PLACEMENT_3D('',#50998,#36907,#36908);
#32327=AXIS2_PLACEMENT_3D('',#51004,#36909,#36910);
#32328=AXIS2_PLACEMENT_3D('',#51010,#36911,#36912);
#32329=AXIS2_PLACEMENT_3D('',#51016,#36913,#36914);
#32330=AXIS2_PLACEMENT_3D('',#51022,#36915,#36916);
#32331=AXIS2_PLACEMENT_3D('',#51028,#36917,#36918);
#32332=AXIS2_PLACEMENT_3D('',#51034,#36919,#36920);
#32333=AXIS2_PLACEMENT_3D('',#51040,#36921,#36922);
#32334=AXIS2_PLACEMENT_3D('',#51046,#36923,#36924);
#32335=AXIS2_PLACEMENT_3D('',#51052,#36925,#36926);
#32336=AXIS2_PLACEMENT_3D('',#51058,#36927,#36928);
#32337=AXIS2_PLACEMENT_3D('',#51064,#36929,#36930);
#32338=AXIS2_PLACEMENT_3D('',#51070,#36931,#36932);
#32339=AXIS2_PLACEMENT_3D('',#51076,#36933,#36934);
#32340=AXIS2_PLACEMENT_3D('',#51082,#36935,#36936);
#32341=AXIS2_PLACEMENT_3D('',#51088,#36937,#36938);
#32342=AXIS2_PLACEMENT_3D('',#51094,#36939,#36940);
#32343=AXIS2_PLACEMENT_3D('',#51100,#36941,#36942);
#32344=AXIS2_PLACEMENT_3D('',#51106,#36943,#36944);
#32345=AXIS2_PLACEMENT_3D('',#51112,#36945,#36946);
#32346=AXIS2_PLACEMENT_3D('',#51118,#36947,#36948);
#32347=AXIS2_PLACEMENT_3D('',#51124,#36949,#36950);
#32348=AXIS2_PLACEMENT_3D('',#51130,#36951,#36952);
#32349=AXIS2_PLACEMENT_3D('',#51136,#36953,#36954);
#32350=AXIS2_PLACEMENT_3D('',#51142,#36955,#36956);
#32351=AXIS2_PLACEMENT_3D('',#51148,#36957,#36958);
#32352=AXIS2_PLACEMENT_3D('',#51154,#36959,#36960);
#32353=AXIS2_PLACEMENT_3D('',#51160,#36961,#36962);
#32354=AXIS2_PLACEMENT_3D('',#51166,#36963,#36964);
#32355=AXIS2_PLACEMENT_3D('',#51172,#36965,#36966);
#32356=AXIS2_PLACEMENT_3D('',#51178,#36967,#36968);
#32357=AXIS2_PLACEMENT_3D('',#51184,#36969,#36970);
#32358=AXIS2_PLACEMENT_3D('',#51190,#36971,#36972);
#32359=AXIS2_PLACEMENT_3D('',#51196,#36973,#36974);
#32360=AXIS2_PLACEMENT_3D('',#51202,#36975,#36976);
#32361=AXIS2_PLACEMENT_3D('',#51208,#36977,#36978);
#32362=AXIS2_PLACEMENT_3D('',#51214,#36979,#36980);
#32363=AXIS2_PLACEMENT_3D('',#51220,#36981,#36982);
#32364=AXIS2_PLACEMENT_3D('',#51226,#36983,#36984);
#32365=AXIS2_PLACEMENT_3D('',#51232,#36985,#36986);
#32366=AXIS2_PLACEMENT_3D('',#51238,#36987,#36988);
#32367=AXIS2_PLACEMENT_3D('',#51244,#36989,#36990);
#32368=AXIS2_PLACEMENT_3D('',#51250,#36991,#36992);
#32369=AXIS2_PLACEMENT_3D('',#51256,#36993,#36994);
#32370=AXIS2_PLACEMENT_3D('',#51262,#36995,#36996);
#32371=AXIS2_PLACEMENT_3D('',#51268,#36997,#36998);
#32372=AXIS2_PLACEMENT_3D('',#51274,#36999,#37000);
#32373=AXIS2_PLACEMENT_3D('',#51280,#37001,#37002);
#32374=AXIS2_PLACEMENT_3D('',#51286,#37003,#37004);
#32375=AXIS2_PLACEMENT_3D('',#51292,#37005,#37006);
#32376=AXIS2_PLACEMENT_3D('',#51298,#37007,#37008);
#32377=AXIS2_PLACEMENT_3D('',#51304,#37009,#37010);
#32378=AXIS2_PLACEMENT_3D('',#51310,#37011,#37012);
#32379=AXIS2_PLACEMENT_3D('',#51316,#37013,#37014);
#32380=AXIS2_PLACEMENT_3D('',#51322,#37015,#37016);
#32381=AXIS2_PLACEMENT_3D('',#51328,#37017,#37018);
#32382=AXIS2_PLACEMENT_3D('',#51334,#37019,#37020);
#32383=AXIS2_PLACEMENT_3D('',#51340,#37021,#37022);
#32384=AXIS2_PLACEMENT_3D('',#51346,#37023,#37024);
#32385=AXIS2_PLACEMENT_3D('',#51352,#37025,#37026);
#32386=AXIS2_PLACEMENT_3D('',#51358,#37027,#37028);
#32387=AXIS2_PLACEMENT_3D('',#51364,#37029,#37030);
#32388=AXIS2_PLACEMENT_3D('',#51370,#37031,#37032);
#32389=AXIS2_PLACEMENT_3D('',#51376,#37033,#37034);
#32390=AXIS2_PLACEMENT_3D('',#51382,#37035,#37036);
#32391=AXIS2_PLACEMENT_3D('',#51388,#37037,#37038);
#32392=AXIS2_PLACEMENT_3D('',#51394,#37039,#37040);
#32393=AXIS2_PLACEMENT_3D('',#51400,#37041,#37042);
#32394=AXIS2_PLACEMENT_3D('',#51406,#37043,#37044);
#32395=AXIS2_PLACEMENT_3D('',#51412,#37045,#37046);
#32396=AXIS2_PLACEMENT_3D('',#51418,#37047,#37048);
#32397=AXIS2_PLACEMENT_3D('',#51424,#37049,#37050);
#32398=AXIS2_PLACEMENT_3D('',#51430,#37051,#37052);
#32399=AXIS2_PLACEMENT_3D('',#51436,#37053,#37054);
#32400=AXIS2_PLACEMENT_3D('',#51442,#37055,#37056);
#32401=AXIS2_PLACEMENT_3D('',#51448,#37057,#37058);
#32402=AXIS2_PLACEMENT_3D('',#51454,#37059,#37060);
#32403=AXIS2_PLACEMENT_3D('',#51460,#37061,#37062);
#32404=AXIS2_PLACEMENT_3D('',#51466,#37063,#37064);
#32405=AXIS2_PLACEMENT_3D('',#51472,#37065,#37066);
#32406=AXIS2_PLACEMENT_3D('',#51478,#37067,#37068);
#32407=AXIS2_PLACEMENT_3D('',#51484,#37069,#37070);
#32408=AXIS2_PLACEMENT_3D('',#51490,#37071,#37072);
#32409=AXIS2_PLACEMENT_3D('',#51496,#37073,#37074);
#32410=AXIS2_PLACEMENT_3D('',#51505,#37075,#37076);
#32411=AXIS2_PLACEMENT_3D('',#51514,#37077,#37078);
#32412=AXIS2_PLACEMENT_3D('',#51523,#37079,#37080);
#32413=AXIS2_PLACEMENT_3D('',#51532,#37081,#37082);
#32414=AXIS2_PLACEMENT_3D('',#51541,#37083,#37084);
#32415=AXIS2_PLACEMENT_3D('',#51550,#37085,#37086);
#32416=AXIS2_PLACEMENT_3D('',#51559,#37087,#37088);
#32417=AXIS2_PLACEMENT_3D('',#51568,#37089,#37090);
#32418=AXIS2_PLACEMENT_3D('',#51577,#37091,#37092);
#32419=AXIS2_PLACEMENT_3D('',#51586,#37093,#37094);
#32420=AXIS2_PLACEMENT_3D('',#51595,#37095,#37096);
#32421=AXIS2_PLACEMENT_3D('',#51604,#37097,#37098);
#32422=AXIS2_PLACEMENT_3D('',#51613,#37099,#37100);
#32423=AXIS2_PLACEMENT_3D('',#51622,#37101,#37102);
#32424=AXIS2_PLACEMENT_3D('',#51631,#37103,#37104);
#32425=AXIS2_PLACEMENT_3D('',#51637,#37105,#37106);
#32426=AXIS2_PLACEMENT_3D('',#51643,#37107,#37108);
#32427=AXIS2_PLACEMENT_3D('',#51649,#37109,#37110);
#32428=AXIS2_PLACEMENT_3D('',#51655,#37111,#37112);
#32429=AXIS2_PLACEMENT_3D('',#51661,#37113,#37114);
#32430=AXIS2_PLACEMENT_3D('',#51667,#37115,#37116);
#32431=AXIS2_PLACEMENT_3D('',#51673,#37117,#37118);
#32432=AXIS2_PLACEMENT_3D('',#51679,#37119,#37120);
#32433=AXIS2_PLACEMENT_3D('',#51685,#37121,#37122);
#32434=AXIS2_PLACEMENT_3D('',#51691,#37123,#37124);
#32435=AXIS2_PLACEMENT_3D('',#51697,#37125,#37126);
#32436=AXIS2_PLACEMENT_3D('',#51703,#37127,#37128);
#32437=AXIS2_PLACEMENT_3D('',#51709,#37129,#37130);
#32438=AXIS2_PLACEMENT_3D('',#51715,#37131,#37132);
#32439=AXIS2_PLACEMENT_3D('',#51721,#37133,#37134);
#32440=AXIS2_PLACEMENT_3D('',#51727,#37135,#37136);
#32441=AXIS2_PLACEMENT_3D('',#51733,#37137,#37138);
#32442=AXIS2_PLACEMENT_3D('',#51739,#37139,#37140);
#32443=AXIS2_PLACEMENT_3D('',#51745,#37141,#37142);
#32444=AXIS2_PLACEMENT_3D('',#51751,#37143,#37144);
#32445=AXIS2_PLACEMENT_3D('',#51757,#37145,#37146);
#32446=AXIS2_PLACEMENT_3D('',#51763,#37147,#37148);
#32447=AXIS2_PLACEMENT_3D('',#51769,#37149,#37150);
#32448=AXIS2_PLACEMENT_3D('',#51775,#37151,#37152);
#32449=AXIS2_PLACEMENT_3D('',#51781,#37153,#37154);
#32450=AXIS2_PLACEMENT_3D('',#51787,#37155,#37156);
#32451=AXIS2_PLACEMENT_3D('',#51793,#37157,#37158);
#32452=AXIS2_PLACEMENT_3D('',#51799,#37159,#37160);
#32453=AXIS2_PLACEMENT_3D('',#51805,#37161,#37162);
#32454=AXIS2_PLACEMENT_3D('',#51811,#37163,#37164);
#32455=AXIS2_PLACEMENT_3D('',#51817,#37165,#37166);
#32456=AXIS2_PLACEMENT_3D('',#51823,#37167,#37168);
#32457=AXIS2_PLACEMENT_3D('',#51829,#37169,#37170);
#32458=AXIS2_PLACEMENT_3D('',#51835,#37171,#37172);
#32459=AXIS2_PLACEMENT_3D('',#51841,#37173,#37174);
#32460=AXIS2_PLACEMENT_3D('',#51847,#37175,#37176);
#32461=AXIS2_PLACEMENT_3D('',#51853,#37177,#37178);
#32462=AXIS2_PLACEMENT_3D('',#51859,#37179,#37180);
#32463=AXIS2_PLACEMENT_3D('',#51873,#37182,#37183);
#32464=AXIS2_PLACEMENT_3D('',#51889,#37184,#37185);
#32465=AXIS2_PLACEMENT_3D('',#51895,#37186,#37187);
#32466=AXIS2_PLACEMENT_3D('',#51901,#37188,#37189);
#32467=AXIS2_PLACEMENT_3D('',#51907,#37190,#37191);
#32468=AXIS2_PLACEMENT_3D('',#51913,#37192,#37193);
#32469=AXIS2_PLACEMENT_3D('',#51919,#37194,#37195);
#32470=AXIS2_PLACEMENT_3D('',#51925,#37196,#37197);
#32471=AXIS2_PLACEMENT_3D('',#51931,#37198,#37199);
#32472=AXIS2_PLACEMENT_3D('',#51937,#37200,#37201);
#32473=AXIS2_PLACEMENT_3D('',#51943,#37202,#37203);
#32474=AXIS2_PLACEMENT_3D('',#51949,#37204,#37205);
#32475=AXIS2_PLACEMENT_3D('',#51955,#37206,#37207);
#32476=AXIS2_PLACEMENT_3D('',#51961,#37208,#37209);
#32477=AXIS2_PLACEMENT_3D('',#51967,#37210,#37211);
#32478=AXIS2_PLACEMENT_3D('',#51973,#37212,#37213);
#32479=AXIS2_PLACEMENT_3D('',#51979,#37214,#37215);
#32480=AXIS2_PLACEMENT_3D('',#51985,#37216,#37217);
#32481=AXIS2_PLACEMENT_3D('',#51991,#37218,#37219);
#32482=AXIS2_PLACEMENT_3D('',#51997,#37220,#37221);
#32483=AXIS2_PLACEMENT_3D('',#52003,#37222,#37223);
#32484=AXIS2_PLACEMENT_3D('',#52009,#37224,#37225);
#32485=AXIS2_PLACEMENT_3D('',#52015,#37226,#37227);
#32486=AXIS2_PLACEMENT_3D('',#52021,#37228,#37229);
#32487=AXIS2_PLACEMENT_3D('',#52027,#37230,#37231);
#32488=AXIS2_PLACEMENT_3D('',#52033,#37232,#37233);
#32489=AXIS2_PLACEMENT_3D('',#52039,#37234,#37235);
#32490=AXIS2_PLACEMENT_3D('',#52045,#37236,#37237);
#32491=AXIS2_PLACEMENT_3D('',#52051,#37238,#37239);
#32492=AXIS2_PLACEMENT_3D('',#52057,#37240,#37241);
#32493=AXIS2_PLACEMENT_3D('',#52063,#37242,#37243);
#32494=AXIS2_PLACEMENT_3D('',#52069,#37244,#37245);
#32495=AXIS2_PLACEMENT_3D('',#52075,#37246,#37247);
#32496=AXIS2_PLACEMENT_3D('',#52081,#37248,#37249);
#32497=AXIS2_PLACEMENT_3D('',#52087,#37250,#37251);
#32498=AXIS2_PLACEMENT_3D('',#52093,#37252,#37253);
#32499=AXIS2_PLACEMENT_3D('',#52099,#37254,#37255);
#32500=AXIS2_PLACEMENT_3D('',#52105,#37256,#37257);
#32501=AXIS2_PLACEMENT_3D('',#52111,#37258,#37259);
#32502=AXIS2_PLACEMENT_3D('',#52117,#37260,#37261);
#32503=AXIS2_PLACEMENT_3D('',#52123,#37262,#37263);
#32504=AXIS2_PLACEMENT_3D('',#52129,#37264,#37265);
#32505=AXIS2_PLACEMENT_3D('',#52135,#37266,#37267);
#32506=AXIS2_PLACEMENT_3D('',#52141,#37268,#37269);
#32507=AXIS2_PLACEMENT_3D('',#52147,#37270,#37271);
#32508=AXIS2_PLACEMENT_3D('',#52153,#37272,#37273);
#32509=AXIS2_PLACEMENT_3D('',#52159,#37274,#37275);
#32510=AXIS2_PLACEMENT_3D('',#52165,#37276,#37277);
#32511=AXIS2_PLACEMENT_3D('',#52171,#37278,#37279);
#32512=AXIS2_PLACEMENT_3D('',#52177,#37280,#37281);
#32513=AXIS2_PLACEMENT_3D('',#52183,#37282,#37283);
#32514=AXIS2_PLACEMENT_3D('',#52189,#37284,#37285);
#32515=AXIS2_PLACEMENT_3D('',#52195,#37286,#37287);
#32516=AXIS2_PLACEMENT_3D('',#52201,#37288,#37289);
#32517=AXIS2_PLACEMENT_3D('',#52207,#37290,#37291);
#32518=AXIS2_PLACEMENT_3D('',#52213,#37292,#37293);
#32519=AXIS2_PLACEMENT_3D('',#52219,#37294,#37295);
#32520=AXIS2_PLACEMENT_3D('',#52225,#37296,#37297);
#32521=AXIS2_PLACEMENT_3D('',#52231,#37298,#37299);
#32522=AXIS2_PLACEMENT_3D('',#52237,#37300,#37301);
#32523=AXIS2_PLACEMENT_3D('',#52243,#37302,#37303);
#32524=AXIS2_PLACEMENT_3D('',#52249,#37304,#37305);
#32525=AXIS2_PLACEMENT_3D('',#52255,#37306,#37307);
#32526=AXIS2_PLACEMENT_3D('',#52261,#37308,#37309);
#32527=AXIS2_PLACEMENT_3D('',#52267,#37310,#37311);
#32528=AXIS2_PLACEMENT_3D('',#52273,#37312,#37313);
#32529=AXIS2_PLACEMENT_3D('',#52279,#37314,#37315);
#32530=AXIS2_PLACEMENT_3D('',#52285,#37316,#37317);
#32531=AXIS2_PLACEMENT_3D('',#52291,#37318,#37319);
#32532=AXIS2_PLACEMENT_3D('',#52297,#37320,#37321);
#32533=AXIS2_PLACEMENT_3D('',#52303,#37322,#37323);
#32534=AXIS2_PLACEMENT_3D('',#52309,#37324,#37325);
#32535=AXIS2_PLACEMENT_3D('',#52315,#37326,#37327);
#32536=AXIS2_PLACEMENT_3D('',#52321,#37328,#37329);
#32537=AXIS2_PLACEMENT_3D('',#52327,#37330,#37331);
#32538=AXIS2_PLACEMENT_3D('',#52333,#37332,#37333);
#32539=AXIS2_PLACEMENT_3D('',#52339,#37334,#37335);
#32540=AXIS2_PLACEMENT_3D('',#52345,#37336,#37337);
#32541=AXIS2_PLACEMENT_3D('',#52351,#37338,#37339);
#32542=AXIS2_PLACEMENT_3D('',#52357,#37340,#37341);
#32543=AXIS2_PLACEMENT_3D('',#52363,#37342,#37343);
#32544=AXIS2_PLACEMENT_3D('',#52369,#37344,#37345);
#32545=AXIS2_PLACEMENT_3D('',#52375,#37346,#37347);
#32546=AXIS2_PLACEMENT_3D('',#52381,#37348,#37349);
#32547=AXIS2_PLACEMENT_3D('',#52387,#37350,#37351);
#32548=AXIS2_PLACEMENT_3D('',#52393,#37352,#37353);
#32549=AXIS2_PLACEMENT_3D('',#52399,#37354,#37355);
#32550=AXIS2_PLACEMENT_3D('',#52405,#37356,#37357);
#32551=AXIS2_PLACEMENT_3D('',#52411,#37358,#37359);
#32552=AXIS2_PLACEMENT_3D('',#52417,#37360,#37361);
#32553=AXIS2_PLACEMENT_3D('',#52423,#37362,#37363);
#32554=AXIS2_PLACEMENT_3D('',#52429,#37364,#37365);
#32555=AXIS2_PLACEMENT_3D('',#52435,#37366,#37367);
#32556=AXIS2_PLACEMENT_3D('',#52441,#37368,#37369);
#32557=AXIS2_PLACEMENT_3D('',#52447,#37370,#37371);
#32558=AXIS2_PLACEMENT_3D('',#52453,#37372,#37373);
#32559=AXIS2_PLACEMENT_3D('',#52459,#37374,#37375);
#32560=AXIS2_PLACEMENT_3D('',#52465,#37376,#37377);
#32561=AXIS2_PLACEMENT_3D('',#52471,#37378,#37379);
#32562=AXIS2_PLACEMENT_3D('',#52477,#37380,#37381);
#32563=AXIS2_PLACEMENT_3D('',#52483,#37382,#37383);
#32564=AXIS2_PLACEMENT_3D('',#52489,#37384,#37385);
#32565=AXIS2_PLACEMENT_3D('',#52495,#37386,#37387);
#32566=AXIS2_PLACEMENT_3D('',#52501,#37388,#37389);
#32567=AXIS2_PLACEMENT_3D('',#52507,#37390,#37391);
#32568=AXIS2_PLACEMENT_3D('',#52513,#37392,#37393);
#32569=AXIS2_PLACEMENT_3D('',#52519,#37394,#37395);
#32570=AXIS2_PLACEMENT_3D('',#52525,#37396,#37397);
#32571=AXIS2_PLACEMENT_3D('',#52531,#37398,#37399);
#32572=AXIS2_PLACEMENT_3D('',#52537,#37400,#37401);
#32573=AXIS2_PLACEMENT_3D('',#52543,#37402,#37403);
#32574=AXIS2_PLACEMENT_3D('',#52549,#37404,#37405);
#32575=AXIS2_PLACEMENT_3D('',#52555,#37406,#37407);
#32576=AXIS2_PLACEMENT_3D('',#52561,#37408,#37409);
#32577=AXIS2_PLACEMENT_3D('',#52567,#37410,#37411);
#32578=AXIS2_PLACEMENT_3D('',#52573,#37412,#37413);
#32579=AXIS2_PLACEMENT_3D('',#52579,#37414,#37415);
#32580=AXIS2_PLACEMENT_3D('',#52585,#37416,#37417);
#32581=AXIS2_PLACEMENT_3D('',#52591,#37418,#37419);
#32582=AXIS2_PLACEMENT_3D('',#52597,#37420,#37421);
#32583=AXIS2_PLACEMENT_3D('',#52606,#37422,#37423);
#32584=AXIS2_PLACEMENT_3D('',#52615,#37424,#37425);
#32585=AXIS2_PLACEMENT_3D('',#52624,#37426,#37427);
#32586=AXIS2_PLACEMENT_3D('',#52633,#37428,#37429);
#32587=AXIS2_PLACEMENT_3D('',#52642,#37430,#37431);
#32588=AXIS2_PLACEMENT_3D('',#52651,#37432,#37433);
#32589=AXIS2_PLACEMENT_3D('',#52660,#37434,#37435);
#32590=AXIS2_PLACEMENT_3D('',#52669,#37436,#37437);
#32591=AXIS2_PLACEMENT_3D('',#52678,#37438,#37439);
#32592=AXIS2_PLACEMENT_3D('',#52687,#37440,#37441);
#32593=AXIS2_PLACEMENT_3D('',#52696,#37442,#37443);
#32594=AXIS2_PLACEMENT_3D('',#52705,#37444,#37445);
#32595=AXIS2_PLACEMENT_3D('',#52714,#37446,#37447);
#32596=AXIS2_PLACEMENT_3D('',#52723,#37448,#37449);
#32597=AXIS2_PLACEMENT_3D('',#52732,#37450,#37451);
#32598=AXIS2_PLACEMENT_3D('',#52738,#37452,#37453);
#32599=AXIS2_PLACEMENT_3D('',#52744,#37454,#37455);
#32600=AXIS2_PLACEMENT_3D('',#52750,#37456,#37457);
#32601=AXIS2_PLACEMENT_3D('',#52756,#37458,#37459);
#32602=AXIS2_PLACEMENT_3D('',#52762,#37460,#37461);
#32603=AXIS2_PLACEMENT_3D('',#52768,#37462,#37463);
#32604=AXIS2_PLACEMENT_3D('',#52774,#37464,#37465);
#32605=AXIS2_PLACEMENT_3D('',#52780,#37466,#37467);
#32606=AXIS2_PLACEMENT_3D('',#52786,#37468,#37469);
#32607=AXIS2_PLACEMENT_3D('',#52792,#37470,#37471);
#32608=AXIS2_PLACEMENT_3D('',#52808,#37473,#37474);
#32609=AXIS2_PLACEMENT_3D('',#52809,#37475,#37476);
#32610=AXIS2_PLACEMENT_3D('',#52810,#37477,#37478);
#32611=AXIS2_PLACEMENT_3D('',#52812,#37479,#37480);
#32612=AXIS2_PLACEMENT_3D('',#52813,#37481,#37482);
#32613=AXIS2_PLACEMENT_3D('',#52814,#37483,#37484);
#32614=AXIS2_PLACEMENT_3D('',#52816,#37485,#37486);
#32615=AXIS2_PLACEMENT_3D('',#52818,#37488,#37489);
#32616=AXIS2_PLACEMENT_3D('',#52820,#37490,#37491);
#32617=AXIS2_PLACEMENT_3D('',#52821,#37492,#37493);
#32618=AXIS2_PLACEMENT_3D('',#52822,#37494,#37495);
#32619=AXIS2_PLACEMENT_3D('',#52824,#37496,#37497);
#32620=AXIS2_PLACEMENT_3D('',#52825,#37498,#37499);
#32621=AXIS2_PLACEMENT_3D('',#52826,#37500,#37501);
#32622=AXIS2_PLACEMENT_3D('',#52828,#37502,#37503);
#32623=AXIS2_PLACEMENT_3D('',#52830,#37504,#37505);
#32624=AXIS2_PLACEMENT_3D('',#52831,#37506,#37507);
#32625=AXIS2_PLACEMENT_3D('',#52832,#37508,#37509);
#32626=AXIS2_PLACEMENT_3D('',#52834,#37510,#37511);
#32627=AXIS2_PLACEMENT_3D('',#52836,#37512,#37513);
#32628=AXIS2_PLACEMENT_3D('',#52837,#37514,#37515);
#32629=AXIS2_PLACEMENT_3D('',#52838,#37516,#37517);
#32630=AXIS2_PLACEMENT_3D('',#52840,#37518,#37519);
#32631=AXIS2_PLACEMENT_3D('',#52842,#37520,#37521);
#32632=AXIS2_PLACEMENT_3D('',#52843,#37522,#37523);
#32633=AXIS2_PLACEMENT_3D('',#52844,#37524,#37525);
#32634=AXIS2_PLACEMENT_3D('',#52846,#37526,#37527);
#32635=AXIS2_PLACEMENT_3D('',#52848,#37528,#37529);
#32636=AXIS2_PLACEMENT_3D('',#52849,#37530,#37531);
#32637=AXIS2_PLACEMENT_3D('',#52850,#37532,#37533);
#32638=AXIS2_PLACEMENT_3D('',#52852,#37534,#37535);
#32639=AXIS2_PLACEMENT_3D('',#52854,#37536,#37537);
#32640=AXIS2_PLACEMENT_3D('',#52855,#37538,#37539);
#32641=AXIS2_PLACEMENT_3D('',#52856,#37540,#37541);
#32642=AXIS2_PLACEMENT_3D('',#52858,#37542,#37543);
#32643=AXIS2_PLACEMENT_3D('',#52860,#37544,#37545);
#32644=AXIS2_PLACEMENT_3D('',#52861,#37546,#37547);
#32645=AXIS2_PLACEMENT_3D('',#52862,#37548,#37549);
#32646=AXIS2_PLACEMENT_3D('',#52864,#37550,#37551);
#32647=AXIS2_PLACEMENT_3D('',#52866,#37552,#37553);
#32648=AXIS2_PLACEMENT_3D('',#52867,#37554,#37555);
#32649=AXIS2_PLACEMENT_3D('',#52868,#37556,#37557);
#32650=AXIS2_PLACEMENT_3D('',#52870,#37558,#37559);
#32651=AXIS2_PLACEMENT_3D('',#52872,#37560,#37561);
#32652=AXIS2_PLACEMENT_3D('',#52873,#37562,#37563);
#32653=AXIS2_PLACEMENT_3D('',#52874,#37564,#37565);
#32654=AXIS2_PLACEMENT_3D('',#52876,#37566,#37567);
#32655=AXIS2_PLACEMENT_3D('',#52878,#37568,#37569);
#32656=AXIS2_PLACEMENT_3D('',#52879,#37570,#37571);
#32657=AXIS2_PLACEMENT_3D('',#52880,#37572,#37573);
#32658=AXIS2_PLACEMENT_3D('',#52882,#37574,#37575);
#32659=AXIS2_PLACEMENT_3D('',#52884,#37576,#37577);
#32660=AXIS2_PLACEMENT_3D('',#52885,#37578,#37579);
#32661=AXIS2_PLACEMENT_3D('',#52886,#37580,#37581);
#32662=AXIS2_PLACEMENT_3D('',#52888,#37582,#37583);
#32663=AXIS2_PLACEMENT_3D('',#52890,#37584,#37585);
#32664=AXIS2_PLACEMENT_3D('',#52891,#37586,#37587);
#32665=AXIS2_PLACEMENT_3D('',#52892,#37588,#37589);
#32666=AXIS2_PLACEMENT_3D('',#52894,#37590,#37591);
#32667=AXIS2_PLACEMENT_3D('',#52896,#37592,#37593);
#32668=AXIS2_PLACEMENT_3D('',#52897,#37594,#37595);
#32669=AXIS2_PLACEMENT_3D('',#52898,#37596,#37597);
#32670=AXIS2_PLACEMENT_3D('',#52900,#37598,#37599);
#32671=AXIS2_PLACEMENT_3D('',#52902,#37600,#37601);
#32672=AXIS2_PLACEMENT_3D('',#52903,#37602,#37603);
#32673=AXIS2_PLACEMENT_3D('',#52904,#37604,#37605);
#32674=AXIS2_PLACEMENT_3D('',#52906,#37606,#37607);
#32675=AXIS2_PLACEMENT_3D('',#52908,#37608,#37609);
#32676=AXIS2_PLACEMENT_3D('',#52909,#37610,#37611);
#32677=AXIS2_PLACEMENT_3D('',#52910,#37612,#37613);
#32678=AXIS2_PLACEMENT_3D('',#52912,#37614,#37615);
#32679=AXIS2_PLACEMENT_3D('',#52914,#37616,#37617);
#32680=AXIS2_PLACEMENT_3D('',#52915,#37618,#37619);
#32681=AXIS2_PLACEMENT_3D('',#52916,#37620,#37621);
#32682=AXIS2_PLACEMENT_3D('',#52918,#37622,#37623);
#32683=AXIS2_PLACEMENT_3D('',#52920,#37624,#37625);
#32684=AXIS2_PLACEMENT_3D('',#52921,#37626,#37627);
#32685=AXIS2_PLACEMENT_3D('',#52922,#37628,#37629);
#32686=AXIS2_PLACEMENT_3D('',#52924,#37630,#37631);
#32687=AXIS2_PLACEMENT_3D('',#52926,#37632,#37633);
#32688=AXIS2_PLACEMENT_3D('',#52927,#37634,#37635);
#32689=AXIS2_PLACEMENT_3D('',#52928,#37636,#37637);
#32690=AXIS2_PLACEMENT_3D('',#52930,#37638,#37639);
#32691=AXIS2_PLACEMENT_3D('',#52932,#37640,#37641);
#32692=AXIS2_PLACEMENT_3D('',#52933,#37642,#37643);
#32693=AXIS2_PLACEMENT_3D('',#52934,#37644,#37645);
#32694=AXIS2_PLACEMENT_3D('',#52936,#37646,#37647);
#32695=AXIS2_PLACEMENT_3D('',#52938,#37648,#37649);
#32696=AXIS2_PLACEMENT_3D('',#52939,#37650,#37651);
#32697=AXIS2_PLACEMENT_3D('',#52940,#37652,#37653);
#32698=AXIS2_PLACEMENT_3D('',#52942,#37654,#37655);
#32699=AXIS2_PLACEMENT_3D('',#52944,#37656,#37657);
#32700=AXIS2_PLACEMENT_3D('',#52945,#37658,#37659);
#32701=AXIS2_PLACEMENT_3D('',#52946,#37660,#37661);
#32702=AXIS2_PLACEMENT_3D('',#52948,#37662,#37663);
#32703=AXIS2_PLACEMENT_3D('',#52950,#37664,#37665);
#32704=AXIS2_PLACEMENT_3D('',#52951,#37666,#37667);
#32705=AXIS2_PLACEMENT_3D('',#52952,#37668,#37669);
#32706=AXIS2_PLACEMENT_3D('',#52954,#37670,#37671);
#32707=AXIS2_PLACEMENT_3D('',#52956,#37672,#37673);
#32708=AXIS2_PLACEMENT_3D('',#52957,#37674,#37675);
#32709=AXIS2_PLACEMENT_3D('',#52958,#37676,#37677);
#32710=AXIS2_PLACEMENT_3D('',#52960,#37678,#37679);
#32711=AXIS2_PLACEMENT_3D('',#52962,#37680,#37681);
#32712=AXIS2_PLACEMENT_3D('',#52963,#37682,#37683);
#32713=AXIS2_PLACEMENT_3D('',#52964,#37684,#37685);
#32714=AXIS2_PLACEMENT_3D('',#52966,#37686,#37687);
#32715=AXIS2_PLACEMENT_3D('',#52968,#37688,#37689);
#32716=AXIS2_PLACEMENT_3D('',#52969,#37690,#37691);
#32717=AXIS2_PLACEMENT_3D('',#52970,#37692,#37693);
#32718=AXIS2_PLACEMENT_3D('',#52972,#37694,#37695);
#32719=AXIS2_PLACEMENT_3D('',#52974,#37696,#37697);
#32720=AXIS2_PLACEMENT_3D('',#52975,#37698,#37699);
#32721=AXIS2_PLACEMENT_3D('',#52976,#37700,#37701);
#32722=AXIS2_PLACEMENT_3D('',#52978,#37702,#37703);
#32723=AXIS2_PLACEMENT_3D('',#52980,#37704,#37705);
#32724=AXIS2_PLACEMENT_3D('',#52981,#37706,#37707);
#32725=AXIS2_PLACEMENT_3D('',#52982,#37708,#37709);
#32726=AXIS2_PLACEMENT_3D('',#52984,#37710,#37711);
#32727=AXIS2_PLACEMENT_3D('',#52986,#37712,#37713);
#32728=AXIS2_PLACEMENT_3D('',#52987,#37714,#37715);
#32729=AXIS2_PLACEMENT_3D('',#52988,#37716,#37717);
#32730=AXIS2_PLACEMENT_3D('',#52990,#37718,#37719);
#32731=AXIS2_PLACEMENT_3D('',#52992,#37720,#37721);
#32732=AXIS2_PLACEMENT_3D('',#52993,#37722,#37723);
#32733=AXIS2_PLACEMENT_3D('',#52994,#37724,#37725);
#32734=AXIS2_PLACEMENT_3D('',#52996,#37726,#37727);
#32735=AXIS2_PLACEMENT_3D('',#52998,#37728,#37729);
#32736=AXIS2_PLACEMENT_3D('',#52999,#37730,#37731);
#32737=AXIS2_PLACEMENT_3D('',#53000,#37732,#37733);
#32738=AXIS2_PLACEMENT_3D('',#53002,#37734,#37735);
#32739=AXIS2_PLACEMENT_3D('',#53004,#37736,#37737);
#32740=AXIS2_PLACEMENT_3D('',#53005,#37738,#37739);
#32741=AXIS2_PLACEMENT_3D('',#53006,#37740,#37741);
#32742=AXIS2_PLACEMENT_3D('',#53008,#37742,#37743);
#32743=AXIS2_PLACEMENT_3D('',#53010,#37744,#37745);
#32744=AXIS2_PLACEMENT_3D('',#53011,#37746,#37747);
#32745=AXIS2_PLACEMENT_3D('',#53012,#37748,#37749);
#32746=AXIS2_PLACEMENT_3D('',#53014,#37750,#37751);
#32747=AXIS2_PLACEMENT_3D('',#53016,#37752,#37753);
#32748=AXIS2_PLACEMENT_3D('',#53017,#37754,#37755);
#32749=AXIS2_PLACEMENT_3D('',#53018,#37756,#37757);
#32750=AXIS2_PLACEMENT_3D('',#53020,#37758,#37759);
#32751=AXIS2_PLACEMENT_3D('',#53022,#37760,#37761);
#32752=AXIS2_PLACEMENT_3D('',#53023,#37762,#37763);
#32753=AXIS2_PLACEMENT_3D('',#53024,#37764,#37765);
#32754=AXIS2_PLACEMENT_3D('',#53026,#37766,#37767);
#32755=AXIS2_PLACEMENT_3D('',#53028,#37768,#37769);
#32756=AXIS2_PLACEMENT_3D('',#53029,#37770,#37771);
#32757=AXIS2_PLACEMENT_3D('',#53030,#37772,#37773);
#32758=AXIS2_PLACEMENT_3D('',#53032,#37774,#37775);
#32759=AXIS2_PLACEMENT_3D('',#53034,#37776,#37777);
#32760=AXIS2_PLACEMENT_3D('',#53035,#37778,#37779);
#32761=AXIS2_PLACEMENT_3D('',#53036,#37780,#37781);
#32762=AXIS2_PLACEMENT_3D('',#53038,#37782,#37783);
#32763=AXIS2_PLACEMENT_3D('',#53040,#37784,#37785);
#32764=AXIS2_PLACEMENT_3D('',#53041,#37786,#37787);
#32765=AXIS2_PLACEMENT_3D('',#53042,#37788,#37789);
#32766=AXIS2_PLACEMENT_3D('',#53044,#37790,#37791);
#32767=AXIS2_PLACEMENT_3D('',#53046,#37792,#37793);
#32768=AXIS2_PLACEMENT_3D('',#53047,#37794,#37795);
#32769=AXIS2_PLACEMENT_3D('',#53048,#37796,#37797);
#32770=AXIS2_PLACEMENT_3D('',#53050,#37798,#37799);
#32771=AXIS2_PLACEMENT_3D('',#53052,#37800,#37801);
#32772=AXIS2_PLACEMENT_3D('',#53053,#37802,#37803);
#32773=AXIS2_PLACEMENT_3D('',#53054,#37804,#37805);
#32774=AXIS2_PLACEMENT_3D('',#53056,#37806,#37807);
#32775=AXIS2_PLACEMENT_3D('',#53058,#37808,#37809);
#32776=AXIS2_PLACEMENT_3D('',#53059,#37810,#37811);
#32777=AXIS2_PLACEMENT_3D('',#53060,#37812,#37813);
#32778=AXIS2_PLACEMENT_3D('',#53062,#37814,#37815);
#32779=AXIS2_PLACEMENT_3D('',#53064,#37816,#37817);
#32780=AXIS2_PLACEMENT_3D('',#53065,#37818,#37819);
#32781=AXIS2_PLACEMENT_3D('',#53066,#37820,#37821);
#32782=AXIS2_PLACEMENT_3D('',#53068,#37822,#37823);
#32783=AXIS2_PLACEMENT_3D('',#53070,#37824,#37825);
#32784=AXIS2_PLACEMENT_3D('',#53071,#37826,#37827);
#32785=AXIS2_PLACEMENT_3D('',#53072,#37828,#37829);
#32786=AXIS2_PLACEMENT_3D('',#53074,#37830,#37831);
#32787=AXIS2_PLACEMENT_3D('',#53076,#37832,#37833);
#32788=AXIS2_PLACEMENT_3D('',#53077,#37834,#37835);
#32789=AXIS2_PLACEMENT_3D('',#53078,#37836,#37837);
#32790=AXIS2_PLACEMENT_3D('',#53080,#37838,#37839);
#32791=AXIS2_PLACEMENT_3D('',#53082,#37840,#37841);
#32792=AXIS2_PLACEMENT_3D('',#53083,#37842,#37843);
#32793=AXIS2_PLACEMENT_3D('',#53084,#37844,#37845);
#32794=AXIS2_PLACEMENT_3D('',#53086,#37846,#37847);
#32795=AXIS2_PLACEMENT_3D('',#53088,#37848,#37849);
#32796=AXIS2_PLACEMENT_3D('',#53089,#37850,#37851);
#32797=AXIS2_PLACEMENT_3D('',#53090,#37852,#37853);
#32798=AXIS2_PLACEMENT_3D('',#53092,#37854,#37855);
#32799=AXIS2_PLACEMENT_3D('',#53094,#37856,#37857);
#32800=AXIS2_PLACEMENT_3D('',#53095,#37858,#37859);
#32801=AXIS2_PLACEMENT_3D('',#53096,#37860,#37861);
#32802=AXIS2_PLACEMENT_3D('',#53098,#37862,#37863);
#32803=AXIS2_PLACEMENT_3D('',#53100,#37864,#37865);
#32804=AXIS2_PLACEMENT_3D('',#53101,#37866,#37867);
#32805=AXIS2_PLACEMENT_3D('',#53102,#37868,#37869);
#32806=AXIS2_PLACEMENT_3D('',#53104,#37870,#37871);
#32807=AXIS2_PLACEMENT_3D('',#53106,#37872,#37873);
#32808=AXIS2_PLACEMENT_3D('',#53107,#37874,#37875);
#32809=AXIS2_PLACEMENT_3D('',#53108,#37876,#37877);
#32810=AXIS2_PLACEMENT_3D('',#53110,#37878,#37879);
#32811=AXIS2_PLACEMENT_3D('',#53112,#37880,#37881);
#32812=AXIS2_PLACEMENT_3D('',#53113,#37882,#37883);
#32813=AXIS2_PLACEMENT_3D('',#53114,#37884,#37885);
#32814=AXIS2_PLACEMENT_3D('',#53116,#37886,#37887);
#32815=AXIS2_PLACEMENT_3D('',#53118,#37888,#37889);
#32816=AXIS2_PLACEMENT_3D('',#53119,#37890,#37891);
#32817=AXIS2_PLACEMENT_3D('',#53120,#37892,#37893);
#32818=AXIS2_PLACEMENT_3D('',#53122,#37894,#37895);
#32819=AXIS2_PLACEMENT_3D('',#53124,#37896,#37897);
#32820=AXIS2_PLACEMENT_3D('',#53125,#37898,#37899);
#32821=AXIS2_PLACEMENT_3D('',#53126,#37900,#37901);
#32822=AXIS2_PLACEMENT_3D('',#53128,#37902,#37903);
#32823=AXIS2_PLACEMENT_3D('',#53130,#37904,#37905);
#32824=AXIS2_PLACEMENT_3D('',#53131,#37906,#37907);
#32825=AXIS2_PLACEMENT_3D('',#53132,#37908,#37909);
#32826=AXIS2_PLACEMENT_3D('',#53134,#37910,#37911);
#32827=AXIS2_PLACEMENT_3D('',#53136,#37912,#37913);
#32828=AXIS2_PLACEMENT_3D('',#53137,#37914,#37915);
#32829=AXIS2_PLACEMENT_3D('',#53138,#37916,#37917);
#32830=AXIS2_PLACEMENT_3D('',#53140,#37918,#37919);
#32831=AXIS2_PLACEMENT_3D('',#53142,#37920,#37921);
#32832=AXIS2_PLACEMENT_3D('',#53143,#37922,#37923);
#32833=AXIS2_PLACEMENT_3D('',#53144,#37924,#37925);
#32834=AXIS2_PLACEMENT_3D('',#53146,#37926,#37927);
#32835=AXIS2_PLACEMENT_3D('',#53148,#37928,#37929);
#32836=AXIS2_PLACEMENT_3D('',#53149,#37930,#37931);
#32837=AXIS2_PLACEMENT_3D('',#53150,#37932,#37933);
#32838=AXIS2_PLACEMENT_3D('',#53152,#37934,#37935);
#32839=AXIS2_PLACEMENT_3D('',#53154,#37936,#37937);
#32840=AXIS2_PLACEMENT_3D('',#53155,#37938,#37939);
#32841=AXIS2_PLACEMENT_3D('',#53156,#37940,#37941);
#32842=AXIS2_PLACEMENT_3D('',#53158,#37942,#37943);
#32843=AXIS2_PLACEMENT_3D('',#53160,#37944,#37945);
#32844=AXIS2_PLACEMENT_3D('',#53161,#37946,#37947);
#32845=AXIS2_PLACEMENT_3D('',#53162,#37948,#37949);
#32846=AXIS2_PLACEMENT_3D('',#53164,#37950,#37951);
#32847=AXIS2_PLACEMENT_3D('',#53166,#37952,#37953);
#32848=AXIS2_PLACEMENT_3D('',#53167,#37954,#37955);
#32849=AXIS2_PLACEMENT_3D('',#53168,#37956,#37957);
#32850=AXIS2_PLACEMENT_3D('',#53170,#37958,#37959);
#32851=AXIS2_PLACEMENT_3D('',#53172,#37960,#37961);
#32852=AXIS2_PLACEMENT_3D('',#53173,#37962,#37963);
#32853=AXIS2_PLACEMENT_3D('',#53174,#37964,#37965);
#32854=AXIS2_PLACEMENT_3D('',#53176,#37966,#37967);
#32855=AXIS2_PLACEMENT_3D('',#53178,#37968,#37969);
#32856=AXIS2_PLACEMENT_3D('',#53179,#37970,#37971);
#32857=AXIS2_PLACEMENT_3D('',#53180,#37972,#37973);
#32858=AXIS2_PLACEMENT_3D('',#53182,#37974,#37975);
#32859=AXIS2_PLACEMENT_3D('',#53184,#37976,#37977);
#32860=AXIS2_PLACEMENT_3D('',#53185,#37978,#37979);
#32861=AXIS2_PLACEMENT_3D('',#53186,#37980,#37981);
#32862=AXIS2_PLACEMENT_3D('',#53188,#37982,#37983);
#32863=AXIS2_PLACEMENT_3D('',#53190,#37984,#37985);
#32864=AXIS2_PLACEMENT_3D('',#53191,#37986,#37987);
#32865=AXIS2_PLACEMENT_3D('',#53192,#37988,#37989);
#32866=AXIS2_PLACEMENT_3D('',#53194,#37990,#37991);
#32867=AXIS2_PLACEMENT_3D('',#53196,#37992,#37993);
#32868=AXIS2_PLACEMENT_3D('',#53197,#37994,#37995);
#32869=AXIS2_PLACEMENT_3D('',#53198,#37996,#37997);
#32870=AXIS2_PLACEMENT_3D('',#53200,#37998,#37999);
#32871=AXIS2_PLACEMENT_3D('',#53202,#38000,#38001);
#32872=AXIS2_PLACEMENT_3D('',#53203,#38002,#38003);
#32873=AXIS2_PLACEMENT_3D('',#53204,#38004,#38005);
#32874=AXIS2_PLACEMENT_3D('',#53206,#38006,#38007);
#32875=AXIS2_PLACEMENT_3D('',#53208,#38008,#38009);
#32876=AXIS2_PLACEMENT_3D('',#53209,#38010,#38011);
#32877=AXIS2_PLACEMENT_3D('',#53210,#38012,#38013);
#32878=AXIS2_PLACEMENT_3D('',#53212,#38014,#38015);
#32879=AXIS2_PLACEMENT_3D('',#53214,#38016,#38017);
#32880=AXIS2_PLACEMENT_3D('',#53215,#38018,#38019);
#32881=AXIS2_PLACEMENT_3D('',#53216,#38020,#38021);
#32882=AXIS2_PLACEMENT_3D('',#53218,#38022,#38023);
#32883=AXIS2_PLACEMENT_3D('',#53220,#38024,#38025);
#32884=AXIS2_PLACEMENT_3D('',#53221,#38026,#38027);
#32885=AXIS2_PLACEMENT_3D('',#53222,#38028,#38029);
#32886=AXIS2_PLACEMENT_3D('',#53224,#38030,#38031);
#32887=AXIS2_PLACEMENT_3D('',#53226,#38032,#38033);
#32888=AXIS2_PLACEMENT_3D('',#53227,#38034,#38035);
#32889=AXIS2_PLACEMENT_3D('',#53228,#38036,#38037);
#32890=AXIS2_PLACEMENT_3D('',#53230,#38038,#38039);
#32891=AXIS2_PLACEMENT_3D('',#53232,#38040,#38041);
#32892=AXIS2_PLACEMENT_3D('',#53233,#38042,#38043);
#32893=AXIS2_PLACEMENT_3D('',#53234,#38044,#38045);
#32894=AXIS2_PLACEMENT_3D('',#53236,#38046,#38047);
#32895=AXIS2_PLACEMENT_3D('',#53238,#38048,#38049);
#32896=AXIS2_PLACEMENT_3D('',#53239,#38050,#38051);
#32897=AXIS2_PLACEMENT_3D('',#53240,#38052,#38053);
#32898=AXIS2_PLACEMENT_3D('',#53242,#38054,#38055);
#32899=AXIS2_PLACEMENT_3D('',#53244,#38056,#38057);
#32900=AXIS2_PLACEMENT_3D('',#53245,#38058,#38059);
#32901=AXIS2_PLACEMENT_3D('',#53246,#38060,#38061);
#32902=AXIS2_PLACEMENT_3D('',#53248,#38062,#38063);
#32903=AXIS2_PLACEMENT_3D('',#53250,#38064,#38065);
#32904=AXIS2_PLACEMENT_3D('',#53251,#38066,#38067);
#32905=AXIS2_PLACEMENT_3D('',#53252,#38068,#38069);
#32906=AXIS2_PLACEMENT_3D('',#53254,#38070,#38071);
#32907=AXIS2_PLACEMENT_3D('',#53256,#38072,#38073);
#32908=AXIS2_PLACEMENT_3D('',#53257,#38074,#38075);
#32909=AXIS2_PLACEMENT_3D('',#53258,#38076,#38077);
#32910=AXIS2_PLACEMENT_3D('',#53260,#38078,#38079);
#32911=AXIS2_PLACEMENT_3D('',#53262,#38080,#38081);
#32912=AXIS2_PLACEMENT_3D('',#53263,#38082,#38083);
#32913=AXIS2_PLACEMENT_3D('',#53264,#38084,#38085);
#32914=AXIS2_PLACEMENT_3D('',#53266,#38086,#38087);
#32915=AXIS2_PLACEMENT_3D('',#53268,#38088,#38089);
#32916=AXIS2_PLACEMENT_3D('',#53269,#38090,#38091);
#32917=AXIS2_PLACEMENT_3D('',#53270,#38092,#38093);
#32918=AXIS2_PLACEMENT_3D('',#53272,#38094,#38095);
#32919=AXIS2_PLACEMENT_3D('',#53274,#38096,#38097);
#32920=AXIS2_PLACEMENT_3D('',#53275,#38098,#38099);
#32921=AXIS2_PLACEMENT_3D('',#53276,#38100,#38101);
#32922=AXIS2_PLACEMENT_3D('',#53278,#38102,#38103);
#32923=AXIS2_PLACEMENT_3D('',#53280,#38104,#38105);
#32924=AXIS2_PLACEMENT_3D('',#53281,#38106,#38107);
#32925=AXIS2_PLACEMENT_3D('',#53282,#38108,#38109);
#32926=AXIS2_PLACEMENT_3D('',#53284,#38110,#38111);
#32927=AXIS2_PLACEMENT_3D('',#53286,#38112,#38113);
#32928=AXIS2_PLACEMENT_3D('',#53287,#38114,#38115);
#32929=AXIS2_PLACEMENT_3D('',#53288,#38116,#38117);
#32930=AXIS2_PLACEMENT_3D('',#53290,#38118,#38119);
#32931=AXIS2_PLACEMENT_3D('',#53292,#38120,#38121);
#32932=AXIS2_PLACEMENT_3D('',#53293,#38122,#38123);
#32933=AXIS2_PLACEMENT_3D('',#53294,#38124,#38125);
#32934=AXIS2_PLACEMENT_3D('',#53296,#38126,#38127);
#32935=AXIS2_PLACEMENT_3D('',#53298,#38128,#38129);
#32936=AXIS2_PLACEMENT_3D('',#53299,#38130,#38131);
#32937=AXIS2_PLACEMENT_3D('',#53300,#38132,#38133);
#32938=AXIS2_PLACEMENT_3D('',#53304,#38135,#38136);
#32939=AXIS2_PLACEMENT_3D('',#53306,#38138,#38139);
#32940=AXIS2_PLACEMENT_3D('',#53311,#38142,#38143);
#32941=AXIS2_PLACEMENT_3D('',#53312,#38144,#38145);
#32942=AXIS2_PLACEMENT_3D('',#53317,#38148,#38149);
#32943=AXIS2_PLACEMENT_3D('',#53318,#38150,#38151);
#32944=AXIS2_PLACEMENT_3D('',#53323,#38154,#38155);
#32945=AXIS2_PLACEMENT_3D('',#53324,#38156,#38157);
#32946=AXIS2_PLACEMENT_3D('',#53329,#38160,#38161);
#32947=AXIS2_PLACEMENT_3D('',#53330,#38162,#38163);
#32948=AXIS2_PLACEMENT_3D('',#53335,#38166,#38167);
#32949=AXIS2_PLACEMENT_3D('',#53336,#38168,#38169);
#32950=AXIS2_PLACEMENT_3D('',#53341,#38172,#38173);
#32951=AXIS2_PLACEMENT_3D('',#53342,#38174,#38175);
#32952=AXIS2_PLACEMENT_3D('',#53347,#38178,#38179);
#32953=AXIS2_PLACEMENT_3D('',#53348,#38180,#38181);
#32954=AXIS2_PLACEMENT_3D('',#53353,#38184,#38185);
#32955=AXIS2_PLACEMENT_3D('',#53354,#38186,#38187);
#32956=AXIS2_PLACEMENT_3D('',#53359,#38190,#38191);
#32957=AXIS2_PLACEMENT_3D('',#53360,#38192,#38193);
#32958=AXIS2_PLACEMENT_3D('',#53365,#38196,#38197);
#32959=AXIS2_PLACEMENT_3D('',#53366,#38198,#38199);
#32960=AXIS2_PLACEMENT_3D('',#53371,#38202,#38203);
#32961=AXIS2_PLACEMENT_3D('',#53372,#38204,#38205);
#32962=AXIS2_PLACEMENT_3D('',#53377,#38208,#38209);
#32963=AXIS2_PLACEMENT_3D('',#53378,#38210,#38211);
#32964=AXIS2_PLACEMENT_3D('',#53383,#38214,#38215);
#32965=AXIS2_PLACEMENT_3D('',#53384,#38216,#38217);
#32966=AXIS2_PLACEMENT_3D('',#53389,#38220,#38221);
#32967=AXIS2_PLACEMENT_3D('',#53390,#38222,#38223);
#32968=AXIS2_PLACEMENT_3D('',#53395,#38226,#38227);
#32969=AXIS2_PLACEMENT_3D('',#53396,#38228,#38229);
#32970=AXIS2_PLACEMENT_3D('',#53401,#38232,#38233);
#32971=AXIS2_PLACEMENT_3D('',#53402,#38234,#38235);
#32972=AXIS2_PLACEMENT_3D('',#53407,#38238,#38239);
#32973=AXIS2_PLACEMENT_3D('',#53408,#38240,#38241);
#32974=AXIS2_PLACEMENT_3D('',#53413,#38244,#38245);
#32975=AXIS2_PLACEMENT_3D('',#53414,#38246,#38247);
#32976=AXIS2_PLACEMENT_3D('',#53419,#38250,#38251);
#32977=AXIS2_PLACEMENT_3D('',#53420,#38252,#38253);
#32978=AXIS2_PLACEMENT_3D('',#53425,#38256,#38257);
#32979=AXIS2_PLACEMENT_3D('',#53426,#38258,#38259);
#32980=AXIS2_PLACEMENT_3D('',#53431,#38262,#38263);
#32981=AXIS2_PLACEMENT_3D('',#53432,#38264,#38265);
#32982=AXIS2_PLACEMENT_3D('',#53437,#38268,#38269);
#32983=AXIS2_PLACEMENT_3D('',#53438,#38270,#38271);
#32984=AXIS2_PLACEMENT_3D('',#53443,#38274,#38275);
#32985=AXIS2_PLACEMENT_3D('',#53444,#38276,#38277);
#32986=AXIS2_PLACEMENT_3D('',#53449,#38280,#38281);
#32987=AXIS2_PLACEMENT_3D('',#53450,#38282,#38283);
#32988=AXIS2_PLACEMENT_3D('',#53455,#38286,#38287);
#32989=AXIS2_PLACEMENT_3D('',#53456,#38288,#38289);
#32990=AXIS2_PLACEMENT_3D('',#53461,#38292,#38293);
#32991=AXIS2_PLACEMENT_3D('',#53462,#38294,#38295);
#32992=AXIS2_PLACEMENT_3D('',#53467,#38298,#38299);
#32993=AXIS2_PLACEMENT_3D('',#53468,#38300,#38301);
#32994=AXIS2_PLACEMENT_3D('',#53473,#38304,#38305);
#32995=AXIS2_PLACEMENT_3D('',#53474,#38306,#38307);
#32996=AXIS2_PLACEMENT_3D('',#53479,#38310,#38311);
#32997=AXIS2_PLACEMENT_3D('',#53480,#38312,#38313);
#32998=AXIS2_PLACEMENT_3D('',#53485,#38316,#38317);
#32999=AXIS2_PLACEMENT_3D('',#53486,#38318,#38319);
#33000=AXIS2_PLACEMENT_3D('',#53491,#38322,#38323);
#33001=AXIS2_PLACEMENT_3D('',#53492,#38324,#38325);
#33002=AXIS2_PLACEMENT_3D('',#53497,#38328,#38329);
#33003=AXIS2_PLACEMENT_3D('',#53498,#38330,#38331);
#33004=AXIS2_PLACEMENT_3D('',#53503,#38334,#38335);
#33005=AXIS2_PLACEMENT_3D('',#53504,#38336,#38337);
#33006=AXIS2_PLACEMENT_3D('',#53509,#38340,#38341);
#33007=AXIS2_PLACEMENT_3D('',#53510,#38342,#38343);
#33008=AXIS2_PLACEMENT_3D('',#53515,#38346,#38347);
#33009=AXIS2_PLACEMENT_3D('',#53516,#38348,#38349);
#33010=AXIS2_PLACEMENT_3D('',#53521,#38352,#38353);
#33011=AXIS2_PLACEMENT_3D('',#53522,#38354,#38355);
#33012=AXIS2_PLACEMENT_3D('',#53527,#38358,#38359);
#33013=AXIS2_PLACEMENT_3D('',#53528,#38360,#38361);
#33014=AXIS2_PLACEMENT_3D('',#53533,#38364,#38365);
#33015=AXIS2_PLACEMENT_3D('',#53534,#38366,#38367);
#33016=AXIS2_PLACEMENT_3D('',#53539,#38370,#38371);
#33017=AXIS2_PLACEMENT_3D('',#53540,#38372,#38373);
#33018=AXIS2_PLACEMENT_3D('',#53545,#38376,#38377);
#33019=AXIS2_PLACEMENT_3D('',#53546,#38378,#38379);
#33020=AXIS2_PLACEMENT_3D('',#53551,#38382,#38383);
#33021=AXIS2_PLACEMENT_3D('',#53552,#38384,#38385);
#33022=AXIS2_PLACEMENT_3D('',#53557,#38388,#38389);
#33023=AXIS2_PLACEMENT_3D('',#53558,#38390,#38391);
#33024=AXIS2_PLACEMENT_3D('',#53563,#38394,#38395);
#33025=AXIS2_PLACEMENT_3D('',#53564,#38396,#38397);
#33026=AXIS2_PLACEMENT_3D('',#53569,#38400,#38401);
#33027=AXIS2_PLACEMENT_3D('',#53570,#38402,#38403);
#33028=AXIS2_PLACEMENT_3D('',#53575,#38406,#38407);
#33029=AXIS2_PLACEMENT_3D('',#53576,#38408,#38409);
#33030=AXIS2_PLACEMENT_3D('',#53581,#38412,#38413);
#33031=AXIS2_PLACEMENT_3D('',#53582,#38414,#38415);
#33032=AXIS2_PLACEMENT_3D('',#53587,#38418,#38419);
#33033=AXIS2_PLACEMENT_3D('',#53588,#38420,#38421);
#33034=AXIS2_PLACEMENT_3D('',#53593,#38424,#38425);
#33035=AXIS2_PLACEMENT_3D('',#53594,#38426,#38427);
#33036=AXIS2_PLACEMENT_3D('',#53599,#38430,#38431);
#33037=AXIS2_PLACEMENT_3D('',#53600,#38432,#38433);
#33038=AXIS2_PLACEMENT_3D('',#53605,#38436,#38437);
#33039=AXIS2_PLACEMENT_3D('',#53606,#38438,#38439);
#33040=AXIS2_PLACEMENT_3D('',#53611,#38442,#38443);
#33041=AXIS2_PLACEMENT_3D('',#53612,#38444,#38445);
#33042=AXIS2_PLACEMENT_3D('',#53617,#38448,#38449);
#33043=AXIS2_PLACEMENT_3D('',#53618,#38450,#38451);
#33044=AXIS2_PLACEMENT_3D('',#53623,#38454,#38455);
#33045=AXIS2_PLACEMENT_3D('',#53624,#38456,#38457);
#33046=AXIS2_PLACEMENT_3D('',#53629,#38460,#38461);
#33047=AXIS2_PLACEMENT_3D('',#53630,#38462,#38463);
#33048=AXIS2_PLACEMENT_3D('',#53635,#38466,#38467);
#33049=AXIS2_PLACEMENT_3D('',#53636,#38468,#38469);
#33050=AXIS2_PLACEMENT_3D('',#53641,#38472,#38473);
#33051=AXIS2_PLACEMENT_3D('',#53642,#38474,#38475);
#33052=AXIS2_PLACEMENT_3D('',#53647,#38478,#38479);
#33053=AXIS2_PLACEMENT_3D('',#53648,#38480,#38481);
#33054=AXIS2_PLACEMENT_3D('',#53653,#38484,#38485);
#33055=AXIS2_PLACEMENT_3D('',#53654,#38486,#38487);
#33056=AXIS2_PLACEMENT_3D('',#53659,#38490,#38491);
#33057=AXIS2_PLACEMENT_3D('',#53660,#38492,#38493);
#33058=AXIS2_PLACEMENT_3D('',#53665,#38496,#38497);
#33059=AXIS2_PLACEMENT_3D('',#53666,#38498,#38499);
#33060=AXIS2_PLACEMENT_3D('',#53671,#38502,#38503);
#33061=AXIS2_PLACEMENT_3D('',#53672,#38504,#38505);
#33062=AXIS2_PLACEMENT_3D('',#53677,#38508,#38509);
#33063=AXIS2_PLACEMENT_3D('',#53678,#38510,#38511);
#33064=AXIS2_PLACEMENT_3D('',#53683,#38514,#38515);
#33065=AXIS2_PLACEMENT_3D('',#53684,#38516,#38517);
#33066=AXIS2_PLACEMENT_3D('',#53688,#38519,#38520);
#33067=AXIS2_PLACEMENT_3D('',#53690,#38522,#38523);
#33068=AXIS2_PLACEMENT_3D('',#53694,#38525,#38526);
#33069=AXIS2_PLACEMENT_3D('',#53696,#38528,#38529);
#33070=AXIS2_PLACEMENT_3D('',#53700,#38531,#38532);
#33071=AXIS2_PLACEMENT_3D('',#53702,#38534,#38535);
#33072=AXIS2_PLACEMENT_3D('',#53706,#38537,#38538);
#33073=AXIS2_PLACEMENT_3D('',#53708,#38540,#38541);
#33074=AXIS2_PLACEMENT_3D('',#53712,#38543,#38544);
#33075=AXIS2_PLACEMENT_3D('',#53714,#38546,#38547);
#33076=AXIS2_PLACEMENT_3D('',#53718,#38549,#38550);
#33077=AXIS2_PLACEMENT_3D('',#53720,#38552,#38553);
#33078=AXIS2_PLACEMENT_3D('',#53724,#38555,#38556);
#33079=AXIS2_PLACEMENT_3D('',#53726,#38558,#38559);
#33080=AXIS2_PLACEMENT_3D('',#53730,#38561,#38562);
#33081=AXIS2_PLACEMENT_3D('',#53732,#38564,#38565);
#33082=AXIS2_PLACEMENT_3D('',#53736,#38567,#38568);
#33083=AXIS2_PLACEMENT_3D('',#53738,#38570,#38571);
#33084=AXIS2_PLACEMENT_3D('',#53742,#38573,#38574);
#33085=AXIS2_PLACEMENT_3D('',#53744,#38576,#38577);
#33086=AXIS2_PLACEMENT_3D('',#53748,#38579,#38580);
#33087=AXIS2_PLACEMENT_3D('',#53750,#38582,#38583);
#33088=AXIS2_PLACEMENT_3D('',#53754,#38585,#38586);
#33089=AXIS2_PLACEMENT_3D('',#53756,#38588,#38589);
#33090=AXIS2_PLACEMENT_3D('',#53760,#38591,#38592);
#33091=AXIS2_PLACEMENT_3D('',#53762,#38594,#38595);
#33092=AXIS2_PLACEMENT_3D('',#53766,#38597,#38598);
#33093=AXIS2_PLACEMENT_3D('',#53768,#38600,#38601);
#33094=AXIS2_PLACEMENT_3D('',#53773,#38604,#38605);
#33095=AXIS2_PLACEMENT_3D('',#53774,#38606,#38607);
#33096=AXIS2_PLACEMENT_3D('',#53775,#38608,#38609);
#33097=AXIS2_PLACEMENT_3D('',#53776,#38610,#38611);
#33098=AXIS2_PLACEMENT_3D('',#53777,#38612,#38613);
#33099=AXIS2_PLACEMENT_3D('',#53778,#38614,#38615);
#33100=AXIS2_PLACEMENT_3D('',#53779,#38616,#38617);
#33101=AXIS2_PLACEMENT_3D('',#53780,#38618,#38619);
#33102=AXIS2_PLACEMENT_3D('',#53781,#38620,#38621);
#33103=AXIS2_PLACEMENT_3D('',#53782,#38622,#38623);
#33104=AXIS2_PLACEMENT_3D('',#53783,#38624,#38625);
#33105=AXIS2_PLACEMENT_3D('',#53784,#38626,#38627);
#33106=AXIS2_PLACEMENT_3D('',#53785,#38628,#38629);
#33107=AXIS2_PLACEMENT_3D('',#53786,#38630,#38631);
#33108=AXIS2_PLACEMENT_3D('',#53787,#38632,#38633);
#33109=AXIS2_PLACEMENT_3D('',#53788,#38634,#38635);
#33110=AXIS2_PLACEMENT_3D('',#53789,#38636,#38637);
#33111=AXIS2_PLACEMENT_3D('',#53790,#38638,#38639);
#33112=AXIS2_PLACEMENT_3D('',#53791,#38640,#38641);
#33113=AXIS2_PLACEMENT_3D('',#53792,#38642,#38643);
#33114=AXIS2_PLACEMENT_3D('',#53793,#38644,#38645);
#33115=AXIS2_PLACEMENT_3D('',#53794,#38646,#38647);
#33116=AXIS2_PLACEMENT_3D('',#53795,#38648,#38649);
#33117=AXIS2_PLACEMENT_3D('',#53796,#38650,#38651);
#33118=AXIS2_PLACEMENT_3D('',#53797,#38652,#38653);
#33119=AXIS2_PLACEMENT_3D('',#53798,#38654,#38655);
#33120=AXIS2_PLACEMENT_3D('',#53799,#38656,#38657);
#33121=AXIS2_PLACEMENT_3D('',#53800,#38658,#38659);
#33122=AXIS2_PLACEMENT_3D('',#53801,#38660,#38661);
#33123=AXIS2_PLACEMENT_3D('',#53802,#38662,#38663);
#33124=AXIS2_PLACEMENT_3D('',#53803,#38664,#38665);
#33125=AXIS2_PLACEMENT_3D('',#53804,#38666,#38667);
#33126=AXIS2_PLACEMENT_3D('',#53805,#38668,#38669);
#33127=AXIS2_PLACEMENT_3D('',#53806,#38670,#38671);
#33128=AXIS2_PLACEMENT_3D('',#53807,#38672,#38673);
#33129=AXIS2_PLACEMENT_3D('',#53808,#38674,#38675);
#33130=AXIS2_PLACEMENT_3D('',#53809,#38676,#38677);
#33131=AXIS2_PLACEMENT_3D('',#53810,#38678,#38679);
#33132=AXIS2_PLACEMENT_3D('',#53811,#38680,#38681);
#33133=AXIS2_PLACEMENT_3D('',#53812,#38682,#38683);
#33134=AXIS2_PLACEMENT_3D('',#53813,#38684,#38685);
#33135=AXIS2_PLACEMENT_3D('',#53814,#38686,#38687);
#33136=AXIS2_PLACEMENT_3D('',#53815,#38688,#38689);
#33137=AXIS2_PLACEMENT_3D('',#53816,#38690,#38691);
#33138=AXIS2_PLACEMENT_3D('',#53817,#38692,#38693);
#33139=AXIS2_PLACEMENT_3D('',#53818,#38694,#38695);
#33140=AXIS2_PLACEMENT_3D('',#53819,#38696,#38697);
#33141=AXIS2_PLACEMENT_3D('',#53820,#38698,#38699);
#33142=AXIS2_PLACEMENT_3D('',#53821,#38700,#38701);
#33143=AXIS2_PLACEMENT_3D('',#53822,#38702,#38703);
#33144=AXIS2_PLACEMENT_3D('',#53823,#38704,#38705);
#33145=AXIS2_PLACEMENT_3D('',#53824,#38706,#38707);
#33146=AXIS2_PLACEMENT_3D('',#53825,#38708,#38709);
#33147=AXIS2_PLACEMENT_3D('',#53826,#38710,#38711);
#33148=AXIS2_PLACEMENT_3D('',#53827,#38712,#38713);
#33149=AXIS2_PLACEMENT_3D('',#53828,#38714,#38715);
#33150=AXIS2_PLACEMENT_3D('',#53829,#38716,#38717);
#33151=AXIS2_PLACEMENT_3D('',#53830,#38718,#38719);
#33152=AXIS2_PLACEMENT_3D('',#53831,#38720,#38721);
#33153=AXIS2_PLACEMENT_3D('',#53832,#38722,#38723);
#33154=AXIS2_PLACEMENT_3D('',#53833,#38724,#38725);
#33155=AXIS2_PLACEMENT_3D('',#53834,#38726,#38727);
#33156=AXIS2_PLACEMENT_3D('',#53835,#38728,#38729);
#33157=AXIS2_PLACEMENT_3D('',#53836,#38730,#38731);
#33158=AXIS2_PLACEMENT_3D('',#53837,#38732,#38733);
#33159=AXIS2_PLACEMENT_3D('',#53838,#38734,#38735);
#33160=AXIS2_PLACEMENT_3D('',#53839,#38736,#38737);
#33161=AXIS2_PLACEMENT_3D('',#53840,#38738,#38739);
#33162=AXIS2_PLACEMENT_3D('',#53841,#38740,#38741);
#33163=AXIS2_PLACEMENT_3D('',#53842,#38742,#38743);
#33164=AXIS2_PLACEMENT_3D('',#53843,#38744,#38745);
#33165=AXIS2_PLACEMENT_3D('',#53844,#38746,#38747);
#33166=AXIS2_PLACEMENT_3D('',#53845,#38748,#38749);
#33167=AXIS2_PLACEMENT_3D('',#53846,#38750,#38751);
#33168=AXIS2_PLACEMENT_3D('',#53847,#38752,#38753);
#33169=AXIS2_PLACEMENT_3D('',#53848,#38754,#38755);
#33170=AXIS2_PLACEMENT_3D('',#53849,#38756,#38757);
#33171=AXIS2_PLACEMENT_3D('',#53850,#38758,#38759);
#33172=AXIS2_PLACEMENT_3D('',#53851,#38760,#38761);
#33173=AXIS2_PLACEMENT_3D('',#53852,#38762,#38763);
#33174=AXIS2_PLACEMENT_3D('',#53853,#38764,#38765);
#33175=AXIS2_PLACEMENT_3D('',#53854,#38766,#38767);
#33176=AXIS2_PLACEMENT_3D('',#53855,#38768,#38769);
#33177=AXIS2_PLACEMENT_3D('',#53856,#38770,#38771);
#33178=AXIS2_PLACEMENT_3D('',#53857,#38772,#38773);
#33179=AXIS2_PLACEMENT_3D('',#53858,#38774,#38775);
#33180=AXIS2_PLACEMENT_3D('',#53859,#38776,#38777);
#33181=AXIS2_PLACEMENT_3D('',#53860,#38778,#38779);
#33182=AXIS2_PLACEMENT_3D('',#53861,#38780,#38781);
#33183=AXIS2_PLACEMENT_3D('',#53862,#38782,#38783);
#33184=AXIS2_PLACEMENT_3D('',#53863,#38784,#38785);
#33185=AXIS2_PLACEMENT_3D('',#53864,#38786,#38787);
#33186=AXIS2_PLACEMENT_3D('',#53865,#38788,#38789);
#33187=AXIS2_PLACEMENT_3D('',#53866,#38790,#38791);
#33188=AXIS2_PLACEMENT_3D('',#53867,#38792,#38793);
#33189=AXIS2_PLACEMENT_3D('',#53868,#38794,#38795);
#33190=AXIS2_PLACEMENT_3D('',#53869,#38796,#38797);
#33191=AXIS2_PLACEMENT_3D('',#53870,#38798,#38799);
#33192=AXIS2_PLACEMENT_3D('',#53871,#38800,#38801);
#33193=AXIS2_PLACEMENT_3D('',#53872,#38802,#38803);
#33194=AXIS2_PLACEMENT_3D('',#53873,#38804,#38805);
#33195=AXIS2_PLACEMENT_3D('',#53874,#38806,#38807);
#33196=AXIS2_PLACEMENT_3D('',#53875,#38808,#38809);
#33197=AXIS2_PLACEMENT_3D('',#53876,#38810,#38811);
#33198=AXIS2_PLACEMENT_3D('',#53877,#38812,#38813);
#33199=AXIS2_PLACEMENT_3D('',#53878,#38814,#38815);
#33200=AXIS2_PLACEMENT_3D('',#53879,#38816,#38817);
#33201=AXIS2_PLACEMENT_3D('',#53880,#38818,#38819);
#33202=AXIS2_PLACEMENT_3D('',#53881,#38820,#38821);
#33203=AXIS2_PLACEMENT_3D('',#53882,#38822,#38823);
#33204=AXIS2_PLACEMENT_3D('',#53883,#38824,#38825);
#33205=AXIS2_PLACEMENT_3D('',#53884,#38826,#38827);
#33206=AXIS2_PLACEMENT_3D('',#53885,#38828,#38829);
#33207=AXIS2_PLACEMENT_3D('',#53886,#38830,#38831);
#33208=AXIS2_PLACEMENT_3D('',#53887,#38832,#38833);
#33209=AXIS2_PLACEMENT_3D('',#53888,#38834,#38835);
#33210=AXIS2_PLACEMENT_3D('',#53889,#38836,#38837);
#33211=AXIS2_PLACEMENT_3D('',#53890,#38838,#38839);
#33212=AXIS2_PLACEMENT_3D('',#53891,#38840,#38841);
#33213=AXIS2_PLACEMENT_3D('',#53892,#38842,#38843);
#33214=AXIS2_PLACEMENT_3D('',#53893,#38844,#38845);
#33215=AXIS2_PLACEMENT_3D('',#53894,#38846,#38847);
#33216=AXIS2_PLACEMENT_3D('',#53895,#38848,#38849);
#33217=AXIS2_PLACEMENT_3D('',#53896,#38850,#38851);
#33218=AXIS2_PLACEMENT_3D('',#53897,#38852,#38853);
#33219=AXIS2_PLACEMENT_3D('',#53898,#38854,#38855);
#33220=AXIS2_PLACEMENT_3D('',#53899,#38856,#38857);
#33221=AXIS2_PLACEMENT_3D('',#53900,#38858,#38859);
#33222=AXIS2_PLACEMENT_3D('',#53901,#38860,#38861);
#33223=AXIS2_PLACEMENT_3D('',#53902,#38862,#38863);
#33224=AXIS2_PLACEMENT_3D('',#53903,#38864,#38865);
#33225=AXIS2_PLACEMENT_3D('',#53904,#38866,#38867);
#33226=AXIS2_PLACEMENT_3D('',#53905,#38868,#38869);
#33227=AXIS2_PLACEMENT_3D('',#53906,#38870,#38871);
#33228=AXIS2_PLACEMENT_3D('',#53907,#38872,#38873);
#33229=AXIS2_PLACEMENT_3D('',#53908,#38874,#38875);
#33230=AXIS2_PLACEMENT_3D('',#53909,#38876,#38877);
#33231=AXIS2_PLACEMENT_3D('',#53910,#38878,#38879);
#33232=AXIS2_PLACEMENT_3D('',#53911,#38880,#38881);
#33233=AXIS2_PLACEMENT_3D('',#53912,#38882,#38883);
#33234=AXIS2_PLACEMENT_3D('',#53913,#38884,#38885);
#33235=AXIS2_PLACEMENT_3D('',#53914,#38886,#38887);
#33236=AXIS2_PLACEMENT_3D('',#53915,#38888,#38889);
#33237=AXIS2_PLACEMENT_3D('',#53916,#38890,#38891);
#33238=AXIS2_PLACEMENT_3D('',#53917,#38892,#38893);
#33239=AXIS2_PLACEMENT_3D('',#53918,#38894,#38895);
#33240=AXIS2_PLACEMENT_3D('',#53919,#38896,#38897);
#33241=AXIS2_PLACEMENT_3D('',#53920,#38898,#38899);
#33242=AXIS2_PLACEMENT_3D('',#53921,#38900,#38901);
#33243=AXIS2_PLACEMENT_3D('',#53922,#38902,#38903);
#33244=AXIS2_PLACEMENT_3D('',#53923,#38904,#38905);
#33245=AXIS2_PLACEMENT_3D('',#53924,#38906,#38907);
#33246=AXIS2_PLACEMENT_3D('',#53925,#38908,#38909);
#33247=AXIS2_PLACEMENT_3D('',#53926,#38910,#38911);
#33248=AXIS2_PLACEMENT_3D('',#53927,#38912,#38913);
#33249=AXIS2_PLACEMENT_3D('',#53928,#38914,#38915);
#33250=AXIS2_PLACEMENT_3D('',#53929,#38916,#38917);
#33251=AXIS2_PLACEMENT_3D('',#53930,#38918,#38919);
#33252=AXIS2_PLACEMENT_3D('',#53931,#38920,#38921);
#33253=AXIS2_PLACEMENT_3D('',#53932,#38922,#38923);
#33254=AXIS2_PLACEMENT_3D('',#53933,#38924,#38925);
#33255=AXIS2_PLACEMENT_3D('',#53934,#38926,#38927);
#33256=AXIS2_PLACEMENT_3D('',#53935,#38928,#38929);
#33257=AXIS2_PLACEMENT_3D('',#53936,#38930,#38931);
#33258=AXIS2_PLACEMENT_3D('',#53937,#38932,#38933);
#33259=AXIS2_PLACEMENT_3D('',#53938,#38934,#38935);
#33260=AXIS2_PLACEMENT_3D('',#53939,#38936,#38937);
#33261=AXIS2_PLACEMENT_3D('',#53940,#38938,#38939);
#33262=AXIS2_PLACEMENT_3D('',#53941,#38940,#38941);
#33263=AXIS2_PLACEMENT_3D('',#53942,#38942,#38943);
#33264=AXIS2_PLACEMENT_3D('',#53943,#38944,#38945);
#33265=AXIS2_PLACEMENT_3D('',#53944,#38946,#38947);
#33266=AXIS2_PLACEMENT_3D('',#53945,#38948,#38949);
#33267=AXIS2_PLACEMENT_3D('',#53946,#38950,#38951);
#33268=AXIS2_PLACEMENT_3D('',#53947,#38952,#38953);
#33269=AXIS2_PLACEMENT_3D('',#53948,#38954,#38955);
#33270=AXIS2_PLACEMENT_3D('',#53949,#38956,#38957);
#33271=AXIS2_PLACEMENT_3D('',#53950,#38958,#38959);
#33272=AXIS2_PLACEMENT_3D('',#53951,#38960,#38961);
#33273=AXIS2_PLACEMENT_3D('',#53952,#38962,#38963);
#33274=AXIS2_PLACEMENT_3D('',#53953,#38964,#38965);
#33275=AXIS2_PLACEMENT_3D('',#53954,#38966,#38967);
#33276=AXIS2_PLACEMENT_3D('',#53955,#38968,#38969);
#33277=AXIS2_PLACEMENT_3D('',#53956,#38970,#38971);
#33278=AXIS2_PLACEMENT_3D('',#53957,#38972,#38973);
#33279=AXIS2_PLACEMENT_3D('',#53958,#38974,#38975);
#33280=AXIS2_PLACEMENT_3D('',#53959,#38976,#38977);
#33281=AXIS2_PLACEMENT_3D('',#53960,#38978,#38979);
#33282=AXIS2_PLACEMENT_3D('',#53961,#38980,#38981);
#33283=AXIS2_PLACEMENT_3D('',#53962,#38982,#38983);
#33284=AXIS2_PLACEMENT_3D('',#53963,#38984,#38985);
#33285=AXIS2_PLACEMENT_3D('',#53964,#38986,#38987);
#33286=AXIS2_PLACEMENT_3D('',#53965,#38988,#38989);
#33287=AXIS2_PLACEMENT_3D('',#53966,#38990,#38991);
#33288=AXIS2_PLACEMENT_3D('',#53967,#38992,#38993);
#33289=AXIS2_PLACEMENT_3D('',#53968,#38994,#38995);
#33290=AXIS2_PLACEMENT_3D('',#53969,#38996,#38997);
#33291=AXIS2_PLACEMENT_3D('',#53970,#38998,#38999);
#33292=AXIS2_PLACEMENT_3D('',#53971,#39000,#39001);
#33293=AXIS2_PLACEMENT_3D('',#53972,#39002,#39003);
#33294=AXIS2_PLACEMENT_3D('',#53973,#39004,#39005);
#33295=AXIS2_PLACEMENT_3D('',#53974,#39006,#39007);
#33296=AXIS2_PLACEMENT_3D('',#53975,#39008,#39009);
#33297=AXIS2_PLACEMENT_3D('',#53976,#39010,#39011);
#33298=AXIS2_PLACEMENT_3D('',#53977,#39012,#39013);
#33299=AXIS2_PLACEMENT_3D('',#53978,#39014,#39015);
#33300=AXIS2_PLACEMENT_3D('',#53979,#39016,#39017);
#33301=AXIS2_PLACEMENT_3D('',#53980,#39018,#39019);
#33302=AXIS2_PLACEMENT_3D('',#53981,#39020,#39021);
#33303=AXIS2_PLACEMENT_3D('',#53982,#39022,#39023);
#33304=AXIS2_PLACEMENT_3D('',#53983,#39024,#39025);
#33305=AXIS2_PLACEMENT_3D('',#53984,#39026,#39027);
#33306=AXIS2_PLACEMENT_3D('',#53985,#39028,#39029);
#33307=AXIS2_PLACEMENT_3D('',#53986,#39030,#39031);
#33308=AXIS2_PLACEMENT_3D('',#53987,#39032,#39033);
#33309=AXIS2_PLACEMENT_3D('',#53988,#39034,#39035);
#33310=AXIS2_PLACEMENT_3D('',#53989,#39036,#39037);
#33311=AXIS2_PLACEMENT_3D('',#53990,#39038,#39039);
#33312=AXIS2_PLACEMENT_3D('',#53991,#39040,#39041);
#33313=AXIS2_PLACEMENT_3D('',#53992,#39042,#39043);
#33314=AXIS2_PLACEMENT_3D('',#53993,#39044,#39045);
#33315=AXIS2_PLACEMENT_3D('',#53994,#39046,#39047);
#33316=AXIS2_PLACEMENT_3D('',#53995,#39048,#39049);
#33317=AXIS2_PLACEMENT_3D('',#53996,#39050,#39051);
#33318=AXIS2_PLACEMENT_3D('',#53997,#39052,#39053);
#33319=AXIS2_PLACEMENT_3D('',#53998,#39054,#39055);
#33320=AXIS2_PLACEMENT_3D('',#53999,#39056,#39057);
#33321=AXIS2_PLACEMENT_3D('',#54000,#39058,#39059);
#33322=AXIS2_PLACEMENT_3D('',#54001,#39060,#39061);
#33323=AXIS2_PLACEMENT_3D('',#54002,#39062,#39063);
#33324=AXIS2_PLACEMENT_3D('',#54003,#39064,#39065);
#33325=AXIS2_PLACEMENT_3D('',#54004,#39066,#39067);
#33326=AXIS2_PLACEMENT_3D('',#54005,#39068,#39069);
#33327=AXIS2_PLACEMENT_3D('',#54006,#39070,#39071);
#33328=AXIS2_PLACEMENT_3D('',#54007,#39072,#39073);
#33329=AXIS2_PLACEMENT_3D('',#54008,#39074,#39075);
#33330=AXIS2_PLACEMENT_3D('',#54009,#39076,#39077);
#33331=AXIS2_PLACEMENT_3D('',#54010,#39078,#39079);
#33332=AXIS2_PLACEMENT_3D('',#54011,#39080,#39081);
#33333=AXIS2_PLACEMENT_3D('',#54012,#39082,#39083);
#33334=AXIS2_PLACEMENT_3D('',#54013,#39084,#39085);
#33335=AXIS2_PLACEMENT_3D('',#54015,#39086,#39087);
#33336=AXIS2_PLACEMENT_3D('',#54017,#39088,#39089);
#33337=AXIS2_PLACEMENT_3D('',#54018,#39090,#39091);
#33338=AXIS2_PLACEMENT_3D('',#54019,#39092,#39093);
#33339=AXIS2_PLACEMENT_3D('',#54024,#39096,#39097);
#33340=AXIS2_PLACEMENT_3D('',#54025,#39098,#39099);
#33341=AXIS2_PLACEMENT_3D('',#54026,#39100,#39101);
#33342=AXIS2_PLACEMENT_3D('',#54027,#39102,#39103);
#33343=AXIS2_PLACEMENT_3D('',#54028,#39104,#39105);
#33344=AXIS2_PLACEMENT_3D('',#54029,#39106,#39107);
#33345=AXIS2_PLACEMENT_3D('',#54042,#39114,#39115);
#33346=AXIS2_PLACEMENT_3D('',#54045,#39118,#39119);
#33347=AXIS2_PLACEMENT_3D('',#54047,#39121,#39122);
#33348=AXIS2_PLACEMENT_3D('',#54049,#39124,#39125);
#33349=AXIS2_PLACEMENT_3D('',#54051,#39127,#39128);
#33350=AXIS2_PLACEMENT_3D('',#54053,#39130,#39131);
#33351=AXIS2_PLACEMENT_3D('',#55575,#39133,#39134);
#33352=AXIS2_PLACEMENT_3D('',#55576,#39135,#39136);
#33353=AXIS2_PLACEMENT_3D('',#55578,#39138,#39139);
#33354=AXIS2_PLACEMENT_3D('',#55580,#39141,#39142);
#33355=AXIS2_PLACEMENT_3D('',#55581,#39143,#39144);
#33356=AXIS2_PLACEMENT_3D('',#55583,#39146,#39147);
#33357=AXIS2_PLACEMENT_3D('',#55585,#39149,#39150);
#33358=AXIS2_PLACEMENT_3D('',#55586,#39151,#39152);
#33359=AXIS2_PLACEMENT_3D('',#55588,#39154,#39155);
#33360=AXIS2_PLACEMENT_3D('',#55590,#39157,#39158);
#33361=AXIS2_PLACEMENT_3D('',#55591,#39159,#39160);
#33362=AXIS2_PLACEMENT_3D('',#55593,#39162,#39163);
#33363=AXIS2_PLACEMENT_3D('',#55595,#39165,#39166);
#33364=AXIS2_PLACEMENT_3D('',#55596,#39167,#39168);
#33365=AXIS2_PLACEMENT_3D('',#55598,#39170,#39171);
#33366=AXIS2_PLACEMENT_3D('',#55600,#39173,#39174);
#33367=AXIS2_PLACEMENT_3D('',#55601,#39175,#39176);
#33368=AXIS2_PLACEMENT_3D('',#55603,#39178,#39179);
#33369=AXIS2_PLACEMENT_3D('',#55605,#39181,#39182);
#33370=AXIS2_PLACEMENT_3D('',#55606,#39183,#39184);
#33371=AXIS2_PLACEMENT_3D('',#55608,#39186,#39187);
#33372=AXIS2_PLACEMENT_3D('',#55610,#39189,#39190);
#33373=AXIS2_PLACEMENT_3D('',#55611,#39191,#39192);
#33374=AXIS2_PLACEMENT_3D('',#55612,#39193,#39194);
#33375=AXIS2_PLACEMENT_3D('',#55613,#39195,#39196);
#33376=AXIS2_PLACEMENT_3D('',#55614,#39197,#39198);
#33377=AXIS2_PLACEMENT_3D('',#55615,#39199,#39200);
#33378=AXIS2_PLACEMENT_3D('',#55616,#39201,#39202);
#33379=AXIS2_PLACEMENT_3D('',#55617,#39203,#39204);
#33380=AXIS2_PLACEMENT_3D('',#55618,#39205,#39206);
#33381=AXIS2_PLACEMENT_3D('',#55619,#39207,#39208);
#33382=AXIS2_PLACEMENT_3D('',#55620,#39209,#39210);
#33383=AXIS2_PLACEMENT_3D('',#55621,#39211,#39212);
#33384=AXIS2_PLACEMENT_3D('',#55622,#39213,#39214);
#33385=AXIS2_PLACEMENT_3D('',#55623,#39215,#39216);
#33386=AXIS2_PLACEMENT_3D('',#55624,#39217,#39218);
#33387=AXIS2_PLACEMENT_3D('',#55625,#39219,#39220);
#33388=AXIS2_PLACEMENT_3D('',#55626,#39221,#39222);
#33389=AXIS2_PLACEMENT_3D('',#55627,#39223,#39224);
#33390=AXIS2_PLACEMENT_3D('',#55628,#39225,#39226);
#33391=AXIS2_PLACEMENT_3D('',#55629,#39227,#39228);
#33392=AXIS2_PLACEMENT_3D('',#55631,#39230,#39231);
#33393=AXIS2_PLACEMENT_3D('',#55633,#39233,#39234);
#33394=AXIS2_PLACEMENT_3D('',#55634,#39235,#39236);
#33395=AXIS2_PLACEMENT_3D('',#55636,#39238,#39239);
#33396=AXIS2_PLACEMENT_3D('',#55638,#39241,#39242);
#33397=AXIS2_PLACEMENT_3D('',#55639,#39243,#39244);
#33398=AXIS2_PLACEMENT_3D('',#55641,#39246,#39247);
#33399=AXIS2_PLACEMENT_3D('',#55643,#39249,#39250);
#33400=AXIS2_PLACEMENT_3D('',#55644,#39251,#39252);
#33401=AXIS2_PLACEMENT_3D('',#55646,#39254,#39255);
#33402=AXIS2_PLACEMENT_3D('',#55648,#39257,#39258);
#33403=AXIS2_PLACEMENT_3D('',#55649,#39259,#39260);
#33404=AXIS2_PLACEMENT_3D('',#55651,#39262,#39263);
#33405=AXIS2_PLACEMENT_3D('',#55653,#39265,#39266);
#33406=AXIS2_PLACEMENT_3D('',#55654,#39267,#39268);
#33407=AXIS2_PLACEMENT_3D('',#55656,#39270,#39271);
#33408=AXIS2_PLACEMENT_3D('',#55658,#39273,#39274);
#33409=AXIS2_PLACEMENT_3D('',#55659,#39275,#39276);
#33410=AXIS2_PLACEMENT_3D('',#55661,#39278,#39279);
#33411=AXIS2_PLACEMENT_3D('',#55663,#39281,#39282);
#33412=AXIS2_PLACEMENT_3D('',#55664,#39283,#39284);
#33413=AXIS2_PLACEMENT_3D('',#55666,#39286,#39287);
#33414=AXIS2_PLACEMENT_3D('',#55668,#39289,#39290);
#33415=AXIS2_PLACEMENT_3D('',#55669,#39291,#39292);
#33416=AXIS2_PLACEMENT_3D('',#55671,#39294,#39295);
#33417=AXIS2_PLACEMENT_3D('',#55673,#39297,#39298);
#33418=AXIS2_PLACEMENT_3D('',#55674,#39299,#39300);
#33419=AXIS2_PLACEMENT_3D('',#55676,#39302,#39303);
#33420=AXIS2_PLACEMENT_3D('',#55678,#39305,#39306);
#33421=AXIS2_PLACEMENT_3D('',#55679,#39307,#39308);
#33422=AXIS2_PLACEMENT_3D('',#55681,#39310,#39311);
#33423=AXIS2_PLACEMENT_3D('',#55683,#39313,#39314);
#33424=AXIS2_PLACEMENT_3D('',#55684,#39315,#39316);
#33425=AXIS2_PLACEMENT_3D('',#55686,#39318,#39319);
#33426=AXIS2_PLACEMENT_3D('',#55688,#39321,#39322);
#33427=AXIS2_PLACEMENT_3D('',#55689,#39323,#39324);
#33428=AXIS2_PLACEMENT_3D('',#55691,#39326,#39327);
#33429=AXIS2_PLACEMENT_3D('',#55693,#39329,#39330);
#33430=AXIS2_PLACEMENT_3D('',#55694,#39331,#39332);
#33431=AXIS2_PLACEMENT_3D('',#55696,#39334,#39335);
#33432=AXIS2_PLACEMENT_3D('',#55698,#39337,#39338);
#33433=AXIS2_PLACEMENT_3D('',#55699,#39339,#39340);
#33434=AXIS2_PLACEMENT_3D('',#55701,#39342,#39343);
#33435=AXIS2_PLACEMENT_3D('',#55703,#39345,#39346);
#33436=AXIS2_PLACEMENT_3D('',#55704,#39347,#39348);
#33437=AXIS2_PLACEMENT_3D('',#55706,#39350,#39351);
#33438=AXIS2_PLACEMENT_3D('',#55708,#39353,#39354);
#33439=AXIS2_PLACEMENT_3D('',#55709,#39355,#39356);
#33440=AXIS2_PLACEMENT_3D('',#55711,#39358,#39359);
#33441=AXIS2_PLACEMENT_3D('',#55713,#39361,#39362);
#33442=AXIS2_PLACEMENT_3D('',#55714,#39363,#39364);
#33443=AXIS2_PLACEMENT_3D('',#55716,#39366,#39367);
#33444=AXIS2_PLACEMENT_3D('',#55718,#39369,#39370);
#33445=AXIS2_PLACEMENT_3D('',#55719,#39371,#39372);
#33446=AXIS2_PLACEMENT_3D('',#55721,#39374,#39375);
#33447=AXIS2_PLACEMENT_3D('',#55723,#39377,#39378);
#33448=AXIS2_PLACEMENT_3D('',#55724,#39379,#39380);
#33449=AXIS2_PLACEMENT_3D('',#55726,#39382,#39383);
#33450=AXIS2_PLACEMENT_3D('',#55728,#39385,#39386);
#33451=AXIS2_PLACEMENT_3D('',#55729,#39387,#39388);
#33452=AXIS2_PLACEMENT_3D('',#55731,#39390,#39391);
#33453=AXIS2_PLACEMENT_3D('',#55733,#39393,#39394);
#33454=AXIS2_PLACEMENT_3D('',#55734,#39395,#39396);
#33455=AXIS2_PLACEMENT_3D('',#55736,#39398,#39399);
#33456=AXIS2_PLACEMENT_3D('',#55738,#39401,#39402);
#33457=AXIS2_PLACEMENT_3D('',#55739,#39403,#39404);
#33458=AXIS2_PLACEMENT_3D('',#55741,#39406,#39407);
#33459=AXIS2_PLACEMENT_3D('',#55743,#39409,#39410);
#33460=AXIS2_PLACEMENT_3D('',#55744,#39411,#39412);
#33461=AXIS2_PLACEMENT_3D('',#55746,#39414,#39415);
#33462=AXIS2_PLACEMENT_3D('',#55748,#39417,#39418);
#33463=AXIS2_PLACEMENT_3D('',#55749,#39419,#39420);
#33464=AXIS2_PLACEMENT_3D('',#55751,#39422,#39423);
#33465=AXIS2_PLACEMENT_3D('',#55753,#39425,#39426);
#33466=AXIS2_PLACEMENT_3D('',#55754,#39427,#39428);
#33467=AXIS2_PLACEMENT_3D('',#55756,#39430,#39431);
#33468=AXIS2_PLACEMENT_3D('',#55758,#39433,#39434);
#33469=AXIS2_PLACEMENT_3D('',#55759,#39435,#39436);
#33470=AXIS2_PLACEMENT_3D('',#55761,#39438,#39439);
#33471=AXIS2_PLACEMENT_3D('',#55763,#39441,#39442);
#33472=AXIS2_PLACEMENT_3D('',#55764,#39443,#39444);
#33473=AXIS2_PLACEMENT_3D('',#55766,#39446,#39447);
#33474=AXIS2_PLACEMENT_3D('',#55768,#39449,#39450);
#33475=AXIS2_PLACEMENT_3D('',#55769,#39451,#39452);
#33476=AXIS2_PLACEMENT_3D('',#55771,#39454,#39455);
#33477=AXIS2_PLACEMENT_3D('',#55773,#39457,#39458);
#33478=AXIS2_PLACEMENT_3D('',#55774,#39459,#39460);
#33479=AXIS2_PLACEMENT_3D('',#55776,#39462,#39463);
#33480=AXIS2_PLACEMENT_3D('',#55778,#39465,#39466);
#33481=AXIS2_PLACEMENT_3D('',#55779,#39467,#39468);
#33482=AXIS2_PLACEMENT_3D('',#55781,#39470,#39471);
#33483=AXIS2_PLACEMENT_3D('',#55783,#39473,#39474);
#33484=AXIS2_PLACEMENT_3D('',#55784,#39475,#39476);
#33485=AXIS2_PLACEMENT_3D('',#55786,#39478,#39479);
#33486=AXIS2_PLACEMENT_3D('',#55788,#39481,#39482);
#33487=AXIS2_PLACEMENT_3D('',#55789,#39483,#39484);
#33488=AXIS2_PLACEMENT_3D('',#55791,#39486,#39487);
#33489=AXIS2_PLACEMENT_3D('',#55793,#39489,#39490);
#33490=AXIS2_PLACEMENT_3D('',#55794,#39491,#39492);
#33491=AXIS2_PLACEMENT_3D('',#55796,#39494,#39495);
#33492=AXIS2_PLACEMENT_3D('',#55798,#39497,#39498);
#33493=AXIS2_PLACEMENT_3D('',#55799,#39499,#39500);
#33494=AXIS2_PLACEMENT_3D('',#55801,#39502,#39503);
#33495=AXIS2_PLACEMENT_3D('',#55803,#39505,#39506);
#33496=AXIS2_PLACEMENT_3D('',#55804,#39507,#39508);
#33497=AXIS2_PLACEMENT_3D('',#55806,#39510,#39511);
#33498=AXIS2_PLACEMENT_3D('',#55808,#39513,#39514);
#33499=AXIS2_PLACEMENT_3D('',#55809,#39515,#39516);
#33500=AXIS2_PLACEMENT_3D('',#55811,#39518,#39519);
#33501=AXIS2_PLACEMENT_3D('',#55813,#39521,#39522);
#33502=AXIS2_PLACEMENT_3D('',#55814,#39523,#39524);
#33503=AXIS2_PLACEMENT_3D('',#55816,#39526,#39527);
#33504=AXIS2_PLACEMENT_3D('',#55818,#39529,#39530);
#33505=AXIS2_PLACEMENT_3D('',#55819,#39531,#39532);
#33506=AXIS2_PLACEMENT_3D('',#55821,#39534,#39535);
#33507=AXIS2_PLACEMENT_3D('',#55823,#39537,#39538);
#33508=AXIS2_PLACEMENT_3D('',#55824,#39539,#39540);
#33509=AXIS2_PLACEMENT_3D('',#55826,#39542,#39543);
#33510=AXIS2_PLACEMENT_3D('',#55828,#39545,#39546);
#33511=AXIS2_PLACEMENT_3D('',#55829,#39547,#39548);
#33512=AXIS2_PLACEMENT_3D('',#55831,#39550,#39551);
#33513=AXIS2_PLACEMENT_3D('',#55833,#39553,#39554);
#33514=AXIS2_PLACEMENT_3D('',#55834,#39555,#39556);
#33515=AXIS2_PLACEMENT_3D('',#55836,#39558,#39559);
#33516=AXIS2_PLACEMENT_3D('',#55838,#39561,#39562);
#33517=AXIS2_PLACEMENT_3D('',#55839,#39563,#39564);
#33518=AXIS2_PLACEMENT_3D('',#55841,#39566,#39567);
#33519=AXIS2_PLACEMENT_3D('',#55843,#39569,#39570);
#33520=AXIS2_PLACEMENT_3D('',#55844,#39571,#39572);
#33521=AXIS2_PLACEMENT_3D('',#55846,#39574,#39575);
#33522=AXIS2_PLACEMENT_3D('',#55848,#39577,#39578);
#33523=AXIS2_PLACEMENT_3D('',#55849,#39579,#39580);
#33524=AXIS2_PLACEMENT_3D('',#55851,#39582,#39583);
#33525=AXIS2_PLACEMENT_3D('',#55853,#39585,#39586);
#33526=AXIS2_PLACEMENT_3D('',#55854,#39587,#39588);
#33527=AXIS2_PLACEMENT_3D('',#55856,#39590,#39591);
#33528=AXIS2_PLACEMENT_3D('',#55858,#39593,#39594);
#33529=AXIS2_PLACEMENT_3D('',#55859,#39595,#39596);
#33530=AXIS2_PLACEMENT_3D('',#55861,#39598,#39599);
#33531=AXIS2_PLACEMENT_3D('',#55863,#39601,#39602);
#33532=AXIS2_PLACEMENT_3D('',#55864,#39603,#39604);
#33533=AXIS2_PLACEMENT_3D('',#55866,#39606,#39607);
#33534=AXIS2_PLACEMENT_3D('',#55868,#39609,#39610);
#33535=AXIS2_PLACEMENT_3D('',#55869,#39611,#39612);
#33536=AXIS2_PLACEMENT_3D('',#55871,#39614,#39615);
#33537=AXIS2_PLACEMENT_3D('',#55873,#39617,#39618);
#33538=AXIS2_PLACEMENT_3D('',#55874,#39619,#39620);
#33539=AXIS2_PLACEMENT_3D('',#55876,#39622,#39623);
#33540=AXIS2_PLACEMENT_3D('',#55878,#39625,#39626);
#33541=AXIS2_PLACEMENT_3D('',#55879,#39627,#39628);
#33542=AXIS2_PLACEMENT_3D('',#55881,#39630,#39631);
#33543=AXIS2_PLACEMENT_3D('',#55883,#39633,#39634);
#33544=AXIS2_PLACEMENT_3D('',#55884,#39635,#39636);
#33545=AXIS2_PLACEMENT_3D('',#55886,#39638,#39639);
#33546=AXIS2_PLACEMENT_3D('',#55888,#39641,#39642);
#33547=AXIS2_PLACEMENT_3D('',#55889,#39643,#39644);
#33548=AXIS2_PLACEMENT_3D('',#55891,#39646,#39647);
#33549=AXIS2_PLACEMENT_3D('',#55893,#39649,#39650);
#33550=AXIS2_PLACEMENT_3D('',#55894,#39651,#39652);
#33551=AXIS2_PLACEMENT_3D('',#55896,#39654,#39655);
#33552=AXIS2_PLACEMENT_3D('',#55898,#39657,#39658);
#33553=AXIS2_PLACEMENT_3D('',#55899,#39659,#39660);
#33554=AXIS2_PLACEMENT_3D('',#55901,#39662,#39663);
#33555=AXIS2_PLACEMENT_3D('',#55903,#39665,#39666);
#33556=AXIS2_PLACEMENT_3D('',#55904,#39667,#39668);
#33557=AXIS2_PLACEMENT_3D('',#55906,#39670,#39671);
#33558=AXIS2_PLACEMENT_3D('',#55908,#39673,#39674);
#33559=AXIS2_PLACEMENT_3D('',#55909,#39675,#39676);
#33560=AXIS2_PLACEMENT_3D('',#55911,#39678,#39679);
#33561=AXIS2_PLACEMENT_3D('',#55913,#39681,#39682);
#33562=AXIS2_PLACEMENT_3D('',#55914,#39683,#39684);
#33563=AXIS2_PLACEMENT_3D('',#55916,#39686,#39687);
#33564=AXIS2_PLACEMENT_3D('',#55918,#39689,#39690);
#33565=AXIS2_PLACEMENT_3D('',#55919,#39691,#39692);
#33566=AXIS2_PLACEMENT_3D('',#55920,#39693,#39694);
#33567=AXIS2_PLACEMENT_3D('',#55921,#39695,#39696);
#33568=AXIS2_PLACEMENT_3D('',#55922,#39697,#39698);
#33569=AXIS2_PLACEMENT_3D('',#55923,#39699,#39700);
#33570=AXIS2_PLACEMENT_3D('',#55924,#39701,#39702);
#33571=AXIS2_PLACEMENT_3D('',#55925,#39703,#39704);
#33572=AXIS2_PLACEMENT_3D('',#55926,#39705,#39706);
#33573=AXIS2_PLACEMENT_3D('',#55927,#39707,#39708);
#33574=AXIS2_PLACEMENT_3D('',#55928,#39709,#39710);
#33575=AXIS2_PLACEMENT_3D('',#55929,#39711,#39712);
#33576=AXIS2_PLACEMENT_3D('',#55930,#39713,#39714);
#36558=DIRECTION('axis',(0.,0.,1.));
#36559=DIRECTION('refdir',(1.,0.,0.));
#36560=DIRECTION('center_axis',(5.15167520928809E-67,-1.18789542670764E-48,
-1.));
#36561=DIRECTION('ref_axis',(-4.33680868994202E-19,1.,-1.18789542670764E-48));
#36562=DIRECTION('',(-5.15167520928809E-67,1.18789542670764E-48,1.));
#36563=DIRECTION('',(-5.15167520928809E-67,1.18789542670764E-48,1.));
#36564=DIRECTION('center_axis',(5.15167520928809E-67,-1.18789542670764E-48,
-1.));
#36565=DIRECTION('ref_axis',(-4.33680868994202E-19,1.,-1.18789542670764E-48));
#36566=DIRECTION('center_axis',(-4.70261923768679E-35,1.08435016942139E-16,
-1.));
#36567=DIRECTION('ref_axis',(-4.33680868994202E-19,1.,1.08435016942139E-16));
#36568=DIRECTION('center_axis',(5.15167520928809E-67,-1.18789542670764E-48,
-1.));
#36569=DIRECTION('ref_axis',(-4.33680868994202E-19,1.,-1.18789542670764E-48));
#36570=DIRECTION('',(-5.15167520928809E-67,1.18789542670764E-48,1.));
#36571=DIRECTION('center_axis',(5.15167520928809E-67,-1.18789542670764E-48,
-1.));
#36572=DIRECTION('ref_axis',(-4.33680868994202E-19,1.,-1.18789542670764E-48));
#36573=DIRECTION('',(-5.15167520928809E-67,1.18789542670764E-48,1.));
#36574=DIRECTION('center_axis',(5.15167520928809E-67,-1.18789542670764E-48,
-1.));
#36575=DIRECTION('ref_axis',(-4.33680868994202E-19,1.,-1.18789542670764E-48));
#36576=DIRECTION('',(-5.15167520928809E-67,1.18789542670764E-48,1.));
#36577=DIRECTION('center_axis',(5.15167520928809E-67,-1.18789542670764E-48,
-1.));
#36578=DIRECTION('ref_axis',(-4.33680868994202E-19,1.,-1.18789542670764E-48));
#36579=DIRECTION('',(-5.15167520928809E-67,1.18789542670764E-48,1.));
#36580=DIRECTION('center_axis',(5.15167520928809E-67,-1.18789542670764E-48,
-1.));
#36581=DIRECTION('ref_axis',(-4.33680868994202E-19,1.,-1.18789542670764E-48));
#36582=DIRECTION('',(-5.15167520928809E-67,1.18789542670764E-48,1.));
#36583=DIRECTION('center_axis',(5.15167520928809E-67,-1.18789542670764E-48,
-1.));
#36584=DIRECTION('ref_axis',(-4.33680868994202E-19,1.,-1.18789542670764E-48));
#36585=DIRECTION('',(-5.15167520928809E-67,1.18789542670764E-48,1.));
#36586=DIRECTION('center_axis',(5.15167520928809E-67,-1.18789542670764E-48,
-1.));
#36587=DIRECTION('ref_axis',(-4.33680868994202E-19,1.,-1.18789542670764E-48));
#36588=DIRECTION('',(-5.15167520928809E-67,1.18789542670764E-48,1.));
#36589=DIRECTION('center_axis',(5.15167520928809E-67,-1.18789542670764E-48,
-1.));
#36590=DIRECTION('ref_axis',(-4.33680868994202E-19,1.,-1.18789542670764E-48));
#36591=DIRECTION('',(-5.15167520928809E-67,1.18789542670764E-48,1.));
#36592=DIRECTION('center_axis',(5.15167520928809E-67,-1.18789542670764E-48,
-1.));
#36593=DIRECTION('ref_axis',(-4.33680868994202E-19,1.,-1.18789542670764E-48));
#36594=DIRECTION('',(-5.15167520928809E-67,1.18789542670764E-48,1.));
#36595=DIRECTION('center_axis',(5.15167520928809E-67,-1.18789542670764E-48,
-1.));
#36596=DIRECTION('ref_axis',(-4.33680868994202E-19,1.,-1.18789542670764E-48));
#36597=DIRECTION('',(-5.15167520928809E-67,1.18789542670764E-48,1.));
#36598=DIRECTION('center_axis',(5.15167520928809E-67,-1.18789542670764E-48,
-1.));
#36599=DIRECTION('ref_axis',(-4.33680868994202E-19,1.,-1.18789542670764E-48));
#36600=DIRECTION('',(-5.15167520928809E-67,1.18789542670764E-48,1.));
#36601=DIRECTION('center_axis',(5.15167520928809E-67,-1.18789542670764E-48,
-1.));
#36602=DIRECTION('ref_axis',(-4.33680868994202E-19,1.,-1.18789542670764E-48));
#36603=DIRECTION('',(-5.15167520928809E-67,1.18789542670764E-48,1.));
#36604=DIRECTION('center_axis',(5.15167520928809E-67,-1.18789542670764E-48,
-1.));
#36605=DIRECTION('ref_axis',(-4.33680868994202E-19,1.,-1.18789542670764E-48));
#36606=DIRECTION('',(-5.15167520928809E-67,1.18789542670764E-48,1.));
#36607=DIRECTION('center_axis',(5.15167520928809E-67,-1.18789542670764E-48,
-1.));
#36608=DIRECTION('ref_axis',(-4.33680868994202E-19,1.,-1.18789542670764E-48));
#36609=DIRECTION('',(-5.15167520928809E-67,1.18789542670764E-48,1.));
#36610=DIRECTION('center_axis',(5.15167520928809E-67,-1.18789542670764E-48,
-1.));
#36611=DIRECTION('ref_axis',(-4.33680868994202E-19,1.,-1.18789542670764E-48));
#36612=DIRECTION('',(-5.15167520928809E-67,1.18789542670764E-48,1.));
#36613=DIRECTION('center_axis',(5.15167520928809E-67,-1.18789542670764E-48,
-1.));
#36614=DIRECTION('ref_axis',(-4.33680868994202E-19,1.,-1.18789542670764E-48));
#36615=DIRECTION('',(-5.15167520928809E-67,1.18789542670764E-48,1.));
#36616=DIRECTION('center_axis',(5.15167520928809E-67,-1.18789542670764E-48,
-1.));
#36617=DIRECTION('ref_axis',(-4.33680868994202E-19,1.,-1.18789542670764E-48));
#36618=DIRECTION('',(-5.15167520928809E-67,1.18789542670764E-48,1.));
#36619=DIRECTION('center_axis',(5.15167520928809E-67,-1.18789542670764E-48,
-1.));
#36620=DIRECTION('ref_axis',(-4.33680868994202E-19,1.,-1.18789542670764E-48));
#36621=DIRECTION('',(-5.15167520928809E-67,1.18789542670764E-48,1.));
#36622=DIRECTION('center_axis',(5.15167520928809E-67,-1.18789542670764E-48,
-1.));
#36623=DIRECTION('ref_axis',(-4.33680868994202E-19,1.,-1.18789542670764E-48));
#36624=DIRECTION('',(-5.15167520928809E-67,1.18789542670764E-48,1.));
#36625=DIRECTION('center_axis',(5.15167520928809E-67,-1.18789542670764E-48,
-1.));
#36626=DIRECTION('ref_axis',(-4.33680868994202E-19,1.,-1.18789542670764E-48));
#36627=DIRECTION('',(-5.15167520928809E-67,1.18789542670764E-48,1.));
#36628=DIRECTION('center_axis',(5.15167520928809E-67,-1.18789542670764E-48,
-1.));
#36629=DIRECTION('ref_axis',(-4.33680868994202E-19,1.,-1.18789542670764E-48));
#36630=DIRECTION('',(-5.15167520928809E-67,1.18789542670764E-48,1.));
#36631=DIRECTION('center_axis',(5.15167520928809E-67,-1.18789542670764E-48,
-1.));
#36632=DIRECTION('ref_axis',(-4.33680868994202E-19,1.,-1.18789542670764E-48));
#36633=DIRECTION('',(-5.15167520928809E-67,1.18789542670764E-48,1.));
#36634=DIRECTION('center_axis',(5.15167520928809E-67,-1.18789542670764E-48,
-1.));
#36635=DIRECTION('ref_axis',(-4.33680868994202E-19,1.,-1.18789542670764E-48));
#36636=DIRECTION('',(-5.15167520928809E-67,1.18789542670764E-48,1.));
#36637=DIRECTION('center_axis',(5.15167520928809E-67,-1.18789542670764E-48,
-1.));
#36638=DIRECTION('ref_axis',(-4.33680868994202E-19,1.,-1.18789542670764E-48));
#36639=DIRECTION('',(-5.15167520928809E-67,1.18789542670764E-48,1.));
#36640=DIRECTION('center_axis',(5.15167520928809E-67,-1.18789542670764E-48,
-1.));
#36641=DIRECTION('ref_axis',(-4.33680868994202E-19,1.,-1.18789542670764E-48));
#36642=DIRECTION('',(-5.15167520928809E-67,1.18789542670764E-48,1.));
#36643=DIRECTION('center_axis',(5.15167520928809E-67,-1.18789542670764E-48,
-1.));
#36644=DIRECTION('ref_axis',(-4.33680868994202E-19,1.,-1.18789542670764E-48));
#36645=DIRECTION('',(-5.15167520928809E-67,1.18789542670764E-48,1.));
#36646=DIRECTION('center_axis',(5.15167520928809E-67,-1.18789542670764E-48,
-1.));
#36647=DIRECTION('ref_axis',(-4.33680868994202E-19,1.,-1.18789542670764E-48));
#36648=DIRECTION('',(-5.15167520928809E-67,1.18789542670764E-48,1.));
#36649=DIRECTION('center_axis',(-5.15167520928809E-67,1.18789542670764E-48,
1.));
#36650=DIRECTION('ref_axis',(4.33680868994202E-19,-1.,1.18789542670764E-48));
#36651=DIRECTION('',(8.69022643068855E-17,-0.707106781186544,-0.707106781186551));
#36652=DIRECTION('center_axis',(5.15167520928809E-67,-1.18789542670764E-48,
-1.));
#36653=DIRECTION('ref_axis',(-4.33680868994202E-19,1.,-1.18789542670764E-48));
#36654=DIRECTION('center_axis',(0.,0.,1.));
#36655=DIRECTION('ref_axis',(5.30947313395831E-16,1.,0.));
#36656=DIRECTION('',(0.,0.,-1.));
#36657=DIRECTION('center_axis',(5.15167520928809E-67,-1.18789542670764E-48,
-1.));
#36658=DIRECTION('ref_axis',(-4.33680868994202E-19,1.,-1.18789542670764E-48));
#36659=DIRECTION('center_axis',(0.,0.,1.));
#36660=DIRECTION('ref_axis',(5.30947313395831E-16,1.,0.));
#36661=DIRECTION('',(0.,0.,-1.));
#36662=DIRECTION('center_axis',(0.,0.,1.));
#36663=DIRECTION('ref_axis',(5.30947313395831E-16,1.,0.));
#36664=DIRECTION('',(0.,0.,-1.));
#36665=DIRECTION('center_axis',(0.,0.,1.));
#36666=DIRECTION('ref_axis',(5.30947313395831E-16,1.,0.));
#36667=DIRECTION('',(0.,0.,-1.));
#36668=DIRECTION('center_axis',(0.,0.,1.));
#36669=DIRECTION('ref_axis',(5.30947313395831E-16,1.,0.));
#36670=DIRECTION('',(0.,0.,-1.));
#36671=DIRECTION('center_axis',(0.,0.,1.));
#36672=DIRECTION('ref_axis',(5.30947313395831E-16,1.,0.));
#36673=DIRECTION('',(0.,0.,-1.));
#36674=DIRECTION('center_axis',(0.,0.,1.));
#36675=DIRECTION('ref_axis',(5.30947313395831E-16,1.,0.));
#36676=DIRECTION('',(0.,0.,-1.));
#36677=DIRECTION('center_axis',(0.,0.,1.));
#36678=DIRECTION('ref_axis',(5.30947313395831E-16,1.,0.));
#36679=DIRECTION('',(0.,0.,-1.));
#36680=DIRECTION('center_axis',(0.,0.,1.));
#36681=DIRECTION('ref_axis',(5.30947313395831E-16,1.,0.));
#36682=DIRECTION('',(0.,0.,-1.));
#36683=DIRECTION('center_axis',(0.,0.,1.));
#36684=DIRECTION('ref_axis',(5.30947313395831E-16,1.,0.));
#36685=DIRECTION('',(0.,0.,-1.));
#36686=DIRECTION('center_axis',(0.,0.,1.));
#36687=DIRECTION('ref_axis',(5.30947313395831E-16,1.,0.));
#36688=DIRECTION('',(0.,0.,-1.));
#36689=DIRECTION('center_axis',(0.,0.,1.));
#36690=DIRECTION('ref_axis',(5.30947313395831E-16,1.,0.));
#36691=DIRECTION('',(0.,0.,-1.));
#36692=DIRECTION('center_axis',(0.,0.,1.));
#36693=DIRECTION('ref_axis',(5.30947313395831E-16,1.,0.));
#36694=DIRECTION('',(0.,0.,-1.));
#36695=DIRECTION('center_axis',(0.,0.,1.));
#36696=DIRECTION('ref_axis',(5.30947313395831E-16,1.,0.));
#36697=DIRECTION('',(0.,0.,-1.));
#36698=DIRECTION('center_axis',(0.,0.,1.));
#36699=DIRECTION('ref_axis',(5.30947313395831E-16,1.,0.));
#36700=DIRECTION('',(0.,0.,-1.));
#36701=DIRECTION('center_axis',(0.,0.,1.));
#36702=DIRECTION('ref_axis',(5.30947313395831E-16,1.,0.));
#36703=DIRECTION('',(0.,0.,-1.));
#36704=DIRECTION('center_axis',(0.,0.,1.));
#36705=DIRECTION('ref_axis',(5.30947313395831E-16,1.,0.));
#36706=DIRECTION('',(0.,0.,-1.));
#36707=DIRECTION('center_axis',(0.,0.,1.));
#36708=DIRECTION('ref_axis',(5.30947313395831E-16,1.,0.));
#36709=DIRECTION('',(0.,0.,-1.));
#36710=DIRECTION('center_axis',(0.,0.,1.));
#36711=DIRECTION('ref_axis',(5.30947313395831E-16,1.,0.));
#36712=DIRECTION('',(0.,0.,-1.));
#36713=DIRECTION('center_axis',(0.,0.,1.));
#36714=DIRECTION('ref_axis',(5.30947313395831E-16,1.,0.));
#36715=DIRECTION('',(0.,0.,-1.));
#36716=DIRECTION('center_axis',(0.,0.,1.));
#36717=DIRECTION('ref_axis',(5.30947313395831E-16,1.,0.));
#36718=DIRECTION('',(0.,0.,-1.));
#36719=DIRECTION('center_axis',(0.,0.,1.));
#36720=DIRECTION('ref_axis',(5.30947313395831E-16,1.,0.));
#36721=DIRECTION('',(0.,0.,-1.));
#36722=DIRECTION('center_axis',(0.,0.,1.));
#36723=DIRECTION('ref_axis',(5.30947313395831E-16,1.,0.));
#36724=DIRECTION('',(0.,0.,-1.));
#36725=DIRECTION('center_axis',(0.,0.,1.));
#36726=DIRECTION('ref_axis',(5.30947313395831E-16,1.,0.));
#36727=DIRECTION('',(0.,0.,-1.));
#36728=DIRECTION('center_axis',(0.,0.,1.));
#36729=DIRECTION('ref_axis',(5.30947313395831E-16,1.,0.));
#36730=DIRECTION('',(0.,0.,-1.));
#36731=DIRECTION('center_axis',(0.,0.,1.));
#36732=DIRECTION('ref_axis',(5.30947313395831E-16,1.,0.));
#36733=DIRECTION('',(0.,0.,-1.));
#36734=DIRECTION('center_axis',(0.,0.,1.));
#36735=DIRECTION('ref_axis',(5.30947313395831E-16,1.,0.));
#36736=DIRECTION('',(0.,0.,-1.));
#36737=DIRECTION('center_axis',(0.,0.,1.));
#36738=DIRECTION('ref_axis',(5.30947313395831E-16,1.,0.));
#36739=DIRECTION('',(0.,0.,-1.));
#36740=DIRECTION('center_axis',(0.,0.,1.));
#36741=DIRECTION('ref_axis',(5.30947313395831E-16,1.,0.));
#36742=DIRECTION('',(0.,0.,-1.));
#36743=DIRECTION('center_axis',(0.,0.,1.));
#36744=DIRECTION('ref_axis',(5.30947313395831E-16,1.,0.));
#36745=DIRECTION('',(0.,0.,-1.));
#36746=DIRECTION('center_axis',(0.,0.,1.));
#36747=DIRECTION('ref_axis',(5.30947313395831E-16,1.,0.));
#36748=DIRECTION('center_axis',(0.,0.,1.));
#36749=DIRECTION('ref_axis',(0.700629269222058,-0.7135254915624,0.));
#36750=DIRECTION('center_axis',(-5.15167520928809E-67,1.18789542670764E-48,
1.));
#36751=DIRECTION('ref_axis',(4.33680868994202E-19,-1.,1.18789542670764E-48));
#36752=DIRECTION('center_axis',(5.15167520928809E-67,-1.18789542670764E-48,
-1.));
#36753=DIRECTION('ref_axis',(-4.33680868994202E-19,1.,-1.18789542670764E-48));
#36754=DIRECTION('center_axis',(5.15167520928809E-67,-1.18789542670764E-48,
-1.));
#36755=DIRECTION('ref_axis',(-4.33680868994202E-19,1.,-1.18789542670764E-48));
#36756=DIRECTION('center_axis',(5.15167520928809E-67,-1.18789542670764E-48,
-1.));
#36757=DIRECTION('ref_axis',(-4.33680868994202E-19,1.,-1.18789542670764E-48));
#36758=DIRECTION('center_axis',(1.09747227149895E-48,7.33307527524356E-49,
1.));
#36759=DIRECTION('ref_axis',(1.,4.33680868994202E-19,-1.09747227149895E-48));
#36760=DIRECTION('center_axis',(-0.654448706060852,0.271081529927754,-0.705841126081008));
#36761=DIRECTION('ref_axis',(0.652112169591586,-0.270113704831613,-0.708370174931649));
#36762=DIRECTION('',(1.09747227149895E-48,7.33307527524356E-49,1.));
#36763=DIRECTION('center_axis',(-0.654448706060939,0.271081529927973,0.705841126080843));
#36764=DIRECTION('ref_axis',(0.652112169592024,-0.270113704830126,0.708370174931813));
#36765=DIRECTION('',(1.09747227149895E-48,7.33307527524356E-49,1.));
#36766=DIRECTION('center_axis',(1.12975568624751E-48,8.20815552314688E-49,
1.));
#36767=DIRECTION('ref_axis',(1.,4.33680868994202E-19,-1.12975568624751E-48));
#36768=DIRECTION('center_axis',(-0.673700070814156,0.218898422362917,-0.705841126084352));
#36769=DIRECTION('ref_axis',(0.671294802430975,-0.218116903290839,-0.708370174928316));
#36770=DIRECTION('',(1.12975568624751E-48,8.20815552314688E-49,1.));
#36771=DIRECTION('center_axis',(-0.673700070814201,0.218898422363249,0.705841126084207));
#36772=DIRECTION('ref_axis',(0.671294802430673,-0.218116903291296,0.708370174928462));
#36773=DIRECTION('',(1.12975568624751E-48,8.20815552314688E-49,1.));
#36774=DIRECTION('center_axis',(1.15507378150847E-48,9.10586746597098E-49,
1.));
#36775=DIRECTION('ref_axis',(1.,4.33680868994202E-19,-1.15507378150847E-48));
#36776=DIRECTION('center_axis',(-0.688797850611722,0.165365733230951,-0.705841126079843));
#36777=DIRECTION('ref_axis',(0.686338679579581,-0.164775338502517,-0.708370174932809));
#36778=DIRECTION('',(1.15507378150847E-48,9.10586746597098E-49,1.));
#36779=DIRECTION('center_axis',(-0.688797850609436,0.165365733233163,0.705841126081556));
#36780=DIRECTION('ref_axis',(0.68633867958204,-0.164775338499612,0.708370174931102));
#36781=DIRECTION('',(1.15507378150847E-48,9.10586746597098E-49,1.));
#36782=DIRECTION('center_axis',(1.17327046280542E-48,1.00206764110688E-48,
1.));
#36783=DIRECTION('ref_axis',(1.,4.33680868994202E-19,-1.17327046280542E-48));
#36784=DIRECTION('center_axis',(-0.699648962604041,0.110813509366852,-0.705841126082132));
#36785=DIRECTION('ref_axis',(0.697151050543932,-0.11041787896162,-0.708370174930529));
#36786=DIRECTION('',(1.17327046280542E-48,1.00206764110688E-48,1.));
#36787=DIRECTION('center_axis',(-0.699648962604175,0.110813509367011,0.705841126081974));
#36788=DIRECTION('ref_axis',(0.697151050543496,-0.110417878963368,0.708370174930686));
#36789=DIRECTION('',(1.17327046280542E-48,1.00206764110688E-48,1.));
#36790=DIRECTION('center_axis',(1.18423354154716E-48,1.09469422570891E-48,
1.));
#36791=DIRECTION('ref_axis',(1.,4.33680868994202E-19,-1.18423354154716E-48));
#36792=DIRECTION('center_axis',(-0.706186506088737,0.0555780833649064,-0.705841126081264));
#36793=DIRECTION('ref_axis',(0.703665253451942,-0.0553796564821394,-0.708370174931394));
#36794=DIRECTION('',(1.18423354154716E-48,1.09469422570891E-48,1.));
#36795=DIRECTION('center_axis',(-0.706186506088284,0.0555780833648712,0.705841126081719));
#36796=DIRECTION('ref_axis',(0.703665253452317,-0.0553796564831855,0.70837017493094));
#36797=DIRECTION('',(1.18423354154716E-48,1.09469422570891E-48,1.));
#36798=DIRECTION('center_axis',(1.18789542670764E-48,1.18789542670763E-48,
1.));
#36799=DIRECTION('ref_axis',(1.,4.33680868994202E-19,-1.18789542670764E-48));
#36800=DIRECTION('center_axis',(-0.70837017493089,-1.25340662871076E-13,
-0.70584112608177));
#36801=DIRECTION('ref_axis',(0.70584112608177,-2.88506822019813E-13,-0.708370174930889));
#36802=DIRECTION('',(1.18789542670764E-48,1.18789542670763E-48,1.));
#36803=DIRECTION('center_axis',(-0.70837017493089,1.25340662871076E-13,
0.70584112608177));
#36804=DIRECTION('ref_axis',(0.70584112608177,2.61497947465894E-13,0.708370174930889));
#36805=DIRECTION('',(1.18789542670764E-48,1.18789542670763E-48,1.));
#36806=DIRECTION('center_axis',(1.05842257525003E-48,6.48602188298306E-49,
1.));
#36807=DIRECTION('ref_axis',(1.,4.33680868994202E-19,-1.05842257525003E-48));
#36808=DIRECTION('center_axis',(-0.631162447404585,0.321593329715507,-0.70584112608203));
#36809=DIRECTION('ref_axis',(0.628909048379288,-0.320445165567225,-0.708370174930631));
#36810=DIRECTION('',(1.05842257525003E-48,6.48602188298306E-49,1.));
#36811=DIRECTION('center_axis',(-0.631162447404969,0.32159332971786,0.705841126080614));
#36812=DIRECTION('ref_axis',(0.628909048378923,-0.320445165564824,0.708370174932041));
#36813=DIRECTION('',(1.05842257525003E-48,6.48602188298306E-49,1.));
#36814=DIRECTION('center_axis',(1.01284735186347E-48,5.67221771220248E-49,
1.));
#36815=DIRECTION('ref_axis',(1.,4.33680868994202E-19,-1.01284735186347E-48));
#36816=DIRECTION('center_axis',(-0.603984862377595,0.370122399687911,-0.705841126081486));
#36817=DIRECTION('ref_axis',(0.601828493750374,-0.368800975294447,-0.708370174931173));
#36818=DIRECTION('',(1.01284735186347E-48,5.67221771220248E-49,1.));
#36819=DIRECTION('center_axis',(-0.603984862377492,0.370122399687834,0.705841126081615));
#36820=DIRECTION('ref_axis',(0.60182849375054,-0.368800975294424,0.708370174931044));
#36821=DIRECTION('',(1.01284735186347E-48,5.67221771220248E-49,1.));
#36822=DIRECTION('center_axis',(9.61027587746754E-49,4.89668013623204E-49,
1.));
#36823=DIRECTION('ref_axis',(1.,4.33680868994202E-19,-9.61027587746754E-49));
#36824=DIRECTION('center_axis',(-0.57308350982942,0.416369541987989,-0.705841126080299));
#36825=DIRECTION('ref_axis',(-0.571037466327478,0.414883004371834,0.708370174932355));
#36826=DIRECTION('',(9.61027587746754E-49,4.89668013623204E-49,1.));
#36827=DIRECTION('center_axis',(-0.573083509826005,0.416369541988967,0.705841126082495));
#36828=DIRECTION('ref_axis',(0.571037466331126,-0.41488300437055,0.708370174930167));
#36829=DIRECTION('',(9.61027587746754E-49,4.89668013623204E-49,1.));
#36830=DIRECTION('center_axis',(9.03282768977476E-49,4.16419060212002E-49,
1.));
#36831=DIRECTION('ref_axis',(1.,4.33680868994202E-19,-9.03282768977476E-49));
#36832=DIRECTION('center_axis',(-0.538648906869708,0.460049627603881,-0.705841126082633));
#36833=DIRECTION('ref_axis',(-0.536725803041031,0.458407141763258,0.70837017493003));
#36834=DIRECTION('',(9.03282768977476E-49,4.16419060212002E-49,1.));
#36835=DIRECTION('center_axis',(-0.53864890686968,0.460049627604191,0.705841126082452));
#36836=DIRECTION('ref_axis',(0.536725803040381,-0.45840714176374,0.70837017493021));
#36837=DIRECTION('',(9.03282768977476E-49,4.16419060212002E-49,1.));
#36838=DIRECTION('center_axis',(8.39968911565451E-49,3.47926515142171E-49,
1.));
#36839=DIRECTION('ref_axis',(1.,4.33680868994202E-19,-8.39968911565451E-49));
#36840=DIRECTION('center_axis',(-0.500893354284786,0.500893354283015,-0.705841126081816));
#36841=DIRECTION('ref_axis',(-0.499105046691526,0.499105046694076,0.708370174930843));
#36842=DIRECTION('',(8.39968911565451E-49,3.47926515142171E-49,1.));
#36843=DIRECTION('center_axis',(-0.500893354285066,0.500893354283687,0.70584112608114));
#36844=DIRECTION('ref_axis',(0.49910504669045,-0.499105046694196,0.708370174931517));
#36845=DIRECTION('',(8.39968911565451E-49,3.47926515142171E-49,1.));
#36846=DIRECTION('center_axis',(7.71476366495618E-49,2.84612657730147E-49,
1.));
#36847=DIRECTION('ref_axis',(1.,4.33680868994202E-19,-7.71476366495618E-49));
#36848=DIRECTION('center_axis',(-0.460049627606723,0.538648906869542,-0.705841126080907));
#36849=DIRECTION('ref_axis',(-0.458407141764148,0.536725803038001,0.708370174931749));
#36850=DIRECTION('',(7.71476366495618E-49,2.84612657730147E-49,1.));
#36851=DIRECTION('center_axis',(-0.460049627603276,0.538648906871872,0.705841126081376));
#36852=DIRECTION('ref_axis',(0.458407141768044,-0.53672580303529,0.708370174931282));
#36853=DIRECTION('',(7.71476366495618E-49,2.84612657730147E-49,1.));
#36854=DIRECTION('center_axis',(6.98227413084414E-49,2.26867838960871E-49,
1.));
#36855=DIRECTION('ref_axis',(1.,4.33680868994202E-19,-6.98227413084414E-49));
#36856=DIRECTION('center_axis',(-0.416369541989573,0.573083509826983,-0.705841126081344));
#36857=DIRECTION('ref_axis',(-0.414883004369422,0.571037466330522,0.708370174931314));
#36858=DIRECTION('',(6.98227413084414E-49,2.26867838960871E-49,1.));
#36859=DIRECTION('center_axis',(-0.416369541986537,0.573083509827722,0.705841126082535));
#36860=DIRECTION('ref_axis',(0.414883004374377,-0.571037466328393,0.708370174930127));
#36861=DIRECTION('',(6.98227413084414E-49,2.26867838960871E-49,1.));
#36862=DIRECTION('center_axis',(6.2067365548737E-49,1.75048074844156E-49,
1.));
#36863=DIRECTION('ref_axis',(1.,4.33680868994202E-19,-6.2067365548737E-49));
#36864=DIRECTION('center_axis',(-0.370122399687787,0.603984862376041,-0.70584112608288));
#36865=DIRECTION('ref_axis',(-0.368800975294937,0.60182849375171,0.708370174929783));
#36866=DIRECTION('',(6.2067365548737E-49,1.75048074844156E-49,1.));
#36867=DIRECTION('center_axis',(-0.370122399687792,0.603984862376936,0.705841126082112));
#36868=DIRECTION('ref_axis',(0.368800975294942,-0.601828493750806,0.708370174930549));
#36869=DIRECTION('',(6.2067365548737E-49,1.75048074844156E-49,1.));
#36870=DIRECTION('center_axis',(5.39293238409311E-49,1.29472851457601E-49,
1.));
#36871=DIRECTION('ref_axis',(1.,4.33680868994202E-19,-5.39293238409311E-49));
#36872=DIRECTION('center_axis',(-0.321593329717153,0.63116244740346,-0.705841126082286));
#36873=DIRECTION('ref_axis',(-0.320445165567263,0.628909048379556,0.708370174930376));
#36874=DIRECTION('',(5.39293238409311E-49,1.29472851457601E-49,1.));
#36875=DIRECTION('center_axis',(-0.321593329716558,0.631162447403966,0.705841126082104));
#36876=DIRECTION('ref_axis',(0.320445165566995,-0.628909048379489,0.708370174930556));
#36877=DIRECTION('',(5.39293238409311E-49,1.29472851457601E-49,1.));
#36878=DIRECTION('center_axis',(0.,0.,1.));
#36879=DIRECTION('ref_axis',(1.,4.33680868994202E-19,0.));
#36880=DIRECTION('',(-0.707106781186549,-8.69022643068862E-17,0.707106781186546));
#36881=DIRECTION('center_axis',(0.,0.,1.));
#36882=DIRECTION('ref_axis',(1.,4.33680868994202E-19,0.));
#36883=DIRECTION('center_axis',(5.15167520928809E-67,-1.18789542670764E-48,
-1.));
#36884=DIRECTION('ref_axis',(0.,1.,0.));
#36885=DIRECTION('center_axis',(5.15167520928809E-67,-1.18789542670764E-48,
-1.));
#36886=DIRECTION('ref_axis',(-4.33680868994202E-19,1.,-1.18789542670764E-48));
#36887=DIRECTION('center_axis',(-1.,0.,-5.15167520928809E-67));
#36888=DIRECTION('ref_axis',(0.,-1.,0.));
#36889=DIRECTION('center_axis',(5.15167520928809E-67,-1.18789542670764E-48,
-1.));
#36890=DIRECTION('ref_axis',(-4.33680868994202E-19,1.,-1.18789542670764E-48));
#36891=DIRECTION('center_axis',(5.15167520928809E-67,-1.18789542670764E-48,
-1.));
#36892=DIRECTION('ref_axis',(-4.33680868994202E-19,1.,-1.18789542670764E-48));
#36893=DIRECTION('center_axis',(5.15167520928809E-67,-1.18789542670764E-48,
-1.));
#36894=DIRECTION('ref_axis',(-4.33680868994202E-19,1.,-1.18789542670764E-48));
#36895=DIRECTION('center_axis',(0.0555758110363288,-0.706157633406642,0.705870190622316));
#36896=DIRECTION('ref_axis',(0.0553775799352608,-0.703694571287346,-0.708341212962532));
#36897=DIRECTION('center_axis',(5.15167520928809E-67,-1.18789542670764E-48,
-1.));
#36898=DIRECTION('ref_axis',(-4.33680868994202E-19,1.,-1.18789542670764E-48));
#36899=DIRECTION('center_axis',(0.11080862020158,-0.699618093636883,0.705872490429338));
#36900=DIRECTION('ref_axis',(0.110419233095995,-0.697182591373234,-0.708338921173046));
#36901=DIRECTION('center_axis',(5.15167520928809E-67,-1.18789542670764E-48,
-1.));
#36902=DIRECTION('ref_axis',(-4.33680868994202E-19,1.,-1.18789542670764E-48));
#36903=DIRECTION('center_axis',(0.165358045050138,-0.688765827029971,0.705874176077378));
#36904=DIRECTION('ref_axis',(0.164780094681068,-0.686371526838389,-0.708337241391723));
#36905=DIRECTION('center_axis',(5.15167520928809E-67,-1.18789542670764E-48,
-1.));
#36906=DIRECTION('ref_axis',(-4.33680868994202E-19,1.,-1.18789542670764E-48));
#36907=DIRECTION('center_axis',(0.218887852522913,-0.673667540197498,0.705875451692549));
#36908=DIRECTION('ref_axis',(0.218125006053852,-0.671328261761447,-0.708335970210719));
#36909=DIRECTION('center_axis',(5.15167520928809E-67,-1.18789542670764E-48,
-1.));
#36910=DIRECTION('ref_axis',(-4.33680868994202E-19,1.,-1.18789542670764E-48));
#36911=DIRECTION('center_axis',(0.271068063822855,-0.654416196007407,0.705876439030603));
#36912=DIRECTION('ref_axis',(0.270125073931967,-0.65214568281518,-0.708334986301518));
#36913=DIRECTION('center_axis',(5.15167520928809E-67,-1.18789542670764E-48,
-1.));
#36914=DIRECTION('ref_axis',(-4.33680868994202E-19,1.,-1.18789542670764E-48));
#36915=DIRECTION('center_axis',(0.321577003370555,-0.631130405143931,0.705877214964523));
#36916=DIRECTION('ref_axis',(0.320459697262731,-0.628942147608601,-0.708334213060304));
#36917=DIRECTION('center_axis',(5.15167520928809E-67,-1.18789542670764E-48,
-1.));
#36918=DIRECTION('ref_axis',(-4.33680868994202E-19,1.,-1.18789542670764E-48));
#36919=DIRECTION('center_axis',(0.370103289326652,-0.603953677099404,0.705877830185721));
#36920=DIRECTION('ref_axis',(0.368818543504099,-0.601860775526205,-0.708333599972859));
#36921=DIRECTION('center_axis',(5.15167520928809E-67,-1.18789542670764E-48,
-1.));
#36922=DIRECTION('ref_axis',(-4.33680868994202E-19,1.,-1.18789542670764E-48));
#36923=DIRECTION('center_axis',(0.416347757295498,-0.573053525770462,0.705878319256975));
#36924=DIRECTION('ref_axis',(0.414903461782555,-0.571068576441932,-0.708333112597058));
#36925=DIRECTION('center_axis',(5.15167520928809E-67,-1.18789542670764E-48,
-1.));
#36926=DIRECTION('ref_axis',(-4.33680868994202E-19,1.,-1.18789542670764E-48));
#36927=DIRECTION('center_axis',(0.460025307051016,-0.538620431161506,0.705878706300177));
#36928=DIRECTION('ref_axis',(0.458430320957564,-0.536755427393206,-0.708332726895123));
#36929=DIRECTION('center_axis',(5.15167520928809E-67,-1.18789542670764E-48,
-1.));
#36930=DIRECTION('ref_axis',(-4.33680868994202E-19,1.,-1.18789542670764E-48));
#36931=DIRECTION('center_axis',(0.500866661619323,-0.500866661619323,0.705879008440277));
#36932=DIRECTION('ref_axis',(0.499130761357991,-0.499132905771573,-0.708332425801768));
#36933=DIRECTION('center_axis',(5.15167520928809E-67,-1.18789542670764E-48,
-1.));
#36934=DIRECTION('ref_axis',(-4.33680868994202E-19,1.,-1.18789542670764E-48));
#36935=DIRECTION('center_axis',(0.53862002836901,-0.46002496303376,0.705879237848482));
#36936=DIRECTION('ref_axis',(0.536753849182443,-0.458432987266868,-0.708332197188161));
#36937=DIRECTION('center_axis',(5.15167520928809E-67,-1.18789542670764E-48,
-1.));
#36938=DIRECTION('ref_axis',(-4.33680868994202E-19,1.,-1.18789542670764E-48));
#36939=DIRECTION('center_axis',(0.573052651970297,-0.416347122442612,0.705879403087785));
#36940=DIRECTION('ref_axis',(0.571067623542823,-0.414906617259439,-0.708332032521106));
#36941=DIRECTION('center_axis',(5.15167520928809E-67,-1.18789542670764E-48,
-1.));
#36942=DIRECTION('ref_axis',(-4.33680868994202E-19,1.,-1.18789542670764E-48));
#36943=DIRECTION('center_axis',(0.603952249837211,-0.370102414699222,0.705879509938047));
#36944=DIRECTION('ref_axis',(0.601860526500507,-0.368822164724135,-0.708331926040847));
#36945=DIRECTION('center_axis',(5.15167520928809E-67,-1.18789542670764E-48,
-1.));
#36946=DIRECTION('ref_axis',(-4.33680868994202E-19,1.,-1.18789542670764E-48));
#36947=DIRECTION('center_axis',(0.631128321247012,-0.321575941572045,0.705879561909807));
#36948=DIRECTION('ref_axis',(0.628942707293582,-0.320463768412346,-0.708331874249054));
#36949=DIRECTION('center_axis',(5.15167520928809E-67,-1.18789542670764E-48,
-1.));
#36950=DIRECTION('ref_axis',(-4.33680868994202E-19,1.,-1.18789542670764E-48));
#36951=DIRECTION('center_axis',(0.654413322126613,-0.271066873422487,0.70587956051735));
#36952=DIRECTION('ref_axis',(0.652147192704133,-0.270129585579022,-0.708331875636714));
#36953=DIRECTION('center_axis',(5.15167520928809E-67,-1.18789542670764E-48,
-1.));
#36954=DIRECTION('ref_axis',(-4.33680868994202E-19,1.,-1.18789542670764E-48));
#36955=DIRECTION('center_axis',(0.673663698306673,-0.218886604216949,0.705879505353533));
#36956=DIRECTION('ref_axis',(0.671330916306432,-0.218129954133086,-0.708331930609559));
#36957=DIRECTION('center_axis',(5.15167520928809E-67,-1.18789542670764E-48,
-1.));
#36958=DIRECTION('ref_axis',(-4.33680868994202E-19,1.,-1.18789542670764E-48));
#36959=DIRECTION('center_axis',(0.688760770927107,-0.165356831187235,0.705879393955946));
#36960=DIRECTION('ref_axis',(0.686375600198304,-0.164785479532649,-0.708332041621451));
#36961=DIRECTION('center_axis',(5.15167520928809E-67,-1.18789542670764E-48,
-1.));
#36962=DIRECTION('ref_axis',(-4.33680868994202E-19,1.,-1.18789542670764E-48));
#36963=DIRECTION('center_axis',(0.699611468639781,-0.110807570905153,0.705879221381242));
#36964=DIRECTION('ref_axis',(0.697188483633051,-0.110425058152577,-0.708332213598567));
#36965=DIRECTION('center_axis',(5.15167520928809E-67,-1.18789542670764E-48,
-1.));
#36966=DIRECTION('ref_axis',(-4.33680868994202E-19,1.,-1.18789542670764E-48));
#36967=DIRECTION('center_axis',(0.706148902304913,-0.0555751238837372,0.705878979272562));
#36968=DIRECTION('ref_axis',(0.703702893729778,-0.0553838490533553,-0.708332454868737));
#36969=DIRECTION('center_axis',(5.15167520928809E-67,-1.18789542670764E-48,
-1.));
#36970=DIRECTION('ref_axis',(-4.33680868994202E-19,1.,-1.18789542670764E-48));
#36971=DIRECTION('center_axis',(0.708332577472403,3.07190287735134E-19,
0.705878856243267));
#36972=DIRECTION('ref_axis',(0.705878856242412,-1.55615277571261E-6,-0.708332577471545));
#36973=DIRECTION('center_axis',(5.15167520928809E-67,-1.18789542670764E-48,
-1.));
#36974=DIRECTION('ref_axis',(-4.33680868994202E-19,1.,-1.18789542670764E-48));
#36975=DIRECTION('center_axis',(0.706157633406551,0.0555758110364317,0.705870190622399));
#36976=DIRECTION('ref_axis',(0.703694571287442,0.0553775799351074,-0.70834121296245));
#36977=DIRECTION('center_axis',(5.15167520928809E-67,-1.18789542670764E-48,
-1.));
#36978=DIRECTION('ref_axis',(-4.33680868994202E-19,1.,-1.18789542670764E-48));
#36979=DIRECTION('center_axis',(0.699618093637069,0.110808620201609,0.705872490429149));
#36980=DIRECTION('ref_axis',(0.697182591372912,0.11041923309682,-0.708338921173234));
#36981=DIRECTION('center_axis',(5.15167520928809E-67,-1.18789542670764E-48,
-1.));
#36982=DIRECTION('ref_axis',(-4.33680868994202E-19,1.,-1.18789542670764E-48));
#36983=DIRECTION('center_axis',(0.688765827030135,0.165358045050174,0.705874176077209));
#36984=DIRECTION('ref_axis',(0.686371526838244,0.16478009468095,-0.708337241391891));
#36985=DIRECTION('center_axis',(5.15167520928809E-67,-1.18789542670764E-48,
-1.));
#36986=DIRECTION('ref_axis',(-4.33680868994202E-19,1.,-1.18789542670764E-48));
#36987=DIRECTION('center_axis',(0.673667540197388,0.21888785252289,0.705875451692661));
#36988=DIRECTION('ref_axis',(0.671328261761852,0.21812500605297,-0.708335970210607));
#36989=DIRECTION('center_axis',(5.15167520928809E-67,-1.18789542670764E-48,
-1.));
#36990=DIRECTION('ref_axis',(-4.33680868994202E-19,1.,-1.18789542670764E-48));
#36991=DIRECTION('center_axis',(0.654416196007382,0.271068063822859,0.705876439030624));
#36992=DIRECTION('ref_axis',(0.652145682814771,0.270125073933009,-0.708334986301497));
#36993=DIRECTION('center_axis',(5.15167520928809E-67,-1.18789542670764E-48,
-1.));
#36994=DIRECTION('ref_axis',(-4.33680868994202E-19,1.,-1.18789542670764E-48));
#36995=DIRECTION('center_axis',(0.631130405143941,0.321577003370555,0.705877214964514));
#36996=DIRECTION('ref_axis',(0.628942147608526,0.320459697262857,-0.708334213060313));
#36997=DIRECTION('center_axis',(5.15167520928809E-67,-1.18789542670764E-48,
-1.));
#36998=DIRECTION('ref_axis',(-4.33680868994202E-19,1.,-1.18789542670764E-48));
#36999=DIRECTION('center_axis',(0.603953677099555,0.370103289326611,0.705877830185613));
#37000=DIRECTION('ref_axis',(0.601860775525942,0.368818543504321,-0.708333599972967));
#37001=DIRECTION('center_axis',(5.15167520928809E-67,-1.18789542670764E-48,
-1.));
#37002=DIRECTION('ref_axis',(-4.33680868994202E-19,1.,-1.18789542670764E-48));
#37003=DIRECTION('center_axis',(0.573053525770564,0.41634775729573,0.705878319256755));
#37004=DIRECTION('ref_axis',(-0.571068576442187,-0.414903461781831,0.708333112597277));
#37005=DIRECTION('center_axis',(5.15167520928809E-67,-1.18789542670764E-48,
-1.));
#37006=DIRECTION('ref_axis',(-4.33680868994202E-19,1.,-1.18789542670764E-48));
#37007=DIRECTION('center_axis',(0.538620431161647,0.46002530705115,0.705878706299982));
#37008=DIRECTION('ref_axis',(-0.536755427393011,-0.458430320957492,0.708332726895318));
#37009=DIRECTION('center_axis',(5.15167520928809E-67,-1.18789542670764E-48,
-1.));
#37010=DIRECTION('ref_axis',(-4.33680868994202E-19,1.,-1.18789542670764E-48));
#37011=DIRECTION('center_axis',(0.500866661619527,0.500866661619527,0.705879008439988));
#37012=DIRECTION('ref_axis',(-0.49913290577155,-0.499130761357605,0.708332425802057));
#37013=DIRECTION('center_axis',(5.15167520928809E-67,-1.18789542670764E-48,
-1.));
#37014=DIRECTION('ref_axis',(-4.33680868994202E-19,1.,-1.18789542670764E-48));
#37015=DIRECTION('center_axis',(0.460024963033642,0.538620028368862,0.705879237848672));
#37016=DIRECTION('ref_axis',(-0.45843298726639,-0.536753849183101,0.708332197187972));
#37017=DIRECTION('center_axis',(5.15167520928809E-67,-1.18789542670764E-48,
-1.));
#37018=DIRECTION('ref_axis',(-4.33680868994202E-19,1.,-1.18789542670764E-48));
#37019=DIRECTION('center_axis',(0.416347122442686,0.573052651970292,0.705879403087744));
#37020=DIRECTION('ref_axis',(-0.414906617258984,-0.571067623543104,0.708332032521146));
#37021=DIRECTION('center_axis',(5.15167520928809E-67,-1.18789542670764E-48,
-1.));
#37022=DIRECTION('ref_axis',(-4.33680868994202E-19,1.,-1.18789542670764E-48));
#37023=DIRECTION('center_axis',(0.370102414699172,0.603952249837277,0.705879509938016));
#37024=DIRECTION('ref_axis',(-0.368822164724246,-0.601860526500403,0.708331926040877));
#37025=DIRECTION('center_axis',(5.15167520928809E-67,-1.18789542670764E-48,
-1.));
#37026=DIRECTION('ref_axis',(-4.33680868994202E-19,1.,-1.18789542670764E-48));
#37027=DIRECTION('center_axis',(0.321575941571924,0.631128321246917,0.705879561909948));
#37028=DIRECTION('ref_axis',(-0.320463768412656,-0.628942707293582,0.708331874248914));
#37029=DIRECTION('center_axis',(5.15167520928809E-67,-1.18789542670764E-48,
-1.));
#37030=DIRECTION('ref_axis',(-4.33680868994202E-19,1.,-1.18789542670764E-48));
#37031=DIRECTION('center_axis',(0.271066873422485,0.654413322126598,0.705879560517365));
#37032=DIRECTION('ref_axis',(-0.270129585579224,-0.652147192704065,0.708331875636699));
#37033=DIRECTION('center_axis',(5.15167520928809E-67,-1.18789542670764E-48,
-1.));
#37034=DIRECTION('ref_axis',(-4.33680868994202E-19,1.,-1.18789542670764E-48));
#37035=DIRECTION('center_axis',(0.218886604216952,0.67366369830668,0.705879505353526));
#37036=DIRECTION('ref_axis',(-0.218129954132996,-0.671330916306453,0.708331930609566));
#37037=DIRECTION('center_axis',(5.15167520928809E-67,-1.18789542670764E-48,
-1.));
#37038=DIRECTION('ref_axis',(-4.33680868994202E-19,1.,-1.18789542670764E-48));
#37039=DIRECTION('center_axis',(0.16535683118711,0.68876077092705,0.705879393956031));
#37040=DIRECTION('ref_axis',(-0.164785479532882,-0.686375600198336,0.708332041621366));
#37041=DIRECTION('center_axis',(5.15167520928809E-67,-1.18789542670764E-48,
-1.));
#37042=DIRECTION('ref_axis',(-4.33680868994202E-19,1.,-1.18789542670764E-48));
#37043=DIRECTION('center_axis',(0.110807570905159,0.699611468639805,0.705879221381218));
#37044=DIRECTION('ref_axis',(-0.11042505815257,-0.697188483633028,0.708332213598592));
#37045=DIRECTION('center_axis',(5.15167520928809E-67,-1.18789542670764E-48,
-1.));
#37046=DIRECTION('ref_axis',(-4.33680868994202E-19,1.,-1.18789542670764E-48));
#37047=DIRECTION('center_axis',(0.055575123883674,0.706148902304893,0.705878979272587));
#37048=DIRECTION('ref_axis',(-0.0553838490533958,-0.7037028937298,0.708332454868712));
#37049=DIRECTION('center_axis',(5.15167520928809E-67,-1.18789542670764E-48,
-1.));
#37050=DIRECTION('ref_axis',(-4.33680868994202E-19,1.,-1.18789542670764E-48));
#37051=DIRECTION('center_axis',(4.84352581305682E-13,0.70837017493119,0.705841126081468));
#37052=DIRECTION('ref_axis',(-1.41156745807278E-12,-0.705841126081468,0.70837017493119));
#37053=DIRECTION('center_axis',(5.15167520928809E-67,-1.18789542670764E-48,
-1.));
#37054=DIRECTION('ref_axis',(-4.33680868994202E-19,1.,-1.18789542670764E-48));
#37055=DIRECTION('center_axis',(-0.0555758110363152,0.706157633406656,0.705870190622303));
#37056=DIRECTION('ref_axis',(0.0553775799350914,-0.703694571287347,0.708341212962545));
#37057=DIRECTION('center_axis',(5.15167520928809E-67,-1.18789542670764E-48,
-1.));
#37058=DIRECTION('ref_axis',(-4.33680868994202E-19,1.,-1.18789542670764E-48));
#37059=DIRECTION('center_axis',(-0.110808620201596,0.699618093636976,0.705872490429243));
#37060=DIRECTION('ref_axis',(0.11041923309583,-0.697182591373165,0.70833892117314));
#37061=DIRECTION('center_axis',(5.15167520928809E-67,-1.18789542670764E-48,
-1.));
#37062=DIRECTION('ref_axis',(-4.33680868994202E-19,1.,-1.18789542670764E-48));
#37063=DIRECTION('center_axis',(-0.165358045050154,0.688765827030126,0.705874176077223));
#37064=DIRECTION('ref_axis',(0.164780094680844,-0.686371526838284,0.708337241391878));
#37065=DIRECTION('center_axis',(5.15167520928809E-67,-1.18789542670764E-48,
-1.));
#37066=DIRECTION('ref_axis',(-4.33680868994202E-19,1.,-1.18789542670764E-48));
#37067=DIRECTION('center_axis',(-0.218887852522867,0.673667540197309,0.705875451692744));
#37068=DIRECTION('ref_axis',(0.218125006054104,-0.67132826176157,0.708335970210525));
#37069=DIRECTION('center_axis',(5.15167520928809E-67,-1.18789542670764E-48,
-1.));
#37070=DIRECTION('ref_axis',(-4.33680868994202E-19,1.,-1.18789542670764E-48));
#37071=DIRECTION('center_axis',(-0.271068063822887,0.654416196007496,0.705876439030507));
#37072=DIRECTION('ref_axis',(0.270125073932604,-0.652145682814813,0.708334986301614));
#37073=DIRECTION('center_axis',(5.15167520928809E-67,-1.18789542670764E-48,
-1.));
#37074=DIRECTION('ref_axis',(-4.33680868994202E-19,1.,-1.18789542670764E-48));
#37075=DIRECTION('center_axis',(5.15167520928809E-67,-1.18789542670764E-48,
-1.));
#37076=DIRECTION('ref_axis',(-4.33680868994202E-19,1.,-1.18789542670764E-48));
#37077=DIRECTION('center_axis',(5.15167520928809E-67,-1.18789542670764E-48,
-1.));
#37078=DIRECTION('ref_axis',(-4.33680868994202E-19,1.,-1.18789542670764E-48));
#37079=DIRECTION('center_axis',(5.15167520928809E-67,-1.18789542670764E-48,
-1.));
#37080=DIRECTION('ref_axis',(-4.33680868994202E-19,1.,-1.18789542670764E-48));
#37081=DIRECTION('center_axis',(5.15167520928809E-67,-1.18789542670764E-48,
-1.));
#37082=DIRECTION('ref_axis',(-4.33680868994202E-19,1.,-1.18789542670764E-48));
#37083=DIRECTION('center_axis',(5.15167520928809E-67,-1.18789542670764E-48,
-1.));
#37084=DIRECTION('ref_axis',(-4.33680868994202E-19,1.,-1.18789542670764E-48));
#37085=DIRECTION('center_axis',(5.15167520928809E-67,-1.18789542670764E-48,
-1.));
#37086=DIRECTION('ref_axis',(-4.33680868994202E-19,1.,-1.18789542670764E-48));
#37087=DIRECTION('center_axis',(5.15167520928809E-67,-1.18789542670764E-48,
-1.));
#37088=DIRECTION('ref_axis',(-4.33680868994202E-19,1.,-1.18789542670764E-48));
#37089=DIRECTION('center_axis',(5.15167520928809E-67,-1.18789542670764E-48,
-1.));
#37090=DIRECTION('ref_axis',(-4.33680868994202E-19,1.,-1.18789542670764E-48));
#37091=DIRECTION('center_axis',(5.15167520928809E-67,-1.18789542670764E-48,
-1.));
#37092=DIRECTION('ref_axis',(-4.33680868994202E-19,1.,-1.18789542670764E-48));
#37093=DIRECTION('center_axis',(5.15167520928809E-67,-1.18789542670764E-48,
-1.));
#37094=DIRECTION('ref_axis',(-4.33680868994202E-19,1.,-1.18789542670764E-48));
#37095=DIRECTION('center_axis',(5.15167520928809E-67,-1.18789542670764E-48,
-1.));
#37096=DIRECTION('ref_axis',(-4.33680868994202E-19,1.,-1.18789542670764E-48));
#37097=DIRECTION('center_axis',(5.15167520928809E-67,-1.18789542670764E-48,
-1.));
#37098=DIRECTION('ref_axis',(-4.33680868994202E-19,1.,-1.18789542670764E-48));
#37099=DIRECTION('center_axis',(5.15167520928809E-67,-1.18789542670764E-48,
-1.));
#37100=DIRECTION('ref_axis',(-4.33680868994202E-19,1.,-1.18789542670764E-48));
#37101=DIRECTION('center_axis',(5.15167520928809E-67,-1.18789542670764E-48,
-1.));
#37102=DIRECTION('ref_axis',(-4.33680868994202E-19,1.,-1.18789542670764E-48));
#37103=DIRECTION('center_axis',(5.15167520928809E-67,-1.18789542670764E-48,
-1.));
#37104=DIRECTION('ref_axis',(-4.33680868994202E-19,1.,-1.18789542670764E-48));
#37105=DIRECTION('center_axis',(-0.7061576334064,-0.0555758110363729,0.705870190622555));
#37106=DIRECTION('ref_axis',(0.703694571287618,0.0553775799348557,0.708341212962294));
#37107=DIRECTION('center_axis',(5.15167520928809E-67,-1.18789542670764E-48,
-1.));
#37108=DIRECTION('ref_axis',(-4.33680868994202E-19,1.,-1.18789542670764E-48));
#37109=DIRECTION('center_axis',(-0.699618093637056,-0.110808620201623,0.70587249042916));
#37110=DIRECTION('ref_axis',(0.697182591373085,0.110419233095803,0.708338921173223));
#37111=DIRECTION('center_axis',(5.15167520928809E-67,-1.18789542670764E-48,
-1.));
#37112=DIRECTION('ref_axis',(-4.33680868994202E-19,1.,-1.18789542670764E-48));
#37113=DIRECTION('center_axis',(-0.68876582703002,-0.165358045050145,0.705874176077329));
#37114=DIRECTION('ref_axis',(0.686371526838198,0.164780094681657,0.708337241391772));
#37115=DIRECTION('center_axis',(5.15167520928809E-67,-1.18789542670764E-48,
-1.));
#37116=DIRECTION('ref_axis',(-4.33680868994202E-19,1.,-1.18789542670764E-48));
#37117=DIRECTION('center_axis',(-0.673667540197642,-0.218887852522971,0.705875451692394));
#37118=DIRECTION('ref_axis',(0.671328261761337,0.218125006053688,0.708335970210874));
#37119=DIRECTION('center_axis',(5.15167520928809E-67,-1.18789542670764E-48,
-1.));
#37120=DIRECTION('ref_axis',(-4.33680868994202E-19,1.,-1.18789542670764E-48));
#37121=DIRECTION('center_axis',(-0.654416196007479,-0.271068063822885,0.705876439030525));
#37122=DIRECTION('ref_axis',(0.652145682815046,0.270125073932086,0.708334986301596));
#37123=DIRECTION('center_axis',(5.15167520928809E-67,-1.18789542670764E-48,
-1.));
#37124=DIRECTION('ref_axis',(-4.33680868994202E-19,1.,-1.18789542670764E-48));
#37125=DIRECTION('center_axis',(-0.631130405143739,-0.321577003370466,0.705877214964735));
#37126=DIRECTION('ref_axis',(0.628942147608447,0.3204596972635,0.708334213060093));
#37127=DIRECTION('center_axis',(5.15167520928809E-67,-1.18789542670764E-48,
-1.));
#37128=DIRECTION('ref_axis',(-4.33680868994202E-19,1.,-1.18789542670764E-48));
#37129=DIRECTION('center_axis',(-0.603953677099563,-0.37010328932661,0.705877830185607));
#37130=DIRECTION('ref_axis',(0.601860775526009,0.3688185435042,0.708333599972973));
#37131=DIRECTION('center_axis',(5.15167520928809E-67,-1.18789542670764E-48,
-1.));
#37132=DIRECTION('ref_axis',(-4.33680868994202E-19,1.,-1.18789542670764E-48));
#37133=DIRECTION('center_axis',(-0.573053525770468,-0.416347757295655,0.705878319256877));
#37134=DIRECTION('ref_axis',(-0.571068576442267,-0.414903461781928,-0.708333112597156));
#37135=DIRECTION('center_axis',(5.15167520928809E-67,-1.18789542670764E-48,
-1.));
#37136=DIRECTION('ref_axis',(-4.33680868994202E-19,1.,-1.18789542670764E-48));
#37137=DIRECTION('center_axis',(-0.5386204311615,-0.460025307051025,0.705878706300176));
#37138=DIRECTION('ref_axis',(-0.53675542739315,-0.458430320957627,-0.708332726895124));
#37139=DIRECTION('center_axis',(5.15167520928809E-67,-1.18789542670764E-48,
-1.));
#37140=DIRECTION('ref_axis',(-4.33680868994202E-19,1.,-1.18789542670764E-48));
#37141=DIRECTION('center_axis',(-0.500866661619536,-0.500866661619512,0.705879008439992));
#37142=DIRECTION('ref_axis',(-0.499132905770748,-0.499130761358414,-0.708332425802052));
#37143=DIRECTION('center_axis',(5.15167520928809E-67,-1.18789542670764E-48,
-1.));
#37144=DIRECTION('ref_axis',(-4.33680868994202E-19,1.,-1.18789542670764E-48));
#37145=DIRECTION('center_axis',(-0.460024963033767,-0.538620028369008,0.70587923784848));
#37146=DIRECTION('ref_axis',(-0.45843298726701,-0.536753849182318,-0.708332197188163));
#37147=DIRECTION('center_axis',(5.15167520928809E-67,-1.18789542670764E-48,
-1.));
#37148=DIRECTION('ref_axis',(-4.33680868994202E-19,1.,-1.18789542670764E-48));
#37149=DIRECTION('center_axis',(-0.416347122442742,-0.573052651970378,0.705879403087642));
#37150=DIRECTION('ref_axis',(-0.414906617259033,-0.571067623542942,-0.708332032521248));
#37151=DIRECTION('center_axis',(5.15167520928809E-67,-1.18789542670764E-48,
-1.));
#37152=DIRECTION('ref_axis',(-4.33680868994202E-19,1.,-1.18789542670764E-48));
#37153=DIRECTION('center_axis',(-0.370102414699178,-0.603952249837274,0.705879509938015));
#37154=DIRECTION('ref_axis',(-0.368822164723695,-0.601860526500739,-0.708331926040878));
#37155=DIRECTION('center_axis',(5.15167520928809E-67,-1.18789542670764E-48,
-1.));
#37156=DIRECTION('ref_axis',(-4.33680868994202E-19,1.,-1.18789542670764E-48));
#37157=DIRECTION('center_axis',(-0.321575941572111,-0.631128321247095,0.705879561909702));
#37158=DIRECTION('ref_axis',(-0.320463768412258,-0.628942707293509,-0.708331874249159));
#37159=DIRECTION('center_axis',(5.15167520928809E-67,-1.18789542670764E-48,
-1.));
#37160=DIRECTION('ref_axis',(-4.33680868994202E-19,1.,-1.18789542670764E-48));
#37161=DIRECTION('center_axis',(-0.271066873422704,-0.654413322126826,0.70587956051707));
#37162=DIRECTION('ref_axis',(-0.270129585579653,-0.652147192703568,-0.708331875636993));
#37163=DIRECTION('center_axis',(5.15167520928809E-67,-1.18789542670764E-48,
-1.));
#37164=DIRECTION('ref_axis',(-4.33680868994202E-19,1.,-1.18789542670764E-48));
#37165=DIRECTION('center_axis',(-0.218886604216915,-0.673663698306575,0.705879505353637));
#37166=DIRECTION('ref_axis',(-0.218129954131654,-0.671330916307006,-0.708331930609455));
#37167=DIRECTION('center_axis',(5.15167520928809E-67,-1.18789542670764E-48,
-1.));
#37168=DIRECTION('ref_axis',(-4.33680868994202E-19,1.,-1.18789542670764E-48));
#37169=DIRECTION('center_axis',(-0.165356831187205,-0.688760770926913,0.705879393956142));
#37170=DIRECTION('ref_axis',(-0.164785479532657,-0.686375600198504,-0.708332041621255));
#37171=DIRECTION('center_axis',(5.15167520928809E-67,-1.18789542670764E-48,
-1.));
#37172=DIRECTION('ref_axis',(-4.33680868994202E-19,1.,-1.18789542670764E-48));
#37173=DIRECTION('center_axis',(-0.110807570905278,-0.699611468639872,0.705879221381132));
#37174=DIRECTION('ref_axis',(-0.110425058152835,-0.697188483632899,-0.708332213598677));
#37175=DIRECTION('center_axis',(5.15167520928809E-67,-1.18789542670764E-48,
-1.));
#37176=DIRECTION('ref_axis',(-4.33680868994202E-19,1.,-1.18789542670764E-48));
#37177=DIRECTION('center_axis',(-0.0555751238837442,-0.706148902305009,
0.705878979272465));
#37178=DIRECTION('ref_axis',(-0.0553838490528384,-0.703702893729722,-0.708332454868834));
#37179=DIRECTION('center_axis',(5.15167520928809E-67,-1.18789542670764E-48,
-1.));
#37180=DIRECTION('ref_axis',(-4.33680868994202E-19,1.,-1.18789542670764E-48));
#37181=DIRECTION('',(8.62889469402126E-17,0.707106781186547,0.707106781186548));
#37182=DIRECTION('center_axis',(-5.15167520928809E-67,1.18789542670764E-48,
1.));
#37183=DIRECTION('ref_axis',(4.33680868994202E-19,-1.,1.18789542670764E-48));
#37184=DIRECTION('center_axis',(5.15167520928809E-67,-1.18789542670764E-48,
-1.));
#37185=DIRECTION('ref_axis',(-4.33680868994202E-19,1.,-1.18789542670764E-48));
#37186=DIRECTION('center_axis',(0.0555758110363494,0.706157633406676,-0.705870190622281));
#37187=DIRECTION('ref_axis',(0.0553775799347821,0.703694571287349,0.708341212962568));
#37188=DIRECTION('center_axis',(5.15167520928809E-67,-1.18789542670764E-48,
-1.));
#37189=DIRECTION('ref_axis',(-4.33680868994202E-19,1.,-1.18789542670764E-48));
#37190=DIRECTION('center_axis',(0.110808620201597,0.699618093636782,-0.705872490429435));
#37191=DIRECTION('ref_axis',(0.110419233096536,0.697182591373247,0.708338921172949));
#37192=DIRECTION('center_axis',(5.15167520928809E-67,-1.18789542670764E-48,
-1.));
#37193=DIRECTION('ref_axis',(-4.33680868994202E-19,1.,-1.18789542670764E-48));
#37194=DIRECTION('center_axis',(0.165358045050176,0.688765827030065,-0.705874176077277));
#37195=DIRECTION('ref_axis',(0.164780094681565,0.686371526838166,0.708337241391824));
#37196=DIRECTION('center_axis',(5.15167520928809E-67,-1.18789542670764E-48,
-1.));
#37197=DIRECTION('ref_axis',(-4.33680868994202E-19,1.,-1.18789542670764E-48));
#37198=DIRECTION('center_axis',(0.218887852522828,0.673667540197125,-0.705875451692931));
#37199=DIRECTION('ref_axis',(0.218125006053502,0.671328261761963,0.708335970210338));
#37200=DIRECTION('center_axis',(5.15167520928809E-67,-1.18789542670764E-48,
-1.));
#37201=DIRECTION('ref_axis',(-4.33680868994202E-19,1.,-1.18789542670764E-48));
#37202=DIRECTION('center_axis',(0.271068063822916,0.654416196007463,-0.705876439030527));
#37203=DIRECTION('ref_axis',(0.270125073931817,0.65214568281516,0.708334986301594));
#37204=DIRECTION('center_axis',(5.15167520928809E-67,-1.18789542670764E-48,
-1.));
#37205=DIRECTION('ref_axis',(-4.33680868994202E-19,1.,-1.18789542670764E-48));
#37206=DIRECTION('center_axis',(0.321577003370433,0.631130405143686,-0.705877214964798));
#37207=DIRECTION('ref_axis',(0.320459697263181,0.62894214760868,0.70833421306003));
#37208=DIRECTION('center_axis',(5.15167520928809E-67,-1.18789542670764E-48,
-1.));
#37209=DIRECTION('ref_axis',(-4.33680868994202E-19,1.,-1.18789542670764E-48));
#37210=DIRECTION('center_axis',(0.37010328932647,0.603953677099309,-0.705877830185898));
#37211=DIRECTION('ref_axis',(0.368818543504439,0.601860775526204,0.708333599972683));
#37212=DIRECTION('center_axis',(5.15167520928809E-67,-1.18789542670764E-48,
-1.));
#37213=DIRECTION('ref_axis',(-4.33680868994202E-19,1.,-1.18789542670764E-48));
#37214=DIRECTION('center_axis',(0.416347757295563,0.573053525770315,-0.705878319257056));
#37215=DIRECTION('ref_axis',(0.414903461782186,0.5710685764423,0.708333112596977));
#37216=DIRECTION('center_axis',(5.15167520928809E-67,-1.18789542670764E-48,
-1.));
#37217=DIRECTION('ref_axis',(-4.33680868994202E-19,1.,-1.18789542670764E-48));
#37218=DIRECTION('center_axis',(0.46002530705103,0.538620431161473,-0.705878706300193));
#37219=DIRECTION('ref_axis',(0.458430320957387,0.536755427393379,0.708332726895108));
#37220=DIRECTION('center_axis',(5.15167520928809E-67,-1.18789542670764E-48,
-1.));
#37221=DIRECTION('ref_axis',(-4.33680868994202E-19,1.,-1.18789542670764E-48));
#37222=DIRECTION('center_axis',(0.500866661619595,0.500866661619595,-0.705879008439891));
#37223=DIRECTION('ref_axis',(0.499130761358023,0.499132905770996,0.708332425802153));
#37224=DIRECTION('center_axis',(5.15167520928809E-67,-1.18789542670764E-48,
-1.));
#37225=DIRECTION('ref_axis',(-4.33680868994202E-19,1.,-1.18789542670764E-48));
#37226=DIRECTION('center_axis',(0.538620028368889,0.460024963033635,-0.705879237848656));
#37227=DIRECTION('ref_axis',(0.536753849182959,0.458432987266531,0.708332197187987));
#37228=DIRECTION('center_axis',(5.15167520928809E-67,-1.18789542670764E-48,
-1.));
#37229=DIRECTION('ref_axis',(-4.33680868994202E-19,1.,-1.18789542670764E-48));
#37230=DIRECTION('center_axis',(0.573052651970233,0.416347122442629,-0.705879403087826));
#37231=DIRECTION('ref_axis',(0.57106762354309,0.414906617259142,0.708332032521065));
#37232=DIRECTION('center_axis',(5.15167520928809E-67,-1.18789542670764E-48,
-1.));
#37233=DIRECTION('ref_axis',(-4.33680868994202E-19,1.,-1.18789542670764E-48));
#37234=DIRECTION('center_axis',(0.603952249837032,0.370102414699012,-0.70587950993831));
#37235=DIRECTION('ref_axis',(0.601860526500475,0.36882216472469,0.708331926040585));
#37236=DIRECTION('center_axis',(5.15167520928809E-67,-1.18789542670764E-48,
-1.));
#37237=DIRECTION('ref_axis',(-4.33680868994202E-19,1.,-1.18789542670764E-48));
#37238=DIRECTION('center_axis',(0.631128321246922,0.32157594157199,-0.705879561909913));
#37239=DIRECTION('ref_axis',(0.628942707293632,0.32046376841248,0.708331874248949));
#37240=DIRECTION('center_axis',(5.15167520928809E-67,-1.18789542670764E-48,
-1.));
#37241=DIRECTION('ref_axis',(-4.33680868994202E-19,1.,-1.18789542670764E-48));
#37242=DIRECTION('center_axis',(0.654413322126609,0.271066873422466,-0.705879560517362));
#37243=DIRECTION('ref_axis',(0.652147192704168,0.270129585578968,0.708331875636702));
#37244=DIRECTION('center_axis',(5.15167520928809E-67,-1.18789542670764E-48,
-1.));
#37245=DIRECTION('ref_axis',(-4.33680868994202E-19,1.,-1.18789542670764E-48));
#37246=DIRECTION('center_axis',(0.673663698306398,0.218886604216837,-0.70587950535383));
#37247=DIRECTION('ref_axis',(0.671330916306662,0.218129954133339,0.708331930609263));
#37248=DIRECTION('center_axis',(5.15167520928809E-67,-1.18789542670764E-48,
-1.));
#37249=DIRECTION('ref_axis',(-4.33680868994202E-19,1.,-1.18789542670764E-48));
#37250=DIRECTION('center_axis',(0.688760770927087,0.165356831187229,-0.705879393955967));
#37251=DIRECTION('ref_axis',(0.686375600198292,0.164785479532791,0.70833204162143));
#37252=DIRECTION('center_axis',(5.15167520928809E-67,-1.18789542670764E-48,
-1.));
#37253=DIRECTION('ref_axis',(-4.33680868994202E-19,1.,-1.18789542670764E-48));
#37254=DIRECTION('center_axis',(0.699611468639904,0.110807570905141,-0.705879221381122));
#37255=DIRECTION('ref_axis',(0.697188483632864,0.11042505815299,0.708332213598687));
#37256=DIRECTION('center_axis',(5.15167520928809E-67,-1.18789542670764E-48,
-1.));
#37257=DIRECTION('ref_axis',(-4.33680868994202E-19,1.,-1.18789542670764E-48));
#37258=DIRECTION('center_axis',(0.706148902304704,0.0555751238836885,-0.705878979272775));
#37259=DIRECTION('ref_axis',(0.703702893729991,0.0553838490533688,0.708332454868525));
#37260=DIRECTION('center_axis',(5.15167520928809E-67,-1.18789542670764E-48,
-1.));
#37261=DIRECTION('ref_axis',(-4.33680868994202E-19,1.,-1.18789542670764E-48));
#37262=DIRECTION('center_axis',(0.708332577472139,3.0719028773502E-19,-0.705878856243532));
#37263=DIRECTION('ref_axis',(0.705878856242677,1.5561538090606E-6,0.708332577471281));
#37264=DIRECTION('center_axis',(5.15167520928809E-67,-1.18789542670764E-48,
-1.));
#37265=DIRECTION('ref_axis',(-4.33680868994202E-19,1.,-1.18789542670764E-48));
#37266=DIRECTION('center_axis',(0.706157633406651,-0.0555758110363464,-0.705870190622306));
#37267=DIRECTION('ref_axis',(0.703694571287399,-0.0553775799344575,0.708341212962543));
#37268=DIRECTION('center_axis',(5.15167520928809E-67,-1.18789542670764E-48,
-1.));
#37269=DIRECTION('ref_axis',(-4.33680868994202E-19,1.,-1.18789542670764E-48));
#37270=DIRECTION('center_axis',(0.699618093636944,-0.110808620201621,-0.705872490429271));
#37271=DIRECTION('ref_axis',(0.697182591373154,-0.110419233096072,0.708338921173112));
#37272=DIRECTION('center_axis',(5.15167520928809E-67,-1.18789542670764E-48,
-1.));
#37273=DIRECTION('ref_axis',(-4.33680868994202E-19,1.,-1.18789542670764E-48));
#37274=DIRECTION('center_axis',(0.688765827030149,-0.165358045050179,-0.705874176077195));
#37275=DIRECTION('ref_axis',(0.686371526838092,-0.164780094681522,0.708337241391906));
#37276=DIRECTION('center_axis',(5.15167520928809E-67,-1.18789542670764E-48,
-1.));
#37277=DIRECTION('ref_axis',(-4.33680868994202E-19,1.,-1.18789542670764E-48));
#37278=DIRECTION('center_axis',(0.673667540197491,-0.218887852522947,-0.705875451692545));
#37279=DIRECTION('ref_axis',(0.671328261761432,-0.218125006053886,0.708335970210723));
#37280=DIRECTION('center_axis',(5.15167520928809E-67,-1.18789542670764E-48,
-1.));
#37281=DIRECTION('ref_axis',(-4.33680868994202E-19,1.,-1.18789542670764E-48));
#37282=DIRECTION('center_axis',(0.654416196007489,-0.271068063822922,-0.705876439030501));
#37283=DIRECTION('ref_axis',(0.652145682814786,-0.270125073932652,0.70833498630162));
#37284=DIRECTION('center_axis',(5.15167520928809E-67,-1.18789542670764E-48,
-1.));
#37285=DIRECTION('ref_axis',(-4.33680868994202E-19,1.,-1.18789542670764E-48));
#37286=DIRECTION('center_axis',(0.631130405143858,-0.321577003370522,-0.705877214964604));
#37287=DIRECTION('ref_axis',(0.628942147608515,-0.320459697263077,0.708334213060224));
#37288=DIRECTION('center_axis',(5.15167520928809E-67,-1.18789542670764E-48,
-1.));
#37289=DIRECTION('ref_axis',(-4.33680868994202E-19,1.,-1.18789542670764E-48));
#37290=DIRECTION('center_axis',(0.603953677099314,-0.37010328932649,-0.705877830185883));
#37291=DIRECTION('ref_axis',(0.60186077552563,-0.368818543505346,0.708333599972698));
#37292=DIRECTION('center_axis',(5.15167520928809E-67,-1.18789542670764E-48,
-1.));
#37293=DIRECTION('ref_axis',(-4.33680868994202E-19,1.,-1.18789542670764E-48));
#37294=DIRECTION('center_axis',(0.573053525770311,-0.416347757295561,-0.70587831925706));
#37295=DIRECTION('ref_axis',(-0.571068576442179,0.41490346178236,-0.708333112596973));
#37296=DIRECTION('center_axis',(5.15167520928809E-67,-1.18789542670764E-48,
-1.));
#37297=DIRECTION('ref_axis',(-4.33680868994202E-19,1.,-1.18789542670764E-48));
#37298=DIRECTION('center_axis',(0.53862043116148,-0.460025307051029,-0.705878706300189));
#37299=DIRECTION('ref_axis',(-0.536755427393413,0.45843032095734,-0.708332726895112));
#37300=DIRECTION('center_axis',(5.15167520928809E-67,-1.18789542670764E-48,
-1.));
#37301=DIRECTION('ref_axis',(-4.33680868994202E-19,1.,-1.18789542670764E-48));
#37302=DIRECTION('center_axis',(0.500866661619453,-0.500866661619453,-0.705879008440093));
#37303=DIRECTION('ref_axis',(-0.499132905770974,0.49913076135833,-0.708332425801952));
#37304=DIRECTION('center_axis',(5.15167520928809E-67,-1.18789542670764E-48,
-1.));
#37305=DIRECTION('ref_axis',(-4.33680868994202E-19,1.,-1.18789542670764E-48));
#37306=DIRECTION('center_axis',(0.460024963033751,-0.538620028369041,-0.705879237848464));
#37307=DIRECTION('ref_axis',(-0.458432987266724,0.536753849182542,-0.708332197188179));
#37308=DIRECTION('center_axis',(5.15167520928809E-67,-1.18789542670764E-48,
-1.));
#37309=DIRECTION('ref_axis',(-4.33680868994202E-19,1.,-1.18789542670764E-48));
#37310=DIRECTION('center_axis',(0.416347122442499,-0.573052651970059,-0.705879403088044));
#37311=DIRECTION('ref_axis',(-0.414906617258677,0.571067623543698,-0.708332032520848));
#37312=DIRECTION('center_axis',(5.15167520928809E-67,-1.18789542670764E-48,
-1.));
#37313=DIRECTION('ref_axis',(-4.33680868994202E-19,1.,-1.18789542670764E-48));
#37314=DIRECTION('center_axis',(0.370102414698996,-0.603952249837027,-0.705879509938322));
#37315=DIRECTION('ref_axis',(-0.36882216472453,0.601860526500588,-0.708331926040572));
#37316=DIRECTION('center_axis',(5.15167520928809E-67,-1.18789542670764E-48,
-1.));
#37317=DIRECTION('ref_axis',(-4.33680868994202E-19,1.,-1.18789542670764E-48));
#37318=DIRECTION('center_axis',(0.321575941571994,-0.631128321246919,-0.705879561909914));
#37319=DIRECTION('ref_axis',(-0.320463768412686,0.628942707293528,-0.708331874248948));
#37320=DIRECTION('center_axis',(5.15167520928809E-67,-1.18789542670764E-48,
-1.));
#37321=DIRECTION('ref_axis',(-4.33680868994202E-19,1.,-1.18789542670764E-48));
#37322=DIRECTION('center_axis',(0.27106687342253,-0.654413322126797,-0.705879560517163));
#37323=DIRECTION('ref_axis',(-0.270129585579053,0.652147192703917,-0.7083318756369));
#37324=DIRECTION('center_axis',(5.15167520928809E-67,-1.18789542670764E-48,
-1.));
#37325=DIRECTION('ref_axis',(-4.33680868994202E-19,1.,-1.18789542670764E-48));
#37326=DIRECTION('center_axis',(0.218886604216888,-0.673663698306596,-0.705879505353626));
#37327=DIRECTION('ref_axis',(-0.218129954133397,0.671330916306428,-0.708331930609466));
#37328=DIRECTION('center_axis',(5.15167520928809E-67,-1.18789542670764E-48,
-1.));
#37329=DIRECTION('ref_axis',(-4.33680868994202E-19,1.,-1.18789542670764E-48));
#37330=DIRECTION('center_axis',(0.165356831187193,-0.688760770926925,-0.705879393956133));
#37331=DIRECTION('ref_axis',(-0.164785479532379,0.686375600198561,-0.708332041621264));
#37332=DIRECTION('center_axis',(5.15167520928809E-67,-1.18789542670764E-48,
-1.));
#37333=DIRECTION('ref_axis',(-4.33680868994202E-19,1.,-1.18789542670764E-48));
#37334=DIRECTION('center_axis',(0.110807570905112,-0.699611468639716,-0.705879221381312));
#37335=DIRECTION('ref_axis',(-0.110425058152835,0.697188483633082,-0.708332213598497));
#37336=DIRECTION('center_axis',(5.15167520928809E-67,-1.18789542670764E-48,
-1.));
#37337=DIRECTION('ref_axis',(-4.33680868994202E-19,1.,-1.18789542670764E-48));
#37338=DIRECTION('center_axis',(0.0555751238837179,-0.706148902304883,-0.705878979272593));
#37339=DIRECTION('ref_axis',(-0.0553838490533129,0.703702893729813,-0.708332454868706));
#37340=DIRECTION('center_axis',(5.15167520928809E-67,-1.18789542670764E-48,
-1.));
#37341=DIRECTION('ref_axis',(-4.33680868994202E-19,1.,-1.18789542670764E-48));
#37342=DIRECTION('center_axis',(4.22129745643424E-13,-0.708370174930854,
-0.705841126081805));
#37343=DIRECTION('ref_axis',(-3.47233154276107E-12,0.705841126081805,-0.708370174930854));
#37344=DIRECTION('center_axis',(5.15167520928809E-67,-1.18789542670764E-48,
-1.));
#37345=DIRECTION('ref_axis',(-4.33680868994202E-19,1.,-1.18789542670764E-48));
#37346=DIRECTION('center_axis',(-0.0555758110363383,-0.706157633406556,
-0.705870190622402));
#37347=DIRECTION('ref_axis',(0.0553775799352142,0.703694571287436,-0.708341212962447));
#37348=DIRECTION('center_axis',(5.15167520928809E-67,-1.18789542670764E-48,
-1.));
#37349=DIRECTION('ref_axis',(-4.33680868994202E-19,1.,-1.18789542670764E-48));
#37350=DIRECTION('center_axis',(-0.110808620201578,-0.699618093636773,-0.705872490429447));
#37351=DIRECTION('ref_axis',(0.110419233096311,0.697182591373295,-0.708338921172937));
#37352=DIRECTION('center_axis',(5.15167520928809E-67,-1.18789542670764E-48,
-1.));
#37353=DIRECTION('ref_axis',(-4.33680868994202E-19,1.,-1.18789542670764E-48));
#37354=DIRECTION('center_axis',(-0.165358045050148,-0.688765827029952,-0.705874176077394));
#37355=DIRECTION('ref_axis',(0.164780094682061,0.686371526838168,-0.708337241391707));
#37356=DIRECTION('center_axis',(5.15167520928809E-67,-1.18789542670764E-48,
-1.));
#37357=DIRECTION('ref_axis',(-4.33680868994202E-19,1.,-1.18789542670764E-48));
#37358=DIRECTION('center_axis',(-0.218887852522884,-0.673667540197305,-0.705875451692742));
#37359=DIRECTION('ref_axis',(0.218125006053241,0.671328261761849,-0.708335970210527));
#37360=DIRECTION('center_axis',(5.15167520928809E-67,-1.18789542670764E-48,
-1.));
#37361=DIRECTION('ref_axis',(-4.33680868994202E-19,1.,-1.18789542670764E-48));
#37362=DIRECTION('center_axis',(-0.271068063822912,-0.654416196007481,-0.705876439030512));
#37363=DIRECTION('ref_axis',(0.270125073931987,0.652145682815073,-0.708334986301609));
#37364=DIRECTION('center_axis',(5.15167520928809E-67,-1.18789542670764E-48,
-1.));
#37365=DIRECTION('ref_axis',(-4.33680868994202E-19,1.,-1.18789542670764E-48));
#37366=DIRECTION('center_axis',(-0.321577003370454,-0.631130405143677,-0.705877214964797));
#37367=DIRECTION('ref_axis',(0.32045969726294,0.628942147608801,-0.708334213060031));
#37368=DIRECTION('center_axis',(5.15167520928809E-67,-1.18789542670764E-48,
-1.));
#37369=DIRECTION('ref_axis',(-4.33680868994202E-19,1.,-1.18789542670764E-48));
#37370=DIRECTION('center_axis',(-0.370103289326527,-0.60395367709939,-0.705877830185799));
#37371=DIRECTION('ref_axis',(0.368818543504467,0.601860775526071,-0.708333599972782));
#37372=DIRECTION('center_axis',(5.15167520928809E-67,-1.18789542670764E-48,
-1.));
#37373=DIRECTION('ref_axis',(-4.33680868994202E-19,1.,-1.18789542670764E-48));
#37374=DIRECTION('center_axis',(-0.41634775729562,-0.5730535257704,-0.705878319256953));
#37375=DIRECTION('ref_axis',(0.414903461781904,0.571068576442378,-0.70833311259708));
#37376=DIRECTION('center_axis',(5.15167520928809E-67,-1.18789542670764E-48,
-1.));
#37377=DIRECTION('ref_axis',(-4.33680868994202E-19,1.,-1.18789542670764E-48));
#37378=DIRECTION('center_axis',(-0.460025307050912,-0.538620431161332,-0.705878706300378));
#37379=DIRECTION('ref_axis',(0.458430320957773,0.536755427393291,-0.708332726894923));
#37380=DIRECTION('center_axis',(5.15167520928809E-67,-1.18789542670764E-48,
-1.));
#37381=DIRECTION('ref_axis',(-4.33680868994202E-19,1.,-1.18789542670764E-48));
#37382=DIRECTION('center_axis',(-0.500866661619468,-0.500866661619444,-0.705879008440089));
#37383=DIRECTION('ref_axis',(0.499130761358181,0.499132905771117,-0.708332425801956));
#37384=DIRECTION('center_axis',(5.15167520928809E-67,-1.18789542670764E-48,
-1.));
#37385=DIRECTION('ref_axis',(-4.33680868994202E-19,1.,-1.18789542670764E-48));
#37386=DIRECTION('center_axis',(-0.538620028368883,-0.46002496303363,-0.705879237848664));
#37387=DIRECTION('ref_axis',(0.536753849182796,0.458432987266734,-0.70833219718798));
#37388=DIRECTION('center_axis',(5.15167520928809E-67,-1.18789542670764E-48,
-1.));
#37389=DIRECTION('ref_axis',(-4.33680868994202E-19,1.,-1.18789542670764E-48));
#37390=DIRECTION('center_axis',(-0.573052651970218,-0.416347122442612,-0.705879403087848));
#37391=DIRECTION('ref_axis',(0.571067623543181,0.414906617259055,-0.708332032521043));
#37392=DIRECTION('center_axis',(5.15167520928809E-67,-1.18789542670764E-48,
-1.));
#37393=DIRECTION('ref_axis',(-4.33680868994202E-19,1.,-1.18789542670764E-48));
#37394=DIRECTION('center_axis',(-0.603952249837038,-0.37010241469901,-0.705879509938305));
#37395=DIRECTION('ref_axis',(0.601860526500551,0.368822164724558,-0.708331926040589));
#37396=DIRECTION('center_axis',(5.15167520928809E-67,-1.18789542670764E-48,
-1.));
#37397=DIRECTION('ref_axis',(-4.33680868994202E-19,1.,-1.18789542670764E-48));
#37398=DIRECTION('center_axis',(-0.631128321246897,-0.32157594157199,-0.705879561909935));
#37399=DIRECTION('ref_axis',(0.628942707294004,0.320463768411799,-0.708331874248927));
#37400=DIRECTION('center_axis',(5.15167520928809E-67,-1.18789542670764E-48,
-1.));
#37401=DIRECTION('ref_axis',(-4.33680868994202E-19,1.,-1.18789542670764E-48));
#37402=DIRECTION('center_axis',(-0.654413322126778,-0.271066873422522,-0.705879560517184));
#37403=DIRECTION('ref_axis',(0.65214719270402,0.270129585578859,-0.708331875636879));
#37404=DIRECTION('center_axis',(5.15167520928809E-67,-1.18789542670764E-48,
-1.));
#37405=DIRECTION('ref_axis',(-4.33680868994202E-19,1.,-1.18789542670764E-48));
#37406=DIRECTION('center_axis',(-0.673663698306464,-0.218886604216857,-0.705879505353761));
#37407=DIRECTION('ref_axis',(0.671330916306719,0.218129954132939,-0.708331930609331));
#37408=DIRECTION('center_axis',(5.15167520928809E-67,-1.18789542670764E-48,
-1.));
#37409=DIRECTION('ref_axis',(-4.33680868994202E-19,1.,-1.18789542670764E-48));
#37410=DIRECTION('center_axis',(-0.688760770927255,-0.165356831187267,-0.705879393955794));
#37411=DIRECTION('ref_axis',(0.686375600198197,0.164785479532444,-0.708332041621602));
#37412=DIRECTION('center_axis',(5.15167520928809E-67,-1.18789542670764E-48,
-1.));
#37413=DIRECTION('ref_axis',(-4.33680868994202E-19,1.,-1.18789542670764E-48));
#37414=DIRECTION('center_axis',(-0.699611468639891,-0.110807570905155,-0.705879221381132));
#37415=DIRECTION('ref_axis',(0.697188483632974,0.110425058152362,-0.708332213598677));
#37416=DIRECTION('center_axis',(5.15167520928809E-67,-1.18789542670764E-48,
-1.));
#37417=DIRECTION('ref_axis',(-4.33680868994202E-19,1.,-1.18789542670764E-48));
#37418=DIRECTION('center_axis',(-0.706148902304619,-0.0555751238836977,
-0.705878979272859));
#37419=DIRECTION('ref_axis',(0.703702893730101,0.0553838490530483,-0.708332454868441));
#37420=DIRECTION('center_axis',(5.15167520928809E-67,-1.18789542670764E-48,
-1.));
#37421=DIRECTION('ref_axis',(-4.33680868994202E-19,1.,-1.18789542670764E-48));
#37422=DIRECTION('center_axis',(5.15167520928809E-67,-1.18789542670764E-48,
-1.));
#37423=DIRECTION('ref_axis',(-4.33680868994202E-19,1.,-1.18789542670764E-48));
#37424=DIRECTION('center_axis',(5.15167520928809E-67,-1.18789542670764E-48,
-1.));
#37425=DIRECTION('ref_axis',(-4.33680868994202E-19,1.,-1.18789542670764E-48));
#37426=DIRECTION('center_axis',(5.15167520928809E-67,-1.18789542670764E-48,
-1.));
#37427=DIRECTION('ref_axis',(-4.33680868994202E-19,1.,-1.18789542670764E-48));
#37428=DIRECTION('center_axis',(5.15167520928809E-67,-1.18789542670764E-48,
-1.));
#37429=DIRECTION('ref_axis',(-4.33680868994202E-19,1.,-1.18789542670764E-48));
#37430=DIRECTION('center_axis',(5.15167520928809E-67,-1.18789542670764E-48,
-1.));
#37431=DIRECTION('ref_axis',(-4.33680868994202E-19,1.,-1.18789542670764E-48));
#37432=DIRECTION('center_axis',(5.15167520928809E-67,-1.18789542670764E-48,
-1.));
#37433=DIRECTION('ref_axis',(-4.33680868994202E-19,1.,-1.18789542670764E-48));
#37434=DIRECTION('center_axis',(5.15167520928809E-67,-1.18789542670764E-48,
-1.));
#37435=DIRECTION('ref_axis',(-4.33680868994202E-19,1.,-1.18789542670764E-48));
#37436=DIRECTION('center_axis',(5.15167520928809E-67,-1.18789542670764E-48,
-1.));
#37437=DIRECTION('ref_axis',(-4.33680868994202E-19,1.,-1.18789542670764E-48));
#37438=DIRECTION('center_axis',(5.15167520928809E-67,-1.18789542670764E-48,
-1.));
#37439=DIRECTION('ref_axis',(-4.33680868994202E-19,1.,-1.18789542670764E-48));
#37440=DIRECTION('center_axis',(5.15167520928809E-67,-1.18789542670764E-48,
-1.));
#37441=DIRECTION('ref_axis',(-4.33680868994202E-19,1.,-1.18789542670764E-48));
#37442=DIRECTION('center_axis',(5.15167520928809E-67,-1.18789542670764E-48,
-1.));
#37443=DIRECTION('ref_axis',(-4.33680868994202E-19,1.,-1.18789542670764E-48));
#37444=DIRECTION('center_axis',(5.15167520928809E-67,-1.18789542670764E-48,
-1.));
#37445=DIRECTION('ref_axis',(-4.33680868994202E-19,1.,-1.18789542670764E-48));
#37446=DIRECTION('center_axis',(5.15167520928809E-67,-1.18789542670764E-48,
-1.));
#37447=DIRECTION('ref_axis',(-4.33680868994202E-19,1.,-1.18789542670764E-48));
#37448=DIRECTION('center_axis',(5.15167520928809E-67,-1.18789542670764E-48,
-1.));
#37449=DIRECTION('ref_axis',(-4.33680868994202E-19,1.,-1.18789542670764E-48));
#37450=DIRECTION('center_axis',(5.15167520928809E-67,-1.18789542670764E-48,
-1.));
#37451=DIRECTION('ref_axis',(-4.33680868994202E-19,1.,-1.18789542670764E-48));
#37452=DIRECTION('center_axis',(-0.271066873422527,0.654413322126802,-0.70587956051716));
#37453=DIRECTION('ref_axis',(-0.270129585578839,0.652147192704003,0.708331875636903));
#37454=DIRECTION('center_axis',(5.15167520928809E-67,-1.18789542670764E-48,
-1.));
#37455=DIRECTION('ref_axis',(-4.33680868994202E-19,1.,-1.18789542670764E-48));
#37456=DIRECTION('center_axis',(-0.218886604216929,0.673663698306674,-0.705879505353539));
#37457=DIRECTION('ref_axis',(-0.218129954131946,0.671330916306808,0.708331930609553));
#37458=DIRECTION('center_axis',(5.15167520928809E-67,-1.18789542670764E-48,
-1.));
#37459=DIRECTION('ref_axis',(-4.33680868994202E-19,1.,-1.18789542670764E-48));
#37460=DIRECTION('center_axis',(-0.16535683118721,0.688760770927084,-0.705879393955974));
#37461=DIRECTION('ref_axis',(-0.164785479532737,0.686375600198312,0.708332041621423));
#37462=DIRECTION('center_axis',(5.15167520928809E-67,-1.18789542670764E-48,
-1.));
#37463=DIRECTION('ref_axis',(-4.33680868994202E-19,1.,-1.18789542670764E-48));
#37464=DIRECTION('center_axis',(-0.110807570905113,0.699611468639715,-0.705879221381313));
#37465=DIRECTION('ref_axis',(-0.110425058151779,0.69718848363325,0.708332213598496));
#37466=DIRECTION('center_axis',(5.15167520928809E-67,-1.18789542670764E-48,
-1.));
#37467=DIRECTION('ref_axis',(-4.33680868994202E-19,1.,-1.18789542670764E-48));
#37468=DIRECTION('center_axis',(-0.0555751238836985,0.706148902304822,-0.705878979272656));
#37469=DIRECTION('ref_axis',(-0.0553838490532064,0.703702893729884,0.708332454868643));
#37470=DIRECTION('center_axis',(5.15167520928809E-67,-1.18789542670764E-48,
-1.));
#37471=DIRECTION('ref_axis',(-4.33680868994202E-19,1.,-1.18789542670764E-48));
#37472=DIRECTION('',(8.69022643068848E-17,-0.707106781186538,-0.707106781186557));
#37473=DIRECTION('center_axis',(5.15167520928809E-67,-1.18789542670764E-48,
-1.));
#37474=DIRECTION('ref_axis',(-4.33680868994202E-19,1.,-1.18789542670764E-48));
#37475=DIRECTION('center_axis',(5.15167520928809E-67,-1.18789542670764E-48,
-1.));
#37476=DIRECTION('ref_axis',(-4.33680868994202E-19,1.,-1.18789542670764E-48));
#37477=DIRECTION('center_axis',(5.15167520928809E-67,-1.18789542670764E-48,
-1.));
#37478=DIRECTION('ref_axis',(0.,1.,0.));
#37479=DIRECTION('center_axis',(5.15167520928809E-67,-1.18789542670764E-48,
-1.));
#37480=DIRECTION('ref_axis',(-4.33680868994202E-19,1.,-1.18789542670764E-48));
#37481=DIRECTION('center_axis',(1.,0.,5.15167520928809E-67));
#37482=DIRECTION('ref_axis',(0.,-1.,0.));
#37483=DIRECTION('center_axis',(5.15167520928809E-67,-1.18789542670764E-48,
-1.));
#37484=DIRECTION('ref_axis',(-4.33680868994202E-19,1.,-1.18789542670764E-48));
#37485=DIRECTION('center_axis',(5.15167520928809E-67,-1.18789542670764E-48,
-1.));
#37486=DIRECTION('ref_axis',(-4.33680868994202E-19,1.,-1.18789542670764E-48));
#37487=DIRECTION('',(-5.15167520928809E-67,1.18789542670764E-48,1.));
#37488=DIRECTION('center_axis',(5.15167520928809E-67,-1.18789542670764E-48,
-1.));
#37489=DIRECTION('ref_axis',(0.,1.,0.));
#37490=DIRECTION('center_axis',(5.15167520928809E-67,-1.18789542670764E-48,
-1.));
#37491=DIRECTION('ref_axis',(-4.33680868994202E-19,1.,-1.18789542670764E-48));
#37492=DIRECTION('center_axis',(-1.,0.,-5.15167520928809E-67));
#37493=DIRECTION('ref_axis',(0.,-1.,0.));
#37494=DIRECTION('center_axis',(5.15167520928809E-67,-1.18789542670764E-48,
-1.));
#37495=DIRECTION('ref_axis',(0.,1.,0.));
#37496=DIRECTION('center_axis',(1.,0.,5.15167520928809E-67));
#37497=DIRECTION('ref_axis',(0.,-1.,0.));
#37498=DIRECTION('center_axis',(5.15167520928809E-67,-1.18789542670764E-48,
-1.));
#37499=DIRECTION('ref_axis',(-4.33680868994202E-19,1.,-1.18789542670764E-48));
#37500=DIRECTION('center_axis',(5.15167520928809E-67,-1.18789542670764E-48,
-1.));
#37501=DIRECTION('ref_axis',(0.,1.,0.));
#37502=DIRECTION('center_axis',(-0.726741019926939,-0.686911553067863,9.06501466507717E-5));
#37503=DIRECTION('ref_axis',(0.686840456252471,-0.726663889286196,0.0144837723800636));
#37504=DIRECTION('center_axis',(5.15167520928809E-67,-1.18789542670764E-48,
-1.));
#37505=DIRECTION('ref_axis',(-4.33680868994202E-19,1.,-1.18789542670764E-48));
#37506=DIRECTION('center_axis',(0.0503838293498797,0.99872992276226,0.000105448247773495));
#37507=DIRECTION('ref_axis',(0.998655285166785,-0.0503813543085061,0.012220496982052));
#37508=DIRECTION('center_axis',(5.15167520928809E-67,-1.18789542670764E-48,
-1.));
#37509=DIRECTION('ref_axis',(0.,1.,0.));
#37510=DIRECTION('center_axis',(-0.0281309337977199,0.999604241409737,0.000105448247664664));
#37511=DIRECTION('ref_axis',(0.999529639708461,0.0281275452111534,0.0122204969076063));
#37512=DIRECTION('center_axis',(-0.670606260601171,-0.741813477246852,9.06501467500846E-5));
#37513=DIRECTION('ref_axis',(0.741736547998884,-0.670534945920291,0.0144837723805249));
#37514=DIRECTION('center_axis',(5.15167520928809E-67,-1.18789542670764E-48,
-1.));
#37515=DIRECTION('ref_axis',(-4.33680868994202E-19,1.,-1.18789542670764E-48));
#37516=DIRECTION('center_axis',(5.15167520928809E-67,-1.18789542670764E-48,
-1.));
#37517=DIRECTION('ref_axis',(0.,1.,0.));
#37518=DIRECTION('center_axis',(-0.106472260383779,0.994315667506771,0.000105448247699395));
#37519=DIRECTION('ref_axis',(0.99424156164256,0.106463029061011,0.0122204969504906));
#37520=DIRECTION('center_axis',(-0.610336990679751,-0.792141874660428,9.06501467512865E-5));
#37521=DIRECTION('ref_axis',(0.792059587274889,-0.610271931637935,0.0144837723275367));
#37522=DIRECTION('center_axis',(5.15167520928809E-67,-1.18789542670764E-48,
-1.));
#37523=DIRECTION('ref_axis',(-4.33680868994202E-19,1.,-1.18789542670764E-48));
#37524=DIRECTION('center_axis',(5.15167520928809E-67,-1.18789542670764E-48,
-1.));
#37525=DIRECTION('ref_axis',(0.,1.,0.));
#37526=DIRECTION('center_axis',(-0.18415715007879,0.982896806870144,0.000105448247763879));
#37527=DIRECTION('ref_axis',(0.982823653730846,0.18414213293402,0.0122204969481005));
#37528=DIRECTION('center_axis',(-0.546304790252955,-0.837586454002944,9.06501468511952E-5));
#37529=DIRECTION('ref_axis',(0.837499315807933,-0.546246387960026,0.0144837723631749));
#37530=DIRECTION('center_axis',(5.15167520928809E-67,-1.18789542670764E-48,
-1.));
#37531=DIRECTION('ref_axis',(-4.33680868994202E-19,1.,-1.18789542670764E-48));
#37532=DIRECTION('center_axis',(5.15167520928809E-67,-1.18789542670764E-48,
-1.));
#37533=DIRECTION('ref_axis',(0.,1.,0.));
#37534=DIRECTION('center_axis',(-0.260706649705391,0.965418060572754,0.000105448247684059));
#37535=DIRECTION('ref_axis',(0.965346311171948,0.260685939324359,0.0122204969329739));
#37536=DIRECTION('center_axis',(-0.478904439129961,-0.877867034330466,9.06501466909999E-5));
#37537=DIRECTION('ref_axis',(0.877775582562065,-0.478853053655646,0.0144837723846339));
#37538=DIRECTION('center_axis',(5.15167520928809E-67,-1.18789542670764E-48,
-1.));
#37539=DIRECTION('ref_axis',(-4.33680868994202E-19,1.,-1.18789542670764E-48));
#37540=DIRECTION('center_axis',(5.15167520928809E-67,-1.18789542670764E-48,
-1.));
#37541=DIRECTION('ref_axis',(0.,1.,0.));
#37542=DIRECTION('center_axis',(-0.33564880614276,0.941987190897842,0.000105448247631265));
#37543=DIRECTION('ref_axis',(0.941917287593993,0.335622530211717,0.0122204969563928));
#37544=DIRECTION('center_axis',(-0.408551482887427,-0.912735272471178,9.06501467675252E-5));
#37545=DIRECTION('ref_axis',(0.91264007095957,-0.408507431040139,0.0144837724331839));
#37546=DIRECTION('center_axis',(5.15167520928809E-67,-1.18789542670764E-48,
-1.));
#37547=DIRECTION('ref_axis',(-4.33680868994202E-19,1.,-1.18789542670764E-48));
#37548=DIRECTION('center_axis',(5.15167520928809E-67,-1.18789542670764E-48,
-1.));
#37549=DIRECTION('ref_axis',(0.,1.,0.));
#37550=DIRECTION('center_axis',(-0.408521576075341,0.912748656948662,0.000105448247753309));
#37551=DIRECTION('ref_axis',(0.912681030719062,0.40848989659417,0.0122204969651243));
#37552=DIRECTION('center_axis',(-0.335679670896088,-0.941976194141681,9.06501466394305E-5));
#37553=DIRECTION('ref_axis',(0.941877829837658,-0.335643224270894,0.0144837723450194));
#37554=DIRECTION('center_axis',(5.15167520928809E-67,-1.18789542670764E-48,
-1.));
#37555=DIRECTION('ref_axis',(-4.33680868994202E-19,1.,-1.18789542670764E-48));
#37556=DIRECTION('center_axis',(5.15167520928809E-67,-1.18789542670764E-48,
-1.));
#37557=DIRECTION('ref_axis',(0.,1.,0.));
#37558=DIRECTION('center_axis',(-0.478875674645407,0.877882724009063,0.000105448247283112));
#37559=DIRECTION('ref_axis',(0.877817791790398,0.478838786927794,0.012220497115417));
#37560=DIRECTION('center_axis',(-0.260738282108194,-0.965409519336649,9.06501468435925E-5));
#37561=DIRECTION('ref_axis',(0.965308598687812,-0.260709665410158,0.0144837723364994));
#37562=DIRECTION('center_axis',(5.15167520928809E-67,-1.18789542670764E-48,
-1.));
#37563=DIRECTION('ref_axis',(-4.33680868994202E-19,1.,-1.18789542670764E-48));
#37564=DIRECTION('center_axis',(5.15167520928809E-67,-1.18789542670764E-48,
-1.));
#37565=DIRECTION('ref_axis',(0.,1.,0.));
#37566=DIRECTION('center_axis',(-0.546277345437336,0.837604352151184,0.000105448247639474));
#37567=DIRECTION('ref_axis',(0.837542514276272,0.546235476910692,0.0122204968773897));
#37568=DIRECTION('center_axis',(-0.184189355107295,-0.982890773813505,9.06501468099581E-5));
#37569=DIRECTION('ref_axis',(0.982787919029019,-0.184168744767822,0.0144837723419927));
#37570=DIRECTION('center_axis',(5.15167520928809E-67,-1.18789542670764E-48,
-1.));
#37571=DIRECTION('ref_axis',(-4.33680868994202E-19,1.,-1.18789542670764E-48));
#37572=DIRECTION('center_axis',(5.15167520928809E-67,-1.18789542670764E-48,
-1.));
#37573=DIRECTION('ref_axis',(0.,1.,0.));
#37574=DIRECTION('center_axis',(-0.610311034740724,0.792161870929404,0.000105448247072483));
#37575=DIRECTION('ref_axis',(0.792103508642798,0.610264443533926,0.0122204972891987));
#37576=DIRECTION('center_axis',(-0.106504839483277,-0.994312179825427,9.06501466463657E-5));
#37577=DIRECTION('ref_axis',(0.994208025037708,-0.106492362571804,0.014483772453865));
#37578=DIRECTION('center_axis',(5.15167520928809E-67,-1.18789542670764E-48,
-1.));
#37579=DIRECTION('ref_axis',(-4.33680868994202E-19,1.,-1.18789542670764E-48));
#37580=DIRECTION('center_axis',(5.15167520928809E-67,-1.18789542670764E-48,
-1.));
#37581=DIRECTION('ref_axis',(0.,1.,0.));
#37582=DIRECTION('center_axis',(-0.670581953563772,0.74183544835446,0.000105448247723866));
#37583=DIRECTION('ref_axis',(0.741780921486778,0.670530926933108,0.012220496898794));
#37584=DIRECTION('center_axis',(-0.0281636861068304,-0.999603320606443,
9.06501467794172E-5));
#37585=DIRECTION('ref_axis',(0.999498507966719,-0.0281594195479949,0.0144837724030356));
#37586=DIRECTION('center_axis',(5.15167520928809E-67,-1.18789542670764E-48,
-1.));
#37587=DIRECTION('ref_axis',(-4.33680868994202E-19,1.,-1.18789542670764E-48));
#37588=DIRECTION('center_axis',(5.15167520928809E-67,-1.18789542670764E-48,
-1.));
#37589=DIRECTION('ref_axis',(0.,1.,0.));
#37590=DIRECTION('center_axis',(-0.726718511653027,0.686935363554299,0.000105448247728815));
#37591=DIRECTION('ref_axis',(0.686885008277766,0.726663364191397,0.0122204969332444));
#37592=DIRECTION('center_axis',(0.050351105759542,-0.998731574514065,9.06501467573609E-5));
#37593=DIRECTION('ref_axis',(0.998626750226961,0.0503471356610921,0.014483772362966));
#37594=DIRECTION('center_axis',(5.15167520928809E-67,-1.18789542670764E-48,
-1.));
#37595=DIRECTION('ref_axis',(-4.33680868994202E-19,1.,-1.18789542670764E-48));
#37596=DIRECTION('center_axis',(5.15167520928809E-67,-1.18789542670764E-48,
-1.));
#37597=DIRECTION('ref_axis',(0.,1.,0.));
#37598=DIRECTION('center_axis',(-0.778374608459537,0.627800093808634,0.000105448247783041));
#37599=DIRECTION('ref_axis',(0.627754220580437,0.778315680169477,0.01222049695274));
#37600=DIRECTION('center_axis',(0.128555466315269,-0.991702316152894,9.06501465984867E-5));
#37601=DIRECTION('ref_axis',(0.99159812649388,0.128543284036463,0.0144837724004731));
#37602=DIRECTION('center_axis',(5.15167520928809E-67,-1.18789542670764E-48,
-1.));
#37603=DIRECTION('ref_axis',(-4.33680868994202E-19,1.,-1.18789542670764E-48));
#37604=DIRECTION('center_axis',(5.15167520928809E-67,-1.18789542670764E-48,
-1.));
#37605=DIRECTION('ref_axis',(0.,1.,0.));
#37606=DIRECTION('center_axis',(-0.825231766969855,0.564794227718802,0.000105448247237627));
#37607=DIRECTION('ref_axis',(0.564753119361559,0.825169421162197,0.0122204971352771));
#37608=DIRECTION('center_axis',(0.205967239672467,-0.97855888323813,9.06501466256469E-5));
#37609=DIRECTION('ref_axis',(0.978455970572454,0.205946920321296,0.0144837723432324));
#37610=DIRECTION('center_axis',(5.15167520928809E-67,-1.18789542670764E-48,
-1.));
#37611=DIRECTION('ref_axis',(-4.33680868994202E-19,1.,-1.18789542670764E-48));
#37612=DIRECTION('center_axis',(5.15167520928809E-67,-1.18789542670764E-48,
-1.));
#37613=DIRECTION('ref_axis',(0.,1.,0.));
#37614=DIRECTION('center_axis',(-0.867001097222074,0.498306217396881,0.00010544824406792));
#37615=DIRECTION('ref_axis',(0.498270127350421,0.866935718266621,0.0122204985059196));
#37616=DIRECTION('center_axis',(0.282109156506117,-0.959382309404316,9.06501467341775E-5));
#37617=DIRECTION('ref_axis',(0.959281308220891,0.282080825357731,0.0144837724201092));
#37618=DIRECTION('center_axis',(5.15167520928809E-67,-1.18789542670764E-48,
-1.));
#37619=DIRECTION('ref_axis',(-4.33680868994202E-19,1.,-1.18789542670764E-48));
#37620=DIRECTION('center_axis',(5.15167520928809E-67,-1.18789542670764E-48,
-1.));
#37621=DIRECTION('ref_axis',(0.,1.,0.));
#37622=DIRECTION('center_axis',(-0.903425077395399,0.428745983554114,0.00010544824771057));
#37623=DIRECTION('ref_axis',(0.42871513434286,0.903357068405985,0.0122204969754959));
#37624=DIRECTION('center_axis',(0.356511776578972,-0.934290824606052,9.06501467185522E-5));
#37625=DIRECTION('ref_axis',(0.934192357612503,0.356475608304786,0.0144837723720686));
#37626=DIRECTION('center_axis',(5.15167520928809E-67,-1.18789542670764E-48,
-1.));
#37627=DIRECTION('ref_axis',(-4.33680868994202E-19,1.,-1.18789542670764E-48));
#37628=DIRECTION('center_axis',(5.15167520928809E-67,-1.18789542670764E-48,
-1.));
#37629=DIRECTION('ref_axis',(0.,1.,0.));
#37630=DIRECTION('center_axis',(-0.934279141551227,0.35654238814336,0.000105448247725771));
#37631=DIRECTION('ref_axis',(0.356516969954114,0.934208921810617,0.0122204968876431));
#37632=DIRECTION('center_axis',(0.428716382996855,-0.903439126190938,9.06501466905075E-5));
#37633=DIRECTION('ref_axis',(0.903343800467886,0.428672600585895,0.0144837724078269));
#37634=DIRECTION('center_axis',(5.15167520928809E-67,-1.18789542670764E-48,
-1.));
#37635=DIRECTION('ref_axis',(-4.33680868994202E-19,1.,-1.18789542670764E-48));
#37636=DIRECTION('center_axis',(5.15167520928809E-67,-1.18789542670764E-48,
-1.));
#37637=DIRECTION('ref_axis',(0.,1.,0.));
#37638=DIRECTION('center_axis',(-0.959373064120116,0.282140590347166,0.000105448247704078));
#37639=DIRECTION('ref_axis',(0.282120759890668,0.959301066553995,0.0122204970062476));
#37640=DIRECTION('center_axis',(0.498277810351468,-0.867017425138559,9.06501469271671E-5));
#37641=DIRECTION('ref_axis',(0.86692582840188,0.498226683737388,0.0144837723593644));
#37642=DIRECTION('center_axis',(5.15167520928809E-67,-1.18789542670764E-48,
-1.));
#37643=DIRECTION('ref_axis',(-4.33680868994202E-19,1.,-1.18789542670764E-48));
#37644=DIRECTION('center_axis',(5.15167520928809E-67,-1.18789542670764E-48,
-1.));
#37645=DIRECTION('ref_axis',(0.,1.,0.));
#37646=DIRECTION('center_axis',(-0.978552132724721,0.205999301990486,0.000105448247790145));
#37647=DIRECTION('ref_axis',(0.205985181528783,0.978478801224291,0.0122204969305395));
#37648=DIRECTION('center_axis',(0.564767189310343,-0.825250273348059,9.06501467424166E-5));
#37649=DIRECTION('ref_axis',(0.825162970321744,0.56470903370561,0.0144837723356968));
#37650=DIRECTION('center_axis',(5.15167520928809E-67,-1.18789542670764E-48,
-1.));
#37651=DIRECTION('ref_axis',(-4.33680868994202E-19,1.,-1.18789542670764E-48));
#37652=DIRECTION('center_axis',(5.15167520928809E-67,-1.18789542670764E-48,
-1.));
#37653=DIRECTION('ref_axis',(0.,1.,0.));
#37654=DIRECTION('center_axis',(-0.991698102029505,0.128587959435343,0.000105448247905715));
#37655=DIRECTION('ref_axis',(0.12857963602553,0.991623888707005,0.0122204969268892));
#37656=DIRECTION('center_axis',(0.627774590743107,-0.778395179198763,9.06501466692162E-5));
#37657=DIRECTION('ref_axis',(0.778312708134479,0.627709764696018,0.0144837723553914));
#37658=DIRECTION('center_axis',(5.15167520928809E-67,-1.18789542670764E-48,
-1.));
#37659=DIRECTION('ref_axis',(-4.33680868994202E-19,1.,-1.18789542670764E-48));
#37660=DIRECTION('center_axis',(5.15167520928809E-67,-1.18789542670764E-48,
-1.));
#37661=DIRECTION('ref_axis',(0.,1.,0.));
#37662=DIRECTION('center_axis',(-0.998729922762266,0.05038382934976,0.000105448247701369));
#37663=DIRECTION('ref_axis',(0.0503813543083786,0.998655285166624,0.0122204969957313));
#37664=DIRECTION('center_axis',(0.686911553067687,-0.726741019927105,9.06501465529425E-5));
#37665=DIRECTION('ref_axis',(0.726663889286156,0.686840456252101,0.0144837723995786));
#37666=DIRECTION('center_axis',(5.15167520928809E-67,-1.18789542670764E-48,
-1.));
#37667=DIRECTION('ref_axis',(-4.33680868994202E-19,1.,-1.18789542670764E-48));
#37668=DIRECTION('center_axis',(5.15167520928809E-67,-1.18789542670764E-48,
-1.));
#37669=DIRECTION('ref_axis',(0.,1.,0.));
#37670=DIRECTION('center_axis',(-0.999604241409733,-0.0281309337978441,
0.000105448247608528));
#37671=DIRECTION('ref_axis',(0.0281275452112647,-0.999529639708088,-0.0122204969378127));
#37672=DIRECTION('center_axis',(0.741813477246663,-0.67060626060138,9.06501466416355E-5));
#37673=DIRECTION('ref_axis',(0.670534945920398,0.741736547998582,0.0144837723910712));
#37674=DIRECTION('center_axis',(5.15167520928809E-67,-1.18789542670764E-48,
-1.));
#37675=DIRECTION('ref_axis',(-4.33680868994202E-19,1.,-1.18789542670764E-48));
#37676=DIRECTION('center_axis',(5.15167520928809E-67,-1.18789542670764E-48,
-1.));
#37677=DIRECTION('ref_axis',(0.,1.,0.));
#37678=DIRECTION('center_axis',(-0.994315667506803,-0.106472260383486,0.000105448247832577));
#37679=DIRECTION('ref_axis',(0.10646302906079,-0.994241561643227,-0.0122204968981425));
#37680=DIRECTION('center_axis',(0.792141874660394,-0.610336990679795,9.06501467163515E-5));
#37681=DIRECTION('ref_axis',(0.610271931637984,0.792059587274861,0.0144837723269713));
#37682=DIRECTION('center_axis',(5.15167520928809E-67,-1.18789542670764E-48,
-1.));
#37683=DIRECTION('ref_axis',(-4.33680868994202E-19,1.,-1.18789542670764E-48));
#37684=DIRECTION('center_axis',(5.15167520928809E-67,-1.18789542670764E-48,
-1.));
#37685=DIRECTION('ref_axis',(0.,1.,0.));
#37686=DIRECTION('center_axis',(-0.982896806870098,-0.184157150079038,0.000105448247610839));
#37687=DIRECTION('ref_axis',(0.184142132934261,-0.982823653730751,-0.0122204969521754));
#37688=DIRECTION('center_axis',(0.837586454002892,-0.546304790253034,9.06501468389122E-5));
#37689=DIRECTION('ref_axis',(0.546246387959946,0.837499315807641,0.014483772383082));
#37690=DIRECTION('center_axis',(5.15167520928809E-67,-1.18789542670764E-48,
-1.));
#37691=DIRECTION('ref_axis',(-4.33680868994202E-19,1.,-1.18789542670764E-48));
#37692=DIRECTION('center_axis',(5.15167520928809E-67,-1.18789542670764E-48,
-1.));
#37693=DIRECTION('ref_axis',(0.,1.,0.));
#37694=DIRECTION('center_axis',(-0.965418060572767,-0.260706649705342,0.000105448247695262));
#37695=DIRECTION('ref_axis',(0.260685939324476,-0.965346311172558,-0.0122204968822783));
#37696=DIRECTION('center_axis',(0.877867034330398,-0.478904439130086,9.06501466177592E-5));
#37697=DIRECTION('ref_axis',(0.478853053655353,0.877775582561241,0.0144837724443041));
#37698=DIRECTION('center_axis',(5.15167520928809E-67,-1.18789542670764E-48,
-1.));
#37699=DIRECTION('ref_axis',(-4.33680868994202E-19,1.,-1.18789542670764E-48));
#37700=DIRECTION('center_axis',(5.15167520928809E-67,-1.18789542670764E-48,
-1.));
#37701=DIRECTION('ref_axis',(0.,1.,0.));
#37702=DIRECTION('center_axis',(-0.941987190897914,-0.335648806142557,0.000105448247712849));
#37703=DIRECTION('ref_axis',(0.335622530211483,-0.941917287593983,-0.0122204969636003));
#37704=DIRECTION('center_axis',(0.912735272471151,-0.408551482887487,9.06501467033935E-5));
#37705=DIRECTION('ref_axis',(0.408507431040848,0.912640070960968,0.0144837723251257));
#37706=DIRECTION('center_axis',(5.15167520928809E-67,-1.18789542670764E-48,
-1.));
#37707=DIRECTION('ref_axis',(-4.33680868994202E-19,1.,-1.18789542670764E-48));
#37708=DIRECTION('center_axis',(5.15167520928809E-67,-1.18789542670764E-48,
-1.));
#37709=DIRECTION('ref_axis',(0.,1.,0.));
#37710=DIRECTION('center_axis',(-0.912748656948201,-0.408521576076371,0.000105448247247158));
#37711=DIRECTION('ref_axis',(0.408489896594259,-0.912681030716532,-0.012220497151094));
#37712=DIRECTION('center_axis',(0.941976194141716,-0.335679670895989,9.06501466623777E-5));
#37713=DIRECTION('ref_axis',(0.335643224270751,0.941877829837572,0.0144837723539316));
#37714=DIRECTION('center_axis',(5.15167520928809E-67,-1.18789542670764E-48,
-1.));
#37715=DIRECTION('ref_axis',(-4.33680868994202E-19,1.,-1.18789542670764E-48));
#37716=DIRECTION('center_axis',(5.15167520928809E-67,-1.18789542670764E-48,
-1.));
#37717=DIRECTION('ref_axis',(0.,1.,0.));
#37718=DIRECTION('center_axis',(-0.877882724009451,-0.478875674644697,0.000105448247674909));
#37719=DIRECTION('ref_axis',(0.478838786928496,-0.877817791793333,-0.0122204968770904));
#37720=DIRECTION('center_axis',(0.965409519336493,-0.26073828210877,9.06501465579451E-5));
#37721=DIRECTION('ref_axis',(0.260709665410522,0.965308598686875,0.0144837723924504));
#37722=DIRECTION('center_axis',(5.15167520928809E-67,-1.18789542670764E-48,
-1.));
#37723=DIRECTION('ref_axis',(-4.33680868994202E-19,1.,-1.18789542670764E-48));
#37724=DIRECTION('center_axis',(5.15167520928809E-67,-1.18789542670764E-48,
-1.));
#37725=DIRECTION('ref_axis',(0.,1.,0.));
#37726=DIRECTION('center_axis',(-0.837604352151306,-0.546277345437149,0.00010544824776483));
#37727=DIRECTION('ref_axis',(0.546235476910197,-0.837542514275933,-0.0122204969227218));
#37728=DIRECTION('center_axis',(0.982890773813463,-0.184189355107518,9.06501466980053E-5));
#37729=DIRECTION('ref_axis',(0.184168744767822,0.982787919027818,0.0144837724235038));
#37730=DIRECTION('center_axis',(5.15167520928809E-67,-1.18789542670764E-48,
-1.));
#37731=DIRECTION('ref_axis',(-4.33680868994202E-19,1.,-1.18789542670764E-48));
#37732=DIRECTION('center_axis',(5.15167520928809E-67,-1.18789542670764E-48,
-1.));
#37733=DIRECTION('ref_axis',(0.,1.,0.));
#37734=DIRECTION('center_axis',(-0.792161870930109,-0.610311034739809,0.000105448247597277));
#37735=DIRECTION('ref_axis',(0.610264443535208,-0.792103508646315,-0.0122204969972532));
#37736=DIRECTION('center_axis',(0.994312179825469,-0.106504839482882,9.06501468290203E-5));
#37737=DIRECTION('ref_axis',(0.106492362571566,0.994208025039157,0.0144837723561435));
#37738=DIRECTION('center_axis',(5.15167520928809E-67,-1.18789542670764E-48,
-1.));
#37739=DIRECTION('ref_axis',(-4.33680868994202E-19,1.,-1.18789542670764E-48));
#37740=DIRECTION('center_axis',(5.15167520928809E-67,-1.18789542670764E-48,
-1.));
#37741=DIRECTION('ref_axis',(0.,1.,0.));
#37742=DIRECTION('center_axis',(-0.741835448354634,-0.670581953563579,0.000105448247853962));
#37743=DIRECTION('ref_axis',(0.67053092693267,-0.741780921486687,-0.0122204969283275));
#37744=DIRECTION('center_axis',(0.99960332060645,-0.0281636861065795,9.06501468718404E-5));
#37745=DIRECTION('ref_axis',(0.0281594195477731,0.999498507967606,0.014483772342229));
#37746=DIRECTION('center_axis',(5.15167520928809E-67,-1.18789542670764E-48,
-1.));
#37747=DIRECTION('ref_axis',(-4.33680868994202E-19,1.,-1.18789542670764E-48));
#37748=DIRECTION('center_axis',(5.15167520928809E-67,-1.18789542670764E-48,
-1.));
#37749=DIRECTION('ref_axis',(0.,1.,0.));
#37750=DIRECTION('center_axis',(-0.686935363552547,-0.726718511654683,0.000105448246665782));
#37751=DIRECTION('ref_axis',(0.726663364188996,-0.686885008272227,-0.0122204973873402));
#37752=DIRECTION('center_axis',(0.998731574514055,0.0503511057597249,9.06501467982717E-5));
#37753=DIRECTION('ref_axis',(0.050347135661256,-0.998626750226507,-0.0144837723936806));
#37754=DIRECTION('center_axis',(5.15167520928809E-67,-1.18789542670764E-48,
-1.));
#37755=DIRECTION('ref_axis',(-4.33680868994202E-19,1.,-1.18789542670764E-48));
#37756=DIRECTION('center_axis',(5.15167520928809E-67,-1.18789542670764E-48,
-1.));
#37757=DIRECTION('ref_axis',(0.,1.,0.));
#37758=DIRECTION('center_axis',(-0.627800093808639,-0.778374608459533,0.000105448247779514));
#37759=DIRECTION('ref_axis',(0.778315680170178,-0.627754220581,-0.0122204968791585));
#37760=DIRECTION('center_axis',(0.991702316152886,0.12855546631533,9.06501466251883E-5));
#37761=DIRECTION('ref_axis',(0.128543284036466,-0.991598126493403,-0.0144837724330683));
#37762=DIRECTION('center_axis',(5.15167520928809E-67,-1.18789542670764E-48,
-1.));
#37763=DIRECTION('ref_axis',(-4.33680868994202E-19,1.,-1.18789542670764E-48));
#37764=DIRECTION('center_axis',(5.15167520928809E-67,-1.18789542670764E-48,
-1.));
#37765=DIRECTION('ref_axis',(0.,1.,0.));
#37766=DIRECTION('center_axis',(-0.564794227719968,-0.825231766969057,0.000105448247863909));
#37767=DIRECTION('ref_axis',(0.825169421163414,-0.564753119364088,-0.0122204969362205));
#37768=DIRECTION('center_axis',(0.978558883238036,0.205967239672914,9.06501468463484E-5));
#37769=DIRECTION('ref_axis',(0.205946920321936,-0.978455970573291,-0.014483772277592));
#37770=DIRECTION('center_axis',(5.15167520928809E-67,-1.18789542670764E-48,
-1.));
#37771=DIRECTION('ref_axis',(-4.33680868994202E-19,1.,-1.18789542670764E-48));
#37772=DIRECTION('center_axis',(5.15167520928809E-67,-1.18789542670764E-48,
-1.));
#37773=DIRECTION('ref_axis',(0.,1.,0.));
#37774=DIRECTION('center_axis',(-0.498306217403848,-0.86700109721807,0.000105448247661773));
#37775=DIRECTION('ref_axis',(0.866935718279092,-0.498270127366718,-0.0122204969566953));
#37776=DIRECTION('center_axis',(0.959382309404258,0.282109156506314,9.06501467982869E-5));
#37777=DIRECTION('ref_axis',(0.282080825358155,-0.959281308221622,-0.014483772363392));
#37778=DIRECTION('center_axis',(5.15167520928809E-67,-1.18789542670764E-48,
-1.));
#37779=DIRECTION('ref_axis',(-4.33680868994202E-19,1.,-1.18789542670764E-48));
#37780=DIRECTION('center_axis',(5.15167520928809E-67,-1.18789542670764E-48,
-1.));
#37781=DIRECTION('ref_axis',(0.,1.,0.));
#37782=DIRECTION('center_axis',(-0.428745983554159,-0.903425077395378,0.000105448247692435));
#37783=DIRECTION('ref_axis',(0.903357068405516,-0.428715134342697,-0.0122204970158381));
#37784=DIRECTION('center_axis',(0.934290824605943,0.356511776579256,9.06501468588022E-5));
#37785=DIRECTION('ref_axis',(0.35647560830508,-0.934192357612417,-0.0144837723703894));
#37786=DIRECTION('center_axis',(5.15167520928809E-67,-1.18789542670764E-48,
-1.));
#37787=DIRECTION('ref_axis',(-4.33680868994202E-19,1.,-1.18789542670764E-48));
#37788=DIRECTION('center_axis',(5.15167520928809E-67,-1.18789542670764E-48,
-1.));
#37789=DIRECTION('ref_axis',(0.,1.,0.));
#37790=DIRECTION('center_axis',(-0.356542388142294,-0.934279141551633,0.000105448247232403));
#37791=DIRECTION('ref_axis',(0.934208921807365,-0.356516969951681,-0.0122204972072322));
#37792=DIRECTION('center_axis',(0.903439126190767,0.428716382997215,9.06501468179925E-5));
#37793=DIRECTION('ref_axis',(0.428672600586429,-0.903343800468082,-0.0144837723797852));
#37794=DIRECTION('center_axis',(5.15167520928809E-67,-1.18789542670764E-48,
-1.));
#37795=DIRECTION('ref_axis',(-4.33680868994202E-19,1.,-1.18789542670764E-48));
#37796=DIRECTION('center_axis',(5.15167520928809E-67,-1.18789542670764E-48,
-1.));
#37797=DIRECTION('ref_axis',(0.,1.,0.));
#37798=DIRECTION('center_axis',(-0.282140590347279,-0.959373064120083,0.000105448247741099));
#37799=DIRECTION('ref_axis',(0.959301066555032,-0.282120759891086,-0.012220496915153));
#37800=DIRECTION('center_axis',(0.867017425138588,0.498277810351419,9.06501468672452E-5));
#37801=DIRECTION('ref_axis',(0.498226683737162,-0.866925828401598,-0.0144837723840689));
#37802=DIRECTION('center_axis',(5.15167520928809E-67,-1.18789542670764E-48,
-1.));
#37803=DIRECTION('ref_axis',(-4.33680868994202E-19,1.,-1.18789542670764E-48));
#37804=DIRECTION('center_axis',(5.15167520928809E-67,-1.18789542670764E-48,
-1.));
#37805=DIRECTION('ref_axis',(0.,1.,0.));
#37806=DIRECTION('center_axis',(-0.20599930198994,-0.978552132724836,0.000105448247552452));
#37807=DIRECTION('ref_axis',(0.97847880122346,-0.205985181528044,-0.0122204970095074));
#37808=DIRECTION('center_axis',(0.825250273348004,0.564767189310424,9.06501467639861E-5));
#37809=DIRECTION('ref_axis',(0.56470903370563,-0.825162970321598,-0.0144837723432248));
#37810=DIRECTION('center_axis',(5.15167520928809E-67,-1.18789542670764E-48,
-1.));
#37811=DIRECTION('ref_axis',(-4.33680868994202E-19,1.,-1.18789542670764E-48));
#37812=DIRECTION('center_axis',(5.15167520928809E-67,-1.18789542670764E-48,
-1.));
#37813=DIRECTION('ref_axis',(0.,1.,0.));
#37814=DIRECTION('center_axis',(-0.128587959431095,-0.991698102030056,0.000105448246015545));
#37815=DIRECTION('ref_axis',(0.991623888697772,-0.128579636020076,-0.0122204977334817));
#37816=DIRECTION('center_axis',(0.778395179198649,0.627774590743249,9.06501467187627E-5));
#37817=DIRECTION('ref_axis',(0.62770976469618,-0.778312708134389,-0.0144837723532511));
#37818=DIRECTION('center_axis',(5.15167520928809E-67,-1.18789542670764E-48,
-1.));
#37819=DIRECTION('ref_axis',(-4.33680868994202E-19,1.,-1.18789542670764E-48));
#37820=DIRECTION('center_axis',(5.15167520928809E-67,-1.18789542670764E-48,
-1.));
#37821=DIRECTION('ref_axis',(0.,1.,0.));
#37822=DIRECTION('center_axis',(-0.0503838293498799,-0.99872992276226,0.000105448247790322));
#37823=DIRECTION('ref_axis',(0.998655285167012,-0.050381354308516,-0.0122204969634886));
#37824=DIRECTION('center_axis',(0.726741019926698,0.686911553068118,9.06501468063716E-5));
#37825=DIRECTION('ref_axis',(0.686840456253071,-0.726663889286322,-0.0144837723452766));
#37826=DIRECTION('center_axis',(5.15167520928809E-67,-1.18789542670764E-48,
-1.));
#37827=DIRECTION('ref_axis',(-4.33680868994202E-19,1.,-1.18789542670764E-48));
#37828=DIRECTION('center_axis',(5.15167520928809E-67,-1.18789542670764E-48,
-1.));
#37829=DIRECTION('ref_axis',(0.,1.,0.));
#37830=DIRECTION('center_axis',(0.0281309337977714,-0.999604241409735,0.000105448247661813));
#37831=DIRECTION('ref_axis',(0.999529639707556,0.0281275452111717,-0.0122204969816086));
#37832=DIRECTION('center_axis',(0.670606260601294,0.741813477246741,9.06501466782892E-5));
#37833=DIRECTION('ref_axis',(0.741736547997904,-0.67053494591962,-0.0144837724617815));
#37834=DIRECTION('center_axis',(5.15167520928809E-67,-1.18789542670764E-48,
-1.));
#37835=DIRECTION('ref_axis',(-4.33680868994202E-19,1.,-1.18789542670764E-48));
#37836=DIRECTION('center_axis',(5.15167520928809E-67,-1.18789542670764E-48,
-1.));
#37837=DIRECTION('ref_axis',(0.,1.,0.));
#37838=DIRECTION('center_axis',(0.106472260384112,-0.994315667506736,0.000105448247531298));
#37839=DIRECTION('ref_axis',(0.994241561642015,0.106463029061287,-0.01222049699245));
#37840=DIRECTION('center_axis',(0.610336990679746,0.792141874660432,9.06501467541659E-5));
#37841=DIRECTION('ref_axis',(0.792059587274579,-0.610271931637685,-0.0144837723550388));
#37842=DIRECTION('center_axis',(5.15167520928809E-67,-1.18789542670764E-48,
-1.));
#37843=DIRECTION('ref_axis',(-4.33680868994202E-19,1.,-1.18789542670764E-48));
#37844=DIRECTION('center_axis',(5.15167520928809E-67,-1.18789542670764E-48,
-1.));
#37845=DIRECTION('ref_axis',(0.,1.,0.));
#37846=DIRECTION('center_axis',(0.184157150078655,-0.982896806870169,0.000105448247826086));
#37847=DIRECTION('ref_axis',(0.982823653731041,0.184142132933918,-0.01222049693405));
#37848=DIRECTION('center_axis',(0.546304790253063,0.837586454002874,9.06501468026834E-5));
#37849=DIRECTION('ref_axis',(0.837499315807096,-0.546246387959628,-0.0144837724265968));
#37850=DIRECTION('center_axis',(5.15167520928809E-67,-1.18789542670764E-48,
-1.));
#37851=DIRECTION('ref_axis',(-4.33680868994202E-19,1.,-1.18789542670764E-48));
#37852=DIRECTION('center_axis',(5.15167520928809E-67,-1.18789542670764E-48,
-1.));
#37853=DIRECTION('ref_axis',(0.,1.,0.));
#37854=DIRECTION('center_axis',(0.260706649723291,-0.965418060567921,0.000105448239312411));
#37855=DIRECTION('ref_axis',(0.965346311124436,0.260685939330442,-0.0122205005564138));
#37856=DIRECTION('center_axis',(0.478904439129984,0.877867034330454,9.06501466836614E-5));
#37857=DIRECTION('ref_axis',(0.877775582561938,-0.478853053655605,-0.0144837723936657));
#37858=DIRECTION('center_axis',(5.15167520928809E-67,-1.18789542670764E-48,
-1.));
#37859=DIRECTION('ref_axis',(-4.33680868994202E-19,1.,-1.18789542670764E-48));
#37860=DIRECTION('center_axis',(5.15167520928809E-67,-1.18789542670764E-48,
-1.));
#37861=DIRECTION('ref_axis',(0.,1.,0.));
#37862=DIRECTION('center_axis',(0.335648806142683,-0.941987190897869,0.000105448247681778));
#37863=DIRECTION('ref_axis',(0.941917287594608,0.335622530211854,-0.012220496905163));
#37864=DIRECTION('center_axis',(0.408551482887321,0.912735272471225,9.06501468104788E-5));
#37865=DIRECTION('ref_axis',(0.912640070960436,-0.408507431040405,-0.014483772371131));
#37866=DIRECTION('center_axis',(5.15167520928809E-67,-1.18789542670764E-48,
-1.));
#37867=DIRECTION('ref_axis',(-4.33680868994202E-19,1.,-1.18789542670764E-48));
#37868=DIRECTION('center_axis',(5.15167520928809E-67,-1.18789542670764E-48,
-1.));
#37869=DIRECTION('ref_axis',(0.,1.,0.));
#37870=DIRECTION('center_axis',(0.408521576076219,-0.912748656948269,0.000105448247344423));
#37871=DIRECTION('ref_axis',(0.912681030717311,0.408489896594431,-0.0122204970871443));
#37872=DIRECTION('center_axis',(0.335679670895796,0.941976194141785,9.06501467685389E-5));
#37873=DIRECTION('ref_axis',(0.941877829836932,-0.335643224270299,-0.0144837724059784));
#37874=DIRECTION('center_axis',(5.15167520928809E-67,-1.18789542670764E-48,
-1.));
#37875=DIRECTION('ref_axis',(-4.33680868994202E-19,1.,-1.18789542670764E-48));
#37876=DIRECTION('center_axis',(5.15167520928809E-67,-1.18789542670764E-48,
-1.));
#37877=DIRECTION('ref_axis',(0.,1.,0.));
#37878=DIRECTION('center_axis',(0.478875674644822,-0.877882724009383,0.000105448247602163));
#37879=DIRECTION('ref_axis',(0.877817791792273,0.47883878692807,-0.0122204969699355));
#37880=DIRECTION('center_axis',(0.260738282108074,0.965409519336681,9.06501468936573E-5));
#37881=DIRECTION('ref_axis',(0.965308598687316,-0.260709665409891,-0.0144837723743816));
#37882=DIRECTION('center_axis',(5.15167520928809E-67,-1.18789542670764E-48,
-1.));
#37883=DIRECTION('ref_axis',(-4.33680868994202E-19,1.,-1.18789542670764E-48));
#37884=DIRECTION('center_axis',(5.15167520928809E-67,-1.18789542670764E-48,
-1.));
#37885=DIRECTION('ref_axis',(0.,1.,0.));
#37886=DIRECTION('center_axis',(0.546277345437349,-0.837604352151176,0.000105448247639465));
#37887=DIRECTION('ref_axis',(0.837542514275712,0.546235476910338,-0.0122204969316073));
#37888=DIRECTION('center_axis',(0.184189355107516,0.982890773813463,9.06501467024073E-5));
#37889=DIRECTION('ref_axis',(0.982787919028468,-0.184168744767946,-0.0144837723778112));
#37890=DIRECTION('center_axis',(5.15167520928809E-67,-1.18789542670764E-48,
-1.));
#37891=DIRECTION('ref_axis',(-4.33680868994202E-19,1.,-1.18789542670764E-48));
#37892=DIRECTION('center_axis',(5.15167520928809E-67,-1.18789542670764E-48,
-1.));
#37893=DIRECTION('ref_axis',(0.,1.,0.));
#37894=DIRECTION('center_axis',(0.610311034750668,-0.792161870921744,0.000105448241406271));
#37895=DIRECTION('ref_axis',(0.79210350861157,0.610264443525473,-0.0122204997355093));
#37896=DIRECTION('center_axis',(0.106504839483129,0.994312179825443,9.06501467375791E-5));
#37897=DIRECTION('ref_axis',(0.994208025038601,-0.106492362571754,-0.0144837723929676));
#37898=DIRECTION('center_axis',(5.15167520928809E-67,-1.18789542670764E-48,
-1.));
#37899=DIRECTION('ref_axis',(-4.33680868994202E-19,1.,-1.18789542670764E-48));
#37900=DIRECTION('center_axis',(5.15167520928809E-67,-1.18789542670764E-48,
-1.));
#37901=DIRECTION('ref_axis',(0.,1.,0.));
#37902=DIRECTION('center_axis',(0.670581953563674,-0.741835448354548,0.000105448247759945));
#37903=DIRECTION('ref_axis',(0.741780921486581,0.670530926932748,-0.0122204969305506));
#37904=DIRECTION('center_axis',(0.0281636861069903,0.999603320606438,9.06501466992701E-5));
#37905=DIRECTION('ref_axis',(0.999498507967367,-0.0281594195481785,-0.0144837723579484));
#37906=DIRECTION('center_axis',(5.15167520928809E-67,-1.18789542670764E-48,
-1.));
#37907=DIRECTION('ref_axis',(-4.33680868994202E-19,1.,-1.18789542670764E-48));
#37908=DIRECTION('center_axis',(5.15167520928809E-67,-1.18789542670764E-48,
-1.));
#37909=DIRECTION('ref_axis',(0.,1.,0.));
#37910=DIRECTION('center_axis',(0.726718511653026,-0.6869353635543,0.000105448247761845));
#37911=DIRECTION('ref_axis',(0.686885008277897,0.726663364191536,-0.0122204969175564));
#37912=DIRECTION('center_axis',(-0.0503511057596336,0.99873157451406,9.06501467774672E-5));
#37913=DIRECTION('ref_axis',(0.998626750226755,0.0503471356611751,-0.0144837723768601));
#37914=DIRECTION('center_axis',(5.15167520928809E-67,-1.18789542670764E-48,
-1.));
#37915=DIRECTION('ref_axis',(-4.33680868994202E-19,1.,-1.18789542670764E-48));
#37916=DIRECTION('center_axis',(5.15167520928809E-67,-1.18789542670764E-48,
-1.));
#37917=DIRECTION('ref_axis',(0.,1.,0.));
#37918=DIRECTION('center_axis',(0.778374608459656,-0.627800093808486,0.000105448247696036));
#37919=DIRECTION('ref_axis',(0.627754220580537,0.778315680169911,-0.0122204969200215));
#37920=DIRECTION('center_axis',(-0.128555466315276,0.991702316152893,9.06501466266556E-5));
#37921=DIRECTION('ref_axis',(0.991598126493641,0.128543284036441,-0.0144837724170315));
#37922=DIRECTION('center_axis',(5.15167520928809E-67,-1.18789542670764E-48,
-1.));
#37923=DIRECTION('ref_axis',(-4.33680868994202E-19,1.,-1.18789542670764E-48));
#37924=DIRECTION('center_axis',(5.15167520928809E-67,-1.18789542670764E-48,
-1.));
#37925=DIRECTION('ref_axis',(0.,1.,0.));
#37926=DIRECTION('center_axis',(0.825231766969182,-0.564794227719785,0.000105448247768853));
#37927=DIRECTION('ref_axis',(0.564753119363901,0.825169421163535,-0.0122204969367096));
#37928=DIRECTION('center_axis',(-0.205967239672835,0.978558883238052,9.06501467925213E-5));
#37929=DIRECTION('ref_axis',(0.978455970572528,0.205946920321698,-0.0144837723325158));
#37930=DIRECTION('center_axis',(5.15167520928809E-67,-1.18789542670764E-48,
-1.));
#37931=DIRECTION('ref_axis',(-4.33680868994202E-19,1.,-1.18789542670764E-48));
#37932=DIRECTION('center_axis',(5.15167520928809E-67,-1.18789542670764E-48,
-1.));
#37933=DIRECTION('ref_axis',(0.,1.,0.));
#37934=DIRECTION('center_axis',(0.867001097218019,-0.498306217403936,0.000105448247742928));
#37935=DIRECTION('ref_axis',(0.498270127367224,0.866935718279781,-0.0122204968872419));
#37936=DIRECTION('center_axis',(-0.282109156506148,0.959382309404307,9.06501467249393E-5));
#37937=DIRECTION('ref_axis',(0.959281308221143,0.282080825357837,-0.0144837724013445));
#37938=DIRECTION('center_axis',(5.15167520928809E-67,-1.18789542670764E-48,
-1.));
#37939=DIRECTION('ref_axis',(-4.33680868994202E-19,1.,-1.18789542670764E-48));
#37940=DIRECTION('center_axis',(5.15167520928809E-67,-1.18789542670764E-48,
-1.));
#37941=DIRECTION('ref_axis',(0.,1.,0.));
#37942=DIRECTION('center_axis',(0.903425077395463,-0.428745983553979,0.000105448247628158));
#37943=DIRECTION('ref_axis',(0.428715134343002,0.903357068406648,-0.0122204969215573));
#37944=DIRECTION('center_axis',(-0.356511776579108,0.934290824606,9.06501467950618E-5));
#37945=DIRECTION('ref_axis',(0.934192357613078,0.356475608305158,-0.0144837723258434));
#37946=DIRECTION('center_axis',(5.15167520928809E-67,-1.18789542670764E-48,
-1.));
#37947=DIRECTION('ref_axis',(-4.33680868994202E-19,1.,-1.18789542670764E-48));
#37948=DIRECTION('center_axis',(5.15167520928809E-67,-1.18789542670764E-48,
-1.));
#37949=DIRECTION('ref_axis',(0.,1.,0.));
#37950=DIRECTION('center_axis',(0.93427914155167,-0.356542388142199,0.000105448247170392));
#37951=DIRECTION('ref_axis',(0.356516969951772,0.934208921807903,-0.012220497163456));
#37952=DIRECTION('center_axis',(-0.428716382997142,0.903439126190801,9.06501468381065E-5));
#37953=DIRECTION('ref_axis',(0.903343800468038,0.42867260058632,-0.0144837723857595));
#37954=DIRECTION('center_axis',(5.15167520928809E-67,-1.18789542670764E-48,
-1.));
#37955=DIRECTION('ref_axis',(-4.33680868994202E-19,1.,-1.18789542670764E-48));
#37956=DIRECTION('center_axis',(5.15167520928809E-67,-1.18789542670764E-48,
-1.));
#37957=DIRECTION('ref_axis',(0.,1.,0.));
#37958=DIRECTION('center_axis',(0.959373064120116,-0.282140590347164,0.000105448247729292));
#37959=DIRECTION('ref_axis',(0.282120759890968,0.959301066555056,-0.0122204969160199));
#37960=DIRECTION('center_axis',(-0.498277810351142,0.867017425138747,9.06501467342992E-5));
#37961=DIRECTION('ref_axis',(0.866925828401964,0.498226683737,-0.0144837723677419));
#37962=DIRECTION('center_axis',(5.15167520928809E-67,-1.18789542670764E-48,
-1.));
#37963=DIRECTION('ref_axis',(-4.33680868994202E-19,1.,-1.18789542670764E-48));
#37964=DIRECTION('center_axis',(5.15167520928809E-67,-1.18789542670764E-48,
-1.));
#37965=DIRECTION('ref_axis',(0.,1.,0.));
#37966=DIRECTION('center_axis',(0.978552132724802,-0.205999301990102,0.000105448247615573));
#37967=DIRECTION('ref_axis',(0.205985181528349,0.978478801224133,-0.0122204969505153));
#37968=DIRECTION('center_axis',(-0.564767189310334,0.825250273348065,9.0650146758551E-5));
#37969=DIRECTION('ref_axis',(0.82516297032109,0.564709033705155,-0.014483772390721));
#37970=DIRECTION('center_axis',(5.15167520928809E-67,-1.18789542670764E-48,
-1.));
#37971=DIRECTION('ref_axis',(-4.33680868994202E-19,1.,-1.18789542670764E-48));
#37972=DIRECTION('center_axis',(5.15167520928809E-67,-1.18789542670764E-48,
-1.));
#37973=DIRECTION('ref_axis',(0.,1.,0.));
#37974=DIRECTION('center_axis',(0.991698102030069,-0.128587959430995,0.000105448245943976));
#37975=DIRECTION('ref_axis',(0.128579636019992,0.99162388869792,-0.0122204977223251));
#37976=DIRECTION('center_axis',(-0.627774590743336,0.778395179198579,9.06501467764949E-5));
#37977=DIRECTION('ref_axis',(0.778312708134504,0.627709764696415,-0.014483772336843));
#37978=DIRECTION('center_axis',(5.15167520928809E-67,-1.18789542670764E-48,
-1.));
#37979=DIRECTION('ref_axis',(-4.33680868994202E-19,1.,-1.18789542670764E-48));
#37980=DIRECTION('center_axis',(5.15167520928809E-67,-1.18789542670764E-48,
-1.));
#37981=DIRECTION('ref_axis',(0.,1.,0.));
#37982=DIRECTION('center_axis',(0.998729922762269,-0.0503838293497056,0.000105448247690158));
#37983=DIRECTION('ref_axis',(0.0503813543083624,0.998655285167543,-0.0122204969206726));
#37984=DIRECTION('center_axis',(-0.686911553068082,0.726741019926732,9.065014676939E-5));
#37985=DIRECTION('ref_axis',(0.726663889285701,0.686840456252424,-0.0144837724071123));
#37986=DIRECTION('center_axis',(5.15167520928809E-67,-1.18789542670764E-48,
-1.));
#37987=DIRECTION('ref_axis',(-4.33680868994202E-19,1.,-1.18789542670764E-48));
#37988=DIRECTION('center_axis',(5.15167520928809E-67,-1.18789542670764E-48,
-1.));
#37989=DIRECTION('ref_axis',(0.,1.,0.));
#37990=DIRECTION('center_axis',(0.999604241409737,0.0281309337977193,0.000105448247673278));
#37991=DIRECTION('ref_axis',(0.0281275452111183,-0.999529639707527,0.0122204969841135));
#37992=DIRECTION('center_axis',(-0.741813477246845,0.670606260601179,9.06501467534462E-5));
#37993=DIRECTION('ref_axis',(0.670534945920493,0.741736547999089,-0.0144837723606804));
#37994=DIRECTION('center_axis',(5.15167520928809E-67,-1.18789542670764E-48,
-1.));
#37995=DIRECTION('ref_axis',(-4.33680868994202E-19,1.,-1.18789542670764E-48));
#37996=DIRECTION('center_axis',(5.15167520928809E-67,-1.18789542670764E-48,
-1.));
#37997=DIRECTION('ref_axis',(0.,1.,0.));
#37998=DIRECTION('center_axis',(0.994315667506773,0.106472260383761,0.000105448247684943));
#37999=DIRECTION('ref_axis',(0.106463029060952,-0.994241561642206,0.0122204969798675));
#38000=DIRECTION('center_axis',(-0.792141874660476,0.610336990679688,9.06501468075157E-5));
#38001=DIRECTION('ref_axis',(0.610271931637649,0.792059587274653,-0.0144837723525293));
#38002=DIRECTION('center_axis',(5.15167520928809E-67,-1.18789542670764E-48,
-1.));
#38003=DIRECTION('ref_axis',(-4.33680868994202E-19,1.,-1.18789542670764E-48));
#38004=DIRECTION('center_axis',(5.15167520928809E-67,-1.18789542670764E-48,
-1.));
#38005=DIRECTION('ref_axis',(0.,1.,0.));
#38006=DIRECTION('center_axis',(0.982896806870138,0.184157150078822,0.000105448247739781));
#38007=DIRECTION('ref_axis',(0.184142132934029,-0.982823653730722,0.0122204969580191));
#38008=DIRECTION('center_axis',(-0.837586454002804,0.546304790253169,9.06501467452083E-5));
#38009=DIRECTION('ref_axis',(0.546246387960594,0.837499315808325,-0.0144837723191043));
#38010=DIRECTION('center_axis',(5.15167520928809E-67,-1.18789542670764E-48,
-1.));
#38011=DIRECTION('ref_axis',(-4.33680868994202E-19,1.,-1.18789542670764E-48));
#38012=DIRECTION('center_axis',(5.15167520928809E-67,-1.18789542670764E-48,
-1.));
#38013=DIRECTION('ref_axis',(0.,1.,0.));
#38014=DIRECTION('center_axis',(-0.778395179198544,-0.62777459074338,9.06501468008605E-5));
#38015=DIRECTION('ref_axis',(0.62770976469586,-0.778312708133716,0.0144837724032618));
#38016=DIRECTION('center_axis',(5.15167520928809E-67,-1.18789542670764E-48,
-1.));
#38017=DIRECTION('ref_axis',(-4.33680868994202E-19,1.,-1.18789542670764E-48));
#38018=DIRECTION('center_axis',(0.128587959434843,0.991698102029569,0.000105448247713068));
#38019=DIRECTION('ref_axis',(0.991623888707174,-0.128579636025041,0.0122204969182792));
#38020=DIRECTION('center_axis',(5.15167520928809E-67,-1.18789542670764E-48,
-1.));
#38021=DIRECTION('ref_axis',(0.,1.,0.));
#38022=DIRECTION('center_axis',(-0.82525027334801,-0.564767189310415,9.06501467887519E-5));
#38023=DIRECTION('ref_axis',(0.56470903370554,-0.825162970321483,0.0144837723533119));
#38024=DIRECTION('center_axis',(5.15167520928809E-67,-1.18789542670764E-48,
-1.));
#38025=DIRECTION('ref_axis',(-4.33680868994202E-19,1.,-1.18789542670764E-48));
#38026=DIRECTION('center_axis',(0.205999301990312,0.978552132724757,0.000105448247717959));
#38027=DIRECTION('ref_axis',(0.978478801224664,-0.205985181528676,0.0122204969024898));
#38028=DIRECTION('center_axis',(5.15167520928809E-67,-1.18789542670764E-48,
-1.));
#38029=DIRECTION('ref_axis',(0.,1.,0.));
#38030=DIRECTION('center_axis',(-0.867017425138643,-0.498277810351323,9.06501468256068E-5));
#38031=DIRECTION('ref_axis',(0.498226683737087,-0.866925828401692,0.014483772381015));
#38032=DIRECTION('center_axis',(5.15167520928809E-67,-1.18789542670764E-48,
-1.));
#38033=DIRECTION('ref_axis',(-4.33680868994202E-19,1.,-1.18789542670764E-48));
#38034=DIRECTION('center_axis',(0.282140590347035,0.959373064120154,0.000105448247634384));
#38035=DIRECTION('ref_axis',(0.959301066555324,-0.282120759890904,0.0122204968965099));
#38036=DIRECTION('center_axis',(5.15167520928809E-67,-1.18789542670764E-48,
-1.));
#38037=DIRECTION('ref_axis',(0.,1.,0.));
#38038=DIRECTION('center_axis',(-0.903439126190879,-0.428716382996979,9.06501467301661E-5));
#38039=DIRECTION('ref_axis',(0.428672600586422,-0.903343800468688,0.0144837723422516));
#38040=DIRECTION('center_axis',(5.15167520928809E-67,-1.18789542670764E-48,
-1.));
#38041=DIRECTION('ref_axis',(-4.33680868994202E-19,1.,-1.18789542670764E-48));
#38042=DIRECTION('center_axis',(0.356542388143256,0.934279141551266,0.000105448247681697));
#38043=DIRECTION('ref_axis',(0.934208921810558,-0.356516969953973,0.0122204968962765));
#38044=DIRECTION('center_axis',(5.15167520928809E-67,-1.18789542670764E-48,
-1.));
#38045=DIRECTION('ref_axis',(0.,1.,0.));
#38046=DIRECTION('center_axis',(-0.934290824606111,-0.356511776578816,9.06501466618288E-5));
#38047=DIRECTION('ref_axis',(0.356475608304419,-0.934192357612002,0.0144837724134131));
#38048=DIRECTION('center_axis',(5.15167520928809E-67,-1.18789542670764E-48,
-1.));
#38049=DIRECTION('ref_axis',(-4.33680868994202E-19,1.,-1.18789542670764E-48));
#38050=DIRECTION('center_axis',(0.428745983554273,0.903425077395324,0.000105448247749283));
#38051=DIRECTION('ref_axis',(0.903357068406257,-0.428715134343181,0.0122204969441668));
#38052=DIRECTION('center_axis',(5.15167520928809E-67,-1.18789542670764E-48,
-1.));
#38053=DIRECTION('ref_axis',(0.,1.,0.));
#38054=DIRECTION('center_axis',(-0.959382309404256,-0.282109156506322,9.06501468215648E-5));
#38055=DIRECTION('ref_axis',(0.282080825358184,-0.959281308221691,0.0144837723582998));
#38056=DIRECTION('center_axis',(5.15167520928809E-67,-1.18789542670764E-48,
-1.));
#38057=DIRECTION('ref_axis',(-4.33680868994202E-19,1.,-1.18789542670764E-48));
#38058=DIRECTION('center_axis',(0.498306217397306,0.86700109722183,0.000105448244261109));
#38059=DIRECTION('ref_axis',(0.866935718266673,-0.498270127351015,0.0122204984779969));
#38060=DIRECTION('center_axis',(5.15167520928809E-67,-1.18789542670764E-48,
-1.));
#38061=DIRECTION('ref_axis',(0.,1.,0.));
#38062=DIRECTION('center_axis',(-0.978558883238081,-0.205967239672699,9.06501467769327E-5));
#38063=DIRECTION('ref_axis',(0.205946920321355,-0.978455970571544,0.0144837724038677));
#38064=DIRECTION('center_axis',(5.15167520928809E-67,-1.18789542670764E-48,
-1.));
#38065=DIRECTION('ref_axis',(-4.33680868994202E-19,1.,-1.18789542670764E-48));
#38066=DIRECTION('center_axis',(0.564794227718686,0.825231766969935,0.000105448247134299));
#38067=DIRECTION('ref_axis',(0.825169421162366,-0.564753119361502,0.0122204971264834));
#38068=DIRECTION('center_axis',(5.15167520928809E-67,-1.18789542670764E-48,
-1.));
#38069=DIRECTION('ref_axis',(0.,1.,0.));
#38070=DIRECTION('center_axis',(-0.991702316152861,-0.128555466315523,9.06501467288715E-5));
#38071=DIRECTION('ref_axis',(0.12854328403675,-0.991598126494102,0.0144837723826971));
#38072=DIRECTION('center_axis',(5.15167520928809E-67,-1.18789542670764E-48,
-1.));
#38073=DIRECTION('ref_axis',(-4.33680868994202E-19,1.,-1.18789542670764E-48));
#38074=DIRECTION('center_axis',(0.627800093808552,0.778374608459603,0.000105448247728723));
#38075=DIRECTION('ref_axis',(0.778315680170199,-0.627754220580874,0.0122204968843025));
#38076=DIRECTION('center_axis',(5.15167520928809E-67,-1.18789542670764E-48,
-1.));
#38077=DIRECTION('ref_axis',(0.,1.,0.));
#38078=DIRECTION('center_axis',(-0.998731574514058,-0.0503511057596628,
9.06501468007229E-5));
#38079=DIRECTION('ref_axis',(0.0503471356611987,-0.998626750226619,0.0144837723861814));
#38080=DIRECTION('center_axis',(5.15167520928809E-67,-1.18789542670764E-48,
-1.));
#38081=DIRECTION('ref_axis',(-4.33680868994202E-19,1.,-1.18789542670764E-48));
#38082=DIRECTION('center_axis',(0.686935363554282,0.726718511653043,0.000105448247718559));
#38083=DIRECTION('ref_axis',(0.726663364191442,-0.686885008277775,0.012220496930023));
#38084=DIRECTION('center_axis',(5.15167520928809E-67,-1.18789542670764E-48,
-1.));
#38085=DIRECTION('ref_axis',(0.,1.,0.));
#38086=DIRECTION('center_axis',(-0.99960332060644,0.0281636861069471,9.06501467308329E-5));
#38087=DIRECTION('ref_axis',(0.0281594195481261,0.999498507967114,-0.0144837723754724));
#38088=DIRECTION('center_axis',(5.15167520928809E-67,-1.18789542670764E-48,
-1.));
#38089=DIRECTION('ref_axis',(-4.33680868994202E-19,1.,-1.18789542670764E-48));
#38090=DIRECTION('center_axis',(0.741835448354451,0.670581953563782,0.00010544824772104));
#38091=DIRECTION('ref_axis',(0.670530926933101,-0.74178092148675,0.0122204969008548));
#38092=DIRECTION('center_axis',(5.15167520928809E-67,-1.18789542670764E-48,
-1.));
#38093=DIRECTION('ref_axis',(0.,1.,0.));
#38094=DIRECTION('center_axis',(-0.994312179825441,0.106504839483146,9.06501467381912E-5));
#38095=DIRECTION('ref_axis',(0.106492362571802,0.99420802503887,-0.0144837723741357));
#38096=DIRECTION('center_axis',(5.15167520928809E-67,-1.18789542670764E-48,
-1.));
#38097=DIRECTION('ref_axis',(-4.33680868994202E-19,1.,-1.18789542670764E-48));
#38098=DIRECTION('center_axis',(0.792161870929241,0.610311034740936,0.000105448246928053));
#38099=DIRECTION('ref_axis',(0.610264443534212,-0.792103508642726,0.0122204972796185));
#38100=DIRECTION('center_axis',(5.15167520928809E-67,-1.18789542670764E-48,
-1.));
#38101=DIRECTION('ref_axis',(0.,1.,0.));
#38102=DIRECTION('center_axis',(-0.982890773813477,0.184189355107443,9.06501467544422E-5));
#38103=DIRECTION('ref_axis',(0.184168744767819,0.982787919028209,-0.0144837723970302));
#38104=DIRECTION('center_axis',(5.15167520928809E-67,-1.18789542670764E-48,
-1.));
#38105=DIRECTION('ref_axis',(-4.33680868994202E-19,1.,-1.18789542670764E-48));
#38106=DIRECTION('center_axis',(0.837604352151223,0.546277345437276,0.000105448247675196));
#38107=DIRECTION('ref_axis',(0.546235476910048,-0.837542514275434,0.0122204969635834));
#38108=DIRECTION('center_axis',(5.15167520928809E-67,-1.18789542670764E-48,
-1.));
#38109=DIRECTION('ref_axis',(0.,1.,0.));
#38110=DIRECTION('center_axis',(-0.96540951933663,0.260738282108263,9.06501468112521E-5));
#38111=DIRECTION('ref_axis',(0.26070966540993,0.965308598686718,-0.0144837724135372));
#38112=DIRECTION('center_axis',(5.15167520928809E-67,-1.18789542670764E-48,
-1.));
#38113=DIRECTION('ref_axis',(-4.33680868994202E-19,1.,-1.18789542670764E-48));
#38114=DIRECTION('center_axis',(0.877882724009476,0.478875674644651,0.000105448247670176));
#38115=DIRECTION('ref_axis',(0.478838786927941,-0.877817791792444,0.0122204969627255));
#38116=DIRECTION('center_axis',(5.15167520928809E-67,-1.18789542670764E-48,
-1.));
#38117=DIRECTION('ref_axis',(0.,1.,0.));
#38118=DIRECTION('center_axis',(-0.941976194141744,0.33567967089591,9.06501467361574E-5));
#38119=DIRECTION('ref_axis',(0.335643224270696,0.941877829837669,-0.0144837723488913));
#38120=DIRECTION('center_axis',(5.15167520928809E-67,-1.18789542670764E-48,
-1.));
#38121=DIRECTION('ref_axis',(-4.33680868994202E-19,1.,-1.18789542670764E-48));
#38122=DIRECTION('center_axis',(0.912748656948457,0.408521576075799,0.000105448247549386));
#38123=DIRECTION('ref_axis',(0.408489896594413,-0.912681030718381,0.0122204970078645));
#38124=DIRECTION('center_axis',(5.15167520928809E-67,-1.18789542670764E-48,
-1.));
#38125=DIRECTION('ref_axis',(0.,1.,0.));
#38126=DIRECTION('center_axis',(0.965418060567994,0.260706649723021,0.000105448239440975));
#38127=DIRECTION('ref_axis',(0.260685939330027,-0.965346311123993,0.0122205006002244));
#38128=DIRECTION('center_axis',(-0.877867034330543,0.478904439129822,9.06501467527618E-5));
#38129=DIRECTION('ref_axis',(0.478853053655558,0.877775582562237,-0.014483772377146));
#38130=DIRECTION('center_axis',(5.15167520928809E-67,-1.18789542670764E-48,
-1.));
#38131=DIRECTION('ref_axis',(-4.33680868994202E-19,1.,-1.18789542670764E-48));
#38132=DIRECTION('center_axis',(5.15167520928809E-67,-1.18789542670764E-48,
-1.));
#38133=DIRECTION('ref_axis',(-4.33680868994202E-19,1.,-1.18789542670764E-48));
#38134=DIRECTION('',(5.15167520928809E-67,-1.18789542670764E-48,-1.));
#38135=DIRECTION('center_axis',(5.15167520928809E-67,-1.18789542670764E-48,
-1.));
#38136=DIRECTION('ref_axis',(-4.33680868994202E-19,1.,-1.18789542670764E-48));
#38137=DIRECTION('',(-5.15167520928809E-67,1.18789542670764E-48,1.));
#38138=DIRECTION('center_axis',(5.15167520928809E-67,-1.18789542670764E-48,
-1.));
#38139=DIRECTION('ref_axis',(-4.33680868994202E-19,1.,-1.18789542670764E-48));
#38140=DIRECTION('',(-5.15167520928809E-67,1.18789542670764E-48,1.));
#38141=DIRECTION('',(5.15167520928809E-67,-1.18789542670764E-48,-1.));
#38142=DIRECTION('center_axis',(5.15167520928809E-67,-1.18789542670764E-48,
-1.));
#38143=DIRECTION('ref_axis',(-4.33680868994202E-19,1.,-1.18789542670764E-48));
#38144=DIRECTION('center_axis',(5.15167520928809E-67,-1.18789542670764E-48,
-1.));
#38145=DIRECTION('ref_axis',(-4.33680868994202E-19,1.,-1.18789542670764E-48));
#38146=DIRECTION('',(-5.15167520928809E-67,1.18789542670764E-48,1.));
#38147=DIRECTION('',(5.15167520928809E-67,-1.18789542670764E-48,-1.));
#38148=DIRECTION('center_axis',(5.15167520928809E-67,-1.18789542670764E-48,
-1.));
#38149=DIRECTION('ref_axis',(-4.33680868994202E-19,1.,-1.18789542670764E-48));
#38150=DIRECTION('center_axis',(5.15167520928809E-67,-1.18789542670764E-48,
-1.));
#38151=DIRECTION('ref_axis',(-4.33680868994202E-19,1.,-1.18789542670764E-48));
#38152=DIRECTION('',(-5.15167520928809E-67,1.18789542670764E-48,1.));
#38153=DIRECTION('',(5.15167520928809E-67,-1.18789542670764E-48,-1.));
#38154=DIRECTION('center_axis',(5.15167520928809E-67,-1.18789542670764E-48,
-1.));
#38155=DIRECTION('ref_axis',(-4.33680868994202E-19,1.,-1.18789542670764E-48));
#38156=DIRECTION('center_axis',(5.15167520928809E-67,-1.18789542670764E-48,
-1.));
#38157=DIRECTION('ref_axis',(-4.33680868994202E-19,1.,-1.18789542670764E-48));
#38158=DIRECTION('',(-5.15167520928809E-67,1.18789542670764E-48,1.));
#38159=DIRECTION('',(5.15167520928809E-67,-1.18789542670764E-48,-1.));
#38160=DIRECTION('center_axis',(5.15167520928809E-67,-1.18789542670764E-48,
-1.));
#38161=DIRECTION('ref_axis',(-4.33680868994202E-19,1.,-1.18789542670764E-48));
#38162=DIRECTION('center_axis',(5.15167520928809E-67,-1.18789542670764E-48,
-1.));
#38163=DIRECTION('ref_axis',(-4.33680868994202E-19,1.,-1.18789542670764E-48));
#38164=DIRECTION('',(-5.15167520928809E-67,1.18789542670764E-48,1.));
#38165=DIRECTION('',(5.15167520928809E-67,-1.18789542670764E-48,-1.));
#38166=DIRECTION('center_axis',(5.15167520928809E-67,-1.18789542670764E-48,
-1.));
#38167=DIRECTION('ref_axis',(-4.33680868994202E-19,1.,-1.18789542670764E-48));
#38168=DIRECTION('center_axis',(5.15167520928809E-67,-1.18789542670764E-48,
-1.));
#38169=DIRECTION('ref_axis',(-4.33680868994202E-19,1.,-1.18789542670764E-48));
#38170=DIRECTION('',(-5.15167520928809E-67,1.18789542670764E-48,1.));
#38171=DIRECTION('',(5.15167520928809E-67,-1.18789542670764E-48,-1.));
#38172=DIRECTION('center_axis',(5.15167520928809E-67,-1.18789542670764E-48,
-1.));
#38173=DIRECTION('ref_axis',(-4.33680868994202E-19,1.,-1.18789542670764E-48));
#38174=DIRECTION('center_axis',(5.15167520928809E-67,-1.18789542670764E-48,
-1.));
#38175=DIRECTION('ref_axis',(-4.33680868994202E-19,1.,-1.18789542670764E-48));
#38176=DIRECTION('',(-5.15167520928809E-67,1.18789542670764E-48,1.));
#38177=DIRECTION('',(5.15167520928809E-67,-1.18789542670764E-48,-1.));
#38178=DIRECTION('center_axis',(5.15167520928809E-67,-1.18789542670764E-48,
-1.));
#38179=DIRECTION('ref_axis',(-4.33680868994202E-19,1.,-1.18789542670764E-48));
#38180=DIRECTION('center_axis',(5.15167520928809E-67,-1.18789542670764E-48,
-1.));
#38181=DIRECTION('ref_axis',(-4.33680868994202E-19,1.,-1.18789542670764E-48));
#38182=DIRECTION('',(-5.15167520928809E-67,1.18789542670764E-48,1.));
#38183=DIRECTION('',(5.15167520928809E-67,-1.18789542670764E-48,-1.));
#38184=DIRECTION('center_axis',(5.15167520928809E-67,-1.18789542670764E-48,
-1.));
#38185=DIRECTION('ref_axis',(-4.33680868994202E-19,1.,-1.18789542670764E-48));
#38186=DIRECTION('center_axis',(5.15167520928809E-67,-1.18789542670764E-48,
-1.));
#38187=DIRECTION('ref_axis',(-4.33680868994202E-19,1.,-1.18789542670764E-48));
#38188=DIRECTION('',(-5.15167520928809E-67,1.18789542670764E-48,1.));
#38189=DIRECTION('',(5.15167520928809E-67,-1.18789542670764E-48,-1.));
#38190=DIRECTION('center_axis',(5.15167520928809E-67,-1.18789542670764E-48,
-1.));
#38191=DIRECTION('ref_axis',(-4.33680868994202E-19,1.,-1.18789542670764E-48));
#38192=DIRECTION('center_axis',(5.15167520928809E-67,-1.18789542670764E-48,
-1.));
#38193=DIRECTION('ref_axis',(-4.33680868994202E-19,1.,-1.18789542670764E-48));
#38194=DIRECTION('',(-5.15167520928809E-67,1.18789542670764E-48,1.));
#38195=DIRECTION('',(5.15167520928809E-67,-1.18789542670764E-48,-1.));
#38196=DIRECTION('center_axis',(5.15167520928809E-67,-1.18789542670764E-48,
-1.));
#38197=DIRECTION('ref_axis',(-4.33680868994202E-19,1.,-1.18789542670764E-48));
#38198=DIRECTION('center_axis',(5.15167520928809E-67,-1.18789542670764E-48,
-1.));
#38199=DIRECTION('ref_axis',(-4.33680868994202E-19,1.,-1.18789542670764E-48));
#38200=DIRECTION('',(-5.15167520928809E-67,1.18789542670764E-48,1.));
#38201=DIRECTION('',(5.15167520928809E-67,-1.18789542670764E-48,-1.));
#38202=DIRECTION('center_axis',(5.15167520928809E-67,-1.18789542670764E-48,
-1.));
#38203=DIRECTION('ref_axis',(-4.33680868994202E-19,1.,-1.18789542670764E-48));
#38204=DIRECTION('center_axis',(5.15167520928809E-67,-1.18789542670764E-48,
-1.));
#38205=DIRECTION('ref_axis',(-4.33680868994202E-19,1.,-1.18789542670764E-48));
#38206=DIRECTION('',(-5.15167520928809E-67,1.18789542670764E-48,1.));
#38207=DIRECTION('',(5.15167520928809E-67,-1.18789542670764E-48,-1.));
#38208=DIRECTION('center_axis',(5.15167520928809E-67,-1.18789542670764E-48,
-1.));
#38209=DIRECTION('ref_axis',(-4.33680868994202E-19,1.,-1.18789542670764E-48));
#38210=DIRECTION('center_axis',(5.15167520928809E-67,-1.18789542670764E-48,
-1.));
#38211=DIRECTION('ref_axis',(-4.33680868994202E-19,1.,-1.18789542670764E-48));
#38212=DIRECTION('',(-5.15167520928809E-67,1.18789542670764E-48,1.));
#38213=DIRECTION('',(5.15167520928809E-67,-1.18789542670764E-48,-1.));
#38214=DIRECTION('center_axis',(5.15167520928809E-67,-1.18789542670764E-48,
-1.));
#38215=DIRECTION('ref_axis',(-4.33680868994202E-19,1.,-1.18789542670764E-48));
#38216=DIRECTION('center_axis',(5.15167520928809E-67,-1.18789542670764E-48,
-1.));
#38217=DIRECTION('ref_axis',(-4.33680868994202E-19,1.,-1.18789542670764E-48));
#38218=DIRECTION('',(-5.15167520928809E-67,1.18789542670764E-48,1.));
#38219=DIRECTION('',(5.15167520928809E-67,-1.18789542670764E-48,-1.));
#38220=DIRECTION('center_axis',(5.15167520928809E-67,-1.18789542670764E-48,
-1.));
#38221=DIRECTION('ref_axis',(-4.33680868994202E-19,1.,-1.18789542670764E-48));
#38222=DIRECTION('center_axis',(5.15167520928809E-67,-1.18789542670764E-48,
-1.));
#38223=DIRECTION('ref_axis',(-4.33680868994202E-19,1.,-1.18789542670764E-48));
#38224=DIRECTION('',(-5.15167520928809E-67,1.18789542670764E-48,1.));
#38225=DIRECTION('',(5.15167520928809E-67,-1.18789542670764E-48,-1.));
#38226=DIRECTION('center_axis',(5.15167520928809E-67,-1.18789542670764E-48,
-1.));
#38227=DIRECTION('ref_axis',(-4.33680868994202E-19,1.,-1.18789542670764E-48));
#38228=DIRECTION('center_axis',(5.15167520928809E-67,-1.18789542670764E-48,
-1.));
#38229=DIRECTION('ref_axis',(-4.33680868994202E-19,1.,-1.18789542670764E-48));
#38230=DIRECTION('',(-5.15167520928809E-67,1.18789542670764E-48,1.));
#38231=DIRECTION('',(5.15167520928809E-67,-1.18789542670764E-48,-1.));
#38232=DIRECTION('center_axis',(5.15167520928809E-67,-1.18789542670764E-48,
-1.));
#38233=DIRECTION('ref_axis',(-4.33680868994202E-19,1.,-1.18789542670764E-48));
#38234=DIRECTION('center_axis',(5.15167520928809E-67,-1.18789542670764E-48,
-1.));
#38235=DIRECTION('ref_axis',(-4.33680868994202E-19,1.,-1.18789542670764E-48));
#38236=DIRECTION('',(-5.15167520928809E-67,1.18789542670764E-48,1.));
#38237=DIRECTION('',(5.15167520928809E-67,-1.18789542670764E-48,-1.));
#38238=DIRECTION('center_axis',(5.15167520928809E-67,-1.18789542670764E-48,
-1.));
#38239=DIRECTION('ref_axis',(-4.33680868994202E-19,1.,-1.18789542670764E-48));
#38240=DIRECTION('center_axis',(5.15167520928809E-67,-1.18789542670764E-48,
-1.));
#38241=DIRECTION('ref_axis',(-4.33680868994202E-19,1.,-1.18789542670764E-48));
#38242=DIRECTION('',(-5.15167520928809E-67,1.18789542670764E-48,1.));
#38243=DIRECTION('',(5.15167520928809E-67,-1.18789542670764E-48,-1.));
#38244=DIRECTION('center_axis',(5.15167520928809E-67,-1.18789542670764E-48,
-1.));
#38245=DIRECTION('ref_axis',(-4.33680868994202E-19,1.,-1.18789542670764E-48));
#38246=DIRECTION('center_axis',(5.15167520928809E-67,-1.18789542670764E-48,
-1.));
#38247=DIRECTION('ref_axis',(-4.33680868994202E-19,1.,-1.18789542670764E-48));
#38248=DIRECTION('',(-5.15167520928809E-67,1.18789542670764E-48,1.));
#38249=DIRECTION('',(5.15167520928809E-67,-1.18789542670764E-48,-1.));
#38250=DIRECTION('center_axis',(5.15167520928809E-67,-1.18789542670764E-48,
-1.));
#38251=DIRECTION('ref_axis',(-4.33680868994202E-19,1.,-1.18789542670764E-48));
#38252=DIRECTION('center_axis',(5.15167520928809E-67,-1.18789542670764E-48,
-1.));
#38253=DIRECTION('ref_axis',(-4.33680868994202E-19,1.,-1.18789542670764E-48));
#38254=DIRECTION('',(-5.15167520928809E-67,1.18789542670764E-48,1.));
#38255=DIRECTION('',(5.15167520928809E-67,-1.18789542670764E-48,-1.));
#38256=DIRECTION('center_axis',(5.15167520928809E-67,-1.18789542670764E-48,
-1.));
#38257=DIRECTION('ref_axis',(-4.33680868994202E-19,1.,-1.18789542670764E-48));
#38258=DIRECTION('center_axis',(5.15167520928809E-67,-1.18789542670764E-48,
-1.));
#38259=DIRECTION('ref_axis',(-4.33680868994202E-19,1.,-1.18789542670764E-48));
#38260=DIRECTION('',(-5.15167520928809E-67,1.18789542670764E-48,1.));
#38261=DIRECTION('',(5.15167520928809E-67,-1.18789542670764E-48,-1.));
#38262=DIRECTION('center_axis',(5.15167520928809E-67,-1.18789542670764E-48,
-1.));
#38263=DIRECTION('ref_axis',(-4.33680868994202E-19,1.,-1.18789542670764E-48));
#38264=DIRECTION('center_axis',(5.15167520928809E-67,-1.18789542670764E-48,
-1.));
#38265=DIRECTION('ref_axis',(-4.33680868994202E-19,1.,-1.18789542670764E-48));
#38266=DIRECTION('',(-5.15167520928809E-67,1.18789542670764E-48,1.));
#38267=DIRECTION('',(5.15167520928809E-67,-1.18789542670764E-48,-1.));
#38268=DIRECTION('center_axis',(5.15167520928809E-67,-1.18789542670764E-48,
-1.));
#38269=DIRECTION('ref_axis',(-4.33680868994202E-19,1.,-1.18789542670764E-48));
#38270=DIRECTION('center_axis',(5.15167520928809E-67,-1.18789542670764E-48,
-1.));
#38271=DIRECTION('ref_axis',(-4.33680868994202E-19,1.,-1.18789542670764E-48));
#38272=DIRECTION('',(-5.15167520928809E-67,1.18789542670764E-48,1.));
#38273=DIRECTION('',(5.15167520928809E-67,-1.18789542670764E-48,-1.));
#38274=DIRECTION('center_axis',(5.15167520928809E-67,-1.18789542670764E-48,
-1.));
#38275=DIRECTION('ref_axis',(-4.33680868994202E-19,1.,-1.18789542670764E-48));
#38276=DIRECTION('center_axis',(5.15167520928809E-67,-1.18789542670764E-48,
-1.));
#38277=DIRECTION('ref_axis',(-4.33680868994202E-19,1.,-1.18789542670764E-48));
#38278=DIRECTION('',(-5.15167520928809E-67,1.18789542670764E-48,1.));
#38279=DIRECTION('',(5.15167520928809E-67,-1.18789542670764E-48,-1.));
#38280=DIRECTION('center_axis',(5.15167520928809E-67,-1.18789542670764E-48,
-1.));
#38281=DIRECTION('ref_axis',(-4.33680868994202E-19,1.,-1.18789542670764E-48));
#38282=DIRECTION('center_axis',(5.15167520928809E-67,-1.18789542670764E-48,
-1.));
#38283=DIRECTION('ref_axis',(-4.33680868994202E-19,1.,-1.18789542670764E-48));
#38284=DIRECTION('',(-5.15167520928809E-67,1.18789542670764E-48,1.));
#38285=DIRECTION('',(5.15167520928809E-67,-1.18789542670764E-48,-1.));
#38286=DIRECTION('center_axis',(5.15167520928809E-67,-1.18789542670764E-48,
-1.));
#38287=DIRECTION('ref_axis',(-4.33680868994202E-19,1.,-1.18789542670764E-48));
#38288=DIRECTION('center_axis',(5.15167520928809E-67,-1.18789542670764E-48,
-1.));
#38289=DIRECTION('ref_axis',(-4.33680868994202E-19,1.,-1.18789542670764E-48));
#38290=DIRECTION('',(-5.15167520928809E-67,1.18789542670764E-48,1.));
#38291=DIRECTION('',(5.15167520928809E-67,-1.18789542670764E-48,-1.));
#38292=DIRECTION('center_axis',(5.15167520928809E-67,-1.18789542670764E-48,
-1.));
#38293=DIRECTION('ref_axis',(-4.33680868994202E-19,1.,-1.18789542670764E-48));
#38294=DIRECTION('center_axis',(5.15167520928809E-67,-1.18789542670764E-48,
-1.));
#38295=DIRECTION('ref_axis',(-4.33680868994202E-19,1.,-1.18789542670764E-48));
#38296=DIRECTION('',(-5.15167520928809E-67,1.18789542670764E-48,1.));
#38297=DIRECTION('',(5.15167520928809E-67,-1.18789542670764E-48,-1.));
#38298=DIRECTION('center_axis',(5.15167520928809E-67,-1.18789542670764E-48,
-1.));
#38299=DIRECTION('ref_axis',(-4.33680868994202E-19,1.,-1.18789542670764E-48));
#38300=DIRECTION('center_axis',(5.15167520928809E-67,-1.18789542670764E-48,
-1.));
#38301=DIRECTION('ref_axis',(-4.33680868994202E-19,1.,-1.18789542670764E-48));
#38302=DIRECTION('',(-5.15167520928809E-67,1.18789542670764E-48,1.));
#38303=DIRECTION('',(5.15167520928809E-67,-1.18789542670764E-48,-1.));
#38304=DIRECTION('center_axis',(5.15167520928809E-67,-1.18789542670764E-48,
-1.));
#38305=DIRECTION('ref_axis',(-4.33680868994202E-19,1.,-1.18789542670764E-48));
#38306=DIRECTION('center_axis',(5.15167520928809E-67,-1.18789542670764E-48,
-1.));
#38307=DIRECTION('ref_axis',(-4.33680868994202E-19,1.,-1.18789542670764E-48));
#38308=DIRECTION('',(-5.15167520928809E-67,1.18789542670764E-48,1.));
#38309=DIRECTION('',(5.15167520928809E-67,-1.18789542670764E-48,-1.));
#38310=DIRECTION('center_axis',(5.15167520928809E-67,-1.18789542670764E-48,
-1.));
#38311=DIRECTION('ref_axis',(-4.33680868994202E-19,1.,-1.18789542670764E-48));
#38312=DIRECTION('center_axis',(5.15167520928809E-67,-1.18789542670764E-48,
-1.));
#38313=DIRECTION('ref_axis',(-4.33680868994202E-19,1.,-1.18789542670764E-48));
#38314=DIRECTION('',(-5.15167520928809E-67,1.18789542670764E-48,1.));
#38315=DIRECTION('',(5.15167520928809E-67,-1.18789542670764E-48,-1.));
#38316=DIRECTION('center_axis',(5.15167520928809E-67,-1.18789542670764E-48,
-1.));
#38317=DIRECTION('ref_axis',(-4.33680868994202E-19,1.,-1.18789542670764E-48));
#38318=DIRECTION('center_axis',(5.15167520928809E-67,-1.18789542670764E-48,
-1.));
#38319=DIRECTION('ref_axis',(-4.33680868994202E-19,1.,-1.18789542670764E-48));
#38320=DIRECTION('',(-5.15167520928809E-67,1.18789542670764E-48,1.));
#38321=DIRECTION('',(5.15167520928809E-67,-1.18789542670764E-48,-1.));
#38322=DIRECTION('center_axis',(5.15167520928809E-67,-1.18789542670764E-48,
-1.));
#38323=DIRECTION('ref_axis',(-4.33680868994202E-19,1.,-1.18789542670764E-48));
#38324=DIRECTION('center_axis',(5.15167520928809E-67,-1.18789542670764E-48,
-1.));
#38325=DIRECTION('ref_axis',(-4.33680868994202E-19,1.,-1.18789542670764E-48));
#38326=DIRECTION('',(-5.15167520928809E-67,1.18789542670764E-48,1.));
#38327=DIRECTION('',(5.15167520928809E-67,-1.18789542670764E-48,-1.));
#38328=DIRECTION('center_axis',(5.15167520928809E-67,-1.18789542670764E-48,
-1.));
#38329=DIRECTION('ref_axis',(-4.33680868994202E-19,1.,-1.18789542670764E-48));
#38330=DIRECTION('center_axis',(5.15167520928809E-67,-1.18789542670764E-48,
-1.));
#38331=DIRECTION('ref_axis',(-4.33680868994202E-19,1.,-1.18789542670764E-48));
#38332=DIRECTION('',(-5.15167520928809E-67,1.18789542670764E-48,1.));
#38333=DIRECTION('',(5.15167520928809E-67,-1.18789542670764E-48,-1.));
#38334=DIRECTION('center_axis',(5.15167520928809E-67,-1.18789542670764E-48,
-1.));
#38335=DIRECTION('ref_axis',(-4.33680868994202E-19,1.,-1.18789542670764E-48));
#38336=DIRECTION('center_axis',(5.15167520928809E-67,-1.18789542670764E-48,
-1.));
#38337=DIRECTION('ref_axis',(-4.33680868994202E-19,1.,-1.18789542670764E-48));
#38338=DIRECTION('',(-5.15167520928809E-67,1.18789542670764E-48,1.));
#38339=DIRECTION('',(5.15167520928809E-67,-1.18789542670764E-48,-1.));
#38340=DIRECTION('center_axis',(5.15167520928809E-67,-1.18789542670764E-48,
-1.));
#38341=DIRECTION('ref_axis',(-4.33680868994202E-19,1.,-1.18789542670764E-48));
#38342=DIRECTION('center_axis',(5.15167520928809E-67,-1.18789542670764E-48,
-1.));
#38343=DIRECTION('ref_axis',(-4.33680868994202E-19,1.,-1.18789542670764E-48));
#38344=DIRECTION('',(-5.15167520928809E-67,1.18789542670764E-48,1.));
#38345=DIRECTION('',(5.15167520928809E-67,-1.18789542670764E-48,-1.));
#38346=DIRECTION('center_axis',(5.15167520928809E-67,-1.18789542670764E-48,
-1.));
#38347=DIRECTION('ref_axis',(-4.33680868994202E-19,1.,-1.18789542670764E-48));
#38348=DIRECTION('center_axis',(5.15167520928809E-67,-1.18789542670764E-48,
-1.));
#38349=DIRECTION('ref_axis',(-4.33680868994202E-19,1.,-1.18789542670764E-48));
#38350=DIRECTION('',(-5.15167520928809E-67,1.18789542670764E-48,1.));
#38351=DIRECTION('',(5.15167520928809E-67,-1.18789542670764E-48,-1.));
#38352=DIRECTION('center_axis',(5.15167520928809E-67,-1.18789542670764E-48,
-1.));
#38353=DIRECTION('ref_axis',(-4.33680868994202E-19,1.,-1.18789542670764E-48));
#38354=DIRECTION('center_axis',(5.15167520928809E-67,-1.18789542670764E-48,
-1.));
#38355=DIRECTION('ref_axis',(-4.33680868994202E-19,1.,-1.18789542670764E-48));
#38356=DIRECTION('',(-5.15167520928809E-67,1.18789542670764E-48,1.));
#38357=DIRECTION('',(5.15167520928809E-67,-1.18789542670764E-48,-1.));
#38358=DIRECTION('center_axis',(5.15167520928809E-67,-1.18789542670764E-48,
-1.));
#38359=DIRECTION('ref_axis',(-4.33680868994202E-19,1.,-1.18789542670764E-48));
#38360=DIRECTION('center_axis',(5.15167520928809E-67,-1.18789542670764E-48,
-1.));
#38361=DIRECTION('ref_axis',(-4.33680868994202E-19,1.,-1.18789542670764E-48));
#38362=DIRECTION('',(-5.15167520928809E-67,1.18789542670764E-48,1.));
#38363=DIRECTION('',(5.15167520928809E-67,-1.18789542670764E-48,-1.));
#38364=DIRECTION('center_axis',(5.15167520928809E-67,-1.18789542670764E-48,
-1.));
#38365=DIRECTION('ref_axis',(-4.33680868994202E-19,1.,-1.18789542670764E-48));
#38366=DIRECTION('center_axis',(5.15167520928809E-67,-1.18789542670764E-48,
-1.));
#38367=DIRECTION('ref_axis',(-4.33680868994202E-19,1.,-1.18789542670764E-48));
#38368=DIRECTION('',(-5.15167520928809E-67,1.18789542670764E-48,1.));
#38369=DIRECTION('',(5.15167520928809E-67,-1.18789542670764E-48,-1.));
#38370=DIRECTION('center_axis',(5.15167520928809E-67,-1.18789542670764E-48,
-1.));
#38371=DIRECTION('ref_axis',(-4.33680868994202E-19,1.,-1.18789542670764E-48));
#38372=DIRECTION('center_axis',(5.15167520928809E-67,-1.18789542670764E-48,
-1.));
#38373=DIRECTION('ref_axis',(-4.33680868994202E-19,1.,-1.18789542670764E-48));
#38374=DIRECTION('',(-5.15167520928809E-67,1.18789542670764E-48,1.));
#38375=DIRECTION('',(5.15167520928809E-67,-1.18789542670764E-48,-1.));
#38376=DIRECTION('center_axis',(5.15167520928809E-67,-1.18789542670764E-48,
-1.));
#38377=DIRECTION('ref_axis',(-4.33680868994202E-19,1.,-1.18789542670764E-48));
#38378=DIRECTION('center_axis',(5.15167520928809E-67,-1.18789542670764E-48,
-1.));
#38379=DIRECTION('ref_axis',(-4.33680868994202E-19,1.,-1.18789542670764E-48));
#38380=DIRECTION('',(-5.15167520928809E-67,1.18789542670764E-48,1.));
#38381=DIRECTION('',(5.15167520928809E-67,-1.18789542670764E-48,-1.));
#38382=DIRECTION('center_axis',(5.15167520928809E-67,-1.18789542670764E-48,
-1.));
#38383=DIRECTION('ref_axis',(-4.33680868994202E-19,1.,-1.18789542670764E-48));
#38384=DIRECTION('center_axis',(5.15167520928809E-67,-1.18789542670764E-48,
-1.));
#38385=DIRECTION('ref_axis',(-4.33680868994202E-19,1.,-1.18789542670764E-48));
#38386=DIRECTION('',(-5.15167520928809E-67,1.18789542670764E-48,1.));
#38387=DIRECTION('',(5.15167520928809E-67,-1.18789542670764E-48,-1.));
#38388=DIRECTION('center_axis',(5.15167520928809E-67,-1.18789542670764E-48,
-1.));
#38389=DIRECTION('ref_axis',(-4.33680868994202E-19,1.,-1.18789542670764E-48));
#38390=DIRECTION('center_axis',(5.15167520928809E-67,-1.18789542670764E-48,
-1.));
#38391=DIRECTION('ref_axis',(-4.33680868994202E-19,1.,-1.18789542670764E-48));
#38392=DIRECTION('',(-5.15167520928809E-67,1.18789542670764E-48,1.));
#38393=DIRECTION('',(5.15167520928809E-67,-1.18789542670764E-48,-1.));
#38394=DIRECTION('center_axis',(5.15167520928809E-67,-1.18789542670764E-48,
-1.));
#38395=DIRECTION('ref_axis',(-4.33680868994202E-19,1.,-1.18789542670764E-48));
#38396=DIRECTION('center_axis',(5.15167520928809E-67,-1.18789542670764E-48,
-1.));
#38397=DIRECTION('ref_axis',(-4.33680868994202E-19,1.,-1.18789542670764E-48));
#38398=DIRECTION('',(-5.15167520928809E-67,1.18789542670764E-48,1.));
#38399=DIRECTION('',(5.15167520928809E-67,-1.18789542670764E-48,-1.));
#38400=DIRECTION('center_axis',(5.15167520928809E-67,-1.18789542670764E-48,
-1.));
#38401=DIRECTION('ref_axis',(-4.33680868994202E-19,1.,-1.18789542670764E-48));
#38402=DIRECTION('center_axis',(5.15167520928809E-67,-1.18789542670764E-48,
-1.));
#38403=DIRECTION('ref_axis',(-4.33680868994202E-19,1.,-1.18789542670764E-48));
#38404=DIRECTION('',(-5.15167520928809E-67,1.18789542670764E-48,1.));
#38405=DIRECTION('',(5.15167520928809E-67,-1.18789542670764E-48,-1.));
#38406=DIRECTION('center_axis',(5.15167520928809E-67,-1.18789542670764E-48,
-1.));
#38407=DIRECTION('ref_axis',(-4.33680868994202E-19,1.,-1.18789542670764E-48));
#38408=DIRECTION('center_axis',(5.15167520928809E-67,-1.18789542670764E-48,
-1.));
#38409=DIRECTION('ref_axis',(-4.33680868994202E-19,1.,-1.18789542670764E-48));
#38410=DIRECTION('',(-5.15167520928809E-67,1.18789542670764E-48,1.));
#38411=DIRECTION('',(5.15167520928809E-67,-1.18789542670764E-48,-1.));
#38412=DIRECTION('center_axis',(5.15167520928809E-67,-1.18789542670764E-48,
-1.));
#38413=DIRECTION('ref_axis',(-4.33680868994202E-19,1.,-1.18789542670764E-48));
#38414=DIRECTION('center_axis',(5.15167520928809E-67,-1.18789542670764E-48,
-1.));
#38415=DIRECTION('ref_axis',(-4.33680868994202E-19,1.,-1.18789542670764E-48));
#38416=DIRECTION('',(-5.15167520928809E-67,1.18789542670764E-48,1.));
#38417=DIRECTION('',(5.15167520928809E-67,-1.18789542670764E-48,-1.));
#38418=DIRECTION('center_axis',(5.15167520928809E-67,-1.18789542670764E-48,
-1.));
#38419=DIRECTION('ref_axis',(-4.33680868994202E-19,1.,-1.18789542670764E-48));
#38420=DIRECTION('center_axis',(5.15167520928809E-67,-1.18789542670764E-48,
-1.));
#38421=DIRECTION('ref_axis',(-4.33680868994202E-19,1.,-1.18789542670764E-48));
#38422=DIRECTION('',(-5.15167520928809E-67,1.18789542670764E-48,1.));
#38423=DIRECTION('',(5.15167520928809E-67,-1.18789542670764E-48,-1.));
#38424=DIRECTION('center_axis',(5.15167520928809E-67,-1.18789542670764E-48,
-1.));
#38425=DIRECTION('ref_axis',(-4.33680868994202E-19,1.,-1.18789542670764E-48));
#38426=DIRECTION('center_axis',(5.15167520928809E-67,-1.18789542670764E-48,
-1.));
#38427=DIRECTION('ref_axis',(-4.33680868994202E-19,1.,-1.18789542670764E-48));
#38428=DIRECTION('',(-5.15167520928809E-67,1.18789542670764E-48,1.));
#38429=DIRECTION('',(5.15167520928809E-67,-1.18789542670764E-48,-1.));
#38430=DIRECTION('center_axis',(5.15167520928809E-67,-1.18789542670764E-48,
-1.));
#38431=DIRECTION('ref_axis',(-4.33680868994202E-19,1.,-1.18789542670764E-48));
#38432=DIRECTION('center_axis',(5.15167520928809E-67,-1.18789542670764E-48,
-1.));
#38433=DIRECTION('ref_axis',(-4.33680868994202E-19,1.,-1.18789542670764E-48));
#38434=DIRECTION('',(-5.15167520928809E-67,1.18789542670764E-48,1.));
#38435=DIRECTION('',(5.15167520928809E-67,-1.18789542670764E-48,-1.));
#38436=DIRECTION('center_axis',(5.15167520928809E-67,-1.18789542670764E-48,
-1.));
#38437=DIRECTION('ref_axis',(-4.33680868994202E-19,1.,-1.18789542670764E-48));
#38438=DIRECTION('center_axis',(5.15167520928809E-67,-1.18789542670764E-48,
-1.));
#38439=DIRECTION('ref_axis',(-4.33680868994202E-19,1.,-1.18789542670764E-48));
#38440=DIRECTION('',(-5.15167520928809E-67,1.18789542670764E-48,1.));
#38441=DIRECTION('',(5.15167520928809E-67,-1.18789542670764E-48,-1.));
#38442=DIRECTION('center_axis',(5.15167520928809E-67,-1.18789542670764E-48,
-1.));
#38443=DIRECTION('ref_axis',(-4.33680868994202E-19,1.,-1.18789542670764E-48));
#38444=DIRECTION('center_axis',(5.15167520928809E-67,-1.18789542670764E-48,
-1.));
#38445=DIRECTION('ref_axis',(-4.33680868994202E-19,1.,-1.18789542670764E-48));
#38446=DIRECTION('',(-5.15167520928809E-67,1.18789542670764E-48,1.));
#38447=DIRECTION('',(5.15167520928809E-67,-1.18789542670764E-48,-1.));
#38448=DIRECTION('center_axis',(5.15167520928809E-67,-1.18789542670764E-48,
-1.));
#38449=DIRECTION('ref_axis',(-4.33680868994202E-19,1.,-1.18789542670764E-48));
#38450=DIRECTION('center_axis',(5.15167520928809E-67,-1.18789542670764E-48,
-1.));
#38451=DIRECTION('ref_axis',(-4.33680868994202E-19,1.,-1.18789542670764E-48));
#38452=DIRECTION('',(-5.15167520928809E-67,1.18789542670764E-48,1.));
#38453=DIRECTION('',(5.15167520928809E-67,-1.18789542670764E-48,-1.));
#38454=DIRECTION('center_axis',(5.15167520928809E-67,-1.18789542670764E-48,
-1.));
#38455=DIRECTION('ref_axis',(-4.33680868994202E-19,1.,-1.18789542670764E-48));
#38456=DIRECTION('center_axis',(5.15167520928809E-67,-1.18789542670764E-48,
-1.));
#38457=DIRECTION('ref_axis',(-4.33680868994202E-19,1.,-1.18789542670764E-48));
#38458=DIRECTION('',(-5.15167520928809E-67,1.18789542670764E-48,1.));
#38459=DIRECTION('',(5.15167520928809E-67,-1.18789542670764E-48,-1.));
#38460=DIRECTION('center_axis',(5.15167520928809E-67,-1.18789542670764E-48,
-1.));
#38461=DIRECTION('ref_axis',(-4.33680868994202E-19,1.,-1.18789542670764E-48));
#38462=DIRECTION('center_axis',(5.15167520928809E-67,-1.18789542670764E-48,
-1.));
#38463=DIRECTION('ref_axis',(-4.33680868994202E-19,1.,-1.18789542670764E-48));
#38464=DIRECTION('',(-5.15167520928809E-67,1.18789542670764E-48,1.));
#38465=DIRECTION('',(5.15167520928809E-67,-1.18789542670764E-48,-1.));
#38466=DIRECTION('center_axis',(5.15167520928809E-67,-1.18789542670764E-48,
-1.));
#38467=DIRECTION('ref_axis',(-4.33680868994202E-19,1.,-1.18789542670764E-48));
#38468=DIRECTION('center_axis',(5.15167520928809E-67,-1.18789542670764E-48,
-1.));
#38469=DIRECTION('ref_axis',(-4.33680868994202E-19,1.,-1.18789542670764E-48));
#38470=DIRECTION('',(-5.15167520928809E-67,1.18789542670764E-48,1.));
#38471=DIRECTION('',(5.15167520928809E-67,-1.18789542670764E-48,-1.));
#38472=DIRECTION('center_axis',(5.15167520928809E-67,-1.18789542670764E-48,
-1.));
#38473=DIRECTION('ref_axis',(-4.33680868994202E-19,1.,-1.18789542670764E-48));
#38474=DIRECTION('center_axis',(5.15167520928809E-67,-1.18789542670764E-48,
-1.));
#38475=DIRECTION('ref_axis',(-4.33680868994202E-19,1.,-1.18789542670764E-48));
#38476=DIRECTION('',(-5.15167520928809E-67,1.18789542670764E-48,1.));
#38477=DIRECTION('',(5.15167520928809E-67,-1.18789542670764E-48,-1.));
#38478=DIRECTION('center_axis',(5.15167520928809E-67,-1.18789542670764E-48,
-1.));
#38479=DIRECTION('ref_axis',(-4.33680868994202E-19,1.,-1.18789542670764E-48));
#38480=DIRECTION('center_axis',(5.15167520928809E-67,-1.18789542670764E-48,
-1.));
#38481=DIRECTION('ref_axis',(-4.33680868994202E-19,1.,-1.18789542670764E-48));
#38482=DIRECTION('',(-5.15167520928809E-67,1.18789542670764E-48,1.));
#38483=DIRECTION('',(5.15167520928809E-67,-1.18789542670764E-48,-1.));
#38484=DIRECTION('center_axis',(5.15167520928809E-67,-1.18789542670764E-48,
-1.));
#38485=DIRECTION('ref_axis',(-4.33680868994202E-19,1.,-1.18789542670764E-48));
#38486=DIRECTION('center_axis',(5.15167520928809E-67,-1.18789542670764E-48,
-1.));
#38487=DIRECTION('ref_axis',(-4.33680868994202E-19,1.,-1.18789542670764E-48));
#38488=DIRECTION('',(-5.15167520928809E-67,1.18789542670764E-48,1.));
#38489=DIRECTION('',(5.15167520928809E-67,-1.18789542670764E-48,-1.));
#38490=DIRECTION('center_axis',(5.15167520928809E-67,-1.18789542670764E-48,
-1.));
#38491=DIRECTION('ref_axis',(-4.33680868994202E-19,1.,-1.18789542670764E-48));
#38492=DIRECTION('center_axis',(5.15167520928809E-67,-1.18789542670764E-48,
-1.));
#38493=DIRECTION('ref_axis',(-4.33680868994202E-19,1.,-1.18789542670764E-48));
#38494=DIRECTION('',(-5.15167520928809E-67,1.18789542670764E-48,1.));
#38495=DIRECTION('',(5.15167520928809E-67,-1.18789542670764E-48,-1.));
#38496=DIRECTION('center_axis',(5.15167520928809E-67,-1.18789542670764E-48,
-1.));
#38497=DIRECTION('ref_axis',(-4.33680868994202E-19,1.,-1.18789542670764E-48));
#38498=DIRECTION('center_axis',(5.15167520928809E-67,-1.18789542670764E-48,
-1.));
#38499=DIRECTION('ref_axis',(-4.33680868994202E-19,1.,-1.18789542670764E-48));
#38500=DIRECTION('',(-5.15167520928809E-67,1.18789542670764E-48,1.));
#38501=DIRECTION('',(5.15167520928809E-67,-1.18789542670764E-48,-1.));
#38502=DIRECTION('center_axis',(5.15167520928809E-67,-1.18789542670764E-48,
-1.));
#38503=DIRECTION('ref_axis',(-4.33680868994202E-19,1.,-1.18789542670764E-48));
#38504=DIRECTION('center_axis',(5.15167520928809E-67,-1.18789542670764E-48,
-1.));
#38505=DIRECTION('ref_axis',(-4.33680868994202E-19,1.,-1.18789542670764E-48));
#38506=DIRECTION('',(-5.15167520928809E-67,1.18789542670764E-48,1.));
#38507=DIRECTION('',(5.15167520928809E-67,-1.18789542670764E-48,-1.));
#38508=DIRECTION('center_axis',(5.15167520928809E-67,-1.18789542670764E-48,
-1.));
#38509=DIRECTION('ref_axis',(-4.33680868994202E-19,1.,-1.18789542670764E-48));
#38510=DIRECTION('center_axis',(5.15167520928809E-67,-1.18789542670764E-48,
-1.));
#38511=DIRECTION('ref_axis',(-4.33680868994202E-19,1.,-1.18789542670764E-48));
#38512=DIRECTION('',(-5.15167520928809E-67,1.18789542670764E-48,1.));
#38513=DIRECTION('',(5.15167520928809E-67,-1.18789542670764E-48,-1.));
#38514=DIRECTION('center_axis',(5.15167520928809E-67,-1.18789542670764E-48,
-1.));
#38515=DIRECTION('ref_axis',(-4.33680868994202E-19,1.,-1.18789542670764E-48));
#38516=DIRECTION('center_axis',(5.15167520928809E-67,-1.18789542670764E-48,
-1.));
#38517=DIRECTION('ref_axis',(-4.33680868994202E-19,1.,-1.18789542670764E-48));
#38518=DIRECTION('',(5.15167520928809E-67,-1.18789542670764E-48,-1.));
#38519=DIRECTION('center_axis',(5.15167520928809E-67,-1.18789542670764E-48,
-1.));
#38520=DIRECTION('ref_axis',(-4.33680868994202E-19,1.,-1.18789542670764E-48));
#38521=DIRECTION('',(-5.15167520928809E-67,1.18789542670764E-48,1.));
#38522=DIRECTION('center_axis',(5.15167520928809E-67,-1.18789542670764E-48,
-1.));
#38523=DIRECTION('ref_axis',(-4.33680868994202E-19,1.,-1.18789542670764E-48));
#38524=DIRECTION('',(5.15167520928809E-67,-1.18789542670764E-48,-1.));
#38525=DIRECTION('center_axis',(5.15167520928809E-67,-1.18789542670764E-48,
-1.));
#38526=DIRECTION('ref_axis',(-4.33680868994202E-19,1.,-1.18789542670764E-48));
#38527=DIRECTION('',(-5.15167520928809E-67,1.18789542670764E-48,1.));
#38528=DIRECTION('center_axis',(5.15167520928809E-67,-1.18789542670764E-48,
-1.));
#38529=DIRECTION('ref_axis',(-4.33680868994202E-19,1.,-1.18789542670764E-48));
#38530=DIRECTION('',(5.15167520928809E-67,-1.18789542670764E-48,-1.));
#38531=DIRECTION('center_axis',(5.15167520928809E-67,-1.18789542670764E-48,
-1.));
#38532=DIRECTION('ref_axis',(-4.33680868994202E-19,1.,-1.18789542670764E-48));
#38533=DIRECTION('',(-5.15167520928809E-67,1.18789542670764E-48,1.));
#38534=DIRECTION('center_axis',(5.15167520928809E-67,-1.18789542670764E-48,
-1.));
#38535=DIRECTION('ref_axis',(-4.33680868994202E-19,1.,-1.18789542670764E-48));
#38536=DIRECTION('',(5.15167520928809E-67,-1.18789542670764E-48,-1.));
#38537=DIRECTION('center_axis',(5.15167520928809E-67,-1.18789542670764E-48,
-1.));
#38538=DIRECTION('ref_axis',(-4.33680868994202E-19,1.,-1.18789542670764E-48));
#38539=DIRECTION('',(-5.15167520928809E-67,1.18789542670764E-48,1.));
#38540=DIRECTION('center_axis',(5.15167520928809E-67,-1.18789542670764E-48,
-1.));
#38541=DIRECTION('ref_axis',(-4.33680868994202E-19,1.,-1.18789542670764E-48));
#38542=DIRECTION('',(5.15167520928809E-67,-1.18789542670764E-48,-1.));
#38543=DIRECTION('center_axis',(5.15167520928809E-67,-1.18789542670764E-48,
-1.));
#38544=DIRECTION('ref_axis',(-4.33680868994202E-19,1.,-1.18789542670764E-48));
#38545=DIRECTION('',(-5.15167520928809E-67,1.18789542670764E-48,1.));
#38546=DIRECTION('center_axis',(5.15167520928809E-67,-1.18789542670764E-48,
-1.));
#38547=DIRECTION('ref_axis',(-4.33680868994202E-19,1.,-1.18789542670764E-48));
#38548=DIRECTION('',(5.15167520928809E-67,-1.18789542670764E-48,-1.));
#38549=DIRECTION('center_axis',(5.15167520928809E-67,-1.18789542670764E-48,
-1.));
#38550=DIRECTION('ref_axis',(-4.33680868994202E-19,1.,-1.18789542670764E-48));
#38551=DIRECTION('',(-5.15167520928809E-67,1.18789542670764E-48,1.));
#38552=DIRECTION('center_axis',(5.15167520928809E-67,-1.18789542670764E-48,
-1.));
#38553=DIRECTION('ref_axis',(-4.33680868994202E-19,1.,-1.18789542670764E-48));
#38554=DIRECTION('',(5.15167520928809E-67,-1.18789542670764E-48,-1.));
#38555=DIRECTION('center_axis',(5.15167520928809E-67,-1.18789542670764E-48,
-1.));
#38556=DIRECTION('ref_axis',(-4.33680868994202E-19,1.,-1.18789542670764E-48));
#38557=DIRECTION('',(-5.15167520928809E-67,1.18789542670764E-48,1.));
#38558=DIRECTION('center_axis',(5.15167520928809E-67,-1.18789542670764E-48,
-1.));
#38559=DIRECTION('ref_axis',(-4.33680868994202E-19,1.,-1.18789542670764E-48));
#38560=DIRECTION('',(5.15167520928809E-67,-1.18789542670764E-48,-1.));
#38561=DIRECTION('center_axis',(5.15167520928809E-67,-1.18789542670764E-48,
-1.));
#38562=DIRECTION('ref_axis',(-4.33680868994202E-19,1.,-1.18789542670764E-48));
#38563=DIRECTION('',(-5.15167520928809E-67,1.18789542670764E-48,1.));
#38564=DIRECTION('center_axis',(5.15167520928809E-67,-1.18789542670764E-48,
-1.));
#38565=DIRECTION('ref_axis',(-4.33680868994202E-19,1.,-1.18789542670764E-48));
#38566=DIRECTION('',(5.15167520928809E-67,-1.18789542670764E-48,-1.));
#38567=DIRECTION('center_axis',(5.15167520928809E-67,-1.18789542670764E-48,
-1.));
#38568=DIRECTION('ref_axis',(-4.33680868994202E-19,1.,-1.18789542670764E-48));
#38569=DIRECTION('',(-5.15167520928809E-67,1.18789542670764E-48,1.));
#38570=DIRECTION('center_axis',(5.15167520928809E-67,-1.18789542670764E-48,
-1.));
#38571=DIRECTION('ref_axis',(-4.33680868994202E-19,1.,-1.18789542670764E-48));
#38572=DIRECTION('',(5.15167520928809E-67,-1.18789542670764E-48,-1.));
#38573=DIRECTION('center_axis',(5.15167520928809E-67,-1.18789542670764E-48,
-1.));
#38574=DIRECTION('ref_axis',(-4.33680868994202E-19,1.,-1.18789542670764E-48));
#38575=DIRECTION('',(-5.15167520928809E-67,1.18789542670764E-48,1.));
#38576=DIRECTION('center_axis',(5.15167520928809E-67,-1.18789542670764E-48,
-1.));
#38577=DIRECTION('ref_axis',(-4.33680868994202E-19,1.,-1.18789542670764E-48));
#38578=DIRECTION('',(5.15167520928809E-67,-1.18789542670764E-48,-1.));
#38579=DIRECTION('center_axis',(5.15167520928809E-67,-1.18789542670764E-48,
-1.));
#38580=DIRECTION('ref_axis',(-4.33680868994202E-19,1.,-1.18789542670764E-48));
#38581=DIRECTION('',(-5.15167520928809E-67,1.18789542670764E-48,1.));
#38582=DIRECTION('center_axis',(5.15167520928809E-67,-1.18789542670764E-48,
-1.));
#38583=DIRECTION('ref_axis',(-4.33680868994202E-19,1.,-1.18789542670764E-48));
#38584=DIRECTION('',(5.15167520928809E-67,-1.18789542670764E-48,-1.));
#38585=DIRECTION('center_axis',(5.15167520928809E-67,-1.18789542670764E-48,
-1.));
#38586=DIRECTION('ref_axis',(-4.33680868994202E-19,1.,-1.18789542670764E-48));
#38587=DIRECTION('',(-5.15167520928809E-67,1.18789542670764E-48,1.));
#38588=DIRECTION('center_axis',(5.15167520928809E-67,-1.18789542670764E-48,
-1.));
#38589=DIRECTION('ref_axis',(-4.33680868994202E-19,1.,-1.18789542670764E-48));
#38590=DIRECTION('',(5.15167520928809E-67,-1.18789542670764E-48,-1.));
#38591=DIRECTION('center_axis',(5.15167520928809E-67,-1.18789542670764E-48,
-1.));
#38592=DIRECTION('ref_axis',(-4.33680868994202E-19,1.,-1.18789542670764E-48));
#38593=DIRECTION('',(-5.15167520928809E-67,1.18789542670764E-48,1.));
#38594=DIRECTION('center_axis',(5.15167520928809E-67,-1.18789542670764E-48,
-1.));
#38595=DIRECTION('ref_axis',(-4.33680868994202E-19,1.,-1.18789542670764E-48));
#38596=DIRECTION('',(5.15167520928809E-67,-1.18789542670764E-48,-1.));
#38597=DIRECTION('center_axis',(5.15167520928809E-67,-1.18789542670764E-48,
-1.));
#38598=DIRECTION('ref_axis',(-4.33680868994202E-19,1.,-1.18789542670764E-48));
#38599=DIRECTION('',(-5.15167520928809E-67,1.18789542670764E-48,1.));
#38600=DIRECTION('center_axis',(5.15167520928809E-67,-1.18789542670764E-48,
-1.));
#38601=DIRECTION('ref_axis',(-4.33680868994202E-19,1.,-1.18789542670764E-48));
#38602=DIRECTION('',(-5.15167520928809E-67,1.18789542670764E-48,1.));
#38603=DIRECTION('',(5.15167520928809E-67,-1.18789542670764E-48,-1.));
#38604=DIRECTION('center_axis',(5.15167520928809E-67,-1.18789542670764E-48,
-1.));
#38605=DIRECTION('ref_axis',(-4.33680868994202E-19,1.,-1.18789542670764E-48));
#38606=DIRECTION('center_axis',(5.15167520928809E-67,-1.18789542670764E-48,
-1.));
#38607=DIRECTION('ref_axis',(0.,1.,0.));
#38608=DIRECTION('center_axis',(-0.726718511656259,-0.686935363550879,-0.000105448246390915));
#38609=DIRECTION('ref_axis',(0.686885008270217,-0.726663364190208,-0.0122204974282148));
#38610=DIRECTION('center_axis',(0.0503511057571476,0.998731574514185,-9.06501463958382E-5));
#38611=DIRECTION('ref_axis',(0.998626750226923,-0.0503471356586858,-0.0144837723739379));
#38612=DIRECTION('center_axis',(5.15167520928809E-67,-1.18789542670764E-48,
-1.));
#38613=DIRECTION('ref_axis',(0.,1.,0.));
#38614=DIRECTION('center_axis',(-0.0281636861094737,0.999603320606368,-9.06501463234301E-5));
#38615=DIRECTION('ref_axis',(0.999498507968587,0.0281594195507115,-0.0144837722688343));
#38616=DIRECTION('center_axis',(-0.670581953565459,-0.741835448352935,-0.000105448247414229));
#38617=DIRECTION('ref_axis',(0.741780921484837,-0.670530926934418,-0.0122204969447688));
#38618=DIRECTION('center_axis',(5.15167520928809E-67,-1.18789542670764E-48,
-1.));
#38619=DIRECTION('ref_axis',(0.,1.,0.));
#38620=DIRECTION('center_axis',(-0.106504839485416,0.994312179825198,-9.06501464431132E-5));
#38621=DIRECTION('ref_axis',(0.994208025038947,0.106492362574112,-0.014483772351861));
#38622=DIRECTION('center_axis',(-0.610311034741592,-0.792161870928735,-0.000105448247339917));
#38623=DIRECTION('ref_axis',(0.792103508645573,-0.610264443537491,-0.0122204969313235));
#38624=DIRECTION('center_axis',(5.15167520928809E-67,-1.18789542670764E-48,
-1.));
#38625=DIRECTION('ref_axis',(0.,1.,0.));
#38626=DIRECTION('center_axis',(-0.184189355109993,0.982890773812999,-9.06501463311491E-5));
#38627=DIRECTION('ref_axis',(0.982787919029266,0.184168744770673,-0.0144837722890199));
#38628=DIRECTION('center_axis',(-0.546277345439217,-0.837604352149957,-0.000105448247410497));
#38629=DIRECTION('ref_axis',(0.837542514274823,-0.546235476912428,-0.0122204968991007));
#38630=DIRECTION('center_axis',(5.15167520928809E-67,-1.18789542670764E-48,
-1.));
#38631=DIRECTION('ref_axis',(0.,1.,0.));
#38632=DIRECTION('center_axis',(-0.260738282110594,0.965409519336,-9.0650146457266E-5));
#38633=DIRECTION('ref_axis',(0.965308598686112,0.260709665412272,-0.0144837724117514));
#38634=DIRECTION('center_axis',(-0.478875674647023,-0.877882724008182,-0.000105448247224529));
#38635=DIRECTION('ref_axis',(0.877817791791478,-0.478838786930502,-0.0122204969317693));
#38636=DIRECTION('center_axis',(5.15167520928809E-67,-1.18789542670764E-48,
-1.));
#38637=DIRECTION('ref_axis',(0.,1.,0.));
#38638=DIRECTION('center_axis',(-0.335679670898074,0.941976194140973,-9.06501464082373E-5));
#38639=DIRECTION('ref_axis',(0.941877829837014,0.335643224272907,-0.014483772340284));
#38640=DIRECTION('center_axis',(-0.40852157607848,-0.912748656947257,-0.000105448246964389));
#38641=DIRECTION('ref_axis',(0.912681030716442,-0.408489896596762,-0.0122204970741974));
#38642=DIRECTION('center_axis',(5.15167520928809E-67,-1.18789542670764E-48,
-1.));
#38643=DIRECTION('ref_axis',(0.,1.,0.));
#38644=DIRECTION('center_axis',(-0.408551482889657,0.91273527247018,-9.06501463992171E-5));
#38645=DIRECTION('ref_axis',(0.91264007096006,0.408507431043052,-0.014483772320157));
#38646=DIRECTION('center_axis',(-0.335648806144879,-0.941987190897087,-0.000105448247367288));
#38647=DIRECTION('ref_axis',(0.941917287594001,-0.335622530214118,-0.0122204968897907));
#38648=DIRECTION('center_axis',(5.15167520928809E-67,-1.18789542670764E-48,
-1.));
#38649=DIRECTION('ref_axis',(0.,1.,0.));
#38650=DIRECTION('center_axis',(-0.478904439132113,0.877867034329292,-9.06501463430316E-5));
#38651=DIRECTION('ref_axis',(0.877775582560928,0.478853053657823,-0.0144837723815965));
#38652=DIRECTION('center_axis',(-0.260706649707894,-0.965418060572078,-0.000105448247265905));
#38653=DIRECTION('ref_axis',(0.965346311170054,-0.260685939326527,-0.0122204970363453));
#38654=DIRECTION('center_axis',(5.15167520928809E-67,-1.18789542670764E-48,
-1.));
#38655=DIRECTION('ref_axis',(0.,1.,0.));
#38656=DIRECTION('center_axis',(-0.546304790255147,0.837586454001514,-9.06501464163507E-5));
#38657=DIRECTION('ref_axis',(0.837499315806636,0.546246387962313,-0.0144837723519214));
#38658=DIRECTION('center_axis',(-0.184157150081311,-0.982896806869672,-0.00010544824733539));
#38659=DIRECTION('ref_axis',(0.982823653730718,-0.184142132936614,-0.012220496919376));
#38660=DIRECTION('center_axis',(5.15167520928809E-67,-1.18789542670764E-48,
-1.));
#38661=DIRECTION('ref_axis',(0.,1.,0.));
#38662=DIRECTION('center_axis',(-0.610336990681852,0.792141874658809,-9.06501463120476E-5));
#38663=DIRECTION('ref_axis',(0.792059587273495,0.610271931640219,-0.0144837723075503));
#38664=DIRECTION('center_axis',(-0.106472260385922,-0.994315667506542,-0.000105448247451369));
#38665=DIRECTION('ref_axis',(0.994241561642557,-0.106463029063183,-0.0122204969318448));
#38666=DIRECTION('center_axis',(5.15167520928809E-67,-1.18789542670764E-48,
-1.));
#38667=DIRECTION('ref_axis',(0.,1.,0.));
#38668=DIRECTION('center_axis',(-0.670606260603123,0.741813477245087,-9.06501463072396E-5));
#38669=DIRECTION('ref_axis',(0.741736547997548,0.670534945922644,-0.0144837723400245));
#38670=DIRECTION('center_axis',(-0.0281309338001256,-0.999604241409669,
-0.000105448247349234));
#38671=DIRECTION('ref_axis',(0.999529639708615,-0.0281275452135709,-0.012220496889411));
#38672=DIRECTION('center_axis',(5.15167520928809E-67,-1.18789542670764E-48,
-1.));
#38673=DIRECTION('ref_axis',(0.,1.,0.));
#38674=DIRECTION('center_axis',(-0.726741019928497,0.686911553066215,-9.0650146372247E-5));
#38675=DIRECTION('ref_axis',(0.686840456250864,0.726663889287803,-0.014483772375632));
#38676=DIRECTION('center_axis',(0.0503838293471008,-0.9987299227624,-0.000105448247268434));
#38677=DIRECTION('ref_axis',(0.998655285167451,0.0503813543057433,-0.0122204969390446));
#38678=DIRECTION('center_axis',(5.15167520928809E-67,-1.18789542670764E-48,
-1.));
#38679=DIRECTION('ref_axis',(0.,1.,0.));
#38680=DIRECTION('center_axis',(-0.77839517919999,0.627774590741587,-9.06501465192481E-5));
#38681=DIRECTION('ref_axis',(0.62770976469511,0.778312708136478,-0.0144837722873138));
#38682=DIRECTION('center_axis',(0.128587959432554,-0.991698102029866,-0.000105448247403937));
#38683=DIRECTION('ref_axis',(0.991623888707038,0.128579636022696,-0.0122204969540051));
#38684=DIRECTION('center_axis',(5.15167520928809E-67,-1.18789542670764E-48,
-1.));
#38685=DIRECTION('ref_axis',(0.,1.,0.));
#38686=DIRECTION('center_axis',(-0.825250273349494,0.564767189308247,-9.06501463546308E-5));
#38687=DIRECTION('ref_axis',(0.564709033703414,0.82516297032304,-0.0144837723475052));
#38688=DIRECTION('center_axis',(0.205999301987418,-0.978552132725367,-0.000105448247113811));
#38689=DIRECTION('ref_axis',(0.978478801224233,0.205985181525565,-0.0122204969893998));
#38690=DIRECTION('center_axis',(5.15167520928809E-67,-1.18789542670764E-48,
-1.));
#38691=DIRECTION('ref_axis',(0.,1.,0.));
#38692=DIRECTION('center_axis',(-0.867017425140065,0.498277810348848,-9.06501462870057E-5));
#38693=DIRECTION('ref_axis',(0.498226683734515,0.866925828402957,-0.0144837723937473));
#38694=DIRECTION('center_axis',(0.282140590344591,-0.959373064120873,-0.000105448247263863));
#38695=DIRECTION('ref_axis',(0.959301066555575,0.282120759888322,-0.0122204969363817));
#38696=DIRECTION('center_axis',(5.15167520928809E-67,-1.18789542670764E-48,
-1.));
#38697=DIRECTION('ref_axis',(0.,1.,0.));
#38698=DIRECTION('center_axis',(-0.903439126191882,0.428716382994866,-9.06501464245823E-5));
#38699=DIRECTION('ref_axis',(0.42867260058449,0.903343800470088,-0.0144837723120868));
#38700=DIRECTION('center_axis',(0.356542388140961,-0.934279141552142,-0.000105448247299974));
#38701=DIRECTION('ref_axis',(0.934208921811354,0.356516969951643,-0.0122204969034503));
#38702=DIRECTION('center_axis',(5.15167520928809E-67,-1.18789542670764E-48,
-1.));
#38703=DIRECTION('ref_axis',(0.,1.,0.));
#38704=DIRECTION('center_axis',(-0.934290824606917,0.356511776576704,-9.06501463905499E-5));
#38705=DIRECTION('ref_axis',(0.356475608302988,0.934192357614636,-0.0144837722787681));
#38706=DIRECTION('center_axis',(0.428745983551553,-0.903425077396614,-0.000105448247174382));
#38707=DIRECTION('ref_axis',(0.903357068407879,0.428715134340607,-0.0122204969145006));
#38708=DIRECTION('center_axis',(5.15167520928809E-67,-1.18789542670764E-48,
-1.));
#38709=DIRECTION('ref_axis',(0.,1.,0.));
#38710=DIRECTION('center_axis',(-0.959382309405018,0.282109156503729,-9.06501463332588E-5));
#38711=DIRECTION('ref_axis',(0.282080825355611,0.959281308222547,-0.0144837723517365));
#38712=DIRECTION('center_axis',(0.498306217395032,-0.867001097223137,-0.000105448243846677));
#38713=DIRECTION('ref_axis',(0.866935718268405,0.498270127348975,-0.0122204984383232));
#38714=DIRECTION('center_axis',(5.15167520928809E-67,-1.18789542670764E-48,
-1.));
#38715=DIRECTION('ref_axis',(0.,1.,0.));
#38716=DIRECTION('center_axis',(-0.978558883238511,0.205967239670656,-9.06501465473592E-5));
#38717=DIRECTION('ref_axis',(0.205946920319669,0.978455970573743,-0.0144837722792749));
#38718=DIRECTION('center_axis',(0.564794227716619,-0.825231766971349,-0.000105448246777006));
#38719=DIRECTION('ref_axis',(0.825169421163283,0.564753119359096,-0.01222049717581));
#38720=DIRECTION('center_axis',(5.15167520928809E-67,-1.18789542670764E-48,
-1.));
#38721=DIRECTION('ref_axis',(0.,1.,0.));
#38722=DIRECTION('center_axis',(-0.991702316153162,0.128555466313202,-9.0650146420716E-5));
#38723=DIRECTION('ref_axis',(0.128543284034494,0.991598126494967,-0.0144837723435229));
#38724=DIRECTION('center_axis',(0.627800093806525,-0.778374608461238,-0.000105448247294656));
#38725=DIRECTION('ref_axis',(0.778315680171741,0.627754220578766,-0.012220496894383));
#38726=DIRECTION('center_axis',(5.15167520928809E-67,-1.18789542670764E-48,
-1.));
#38727=DIRECTION('ref_axis',(0.,1.,0.));
#38728=DIRECTION('center_axis',(-0.998731574514195,0.0503511057569474,-9.06501463044587E-5));
#38729=DIRECTION('ref_axis',(0.0503471356585215,0.998626750227776,-0.0144837723156803));
#38730=DIRECTION('center_axis',(0.686935363552588,-0.726718511654644,-0.000105448247440854));
#38731=DIRECTION('ref_axis',(0.726663364192637,0.6868850082757,-0.0122204969756106));
#38732=DIRECTION('center_axis',(5.15167520928809E-67,-1.18789542670764E-48,
-1.));
#38733=DIRECTION('ref_axis',(0.,1.,0.));
#38734=DIRECTION('center_axis',(-0.99960332060638,-0.0281636861090561,-9.06501465204533E-5));
#38735=DIRECTION('ref_axis',(0.0281594195503036,-0.999498507968962,0.0144837722437162));
#38736=DIRECTION('center_axis',(0.741835448352776,-0.670581953565635,-0.000105448247295083));
#38737=DIRECTION('ref_axis',(0.67053092693442,0.741780921484487,-0.0122204969658991));
#38738=DIRECTION('center_axis',(5.15167520928809E-67,-1.18789542670764E-48,
-1.));
#38739=DIRECTION('ref_axis',(0.,1.,0.));
#38740=DIRECTION('center_axis',(-0.994312179825187,-0.106504839485521,-9.0650146389517E-5));
#38741=DIRECTION('ref_axis',(0.106492362574174,-0.994208025038546,0.0144837723789195));
#38742=DIRECTION('center_axis',(0.792161870927703,-0.610311034742932,-0.000105448246562834));
#38743=DIRECTION('ref_axis',(0.610264443536631,0.792103508641721,-0.0122204972240042));
#38744=DIRECTION('center_axis',(5.15167520928809E-67,-1.18789542670764E-48,
-1.));
#38745=DIRECTION('ref_axis',(0.,1.,0.));
#38746=DIRECTION('center_axis',(-0.982890773812962,-0.18418935511019,-9.06501462458389E-5));
#38747=DIRECTION('ref_axis',(0.184168744770736,-0.982787919028534,0.0144837723378535));
#38748=DIRECTION('center_axis',(0.837604352149828,-0.546277345439416,-0.000105448247288724));
#38749=DIRECTION('ref_axis',(0.546235476912052,0.837542514273825,-0.0122204969843265));
#38750=DIRECTION('center_axis',(5.15167520928809E-67,-1.18789542670764E-48,
-1.));
#38751=DIRECTION('ref_axis',(0.,1.,0.));
#38752=DIRECTION('center_axis',(-0.965409519335916,-0.260738282110905,-9.06501463158079E-5));
#38753=DIRECTION('ref_axis',(0.260709665413015,-0.965308598687581,0.0144837723005081));
#38754=DIRECTION('center_axis',(0.877882724007609,-0.478875674648073,-0.000105448246644854));
#38755=DIRECTION('ref_axis',(0.47883878693024,0.877817791788535,-0.012220497153411));
#38756=DIRECTION('center_axis',(5.15167520928809E-67,-1.18789542670764E-48,
-1.));
#38757=DIRECTION('ref_axis',(0.,1.,0.));
#38758=DIRECTION('center_axis',(-0.941976194141077,-0.335679670897783,-9.06501465752214E-5));
#38759=DIRECTION('ref_axis',(0.335643224272825,-0.941877829837701,0.0144837722974511));
#38760=DIRECTION('center_axis',(0.912748656947635,-0.408521576077636,-0.000105448247395522));
#38761=DIRECTION('ref_axis',(0.408489896596716,0.912681030718573,-0.0122204969165703));
#38762=DIRECTION('center_axis',(5.15167520928809E-67,-1.18789542670764E-48,
-1.));
#38763=DIRECTION('ref_axis',(0.,1.,0.));
#38764=DIRECTION('center_axis',(-0.912735272470059,-0.408551482889927,-9.0650146236208E-5));
#38765=DIRECTION('ref_axis',(0.408507431042893,-0.912640070958992,0.0144837723919199));
#38766=DIRECTION('center_axis',(0.941987190897161,-0.335648806144671,-0.000105448247475279));
#38767=DIRECTION('ref_axis',(0.335622530214028,0.941917287594399,-0.0122204968616106));
#38768=DIRECTION('center_axis',(5.15167520928809E-67,-1.18789542670764E-48,
-1.));
#38769=DIRECTION('ref_axis',(0.,1.,0.));
#38770=DIRECTION('center_axis',(-0.877867034329361,-0.478904439131988,-9.06501463610722E-5));
#38771=DIRECTION('ref_axis',(0.478853053657853,-0.877775582561276,0.0144837723595397));
#38772=DIRECTION('center_axis',(0.965418060572122,-0.260706649707733,-0.000105448247352975));
#38773=DIRECTION('ref_axis',(0.260685939326823,0.965346311171741,-0.012220496896787));
#38774=DIRECTION('center_axis',(5.15167520928809E-67,-1.18789542670764E-48,
-1.));
#38775=DIRECTION('ref_axis',(0.,1.,0.));
#38776=DIRECTION('center_axis',(-0.837586454001461,-0.546304790255229,-9.06501463408637E-5));
#38777=DIRECTION('ref_axis',(0.54624638796239,-0.837499315806573,0.0144837723526967));
#38778=DIRECTION('center_axis',(0.982896806869685,-0.184157150081241,-0.000105448247384682));
#38779=DIRECTION('ref_axis',(0.184142132936524,0.982823653730634,-0.0122204969274716));
#38780=DIRECTION('center_axis',(5.15167520928809E-67,-1.18789542670764E-48,
-1.));
#38781=DIRECTION('ref_axis',(0.,1.,0.));
#38782=DIRECTION('center_axis',(-0.792141874658961,-0.610336990681655,-9.06501464140886E-5));
#38783=DIRECTION('ref_axis',(0.610271931639049,-0.792059587272402,0.0144837724166105));
#38784=DIRECTION('center_axis',(0.994315667506523,-0.1064722603861,-0.000105448247372999));
#38785=DIRECTION('ref_axis',(0.106463029063429,0.994241561643113,-0.0122204968844733));
#38786=DIRECTION('center_axis',(5.15167520928809E-67,-1.18789542670764E-48,
-1.));
#38787=DIRECTION('ref_axis',(0.,1.,0.));
#38788=DIRECTION('center_axis',(-0.741813477245026,-0.670606260603191,-9.06501462657205E-5));
#38789=DIRECTION('ref_axis',(0.670534945922615,-0.741736547997381,0.0144837723499451));
#38790=DIRECTION('center_axis',(0.999604241409683,-0.0281309337996267,-0.000105448247542078));
#38791=DIRECTION('ref_axis',(0.0281275452130772,0.999529639708833,-0.0122204968727785));
#38792=DIRECTION('center_axis',(5.15167520928809E-67,-1.18789542670764E-48,
-1.));
#38793=DIRECTION('ref_axis',(0.,1.,0.));
#38794=DIRECTION('center_axis',(-0.686911553066313,-0.726741019928404,-9.0650146445407E-5));
#38795=DIRECTION('ref_axis',(0.726663889287897,-0.686840456251137,0.0144837723579623));
#38796=DIRECTION('center_axis',(0.998729922762429,0.0503838293465177,-0.00010544824700806));
#38797=DIRECTION('ref_axis',(0.0503813543051317,-0.998655285166875,0.0122204969886123));
#38798=DIRECTION('center_axis',(5.15167520928809E-67,-1.18789542670764E-48,
-1.));
#38799=DIRECTION('ref_axis',(0.,1.,0.));
#38800=DIRECTION('center_axis',(-0.627774590741284,-0.778395179200234,-9.06501463091932E-5));
#38801=DIRECTION('ref_axis',(0.778312708136324,-0.627709764694486,0.014483772322638));
#38802=DIRECTION('center_axis',(0.991698102029894,0.128587959432343,-0.000105448247307732));
#38803=DIRECTION('ref_axis',(0.128579636022594,-0.991623888707978,0.0122204968787672));
#38804=DIRECTION('center_axis',(5.15167520928809E-67,-1.18789542670764E-48,
-1.));
#38805=DIRECTION('ref_axis',(0.,1.,0.));
#38806=DIRECTION('center_axis',(-0.564767189308512,-0.825250273349312,-9.06501464604225E-5));
#38807=DIRECTION('ref_axis',(0.825162970323365,-0.564709033704023,0.014483772305219));
#38808=DIRECTION('center_axis',(0.978552132725239,0.205999301988023,-0.000105448247439453));
#38809=DIRECTION('ref_axis',(0.205985181526365,-0.978478801225051,0.0122204969104439));
#38810=DIRECTION('center_axis',(5.15167520928809E-67,-1.18789542670764E-48,
-1.));
#38811=DIRECTION('ref_axis',(0.,1.,0.));
#38812=DIRECTION('center_axis',(-0.498277810349565,-0.867017425139653,-9.06501466563663E-5));
#38813=DIRECTION('ref_axis',(0.86692582840462,-0.498226683736414,0.0144837722289047));
#38814=DIRECTION('center_axis',(0.959373064120893,0.282140590344525,-0.00010544824722367));
#38815=DIRECTION('ref_axis',(0.282120759888269,-0.959301066555644,0.0122204969322086));
#38816=DIRECTION('center_axis',(5.15167520928809E-67,-1.18789542670764E-48,
-1.));
#38817=DIRECTION('ref_axis',(0.,1.,0.));
#38818=DIRECTION('center_axis',(-0.428716382994794,-0.903439126191916,-9.06501464376821E-5));
#38819=DIRECTION('ref_axis',(0.903343800470677,-0.428672600584677,0.0144837722698243));
#38820=DIRECTION('center_axis',(0.934279141552165,0.356542388140901,-0.000105448247303552));
#38821=DIRECTION('ref_axis',(0.356516969951467,-0.934208921811066,0.0122204969306124));
#38822=DIRECTION('center_axis',(5.15167520928809E-67,-1.18789542670764E-48,
-1.));
#38823=DIRECTION('ref_axis',(0.,1.,0.));
#38824=DIRECTION('center_axis',(-0.356511776576584,-0.934290824606963,-9.06501462973138E-5));
#38825=DIRECTION('ref_axis',(0.9341923576135,-0.356475608302424,0.0144837723659048));
#38826=DIRECTION('center_axis',(0.903425077396469,0.42874598355186,-0.000105448247323971));
#38827=DIRECTION('ref_axis',(0.428715134340782,-0.903357068407445,0.0122204969404582));
#38828=DIRECTION('center_axis',(5.15167520928809E-67,-1.18789542670764E-48,
-1.));
#38829=DIRECTION('ref_axis',(0.,1.,0.));
#38830=DIRECTION('center_axis',(-0.282109156503611,-0.959382309405053,-9.06501462853803E-5));
#38831=DIRECTION('ref_axis',(0.959281308222382,-0.282080825355435,0.0144837723660616));
#38832=DIRECTION('center_axis',(0.867001097223284,0.498306217394775,-0.000105448243705777));
#38833=DIRECTION('ref_axis',(0.498270127348596,-0.86693571826834,0.0122204984583659));
#38834=DIRECTION('center_axis',(5.15167520928809E-67,-1.18789542670764E-48,
-1.));
#38835=DIRECTION('ref_axis',(0.,1.,0.));
#38836=DIRECTION('center_axis',(-0.205967239670074,-0.978558883238633,-9.06501462899978E-5));
#38837=DIRECTION('ref_axis',(0.978455970573443,-0.205946920318997,0.0144837723091262));
#38838=DIRECTION('center_axis',(0.825231766971361,0.564794227716602,-0.000105448246768021));
#38839=DIRECTION('ref_axis',(0.56475311935916,-0.825169421163415,0.0122204971638891));
#38840=DIRECTION('center_axis',(5.15167520928809E-67,-1.18789542670764E-48,
-1.));
#38841=DIRECTION('ref_axis',(0.,1.,0.));
#38842=DIRECTION('center_axis',(-0.128555466313085,-0.991702316153177,-9.06501463759606E-5));
#38843=DIRECTION('ref_axis',(0.991598126495219,-0.128543284034406,0.014483772327091));
#38844=DIRECTION('center_axis',(0.778374608461285,0.627800093806467,-0.000105448247278628));
#38845=DIRECTION('ref_axis',(0.627754220578617,-0.778315680171672,0.0122204969064386));
#38846=DIRECTION('center_axis',(5.15167520928809E-67,-1.18789542670764E-48,
-1.));
#38847=DIRECTION('ref_axis',(0.,1.,0.));
#38848=DIRECTION('center_axis',(-0.0503511057568215,-0.998731574514202,
-9.06501462140748E-5));
#38849=DIRECTION('ref_axis',(0.998626750226433,-0.0503471356583347,0.0144837724089729));
#38850=DIRECTION('center_axis',(0.72671851165485,0.686935363552371,-0.000105448247305609));
#38851=DIRECTION('ref_axis',(0.68688500827568,-0.726663364193057,0.0122204969517677));
#38852=DIRECTION('center_axis',(5.15167520928809E-67,-1.18789542670764E-48,
-1.));
#38853=DIRECTION('ref_axis',(0.,1.,0.));
#38854=DIRECTION('center_axis',(0.028163686109212,-0.999603320606376,-9.06501464412085E-5));
#38855=DIRECTION('ref_axis',(0.999498507967367,0.0281594195504058,0.0144837723535955));
#38856=DIRECTION('center_axis',(0.670581953565646,0.741835448352765,-0.000105448247317749));
#38857=DIRECTION('ref_axis',(0.741780921484837,-0.670530926934763,0.0122204969257884));
#38858=DIRECTION('center_axis',(5.15167520928809E-67,-1.18789542670764E-48,
-1.));
#38859=DIRECTION('ref_axis',(0.,1.,0.));
#38860=DIRECTION('center_axis',(0.106504839485654,-0.994312179825173,-9.06501463242885E-5));
#38861=DIRECTION('ref_axis',(0.994208025039066,0.106492362574368,0.0144837723417732));
#38862=DIRECTION('center_axis',(0.610311034742769,0.792161870927829,-0.000105448246632335));
#38863=DIRECTION('ref_axis',(0.792103508641049,-0.610264443535841,0.012220497306985));
#38864=DIRECTION('center_axis',(5.15167520928809E-67,-1.18789542670764E-48,
-1.));
#38865=DIRECTION('ref_axis',(0.,1.,0.));
#38866=DIRECTION('center_axis',(0.184189355110076,-0.982890773812984,-9.06501463014399E-5));
#38867=DIRECTION('ref_axis',(0.982787919027527,0.184168744770422,0.0144837724102069));
#38868=DIRECTION('center_axis',(0.546277345439608,0.837604352149702,-0.000105448247164003));
#38869=DIRECTION('ref_axis',(0.837542514274121,-0.546235476912526,0.0122204969428009));
#38870=DIRECTION('center_axis',(5.15167520928809E-67,-1.18789542670764E-48,
-1.));
#38871=DIRECTION('ref_axis',(0.,1.,0.));
#38872=DIRECTION('center_axis',(0.260738282110494,-0.965409519336027,-9.06501465102787E-5));
#38873=DIRECTION('ref_axis',(0.965308598687087,0.260709665412434,0.0144837723438797));
#38874=DIRECTION('center_axis',(0.47887567464682,0.877882724008293,-0.000105448247318393));
#38875=DIRECTION('ref_axis',(0.877817791791359,-0.47883878693017,0.0122204969532827));
#38876=DIRECTION('center_axis',(5.15167520928809E-67,-1.18789542670764E-48,
-1.));
#38877=DIRECTION('ref_axis',(0.,1.,0.));
#38878=DIRECTION('center_axis',(0.335679670898317,-0.941976194140886,-9.06501463025926E-5));
#38879=DIRECTION('ref_axis',(0.941877829837149,0.335643224273232,0.0144837723239312));
#38880=DIRECTION('center_axis',(0.408521576078182,0.912748656947391,-0.000105448247109452));
#38881=DIRECTION('ref_axis',(0.912681030717227,-0.408489896596761,0.0122204970155898));
#38882=DIRECTION('center_axis',(5.15167520928809E-67,-1.18789542670764E-48,
-1.));
#38883=DIRECTION('ref_axis',(0.,1.,0.));
#38884=DIRECTION('center_axis',(0.40855148288974,-0.912735272470143,-9.06501463607514E-5));
#38885=DIRECTION('ref_axis',(0.912640070959719,0.408507431042997,0.0144837723432182));
#38886=DIRECTION('center_axis',(0.33564880614496,0.941987190897058,-0.00010544824731253));
#38887=DIRECTION('ref_axis',(0.941917287593217,-0.335622530213924,0.0122204969555834));
#38888=DIRECTION('center_axis',(5.15167520928809E-67,-1.18789542670764E-48,
-1.));
#38889=DIRECTION('ref_axis',(0.,1.,0.));
#38890=DIRECTION('center_axis',(0.47890443913187,-0.877867034329425,-9.06501464476592E-5));
#38891=DIRECTION('ref_axis',(0.877775582561568,0.47885305365786,0.0144837723415746));
#38892=DIRECTION('center_axis',(0.260706649725499,0.965418060567325,-0.000105448239035086));
#38893=DIRECTION('ref_axis',(0.965346311123191,-0.260685939332472,0.0122205006114622));
#38894=DIRECTION('center_axis',(5.15167520928809E-67,-1.18789542670764E-48,
-1.));
#38895=DIRECTION('ref_axis',(0.,1.,0.));
#38896=DIRECTION('center_axis',(0.546304790255255,-0.837586454001444,-9.0650146342598E-5));
#38897=DIRECTION('ref_axis',(0.837499315807156,0.546246387962813,0.0144837723030219));
#38898=DIRECTION('center_axis',(0.184157150081292,0.982896806869675,-0.000105448247335927));
#38899=DIRECTION('ref_axis',(0.982823653730575,-0.184142132936566,0.0122204969315608));
#38900=DIRECTION('center_axis',(5.15167520928809E-67,-1.18789542670764E-48,
-1.));
#38901=DIRECTION('ref_axis',(0.,1.,0.));
#38902=DIRECTION('center_axis',(0.610336990681674,-0.792141874658946,-9.06501464101343E-5));
#38903=DIRECTION('ref_axis',(0.792059587273886,0.610271931640238,0.0144837722853376));
#38904=DIRECTION('center_axis',(0.106472260386401,0.99431566750649,-0.000105448247238185));
#38905=DIRECTION('ref_axis',(0.994241561642249,-0.106463029063635,0.0122204969529716));
#38906=DIRECTION('center_axis',(5.15167520928809E-67,-1.18789542670764E-48,
-1.));
#38907=DIRECTION('ref_axis',(0.,1.,0.));
#38908=DIRECTION('center_axis',(0.670606260602894,-0.741813477245294,-9.06501464627064E-5));
#38909=DIRECTION('ref_axis',(0.741736547997723,0.670534945922382,0.0144837723432088));
#38910=DIRECTION('center_axis',(0.0281309337999561,0.999604241409674,-0.000105448247417899));
#38911=DIRECTION('ref_axis',(0.999529639708026,-0.0281275452133787,0.0122204969380853));
#38912=DIRECTION('center_axis',(5.15167520928809E-67,-1.18789542670764E-48,
-1.));
#38913=DIRECTION('ref_axis',(0.,1.,0.));
#38914=DIRECTION('center_axis',(0.726741019928368,-0.686911553066351,-9.0650146471134E-5));
#38915=DIRECTION('ref_axis',(0.686840456251459,0.726663889288164,0.0144837723292476));
#38916=DIRECTION('center_axis',(-0.050383829347144,0.998729922762398,-0.000105448247269544));
#38917=DIRECTION('ref_axis',(0.998655285167744,0.0503813543057988,0.0122204969148411));
#38918=DIRECTION('center_axis',(5.15167520928809E-67,-1.18789542670764E-48,
-1.));
#38919=DIRECTION('ref_axis',(0.,1.,0.));
#38920=DIRECTION('center_axis',(0.778395179200218,-0.627774590741304,-9.06501463631465E-5));
#38921=DIRECTION('ref_axis',(0.627709764694807,0.778312708136684,0.0144837722894029));
#38922=DIRECTION('center_axis',(-0.12858795942834,0.991698102030413,-0.000105448245500489));
#38923=DIRECTION('ref_axis',(0.991623888698102,0.128579636017312,0.0122204977357358));
#38924=DIRECTION('center_axis',(5.15167520928809E-67,-1.18789542670764E-48,
-1.));
#38925=DIRECTION('ref_axis',(0.,1.,0.));
#38926=DIRECTION('center_axis',(0.825250273349428,-0.564767189308343,-9.06501464028957E-5));
#38927=DIRECTION('ref_axis',(0.564709033703531,0.825162970323003,0.0144837723450398));
#38928=DIRECTION('center_axis',(-0.205999301987628,0.978552132725322,-0.000105448247257059));
#38929=DIRECTION('ref_axis',(0.978478801225208,0.205985181525983,0.0122204969042825));
#38930=DIRECTION('center_axis',(5.15167520928809E-67,-1.18789542670764E-48,
-1.));
#38931=DIRECTION('ref_axis',(0.,1.,0.));
#38932=DIRECTION('center_axis',(0.867017425139937,-0.498277810349071,-9.06501464136658E-5));
#38933=DIRECTION('ref_axis',(0.498226683735389,0.866925828403975,0.0144837723027363));
#38934=DIRECTION('center_axis',(-0.282140590344626,0.959373064120863,-0.000105448247277017));
#38935=DIRECTION('ref_axis',(0.959301066555094,0.282120759888223,0.0122204969764503));
#38936=DIRECTION('center_axis',(5.15167520928809E-67,-1.18789542670764E-48,
-1.));
#38937=DIRECTION('ref_axis',(0.,1.,0.));
#38938=DIRECTION('center_axis',(0.90343912619187,-0.42871638299489,-9.06501464260602E-5));
#38939=DIRECTION('ref_axis',(0.428672600584421,0.903343800469878,0.0144837723272369));
#38940=DIRECTION('center_axis',(-0.356542388139781,0.934279141552593,-0.000105448246761887));
#38941=DIRECTION('ref_axis',(0.934208921809314,0.35651696994953,0.012220497120973));
#38942=DIRECTION('center_axis',(5.15167520928809E-67,-1.18789542670764E-48,
-1.));
#38943=DIRECTION('ref_axis',(0.,1.,0.));
#38944=DIRECTION('center_axis',(0.934290824606888,-0.35651177657678,-9.06501464134324E-5));
#38945=DIRECTION('ref_axis',(0.356475608302711,0.934192357613664,0.0144837723482609));
#38946=DIRECTION('center_axis',(-0.428745983551679,0.903425077396555,-0.000105448247222545));
#38947=DIRECTION('ref_axis',(0.903357068407448,0.428715134340562,0.0122204969479439));
#38948=DIRECTION('center_axis',(5.15167520928809E-67,-1.18789542670764E-48,
-1.));
#38949=DIRECTION('ref_axis',(0.,1.,0.));
#38950=DIRECTION('center_axis',(0.959382309405034,-0.282109156503675,-9.06501462956451E-5));
#38951=DIRECTION('ref_axis',(0.282080825355574,0.959281308222623,0.0144837723473633));
#38952=DIRECTION('center_axis',(-0.498306217401744,0.867001097219279,-0.000105448247347347));
#38953=DIRECTION('ref_axis',(0.866935718280794,0.498270127364887,0.0122204969106369));
#38954=DIRECTION('center_axis',(5.15167520928809E-67,-1.18789542670764E-48,
-1.));
#38955=DIRECTION('ref_axis',(0.,1.,0.));
#38956=DIRECTION('center_axis',(0.978558883238587,-0.205967239670296,-9.06501464061553E-5));
#38957=DIRECTION('ref_axis',(0.205946920319019,0.978455970572407,0.0144837723787919));
#38958=DIRECTION('center_axis',(-0.564794227717559,0.825231766970706,-0.000105448247271081));
#38959=DIRECTION('ref_axis',(0.825169421165301,0.564753119361831,0.0122204969131223));
#38960=DIRECTION('center_axis',(5.15167520928809E-67,-1.18789542670764E-48,
-1.));
#38961=DIRECTION('ref_axis',(0.,1.,0.));
#38962=DIRECTION('center_axis',(0.99170231615319,-0.128555466312983,-9.06501463191467E-5));
#38963=DIRECTION('ref_axis',(0.128543284034309,0.991598126495285,0.014483772323378));
#38964=DIRECTION('center_axis',(-0.627800093806562,0.778374608461208,-0.000105448247350595));
#38965=DIRECTION('ref_axis',(0.778315680171392,0.627754220578551,0.0122204969276863));
#38966=DIRECTION('center_axis',(5.15167520928809E-67,-1.18789542670764E-48,
-1.));
#38967=DIRECTION('ref_axis',(0.,1.,0.));
#38968=DIRECTION('center_axis',(0.998731574514188,-0.0503511057570843,-9.06501463742907E-5));
#38969=DIRECTION('ref_axis',(0.0503471356586318,0.998626750227146,0.0144837723587898));
#38970=DIRECTION('center_axis',(-0.686935363552425,0.726718511654798,-0.000105448247333776));
#38971=DIRECTION('ref_axis',(0.726663364192883,0.686885008275621,0.0122204969654078));
#38972=DIRECTION('center_axis',(5.15167520928809E-67,-1.18789542670764E-48,
-1.));
#38973=DIRECTION('ref_axis',(0.,1.,0.));
#38974=DIRECTION('center_axis',(0.999603320606373,0.0281636861093081,-9.0650146390368E-5));
#38975=DIRECTION('ref_axis',(0.0281594195505035,-0.99949850796739,-0.0144837723518616));
#38976=DIRECTION('center_axis',(-0.741835448352795,0.670581953565614,-0.000105448247334273));
#38977=DIRECTION('ref_axis',(0.670530926935027,0.741780921485189,0.0122204968899333));
#38978=DIRECTION('center_axis',(5.15167520928809E-67,-1.18789542670764E-48,
-1.));
#38979=DIRECTION('ref_axis',(0.,1.,0.));
#38980=DIRECTION('center_axis',(0.994312179825183,0.106504839485559,-9.06501463756277E-5));
#38981=DIRECTION('ref_axis',(0.106492362574294,-0.994208025039266,-0.0144837723286163));
#38982=DIRECTION('center_axis',(-0.792161870920044,0.610311034752874,-0.00010544824088436));
#38983=DIRECTION('ref_axis',(0.610264443527485,0.792103508609612,0.0122204997619462));
#38984=DIRECTION('center_axis',(5.15167520928809E-67,-1.18789542670764E-48,
-1.));
#38985=DIRECTION('ref_axis',(0.,1.,0.));
#38986=DIRECTION('center_axis',(0.982890773813025,0.184189355109853,-9.06501463812825E-5));
#38987=DIRECTION('ref_axis',(0.184168744770323,-0.982787919028214,-0.0144837723648623));
#38988=DIRECTION('center_axis',(-0.837604352149864,0.54627734543936,-0.00010544824728987));
#38989=DIRECTION('ref_axis',(0.546235476912709,0.837542514274935,0.0122204968788532));
#38990=DIRECTION('center_axis',(5.15167520928809E-67,-1.18789542670764E-48,
-1.));
#38991=DIRECTION('ref_axis',(0.,1.,0.));
#38992=DIRECTION('center_axis',(-0.778374608461274,-0.62780009380648,-0.000105448247267533));
#38993=DIRECTION('ref_axis',(0.627754220578446,-0.77831568017143,-0.0122204969306265));
#38994=DIRECTION('center_axis',(0.128555466313028,0.991702316153185,-9.06501463500336E-5));
#38995=DIRECTION('ref_axis',(0.991598126495177,-0.128543284034342,-0.0144837723304925));
#38996=DIRECTION('center_axis',(5.15167520928809E-67,-1.18789542670764E-48,
-1.));
#38997=DIRECTION('ref_axis',(0.,1.,0.));
#38998=DIRECTION('center_axis',(-0.825231766970672,-0.564794227717608,-0.000105448247309068));
#38999=DIRECTION('ref_axis',(0.564753119361638,-0.825169421164907,-0.012220496948613));
#39000=DIRECTION('center_axis',(0.205967239670274,0.978558883238591,-9.0650146374353E-5));
#39001=DIRECTION('ref_axis',(0.978455970572943,-0.205946920319105,-0.0144837723413512));
#39002=DIRECTION('center_axis',(5.15167520928809E-67,-1.18789542670764E-48,
-1.));
#39003=DIRECTION('ref_axis',(0.,1.,0.));
#39004=DIRECTION('center_axis',(-0.86700109721932,-0.498306217401672,-0.00010544824729092));
#39005=DIRECTION('ref_axis',(0.498270127364739,-0.8669357182807,-0.0122204969233888));
#39006=DIRECTION('center_axis',(0.282109156504052,0.959382309404923,-9.06501464701313E-5));
#39007=DIRECTION('ref_axis',(0.959281308222407,-0.282080825355923,-0.0144837723548786));
#39008=DIRECTION('center_axis',(5.15167520928809E-67,-1.18789542670764E-48,
-1.));
#39009=DIRECTION('ref_axis',(0.,1.,0.));
#39010=DIRECTION('center_axis',(-0.903425077396529,-0.428745983551733,-0.000105448247249315));
#39011=DIRECTION('ref_axis',(0.428715134340504,-0.903357068407182,-0.0122204969696425));
#39012=DIRECTION('center_axis',(0.356511776576785,0.934290824606886,-9.06501464239672E-5));
#39013=DIRECTION('ref_axis',(0.934192357613866,-0.356475608302793,-0.0144837723332318));
#39014=DIRECTION('center_axis',(5.15167520928809E-67,-1.18789542670764E-48,
-1.));
#39015=DIRECTION('ref_axis',(0.,1.,0.));
#39016=DIRECTION('center_axis',(-0.934279141552621,-0.356542388139705,-0.000105448246733279));
#39017=DIRECTION('ref_axis',(0.356516969949183,-0.934208921808614,-0.0122204971846563));
#39018=DIRECTION('center_axis',(0.428716382994808,0.903439126191909,-9.06501463770139E-5));
#39019=DIRECTION('ref_axis',(0.903343800469329,-0.428672600584064,-0.0144837723720362));
#39020=DIRECTION('center_axis',(5.15167520928809E-67,-1.18789542670764E-48,
-1.));
#39021=DIRECTION('ref_axis',(0.,1.,0.));
#39022=DIRECTION('center_axis',(-0.959373064120865,-0.282140590344618,-0.000105448247270857));
#39023=DIRECTION('ref_axis',(0.282120759888191,-0.959301066555013,-0.0122204969835453));
#39024=DIRECTION('center_axis',(0.498277810349034,0.867017425139958,-9.06501463569771E-5));
#39025=DIRECTION('ref_axis',(0.866925828403698,-0.498226683735182,-0.0144837723264648));
#39026=DIRECTION('center_axis',(5.15167520928809E-67,-1.18789542670764E-48,
-1.));
#39027=DIRECTION('ref_axis',(0.,1.,0.));
#39028=DIRECTION('center_axis',(-0.978552132725285,-0.205999301987804,-0.000105448247338301));
#39029=DIRECTION('ref_axis',(0.205985181526041,-0.978478801224581,-0.0122204969535068));
#39030=DIRECTION('center_axis',(0.564767189308271,0.825250273349477,-9.06501463565956E-5));
#39031=DIRECTION('ref_axis',(0.825162970322881,-0.564709033703342,-0.0144837723594094));
#39032=DIRECTION('center_axis',(5.15167520928809E-67,-1.18789542670764E-48,
-1.));
#39033=DIRECTION('ref_axis',(0.,1.,0.));
#39034=DIRECTION('center_axis',(-0.991698102030424,-0.128587959428258,-0.000105448245434831));
#39035=DIRECTION('ref_axis',(0.128579636017166,-0.991623888697594,-0.0122204977785004));
#39036=DIRECTION('center_axis',(0.627774590741263,0.778395179200251,-9.06501463298504E-5));
#39037=DIRECTION('ref_axis',(0.778312708136619,-0.627709764694687,-0.0144837722981268));
#39038=DIRECTION('center_axis',(5.15167520928809E-67,-1.18789542670764E-48,
-1.));
#39039=DIRECTION('ref_axis',(0.,1.,0.));
#39040=DIRECTION('center_axis',(-0.998729922762387,-0.0503838293473624,
-0.000105448247373321));
#39041=DIRECTION('ref_axis',(0.0503813543060242,-0.998655285167869,-0.0122204969036645));
#39042=DIRECTION('center_axis',(0.686911553066443,0.726741019928282,-9.06501464895761E-5));
#39043=DIRECTION('ref_axis',(0.726663889287984,-0.686840456251464,-0.0144837723380814));
#39044=DIRECTION('center_axis',(5.15167520928809E-67,-1.18789542670764E-48,
-1.));
#39045=DIRECTION('ref_axis',(0.,1.,0.));
#39046=DIRECTION('center_axis',(-0.999604241409666,0.0281309338002504,-0.00010544824728445));
#39047=DIRECTION('ref_axis',(0.0281275452136831,0.999529639708247,0.0122204969192793));
#39048=DIRECTION('center_axis',(0.741813477245179,0.670606260603021,-9.06501463486941E-5));
#39049=DIRECTION('ref_axis',(0.670534945922386,-0.741736547997471,-0.0144837723559454));
#39050=DIRECTION('center_axis',(5.15167520928809E-67,-1.18789542670764E-48,
-1.));
#39051=DIRECTION('ref_axis',(0.,1.,0.));
#39052=DIRECTION('center_axis',(-0.994315667506492,0.106472260386385,-0.000105448247246095));
#39053=DIRECTION('ref_axis',(0.106463029063669,0.99424156164268,0.0122204969176238));
#39054=DIRECTION('center_axis',(0.792141874658893,0.610336990681743,-9.06501463537118E-5));
#39055=DIRECTION('ref_axis',(0.610271931639807,-0.792059587273192,-0.0144837723414781));
#39056=DIRECTION('center_axis',(5.15167520928809E-67,-1.18789542670764E-48,
-1.));
#39057=DIRECTION('ref_axis',(0.,1.,0.));
#39058=DIRECTION('center_axis',(-0.98289680686965,0.184157150081429,-0.000105448247288298));
#39059=DIRECTION('ref_axis',(0.184142132936832,0.982823653731204,0.0122204968770007));
#39060=DIRECTION('center_axis',(0.837586454001503,0.546304790255165,-9.06501464022278E-5));
#39061=DIRECTION('ref_axis',(0.546246387962582,-0.837499315807004,-0.0144837723204838));
#39062=DIRECTION('center_axis',(5.15167520928809E-67,-1.18789542670764E-48,
-1.));
#39063=DIRECTION('ref_axis',(0.,1.,0.));
#39064=DIRECTION('center_axis',(-0.965418060567323,0.260706649725506,-0.000105448239021929));
#39065=DIRECTION('ref_axis',(0.260685939332638,0.965346311123758,0.0122205005631217));
#39066=DIRECTION('center_axis',(0.877867034329392,0.478904439131931,-9.06501464072983E-5));
#39067=DIRECTION('ref_axis',(0.478853053658107,-0.87777558256187,-0.0144837723150808));
#39068=DIRECTION('center_axis',(5.15167520928809E-67,-1.18789542670764E-48,
-1.));
#39069=DIRECTION('ref_axis',(0.,1.,0.));
#39070=DIRECTION('center_axis',(-0.94198719089703,0.335648806145038,-0.000105448247300868));
#39071=DIRECTION('ref_axis',(0.335622530213848,0.941917287592769,0.0122204969921728));
#39072=DIRECTION('center_axis',(0.912735272470196,0.40855148288962,-9.06501464040206E-5));
#39073=DIRECTION('ref_axis',(0.408507431043198,-0.912640070960478,-0.01448377228974));
#39074=DIRECTION('center_axis',(5.15167520928809E-67,-1.18789542670764E-48,
-1.));
#39075=DIRECTION('ref_axis',(0.,1.,0.));
#39076=DIRECTION('center_axis',(0.965409519335958,0.260738282110751,-9.06501464007405E-5));
#39077=DIRECTION('ref_axis',(0.260709665412327,-0.965308598685698,-0.0144837724383535));
#39078=DIRECTION('center_axis',(-0.87788272400828,0.478875674646843,-0.000105448247307507));
#39079=DIRECTION('ref_axis',(0.478838786930294,0.877817791791527,0.0122204969363654));
#39080=DIRECTION('center_axis',(5.15167520928809E-67,-1.18789542670764E-48,
-1.));
#39081=DIRECTION('ref_axis',(-4.33680868994202E-19,1.,-1.18789542670764E-48));
#39082=DIRECTION('center_axis',(5.15167520928809E-67,-1.18789542670764E-48,
-1.));
#39083=DIRECTION('ref_axis',(-4.33680868994202E-19,1.,-1.18789542670764E-48));
#39084=DIRECTION('center_axis',(5.15167520928809E-67,-1.18789542670764E-48,
-1.));
#39085=DIRECTION('ref_axis',(0.,1.,0.));
#39086=DIRECTION('center_axis',(0.941987190897879,0.335648806142656,0.000105448247691596));
#39087=DIRECTION('ref_axis',(0.335622530211987,-0.941917287595053,0.0122204968672344));
#39088=DIRECTION('center_axis',(-0.912735272471169,0.408551482887447,9.06501467246596E-5));
#39089=DIRECTION('ref_axis',(0.408507431040732,0.912640070960819,-0.0144837723377799));
#39090=DIRECTION('center_axis',(5.15167520928809E-67,-1.18789542670764E-48,
-1.));
#39091=DIRECTION('ref_axis',(-4.33680868994202E-19,1.,-1.18789542670764E-48));
#39092=DIRECTION('center_axis',(5.15167520928809E-67,-1.18789542670764E-48,
-1.));
#39093=DIRECTION('ref_axis',(-4.33680868994202E-19,1.,-1.18789542670764E-48));
#39094=DIRECTION('',(-5.15167520928809E-67,1.18789542670764E-48,1.));
#39095=DIRECTION('',(5.15167520928809E-67,-1.18789542670764E-48,-1.));
#39096=DIRECTION('center_axis',(5.15167520928809E-67,-1.18789542670764E-48,
-1.));
#39097=DIRECTION('ref_axis',(-4.33680868994202E-19,1.,-1.18789542670764E-48));
#39098=DIRECTION('center_axis',(5.15167520928809E-67,-1.18789542670764E-48,
-1.));
#39099=DIRECTION('ref_axis',(0.,1.,0.));
#39100=DIRECTION('center_axis',(0.941976194140935,0.33567967089818,-9.06501463865783E-5));
#39101=DIRECTION('ref_axis',(0.335643224273153,-0.94187782983736,-0.014483772312066));
#39102=DIRECTION('center_axis',(-0.912748656947277,0.408521576078436,-0.000105448246989675));
#39103=DIRECTION('ref_axis',(0.408489896596946,0.91268103071696,0.012220497029356));
#39104=DIRECTION('center_axis',(-5.15167520928809E-67,1.18789542670764E-48,
1.));
#39105=DIRECTION('ref_axis',(4.33680868994202E-19,-1.,1.18789542670764E-48));
#39106=DIRECTION('center_axis',(0.,0.,1.));
#39107=DIRECTION('ref_axis',(1.,4.33680868994202E-19,0.));
#39108=DIRECTION('',(0.866025403784438,0.5,0.));
#39109=DIRECTION('',(-4.33680868994202E-19,1.,0.));
#39110=DIRECTION('',(-0.866025403784439,0.499999999999999,0.));
#39111=DIRECTION('',(-0.866025403784439,-0.5,0.));
#39112=DIRECTION('',(6.01359520363859E-16,-1.,0.));
#39113=DIRECTION('',(0.866025403784439,-0.5,0.));
#39114=DIRECTION('center_axis',(1.,4.33680868994202E-19,0.));
#39115=DIRECTION('ref_axis',(0.,0.,-1.));
#39116=DIRECTION('',(0.,0.,1.));
#39117=DIRECTION('',(0.,0.,1.));
#39118=DIRECTION('center_axis',(0.499999999999999,0.866025403784439,0.));
#39119=DIRECTION('ref_axis',(-0.866025403784439,0.499999999999999,0.));
#39120=DIRECTION('',(0.,0.,1.));
#39121=DIRECTION('center_axis',(-0.5,0.866025403784439,0.));
#39122=DIRECTION('ref_axis',(-0.866025403784439,-0.5,0.));
#39123=DIRECTION('',(0.,0.,1.));
#39124=DIRECTION('center_axis',(-1.,-6.01359520363859E-16,0.));
#39125=DIRECTION('ref_axis',(6.01359520363859E-16,-1.,0.));
#39126=DIRECTION('',(0.,0.,1.));
#39127=DIRECTION('center_axis',(-0.5,-0.866025403784439,0.));
#39128=DIRECTION('ref_axis',(0.866025403784439,-0.5,0.));
#39129=DIRECTION('',(0.,0.,1.));
#39130=DIRECTION('center_axis',(0.5,-0.866025403784439,0.));
#39131=DIRECTION('ref_axis',(0.866025403784439,0.5,0.));
#39132=DIRECTION('',(1.0568194522281E-16,0.866025403784468,-0.499999999999949));
#39133=DIRECTION('center_axis',(4.70261923768679E-35,-1.08435016942139E-16,
1.));
#39134=DIRECTION('ref_axis',(0.378466979033695,0.925614793410903,1.00369055805406E-16));
#39135=DIRECTION('center_axis',(0.912653256146669,-0.408734674385332,0.));
#39136=DIRECTION('ref_axis',(0.408734674385332,0.912653256146669,0.));
#39137=DIRECTION('',(0.,0.,1.));
#39138=DIRECTION('center_axis',(0.,0.,1.));
#39139=DIRECTION('ref_axis',(1.,4.33680868994202E-19,0.));
#39140=DIRECTION('',(0.,0.,1.));
#39141=DIRECTION('center_axis',(-0.912653256146668,-0.408734674385334,0.));
#39142=DIRECTION('ref_axis',(0.408734674385334,-0.912653256146668,0.));
#39143=DIRECTION('center_axis',(0.877770897795706,-0.479080630982844,8.35636401295593E-50));
#39144=DIRECTION('ref_axis',(0.479080630982844,0.877770897795706,2.97282767021015E-66));
#39145=DIRECTION('',(-9.32012009987243E-50,3.66188516048321E-51,1.));
#39146=DIRECTION('center_axis',(-9.32012009987243E-50,3.66188516048321E-51,
1.));
#39147=DIRECTION('ref_axis',(1.,4.33680868994202E-19,9.32012009987243E-50));
#39148=DIRECTION('',(-9.32012009987243E-50,3.66188516048321E-51,1.));
#39149=DIRECTION('center_axis',(-0.941908803685482,-0.335868732602165,-8.65571190069724E-50));
#39150=DIRECTION('ref_axis',(0.335868732602165,-0.941908803685482,-2.86613947502886E-66));
#39151=DIRECTION('center_axis',(0.941908803685478,-0.335868732602176,-8.65571190069562E-50));
#39152=DIRECTION('ref_axis',(0.335868732602176,0.941908803685478,5.69318196416785E-66));
#39153=DIRECTION('',(9.32012009987071E-50,3.66188516048189E-51,1.));
#39154=DIRECTION('center_axis',(9.32012009987071E-50,3.66188516048189E-51,
1.));
#39155=DIRECTION('ref_axis',(1.,4.33680868994202E-19,-9.32012009987071E-50));
#39156=DIRECTION('',(9.32012009987071E-50,3.66188516048189E-51,1.));
#39157=DIRECTION('center_axis',(-0.877770897795712,-0.479080630982834,8.35636401295441E-50));
#39158=DIRECTION('ref_axis',(0.479080630982834,-0.877770897795712,-1.78392693329902E-66));
#39159=DIRECTION('center_axis',(0.965357170233111,-0.260932048394827,-1.75574063469501E-49));
#39160=DIRECTION('ref_axis',(0.260932048394827,0.965357170233111,-8.03239509524584E-66));
#39161=DIRECTION('',(1.85827785600731E-49,1.46249639022155E-50,1.));
#39162=DIRECTION('center_axis',(1.8582778560073E-49,1.46249639022155E-50,
1.));
#39163=DIRECTION('ref_axis',(1.,4.33680868994202E-19,-1.8582778560073E-49));
#39164=DIRECTION('',(1.85827785600731E-49,1.46249639022155E-50,1.));
#39165=DIRECTION('center_axis',(-0.837476789971396,-0.546472896179862,1.63618603752562E-49));
#39166=DIRECTION('ref_axis',(0.546472896179862,-0.837476789971396,1.23627039651628E-65));
#39167=DIRECTION('center_axis',(0.982853788812423,-0.184386631340412,-2.66502014323869E-49));
#39168=DIRECTION('ref_axis',(0.184386631340412,0.982853788812423,-4.59929189808117E-66));
#39169=DIRECTION('',(2.77308680110516E-49,3.28216451991643E-50,1.));
#39170=DIRECTION('center_axis',(2.77308680110516E-49,3.28216451991643E-50,
1.));
#39171=DIRECTION('ref_axis',(1.,4.33680868994202E-19,-2.77308680110516E-49));
#39172=DIRECTION('',(2.77308680110516E-49,3.28216451991643E-50,1.));
#39173=DIRECTION('center_axis',(-0.792019359247614,-0.610495974251263,2.39671325397326E-49));
#39174=DIRECTION('ref_axis',(0.610495974251263,-0.792019359247614,-2.26955332198497E-65));
#39175=DIRECTION('center_axis',(0.994290786951656,-0.106704409389008,-3.5878037051643E-49));
#39176=DIRECTION('ref_axis',(0.106704409389008,0.994290786951656,1.37166247450949E-66));
#39177=DIRECTION('',(3.67079874392927E-49,5.81397404601223E-50,1.));
#39178=DIRECTION('center_axis',(3.67079874392927E-49,5.81397404601223E-50,
1.));
#39179=DIRECTION('ref_axis',(1.,4.33680868994202E-19,-3.67079874392927E-49));
#39180=DIRECTION('',(3.67079874392927E-49,5.81397404601223E-50,1.));
#39181=DIRECTION('center_axis',(-0.741678865800908,-0.670755141630892,3.11252914744798E-49));
#39182=DIRECTION('ref_axis',(0.670755141630892,-0.741678865800908,-3.59898235302298E-65));
#39183=DIRECTION('center_axis',(0.999597651754094,-0.028364319270904,-4.5184020529559E-49));
#39184=DIRECTION('ref_axis',(0.028364319270904,0.999597651754094,-3.26521667006146E-66));
#39185=DIRECTION('',(4.54587899183259E-49,9.04231552086841E-50,1.));
#39186=DIRECTION('center_axis',(4.54587899183259E-49,9.04231552086841E-50,
1.));
#39187=DIRECTION('ref_axis',(1.,4.33680868994202E-19,-4.54587899183259E-49));
#39188=DIRECTION('',(4.54587899183259E-49,9.04231552086841E-50,1.));
#39189=DIRECTION('center_axis',(-0.68676567551329,-0.726878880513649,3.77922047493358E-49));
#39190=DIRECTION('ref_axis',(0.726878880513649,-0.68676567551329,8.44347396578498E-67));
#39191=DIRECTION('center_axis',(0.998741664633518,0.0501506463075991,-5.45107773834402E-49));
#39192=DIRECTION('ref_axis',(-0.0501506463075991,0.998741664633518,-5.68155672720376E-65));
#39193=DIRECTION('center_axis',(-0.62761834646337,-0.778521169386283,4.39267686269876E-49));
#39194=DIRECTION('ref_axis',(0.778521169386283,-0.62761834646337,2.86838711888421E-65));
#39195=DIRECTION('center_axis',(0.991728103035171,0.128356416474834,-6.38008050558209E-49));
#39196=DIRECTION('ref_axis',(-0.128356416474834,0.991728103035171,2.64164793875071E-66));
#39197=DIRECTION('center_axis',(-0.564601541603225,-0.825363616365092,4.94911614811798E-49));
#39198=DIRECTION('ref_axis',(0.825363616365092,-0.564601541603225,-1.21982614064914E-65));
#39199=DIRECTION('center_axis',(0.978600207898554,0.20577082665166,-7.29968274368531E-49));
#39200=DIRECTION('ref_axis',(-0.20577082665166,0.978600207898554,7.99368498149713E-66));
#39201=DIRECTION('center_axis',(-0.498103780490032,-0.867117422187756,5.44510769796179E-49));
#39202=DIRECTION('ref_axis',(0.867117422187756,-0.498103780490032,-1.67935322369464E-65));
#39203=DIRECTION('center_axis',(0.95943891706265,0.281916591256437,-8.20421479905702E-49));
#39204=DIRECTION('ref_axis',(-0.281916591256437,0.95943891706265,1.24589067679861E-65));
#39205=DIRECTION('center_axis',(-0.428535043933802,-0.903525160756829,5.87759355939149E-49));
#39206=DIRECTION('ref_axis',(0.903525160756829,-0.428535043933802,-8.86364012879408E-65));
#39207=DIRECTION('center_axis',(0.93436236625724,0.356324246329338,-9.08809993078841E-49));
#39208=DIRECTION('ref_axis',(-0.356324246329338,0.93436236625724,-2.69950222050985E-65));
#39209=DIRECTION('center_axis',(-0.356324246329358,-0.934362366257233,6.24390731325522E-49));
#39210=DIRECTION('ref_axis',(0.934362366257233,-0.356324246329358,4.50754916861586E-65));
#39211=DIRECTION('center_axis',(0.903525160756839,0.428535043933782,-9.94588869312071E-49));
#39212=DIRECTION('ref_axis',(-0.428535043933782,0.903525160756839,-3.06876799885187E-65));
#39213=DIRECTION('center_axis',(-0.281916591256458,-0.959438917062644,6.54179051344872E-49));
#39214=DIRECTION('ref_axis',(0.959438917062644,-0.281916591256458,5.46345068117847E-65));
#39215=DIRECTION('center_axis',(0.867117422187767,0.498103780490012,-1.07722925330905E-48));
#39216=DIRECTION('ref_axis',(-0.498103780490012,0.867117422187767,2.63677046246647E-65));
#39217=DIRECTION('center_axis',(-0.205770826651682,-0.978600207898549,6.76940661098659E-49));
#39218=DIRECTION('ref_axis',(0.978600207898549,-0.205770826651682,1.20007194121145E-65));
#39219=DIRECTION('center_axis',(0.825363616365104,0.564601541603207,-1.15622163962171E-48));
#39220=DIRECTION('ref_axis',(-0.564601541603207,0.825363616365104,5.34857418276646E-65));
#39221=DIRECTION('center_axis',(-0.128356416474855,-0.991728103035168,6.92535227693746E-49));
#39222=DIRECTION('ref_axis',(0.991728103035168,-0.128356416474855,1.05782428992148E-64));
#39223=DIRECTION('center_axis',(0.778521169386297,0.627618346463353,-1.2310790139208E-48));
#39224=DIRECTION('ref_axis',(-0.627618346463353,0.778521169386297,-3.24299836420865E-65));
#39225=DIRECTION('center_axis',(-0.0501506463076206,-0.998741664633517,
7.00866605441356E-49));
#39226=DIRECTION('ref_axis',(0.998741664633517,-0.0501506463076206,5.61717615944791E-66));
#39227=DIRECTION('center_axis',(0.83747678997139,-0.546472896179871,1.63618603752577E-49));
#39228=DIRECTION('ref_axis',(0.546472896179871,0.83747678997139,8.18221406165844E-66));
#39229=DIRECTION('',(-1.85827785600747E-49,1.46249639022181E-50,1.));
#39230=DIRECTION('center_axis',(-1.85827785600747E-49,1.46249639022181E-50,
1.));
#39231=DIRECTION('ref_axis',(1.,4.33680868994202E-19,1.85827785600747E-49));
#39232=DIRECTION('',(-1.85827785600747E-49,1.46249639022181E-50,1.));
#39233=DIRECTION('center_axis',(-0.965357170233114,-0.260932048394816,-1.75574063469517E-49));
#39234=DIRECTION('ref_axis',(0.260932048394816,-0.965357170233114,4.85072620126884E-66));
#39235=DIRECTION('center_axis',(0.792019359247608,-0.610495974251272,2.39671325397339E-49));
#39236=DIRECTION('ref_axis',(0.610495974251272,0.792019359247608,6.86514884131891E-66));
#39237=DIRECTION('',(-2.77308680110532E-49,3.28216451991683E-50,1.));
#39238=DIRECTION('center_axis',(-2.77308680110532E-49,3.28216451991683E-50,
1.));
#39239=DIRECTION('ref_axis',(1.,4.33680868994202E-19,2.77308680110532E-49));
#39240=DIRECTION('',(-2.77308680110532E-49,3.28216451991683E-50,1.));
#39241=DIRECTION('center_axis',(-0.982853788812425,-0.184386631340402,-2.66502014323885E-49));
#39242=DIRECTION('ref_axis',(0.184386631340402,-0.982853788812425,5.0100483719309E-66));
#39243=DIRECTION('center_axis',(0.741678865800901,-0.6707551416309,3.11252914744811E-49));
#39244=DIRECTION('ref_axis',(0.6707551416309,0.741678865800901,2.48321099822104E-65));
#39245=DIRECTION('',(-3.67079874392942E-49,5.81397404601274E-50,1.));
#39246=DIRECTION('center_axis',(-3.67079874392942E-49,5.81397404601274E-50,
1.));
#39247=DIRECTION('ref_axis',(1.,4.33680868994202E-19,3.67079874392942E-49));
#39248=DIRECTION('',(-3.67079874392942E-49,5.81397404601274E-50,1.));
#39249=DIRECTION('center_axis',(-0.994290786951657,-0.106704409388997,-3.58780370516446E-49));
#39250=DIRECTION('ref_axis',(0.106704409388997,-0.994290786951657,8.97464790050996E-66));
#39251=DIRECTION('center_axis',(0.686765675513281,-0.726878880513656,3.77922047493371E-49));
#39252=DIRECTION('ref_axis',(0.726878880513657,0.686765675513281,3.1589153081368E-66));
#39253=DIRECTION('',(-4.54587899183275E-49,9.04231552086907E-50,1.));
#39254=DIRECTION('center_axis',(-4.54587899183275E-49,9.04231552086907E-50,
1.));
#39255=DIRECTION('ref_axis',(1.,4.33680868994202E-19,4.54587899183275E-49));
#39256=DIRECTION('',(-4.54587899183275E-49,9.04231552086907E-50,1.));
#39257=DIRECTION('center_axis',(-0.999597651754094,-0.0283643192708926,
-4.51840205295607E-49));
#39258=DIRECTION('ref_axis',(0.0283643192708926,-0.999597651754094,-3.99287521021606E-67));
#39259=DIRECTION('center_axis',(0.627618346463361,-0.77852116938629,4.39267686269887E-49));
#39260=DIRECTION('ref_axis',(0.77852116938629,0.627618346463361,3.8324092947301E-66));
#39261=DIRECTION('',(-5.39293238409326E-49,1.29472851457609E-49,1.));
#39262=DIRECTION('center_axis',(-5.39293238409326E-49,1.29472851457609E-49,
1.));
#39263=DIRECTION('ref_axis',(-0.453990499739606,-0.891006524188338,-1.29472851457643E-49));
#39264=DIRECTION('',(-5.39293238409326E-49,1.29472851457609E-49,1.));
#39265=DIRECTION('center_axis',(-0.998741664633517,0.0501506463076103,-5.45107773834419E-49));
#39266=DIRECTION('ref_axis',(-0.0501506463076103,-0.998741664633517,1.75141110323522E-67));
#39267=DIRECTION('center_axis',(0.564601541603216,-0.825363616365098,4.94911614811808E-49));
#39268=DIRECTION('ref_axis',(0.825363616365098,0.564601541603216,-2.63676715352381E-65));
#39269=DIRECTION('',(-6.20673655487384E-49,1.75048074844164E-49,1.));
#39270=DIRECTION('center_axis',(-6.20673655487384E-49,1.75048074844164E-49,
1.));
#39271=DIRECTION('ref_axis',(-0.52249856471585,-0.852640164354153,-1.75048074844092E-49));
#39272=DIRECTION('',(-6.20673655487384E-49,1.75048074844164E-49,1.));
#39273=DIRECTION('center_axis',(-0.99172810303517,0.128356416474844,-6.38008050558225E-49));
#39274=DIRECTION('ref_axis',(-0.128356416474844,-0.99172810303517,-6.45104663994926E-66));
#39275=DIRECTION('center_axis',(0.498103780490022,-0.867117422187761,5.44510769796189E-49));
#39276=DIRECTION('ref_axis',(0.867117422187761,0.498103780490022,4.62928424055004E-65));
#39277=DIRECTION('',(-6.98227413084428E-49,2.26867838960881E-49,1.));
#39278=DIRECTION('center_axis',(-6.98227413084428E-49,2.26867838960881E-49,
1.));
#39279=DIRECTION('ref_axis',(-0.587785252292493,-0.809016994374933,-2.26867838960897E-49));
#39280=DIRECTION('',(-6.98227413084428E-49,2.26867838960881E-49,1.));
#39281=DIRECTION('center_axis',(-0.978600207898551,0.205770826651671,-7.29968274368548E-49));
#39282=DIRECTION('ref_axis',(-0.205770826651671,-0.978600207898551,-8.37640359713844E-66));
#39283=DIRECTION('center_axis',(0.428535043933792,-0.903525160756834,5.87759355939158E-49));
#39284=DIRECTION('ref_axis',(0.903525160756834,0.428535043933792,-6.0990810847752E-65));
#39285=DIRECTION('',(-7.71476366495631E-49,2.84612657730158E-49,1.));
#39286=DIRECTION('center_axis',(-7.71476366495631E-49,2.84612657730158E-49,
1.));
#39287=DIRECTION('ref_axis',(-0.649448048330161,-0.76040596560005,-2.84612657730134E-49));
#39288=DIRECTION('',(-7.71476366495631E-49,2.84612657730158E-49,1.));
#39289=DIRECTION('center_axis',(-0.959438917062647,0.281916591256448,-8.20421479905718E-49));
#39290=DIRECTION('ref_axis',(-0.281916591256448,-0.959438917062647,-3.25299225253391E-65));
#39291=DIRECTION('center_axis',(0.356324246329348,-0.934362366257237,6.2439073132553E-49));
#39292=DIRECTION('ref_axis',(0.934362366257237,0.356324246329348,-6.3916346242107E-66));
#39293=DIRECTION('',(-8.39968911565463E-49,3.47926515142182E-49,1.));
#39294=DIRECTION('center_axis',(-8.39968911565463E-49,3.47926515142182E-49,
1.));
#39295=DIRECTION('ref_axis',(-0.707106781186566,-0.707106781186529,-3.47926515142204E-49));
#39296=DIRECTION('',(-8.39968911565463E-49,3.47926515142182E-49,1.));
#39297=DIRECTION('center_axis',(-0.934362366257236,0.356324246329348,-9.08809993078856E-49));
#39298=DIRECTION('ref_axis',(-0.356324246329348,-0.934362366257236,-6.41640199023417E-65));
#39299=DIRECTION('center_axis',(0.281916591256447,-0.959438917062647,6.54179051344879E-49));
#39300=DIRECTION('ref_axis',(0.959438917062647,0.281916591256447,-1.09781434718078E-65));
#39301=DIRECTION('',(-9.03282768977487E-49,4.16419060212015E-49,1.));
#39302=DIRECTION('center_axis',(-9.03282768977487E-49,4.16419060212015E-49,
1.));
#39303=DIRECTION('ref_axis',(-0.760405965599942,-0.649448048330288,-4.16419060211889E-49));
#39304=DIRECTION('',(-9.03282768977487E-49,4.16419060212015E-49,1.));
#39305=DIRECTION('center_axis',(-0.903525160756834,0.428535043933793,-9.94588869312087E-49));
#39306=DIRECTION('ref_axis',(-0.428535043933793,-0.903525160756834,3.14193955482054E-65));
#39307=DIRECTION('center_axis',(0.205770826651671,-0.978600207898551,6.76940661098664E-49));
#39308=DIRECTION('ref_axis',(0.978600207898551,0.205770826651671,1.21103353553181E-65));
#39309=DIRECTION('',(-9.61027587746764E-49,4.89668013623218E-49,1.));
#39310=DIRECTION('center_axis',(-9.61027587746764E-49,4.89668013623218E-49,
1.));
#39311=DIRECTION('ref_axis',(-0.809016994374948,-0.587785252292472,-4.89668013623217E-49));
#39312=DIRECTION('',(-9.61027587746764E-49,4.89668013623218E-49,1.));
#39313=DIRECTION('center_axis',(-0.867117422187761,0.498103780490022,-1.07722925330906E-48));
#39314=DIRECTION('ref_axis',(-0.498103780490022,-0.867117422187761,1.20400755006059E-65));
#39315=DIRECTION('center_axis',(0.128356416474844,-0.99172810303517,6.92535227693751E-49));
#39316=DIRECTION('ref_axis',(0.99172810303517,0.128356416474844,1.37955244398014E-65));
#39317=DIRECTION('',(-1.01284735186348E-48,5.67221771220262E-49,1.));
#39318=DIRECTION('center_axis',(-1.01284735186348E-48,5.67221771220262E-49,
1.));
#39319=DIRECTION('ref_axis',(-0.852640164354111,-0.522498564715917,-5.67221771220297E-49));
#39320=DIRECTION('',(-1.01284735186348E-48,5.67221771220262E-49,1.));
#39321=DIRECTION('center_axis',(-0.825363616365097,0.564601541603216,-1.15622163962172E-48));
#39322=DIRECTION('ref_axis',(-0.564601541603216,-0.825363616365097,3.75089637720347E-65));
#39323=DIRECTION('center_axis',(0.0501506463076098,-0.998741664633517,7.0086660544136E-49));
#39324=DIRECTION('ref_axis',(0.998741664633517,0.0501506463076098,-1.39822384050416E-65));
#39325=DIRECTION('',(-1.05842257525004E-48,6.4860218829832E-49,1.));
#39326=DIRECTION('center_axis',(-1.05842257525004E-48,6.4860218829832E-49,
1.));
#39327=DIRECTION('ref_axis',(-0.891006524188326,-0.453990499739629,-6.48602188298224E-49));
#39328=DIRECTION('',(-1.05842257525004E-48,6.4860218829832E-49,1.));
#39329=DIRECTION('center_axis',(-0.77852116938629,0.627618346463361,-1.23107901392082E-48));
#39330=DIRECTION('ref_axis',(-0.627618346463361,-0.77852116938629,-1.0235164758246E-65));
#39331=DIRECTION('center_axis',(-0.0283643192708931,-0.999597651754094,
7.01883428627214E-49));
#39332=DIRECTION('ref_axis',(0.999597651754094,-0.0283643192708931,-4.40612052675408E-66));
#39333=DIRECTION('',(-1.09747227149895E-48,7.33307527524372E-49,1.));
#39334=DIRECTION('center_axis',(-1.09747227149895E-48,7.33307527524372E-49,
1.));
#39335=DIRECTION('ref_axis',(-0.923879532511259,-0.382683432365157,-7.33307527524286E-49));
#39336=DIRECTION('',(-1.09747227149895E-48,7.33307527524372E-49,1.));
#39337=DIRECTION('center_axis',(-0.726878880513656,0.686765675513282,-1.30133985560119E-48));
#39338=DIRECTION('ref_axis',(-0.686765675513282,-0.726878880513656,-1.0460740182702E-64));
#39339=DIRECTION('center_axis',(-0.106704409388998,-0.994290786951657,6.95579428198243E-49));
#39340=DIRECTION('ref_axis',(0.994290786951657,-0.106704409388998,-7.09717408543387E-66));
#39341=DIRECTION('',(-1.12975568624752E-48,8.20815552314704E-49,1.));
#39342=DIRECTION('center_axis',(-1.12975568624752E-48,8.20815552314704E-49,
1.));
#39343=DIRECTION('ref_axis',(-0.951056516295187,-0.309016994374844,-8.20815552314827E-49));
#39344=DIRECTION('',(-1.12975568624752E-48,8.20815552314704E-49,1.));
#39345=DIRECTION('center_axis',(-0.6707551416309,0.741678865800901,-1.36657098320978E-48));
#39346=DIRECTION('ref_axis',(-0.741678865800901,-0.6707551416309,3.57211103088032E-65));
#39347=DIRECTION('center_axis',(-0.184386631340402,-0.982853788812425,6.81993470413386E-49));
#39348=DIRECTION('ref_axis',(0.982853788812425,-0.184386631340402,2.71684956354986E-65));
#39349=DIRECTION('',(-1.15507378150848E-48,9.10586746597114E-49,1.));
#39350=DIRECTION('center_axis',(-1.15507378150848E-48,9.10586746597114E-49,
1.));
#39351=DIRECTION('ref_axis',(-0.972369920397692,-0.233445363855843,-9.1058674659719E-49));
#39352=DIRECTION('',(-1.15507378150848E-48,9.10586746597114E-49,1.));
#39353=DIRECTION('center_axis',(-0.610495974251271,0.792019359247608,-1.42637022515333E-48));
#39354=DIRECTION('ref_axis',(-0.792019359247608,-0.610495974251271,3.09249712984754E-64));
#39355=DIRECTION('center_axis',(-0.260932048394816,-0.965357170233114,6.61209317220174E-49));
#39356=DIRECTION('ref_axis',(0.965357170233114,-0.260932048394816,1.42679734120621E-65));
#39357=DIRECTION('',(-1.17327046280543E-48,1.0020676411069E-48,1.));
#39358=DIRECTION('center_axis',(-1.17327046280543E-48,1.0020676411069E-48,
1.));
#39359=DIRECTION('ref_axis',(-0.987688340595155,-0.156434465040119,-1.00206764110703E-48));
#39360=DIRECTION('',(-1.17327046280543E-48,1.0020676411069E-48,1.));
#39361=DIRECTION('center_axis',(-0.546472896179871,0.83747678997139,-1.48036889921999E-48));
#39362=DIRECTION('ref_axis',(-0.83747678997139,-0.546472896179871,5.98336102584152E-65));
#39363=DIRECTION('center_axis',(-0.335868732602165,-0.941908803685482,6.33355109834478E-49));
#39364=DIRECTION('ref_axis',(0.941908803685482,-0.335868732602165,5.83703495410428E-65));
#39365=DIRECTION('',(-1.18423354154716E-48,1.09469422570892E-48,1.));
#39366=DIRECTION('center_axis',(-1.18423354154716E-48,1.09469422570892E-48,
1.));
#39367=DIRECTION('ref_axis',(-0.996917333733132,-0.0784590957277897,-1.09469422570898E-48));
#39368=DIRECTION('',(-1.18423354154716E-48,1.09469422570892E-48,1.));
#39369=DIRECTION('center_axis',(-0.479080630982844,0.877770897795706,-1.52823408562776E-48));
#39370=DIRECTION('ref_axis',(-0.877770897795706,-0.479080630982844,-1.85065299173653E-65));
#39371=DIRECTION('center_axis',(-0.408734674385335,-0.912653256146667,5.98602578707292E-49));
#39372=DIRECTION('ref_axis',(0.912653256146667,-0.408734674385335,-4.742731066544E-66));
#39373=DIRECTION('',(-1.18789542670764E-48,1.18789542670765E-48,1.));
#39374=DIRECTION('center_axis',(-1.18789542670764E-48,1.18789542670765E-48,
1.));
#39375=DIRECTION('ref_axis',(4.33680868994202E-19,-1.,1.18789542670765E-48));
#39376=DIRECTION('',(-1.18789542670764E-48,1.18789542670765E-48,1.));
#39377=DIRECTION('center_axis',(-0.408734674385331,0.912653256146669,-1.56967067958564E-48));
#39378=DIRECTION('ref_axis',(-0.912653256146669,-0.408734674385331,-1.44539080722799E-64));
#39379=DIRECTION('center_axis',(-0.479080630982847,-0.877770897795704,5.57165984749406E-49));
#39380=DIRECTION('ref_axis',(0.877770897795704,-0.479080630982847,-3.32989513528092E-65));
#39381=DIRECTION('',(-1.18423354154716E-48,1.28109662770637E-48,1.));
#39382=DIRECTION('center_axis',(-1.18423354154716E-48,1.28109662770637E-48,
1.));
#39383=DIRECTION('ref_axis',(4.33680868994202E-19,-1.,1.28109662770637E-48));
#39384=DIRECTION('',(-1.18423354154716E-48,1.28109662770637E-48,1.));
#39385=DIRECTION('center_axis',(-0.335868732602161,0.941908803685483,-1.60442321071283E-48));
#39386=DIRECTION('ref_axis',(-0.941908803685483,-0.335868732602161,-1.10077185323049E-64));
#39387=DIRECTION('center_axis',(-0.546472896179874,-0.837476789971388,5.09300798341636E-49));
#39388=DIRECTION('ref_axis',(0.837476789971388,-0.546472896179874,-4.24396990687181E-65));
#39389=DIRECTION('',(-1.17327046280542E-48,1.37372321230839E-48,1.));
#39390=DIRECTION('center_axis',(-1.17327046280542E-48,1.37372321230839E-48,
1.));
#39391=DIRECTION('ref_axis',(4.33680868994202E-19,-1.,1.37372321230839E-48));
#39392=DIRECTION('',(-1.17327046280542E-48,1.37372321230839E-48,1.));
#39393=DIRECTION('center_axis',(-0.260932048394812,0.965357170233115,-1.63227741809852E-48));
#39394=DIRECTION('ref_axis',(-0.965357170233115,-0.260932048394812,1.79840374663787E-65));
#39395=DIRECTION('center_axis',(-0.610495974251274,-0.792019359247605,4.55302124274975E-49));
#39396=DIRECTION('ref_axis',(0.792019359247605,-0.610495974251274,-1.92107929694605E-65));
#39397=DIRECTION('',(-1.15507378150847E-48,1.46520410681818E-48,1.));
#39398=DIRECTION('center_axis',(-1.15507378150847E-48,1.46520410681818E-48,
1.));
#39399=DIRECTION('ref_axis',(4.33680868994202E-19,-1.,1.46520410681818E-48));
#39400=DIRECTION('',(-1.15507378150847E-48,1.46520410681818E-48,1.));
#39401=DIRECTION('center_axis',(-0.184386631340398,0.982853788812426,-1.65306157129174E-48));
#39402=DIRECTION('ref_axis',(-0.982853788812426,-0.184386631340398,3.00112067034686E-65));
#39403=DIRECTION('center_axis',(-0.670755141630903,-0.741678865800898,3.95502882331426E-49));
#39404=DIRECTION('ref_axis',(0.741678865800898,-0.670755141630903,1.84878394507284E-65));
#39405=DIRECTION('',(-1.12975568624751E-48,1.55497530110059E-48,1.));
#39406=DIRECTION('center_axis',(-1.12975568624751E-48,1.55497530110059E-48,
1.));
#39407=DIRECTION('ref_axis',(4.33680868994202E-19,-1.,1.55497530110059E-48));
#39408=DIRECTION('',(-1.12975568624751E-48,1.55497530110059E-48,1.));
#39409=DIRECTION('center_axis',(-0.106704409388993,0.994290786951657,-1.66664752907659E-48));
#39410=DIRECTION('ref_axis',(-0.994290786951658,-0.106704409388993,-2.84767254643969E-65));
#39411=DIRECTION('center_axis',(-0.726878880513659,-0.686765675513279,3.30271754722836E-49));
#39412=DIRECTION('ref_axis',(0.686765675513279,-0.726878880513659,1.35737227185702E-66));
#39413=DIRECTION('',(-1.09747227149895E-48,1.64248332589092E-48,1.));
#39414=DIRECTION('center_axis',(-1.09747227149895E-48,1.64248332589092E-48,
1.));
#39415=DIRECTION('ref_axis',(4.33680868994202E-19,-1.,1.64248332589092E-48));
#39416=DIRECTION('',(-1.09747227149895E-48,1.64248332589092E-48,1.));
#39417=DIRECTION('center_axis',(-0.0283643192708891,0.999597651754094,-1.67295152950556E-48));
#39418=DIRECTION('ref_axis',(-0.999597651754094,-0.0283643192708891,-1.01926051780483E-65));
#39419=DIRECTION('center_axis',(-0.778521169386292,-0.627618346463358,2.60010913042463E-49));
#39420=DIRECTION('ref_axis',(0.627618346463358,-0.778521169386292,-1.77736454987801E-64));
#39421=DIRECTION('',(-1.05842257525003E-48,1.72718866511697E-48,1.));
#39422=DIRECTION('center_axis',(-1.05842257525003E-48,1.72718866511697E-48,
1.));
#39423=DIRECTION('ref_axis',(-0.891006524188322,0.453990499739636,-1.72718866511707E-48));
#39424=DIRECTION('',(-1.05842257525003E-48,1.72718866511697E-48,1.));
#39425=DIRECTION('center_axis',(0.050150646307614,0.998741664633517,-1.67193470631971E-48));
#39426=DIRECTION('ref_axis',(-0.998741664633517,0.050150646307614,1.52017605534737E-65));
#39427=DIRECTION('center_axis',(-0.8253636163651,-0.564601541603213,1.85153538743368E-49));
#39428=DIRECTION('ref_axis',(0.564601541603213,-0.8253636163651,-7.9609822926636E-66));
#39429=DIRECTION('',(-1.01284735186348E-48,1.80856908219503E-48,1.));
#39430=DIRECTION('center_axis',(-1.01284735186348E-48,1.80856908219503E-48,
1.));
#39431=DIRECTION('ref_axis',(-0.852640164354107,0.522498564715924,-1.808569082195E-48));
#39432=DIRECTION('',(-1.01284735186348E-48,1.80856908219503E-48,1.));
#39433=DIRECTION('center_axis',(0.128356416474848,0.991728103035169,-1.6636033285721E-48));
#39434=DIRECTION('ref_axis',(-0.991728103035169,0.128356416474848,-6.99057875847398E-66));
#39435=DIRECTION('center_axis',(-0.867117422187763,-0.498103780490019,1.06161152430708E-49));
#39436=DIRECTION('ref_axis',(0.498103780490019,-0.867117422187763,1.00088346227585E-65));
#39437=DIRECTION('',(-9.61027587746759E-49,1.88612283979207E-48,1.));
#39438=DIRECTION('center_axis',(-9.61027587746759E-49,1.88612283979207E-48,
1.));
#39439=DIRECTION('ref_axis',(-0.809016994374894,0.587785252292546,-1.88612283979215E-48));
#39440=DIRECTION('',(-9.61027587746759E-49,1.88612283979207E-48,1.));
#39441=DIRECTION('center_axis',(0.205770826651675,0.978600207898551,-1.64800876197701E-48));
#39442=DIRECTION('ref_axis',(-0.978600207898551,0.205770826651675,2.0991990898783E-65));
#39443=DIRECTION('center_axis',(-0.903525160756836,-0.428535043933789,2.35207684337335E-50));
#39444=DIRECTION('ref_axis',(0.428535043933789,-0.903525160756836,-9.18347163738211E-68));
#39445=DIRECTION('',(-9.03282768977482E-49,1.95937179320328E-48,1.));
#39446=DIRECTION('center_axis',(-9.03282768977482E-49,1.95937179320328E-48,
1.));
#39447=DIRECTION('ref_axis',(-0.760405965599999,0.649448048330221,-1.95937179320332E-48));
#39448=DIRECTION('',(-9.03282768977482E-49,1.95937179320328E-48,1.));
#39449=DIRECTION('center_axis',(0.281916591256451,0.959438917062646,-1.62524715222323E-48));
#39450=DIRECTION('ref_axis',(-0.959438917062646,0.281916591256451,8.99283719863503E-66));
#39451=DIRECTION('center_axis',(-0.934362366257238,-0.356324246329344,-6.22581077994971E-50));
#39452=DIRECTION('ref_axis',(0.356324246329344,-0.934362366257238,-2.14283631075808E-67));
#39453=DIRECTION('',(-8.39968911565457E-49,2.02786433827311E-48,1.));
#39454=DIRECTION('center_axis',(-8.39968911565457E-49,2.02786433827311E-48,
1.));
#39455=DIRECTION('ref_axis',(-0.707106781186559,0.707106781186536,-2.02786433827309E-48));
#39456=DIRECTION('',(-8.39968911565457E-49,2.02786433827311E-48,1.));
#39457=DIRECTION('center_axis',(0.356324246329351,0.934362366257235,-1.59545883220388E-48));
#39458=DIRECTION('ref_axis',(-0.934362366257235,0.356324246329351,6.60900149289003E-65));
#39459=DIRECTION('center_axis',(-0.959438917062648,-0.281916591256444,-1.50646620972636E-49));
#39460=DIRECTION('ref_axis',(0.281916591256444,-0.959438917062648,3.84808191287826E-66));
#39461=DIRECTION('',(-7.71476366495624E-49,2.09117819568513E-48,1.));
#39462=DIRECTION('center_axis',(-7.71476366495624E-49,2.09117819568513E-48,
1.));
#39463=DIRECTION('ref_axis',(-0.649448048330135,0.760405965600073,-2.09117819568518E-48));
#39464=DIRECTION('',(-7.71476366495624E-49,2.09117819568513E-48,1.));
#39465=DIRECTION('center_axis',(0.428535043933796,0.903525160756832,-1.5588274568175E-48));
#39466=DIRECTION('ref_axis',(-0.903525160756832,0.428535043933796,-3.10862492143316E-66));
#39467=DIRECTION('center_axis',(-0.978600207898552,-0.205770826651667,-2.41099826509806E-49));
#39468=DIRECTION('ref_axis',(0.205770826651667,-0.978600207898552,1.22158844253494E-66));
#39469=DIRECTION('',(-6.98227413084421E-49,2.14892301445441E-48,1.));
#39470=DIRECTION('center_axis',(-6.98227413084421E-49,2.14892301445441E-48,
1.));
#39471=DIRECTION('ref_axis',(-0.587785252292501,0.809016994374927,-2.14892301445438E-48));
#39472=DIRECTION('',(-6.98227413084421E-49,2.14892301445441E-48,1.));
#39473=DIRECTION('center_axis',(0.498103780490025,0.867117422187759,-1.51557887067454E-48));
#39474=DIRECTION('ref_axis',(-0.867117422187759,0.498103780490025,2.99504754920617E-65));
#39475=DIRECTION('center_axis',(-0.99172810303517,-0.128356416474841,-3.33060050320128E-49));
#39476=DIRECTION('ref_axis',(0.128356416474841,-0.99172810303517,-3.10963647347836E-66));
#39477=DIRECTION('',(-6.20673655487377E-49,2.20074277857113E-48,1.));
#39478=DIRECTION('center_axis',(-6.20673655487377E-49,2.20074277857113E-48,
1.));
#39479=DIRECTION('ref_axis',(-0.522498564715884,0.852640164354132,-2.20074277857117E-48));
#39480=DIRECTION('',(-6.20673655487377E-49,2.20074277857113E-48,1.));
#39481=DIRECTION('center_axis',(0.564601541603219,0.825363616365096,-1.46597971569015E-48));
#39482=DIRECTION('ref_axis',(-0.825363616365096,0.564601541603219,-1.28895308917342E-64));
#39483=DIRECTION('center_axis',(-0.998741664633517,-0.0501506463076061,
-4.25960327043935E-49));
#39484=DIRECTION('ref_axis',(0.0501506463076061,-0.998741664633517,-2.80568036684895E-66));
#39485=DIRECTION('',(-5.39293238409318E-49,2.24631800195768E-48,1.));
#39486=DIRECTION('center_axis',(-5.39293238409318E-49,2.24631800195768E-48,
1.));
#39487=DIRECTION('ref_axis',(-0.453990499739489,0.891006524188397,-2.24631800195771E-48));
#39488=DIRECTION('',(-5.39293238409318E-49,2.24631800195768E-48,1.));
#39489=DIRECTION('center_axis',(0.627618346463364,0.778521169386287,-1.41033578714823E-48));
#39490=DIRECTION('ref_axis',(-0.778521169386288,0.627618346463364,5.07659402759256E-65));
#39491=DIRECTION('center_axis',(-0.999597651754094,0.0283643192708965,-5.19227895582746E-49));
#39492=DIRECTION('ref_axis',(-0.0283643192708965,-0.999597651754094,2.50391620144835E-67));
#39493=DIRECTION('',(-4.54587899183267E-49,2.2853676982066E-48,1.));
#39494=DIRECTION('center_axis',(-4.54587899183267E-49,2.2853676982066E-48,
1.));
#39495=DIRECTION('ref_axis',(-0.382683432365006,0.923879532511321,-2.28536769820664E-48));
#39496=DIRECTION('',(-4.54587899183267E-49,2.2853676982066E-48,1.));
#39497=DIRECTION('center_axis',(0.686765675513284,0.726878880513654,-1.34899014837172E-48));
#39498=DIRECTION('ref_axis',(-0.726878880513654,0.686765675513284,4.51664321804638E-65));
#39499=DIRECTION('center_axis',(-0.994290786951657,0.106704409389001,-6.12287730361908E-49));
#39500=DIRECTION('ref_axis',(-0.106704409389001,-0.994290786951657,-3.36897451344462E-66));
#39501=DIRECTION('',(-3.67079874392934E-49,2.31765111295516E-48,1.));
#39502=DIRECTION('center_axis',(-3.67079874392934E-49,2.31765111295516E-48,
1.));
#39503=DIRECTION('ref_axis',(-0.309016994374936,0.951056516295157,-2.31765111295516E-48));
#39504=DIRECTION('',(-3.67079874392934E-49,2.31765111295516E-48,1.));
#39505=DIRECTION('center_axis',(0.741678865800904,0.670755141630897,-1.28232101562316E-48));
#39506=DIRECTION('ref_axis',(-0.670755141630897,0.741678865800904,-7.13448931820408E-65));
#39507=DIRECTION('center_axis',(-0.982853788812424,0.184386631340406,-7.04566086554469E-49));
#39508=DIRECTION('ref_axis',(-0.184386631340406,-0.982853788812424,1.03257498418151E-65));
#39509=DIRECTION('',(-2.77308680110524E-49,2.34296920821612E-48,1.));
#39510=DIRECTION('center_axis',(-2.77308680110524E-49,2.34296920821612E-48,
1.));
#39511=DIRECTION('ref_axis',(-0.233445363855831,0.972369920397695,-2.34296920821614E-48));
#39512=DIRECTION('',(-2.77308680110524E-49,2.34296920821612E-48,1.));
#39513=DIRECTION('center_axis',(0.79201935924761,0.610495974251268,-1.21073942627568E-48));
#39514=DIRECTION('ref_axis',(-0.610495974251268,0.79201935924761,-4.36775682720849E-65));
#39515=DIRECTION('center_axis',(-0.965357170233113,0.260932048394819,-7.95494037408836E-49));
#39516=DIRECTION('ref_axis',(-0.260932048394819,-0.965357170233113,-3.47978634051958E-65));
#39517=DIRECTION('',(-1.85827785600739E-49,2.36116588951307E-48,1.));
#39518=DIRECTION('center_axis',(-1.85827785600739E-49,2.36116588951307E-48,
1.));
#39519=DIRECTION('ref_axis',(-0.156434465040246,0.987688340595135,-2.36116588951307E-48));
#39520=DIRECTION('',(-1.85827785600739E-49,2.36116588951307E-48,1.));
#39521=DIRECTION('center_axis',(0.837476789971392,0.546472896179868,-1.13468670463092E-48));
#39522=DIRECTION('ref_axis',(-0.546472896179868,0.837476789971392,7.35185048458512E-65));
#39523=DIRECTION('center_axis',(-0.94190880368548,0.335868732602169,-8.84510981871381E-49));
#39524=DIRECTION('ref_axis',(-0.335868732602169,-0.94190880368548,-2.80378683690505E-64));
#39525=DIRECTION('',(-9.32012009987159E-50,2.3721289682548E-48,1.));
#39526=DIRECTION('center_axis',(-9.32012009987159E-50,2.3721289682548E-48,
1.));
#39527=DIRECTION('ref_axis',(-0.0784590957277844,0.996917333733133,-2.3721289682548E-48));
#39528=DIRECTION('',(-9.32012009987159E-50,2.3721289682548E-48,1.));
#39529=DIRECTION('center_axis',(0.877770897795708,0.47908063098284,-1.0546317410079E-48));
#39530=DIRECTION('ref_axis',(-0.47908063098284,0.877770897795708,-1.46432166581228E-64));
#39531=DIRECTION('center_axis',(-0.912653256146669,0.408734674385332,-9.71068100878346E-49));
#39532=DIRECTION('ref_axis',(-0.408734674385332,-0.912653256146669,4.78015562106795E-65));
#39533=DIRECTION('',(-1.03033504185762E-66,2.37579085341529E-48,1.));
#39534=DIRECTION('center_axis',(-1.03033504185762E-66,2.37579085341529E-48,
1.));
#39535=DIRECTION('ref_axis',(-5.51899603821915E-14,1.,-2.37579085341529E-48));
#39536=DIRECTION('',(-1.03033504185762E-66,2.37579085341529E-48,1.));
#39537=DIRECTION('center_axis',(0.912653256146668,0.408734674385334,-9.71068100878352E-49));
#39538=DIRECTION('ref_axis',(-0.408734674385334,0.912653256146668,-3.97320112854764E-64));
#39539=DIRECTION('center_axis',(-0.877770897795703,0.47908063098285,-1.05463174100791E-48));
#39540=DIRECTION('ref_axis',(-0.47908063098285,-0.877770897795703,8.5181126283276E-66));
#39541=DIRECTION('',(9.32012009987329E-50,2.3721289682548E-48,1.));
#39542=DIRECTION('center_axis',(9.32012009987329E-50,2.3721289682548E-48,
1.));
#39543=DIRECTION('ref_axis',(0.078459095727909,0.996917333733123,-2.37212896825479E-48));
#39544=DIRECTION('',(9.32012009987329E-50,2.3721289682548E-48,1.));
#39545=DIRECTION('center_axis',(0.941908803685484,0.335868732602158,-8.84510981871371E-49));
#39546=DIRECTION('ref_axis',(-0.335868732602158,0.941908803685484,-1.44601818635795E-65));
#39547=DIRECTION('center_axis',(-0.837476789971386,0.546472896179877,-1.13468670463093E-48));
#39548=DIRECTION('ref_axis',(-0.546472896179877,-0.837476789971386,1.1507371701338E-64));
#39549=DIRECTION('',(1.85827785600756E-49,2.36116588951307E-48,1.));
#39550=DIRECTION('center_axis',(1.85827785600756E-49,2.36116588951307E-48,
1.));
#39551=DIRECTION('ref_axis',(0.156434465040226,0.987688340595138,-2.36116588951307E-48));
#39552=DIRECTION('',(1.85827785600756E-49,2.36116588951307E-48,1.));
#39553=DIRECTION('center_axis',(0.965357170233116,0.260932048394809,-7.95494037408827E-49));
#39554=DIRECTION('ref_axis',(-0.260932048394809,0.965357170233116,-4.20694512990981E-65));
#39555=DIRECTION('center_axis',(-0.792019359247603,0.610495974251277,-1.21073942627569E-48));
#39556=DIRECTION('ref_axis',(-0.610495974251277,-0.792019359247603,-2.13945998802071E-65));
#39557=DIRECTION('',(2.7730868011054E-49,2.34296920821612E-48,1.));
#39558=DIRECTION('center_axis',(2.7730868011054E-49,2.34296920821612E-48,
1.));
#39559=DIRECTION('ref_axis',(0.233445363855898,0.972369920397678,-2.34296920821612E-48));
#39560=DIRECTION('',(2.7730868011054E-49,2.34296920821612E-48,1.));
#39561=DIRECTION('center_axis',(0.982853788812426,0.184386631340395,-7.04566086554459E-49));
#39562=DIRECTION('ref_axis',(-0.184386631340395,0.982853788812426,-1.76256118611904E-65));
#39563=DIRECTION('center_axis',(-0.741678865800896,0.670755141630906,-1.28232101562316E-48));
#39564=DIRECTION('ref_axis',(-0.670755141630906,-0.741678865800896,1.75561258236883E-65));
#39565=DIRECTION('',(3.6707987439295E-49,2.31765111295516E-48,1.));
#39566=DIRECTION('center_axis',(3.6707987439295E-49,2.31765111295516E-48,
1.));
#39567=DIRECTION('ref_axis',(0.309016994374949,0.951056516295153,-2.31765111295516E-48));
#39568=DIRECTION('',(3.6707987439295E-49,2.31765111295516E-48,1.));
#39569=DIRECTION('center_axis',(0.994290786951658,0.10670440938899,-6.12287730361897E-49));
#39570=DIRECTION('ref_axis',(-0.10670440938899,0.994290786951658,-7.83421067979577E-66));
#39571=DIRECTION('center_axis',(-0.686765675513276,0.726878880513661,-1.34899014837172E-48));
#39572=DIRECTION('ref_axis',(-0.726878880513661,-0.686765675513276,5.3563970103269E-65));
#39573=DIRECTION('',(4.54587899183282E-49,2.28536769820659E-48,1.));
#39574=DIRECTION('center_axis',(4.54587899183282E-49,2.28536769820659E-48,
1.));
#39575=DIRECTION('ref_axis',(0.382683432365024,0.923879532511314,-2.28536769820663E-48));
#39576=DIRECTION('',(4.54587899183282E-49,2.28536769820659E-48,1.));
#39577=DIRECTION('center_axis',(0.999597651754094,0.0283643192708856,-5.19227895582736E-49));
#39578=DIRECTION('ref_axis',(-0.0283643192708856,0.999597651754094,1.94568536261846E-66));
#39579=DIRECTION('center_axis',(-0.627618346463355,0.778521169386295,-1.41033578714824E-48));
#39580=DIRECTION('ref_axis',(-0.778521169386295,-0.627618346463355,-4.32781502974933E-65));
#39581=DIRECTION('',(5.39293238409334E-49,2.24631800195767E-48,1.));
#39582=DIRECTION('center_axis',(5.39293238409334E-49,2.24631800195767E-48,
1.));
#39583=DIRECTION('ref_axis',(0.45399049973962,0.89100652418833,-2.24631800195763E-48));
#39584=DIRECTION('',(5.39293238409334E-49,2.24631800195767E-48,1.));
#39585=DIRECTION('center_axis',(0.998741664633517,-0.0501506463076175,-4.25960327043925E-49));
#39586=DIRECTION('ref_axis',(0.0501506463076175,0.998741664633517,-4.14088422014228E-66));
#39587=DIRECTION('center_axis',(-0.56460154160321,0.825363616365102,-1.46597971569016E-48));
#39588=DIRECTION('ref_axis',(-0.825363616365102,-0.56460154160321,7.97777118454868E-65));
#39589=DIRECTION('',(6.20673655487391E-49,2.20074277857112E-48,1.));
#39590=DIRECTION('center_axis',(6.20673655487391E-49,2.20074277857112E-48,
1.));
#39591=DIRECTION('ref_axis',(0.522498564715976,0.852640164354076,-2.20074277857111E-48));
#39592=DIRECTION('',(6.20673655487391E-49,2.20074277857112E-48,1.));
#39593=DIRECTION('center_axis',(0.991728103035169,-0.128356416474851,-3.33060050320119E-49));
#39594=DIRECTION('ref_axis',(0.128356416474851,0.991728103035169,2.08257490756294E-67));
#39595=DIRECTION('center_axis',(-0.498103780490015,0.867117422187765,-1.51557887067454E-48));
#39596=DIRECTION('ref_axis',(-0.867117422187765,-0.498103780490015,2.18779707200991E-65));
#39597=DIRECTION('',(6.98227413084436E-49,2.1489230144544E-48,1.));
#39598=DIRECTION('center_axis',(6.98227413084435E-49,2.1489230144544E-48,
1.));
#39599=DIRECTION('ref_axis',(0.587785252292489,0.809016994374936,-2.14892301445439E-48));
#39600=DIRECTION('',(6.98227413084436E-49,2.1489230144544E-48,1.));
#39601=DIRECTION('center_axis',(0.97860020789855,-0.205770826651679,-2.41099826509796E-49));
#39602=DIRECTION('ref_axis',(0.205770826651679,0.97860020789855,-2.74077973100627E-66));
#39603=DIRECTION('center_axis',(-0.428535043933785,0.903525160756837,-1.55882745681751E-48));
#39604=DIRECTION('ref_axis',(-0.903525160756837,-0.428535043933785,-8.73188639847288E-65));
#39605=DIRECTION('',(7.71476366495637E-49,2.09117819568512E-48,1.));
#39606=DIRECTION('center_axis',(7.71476366495637E-49,2.09117819568512E-48,
1.));
#39607=DIRECTION('ref_axis',(0.649448048330186,0.760405965600029,-2.09117819568512E-48));
#39608=DIRECTION('',(7.71476366495637E-49,2.09117819568512E-48,1.));
#39609=DIRECTION('center_axis',(0.959438917062645,-0.281916591256455,-1.50646620972626E-49));
#39610=DIRECTION('ref_axis',(0.281916591256455,0.959438917062645,-2.91844467010393E-67));
#39611=DIRECTION('center_axis',(-0.356324246329341,0.934362366257239,-1.59545883220388E-48));
#39612=DIRECTION('ref_axis',(-0.934362366257239,-0.356324246329341,1.49301625507406E-64));
#39613=DIRECTION('',(8.39968911565469E-49,2.0278643382731E-48,1.));
#39614=DIRECTION('center_axis',(8.39968911565469E-49,2.0278643382731E-48,
1.));
#39615=DIRECTION('ref_axis',(0.707106781186573,0.707106781186522,-2.02786433827308E-48));
#39616=DIRECTION('',(8.39968911565469E-49,2.0278643382731E-48,1.));
#39617=DIRECTION('center_axis',(0.934362366257234,-0.356324246329355,-6.22581077994883E-50));
#39618=DIRECTION('ref_axis',(0.356324246329355,0.934362366257234,-4.97582464336991E-66));
#39619=DIRECTION('center_axis',(-0.28191659125644,0.959438917062649,-1.62524715222323E-48));
#39620=DIRECTION('ref_axis',(-0.959438917062649,-0.28191659125644,-5.29515836320384E-66));
#39621=DIRECTION('',(9.03282768977493E-49,1.95937179320326E-48,1.));
#39622=DIRECTION('center_axis',(9.03282768977493E-49,1.95937179320326E-48,
1.));
#39623=DIRECTION('ref_axis',(0.760405965600079,0.649448048330127,-1.9593717932032E-48));
#39624=DIRECTION('',(9.03282768977493E-49,1.95937179320326E-48,1.));
#39625=DIRECTION('center_axis',(0.903525160756831,-0.428535043933799,2.35207684337425E-50));
#39626=DIRECTION('ref_axis',(0.428535043933799,0.903525160756831,3.46790681006673E-67));
#39627=DIRECTION('center_axis',(-0.205770826651664,0.978600207898553,-1.64800876197701E-48));
#39628=DIRECTION('ref_axis',(-0.978600207898553,-0.205770826651664,-5.70930081633759E-65));
#39629=DIRECTION('',(9.61027587746769E-49,1.88612283979206E-48,1.));
#39630=DIRECTION('center_axis',(9.61027587746769E-49,1.88612283979206E-48,
1.));
#39631=DIRECTION('ref_axis',(0.809016994374978,0.587785252292432,-1.88612283979202E-48));
#39632=DIRECTION('',(9.61027587746769E-49,1.88612283979206E-48,1.));
#39633=DIRECTION('center_axis',(0.867117422187757,-0.498103780490029,1.06161152430717E-49));
#39634=DIRECTION('ref_axis',(0.498103780490029,0.867117422187757,8.6756046158998E-66));
#39635=DIRECTION('center_axis',(-0.128356416474837,0.991728103035171,-1.6636033285721E-48));
#39636=DIRECTION('ref_axis',(-0.991728103035171,-0.128356416474837,3.98742758462882E-65));
#39637=DIRECTION('',(1.01284735186348E-48,1.80856908219502E-48,1.));
#39638=DIRECTION('center_axis',(1.01284735186348E-48,1.80856908219502E-48,
1.));
#39639=DIRECTION('ref_axis',(0.852640164354111,0.522498564715918,-1.80856908219499E-48));
#39640=DIRECTION('',(1.01284735186348E-48,1.80856908219502E-48,1.));
#39641=DIRECTION('center_axis',(0.825363616365094,-0.564601541603222,1.85153538743376E-49));
#39642=DIRECTION('ref_axis',(0.564601541603222,0.825363616365094,-1.20460226317478E-65));
#39643=DIRECTION('center_axis',(-0.0501506463076026,0.998741664633518,-1.67193470631971E-48));
#39644=DIRECTION('ref_axis',(-0.998741664633518,-0.0501506463076026,9.17993822873344E-66));
#39645=DIRECTION('',(1.05842257525004E-48,1.72718866511696E-48,1.));
#39646=DIRECTION('center_axis',(1.05842257525004E-48,1.72718866511696E-48,
1.));
#39647=DIRECTION('ref_axis',(0.891006524188331,0.453990499739619,-1.72718866511705E-48));
#39648=DIRECTION('',(1.05842257525004E-48,1.72718866511696E-48,1.));
#39649=DIRECTION('center_axis',(0.778521169386285,-0.627618346463367,2.6001091304247E-49));
#39650=DIRECTION('ref_axis',(0.627618346463367,0.778521169386285,-2.38387219843189E-65));
#39651=DIRECTION('center_axis',(0.0283643192709005,0.999597651754094,-1.67295152950556E-48));
#39652=DIRECTION('ref_axis',(-0.999597651754094,0.0283643192709005,5.71503284305285E-66));
#39653=DIRECTION('',(1.09747227149896E-48,1.6424833258909E-48,1.));
#39654=DIRECTION('center_axis',(1.09747227149896E-48,1.6424833258909E-48,
1.));
#39655=DIRECTION('ref_axis',(4.33680868994202E-19,-1.,1.6424833258909E-48));
#39656=DIRECTION('',(1.09747227149896E-48,1.6424833258909E-48,1.));
#39657=DIRECTION('center_axis',(0.726878880513651,-0.686765675513287,3.30271754722842E-49));
#39658=DIRECTION('ref_axis',(0.686765675513287,0.726878880513651,-2.02185804836064E-65));
#39659=DIRECTION('center_axis',(0.106704409389004,0.994290786951656,-1.66664752907659E-48));
#39660=DIRECTION('ref_axis',(-0.994290786951656,0.106704409389004,-7.60908949083185E-66));
#39661=DIRECTION('',(1.12975568624752E-48,1.55497530110057E-48,1.));
#39662=DIRECTION('center_axis',(1.12975568624752E-48,1.55497530110057E-48,
1.));
#39663=DIRECTION('ref_axis',(4.33680868994202E-19,-1.,1.55497530110057E-48));
#39664=DIRECTION('',(1.12975568624752E-48,1.55497530110057E-48,1.));
#39665=DIRECTION('center_axis',(0.670755141630895,-0.741678865800906,3.95502882331431E-49));
#39666=DIRECTION('ref_axis',(0.741678865800906,0.670755141630895,-5.99583083400171E-67));
#39667=DIRECTION('center_axis',(0.184386631340409,0.982853788812424,-1.65306157129173E-48));
#39668=DIRECTION('ref_axis',(-0.982853788812424,0.184386631340409,2.90870213757036E-65));
#39669=DIRECTION('',(1.15507378150848E-48,1.46520410681816E-48,1.));
#39670=DIRECTION('center_axis',(1.15507378150848E-48,1.46520410681816E-48,
1.));
#39671=DIRECTION('ref_axis',(4.33680868994202E-19,-1.,1.46520410681816E-48));
#39672=DIRECTION('',(1.15507378150848E-48,1.46520410681816E-48,1.));
#39673=DIRECTION('center_axis',(0.610495974251266,-0.792019359247612,4.5530212427498E-49));
#39674=DIRECTION('ref_axis',(0.792019359247612,0.610495974251266,2.91962028883906E-65));
#39675=DIRECTION('center_axis',(0.260932048394823,0.965357170233112,-1.63227741809852E-48));
#39676=DIRECTION('ref_axis',(-0.965357170233112,0.260932048394823,3.06323067308603E-65));
#39677=DIRECTION('',(1.17327046280543E-48,1.37372321230838E-48,1.));
#39678=DIRECTION('center_axis',(1.17327046280543E-48,1.37372321230838E-48,
1.));
#39679=DIRECTION('ref_axis',(4.33680868994202E-19,-1.,1.37372321230838E-48));
#39680=DIRECTION('',(1.17327046280543E-48,1.37372321230838E-48,1.));
#39681=DIRECTION('center_axis',(0.546472896179865,-0.837476789971394,5.0930079834164E-49));
#39682=DIRECTION('ref_axis',(0.837476789971394,0.546472896179865,-4.56422939014991E-65));
#39683=DIRECTION('center_axis',(0.335868732602171,0.94190880368548,-1.60442321071282E-48));
#39684=DIRECTION('ref_axis',(-0.94190880368548,0.335868732602171,4.87630450545203E-65));
#39685=DIRECTION('',(1.18423354154716E-48,1.28109662770635E-48,1.));
#39686=DIRECTION('center_axis',(1.18423354154716E-48,1.28109662770635E-48,
1.));
#39687=DIRECTION('ref_axis',(4.33680868994202E-19,-1.,1.28109662770635E-48));
#39688=DIRECTION('',(1.18423354154716E-48,1.28109662770635E-48,1.));
#39689=DIRECTION('center_axis',(0.479080630982838,-0.87777089779571,5.57165984749409E-49));
#39690=DIRECTION('ref_axis',(0.87777089779571,0.479080630982838,-3.73128804317402E-67));
#39691=DIRECTION('center_axis',(0.408734674385341,0.912653256146664,-1.56967067958563E-48));
#39692=DIRECTION('ref_axis',(-0.912653256146664,0.408734674385341,1.45818743306131E-64));
#39693=DIRECTION('center_axis',(0.408734674385325,-0.912653256146672,5.98602578707294E-49));
#39694=DIRECTION('ref_axis',(0.912653256146672,0.408734674385325,1.90174553100142E-65));
#39695=DIRECTION('center_axis',(0.479080630982853,0.877770897795701,-1.52823408562775E-48));
#39696=DIRECTION('ref_axis',(-0.877770897795701,0.479080630982853,5.61428358120402E-65));
#39697=DIRECTION('center_axis',(0.335868732602155,-0.941908803685485,6.33355109834479E-49));
#39698=DIRECTION('ref_axis',(0.941908803685485,0.335868732602155,-2.18452554190007E-64));
#39699=DIRECTION('center_axis',(0.54647289617988,0.837476789971384,-1.48036889921998E-48));
#39700=DIRECTION('ref_axis',(-0.837476789971384,0.54647289617988,1.0038841655118E-64));
#39701=DIRECTION('center_axis',(0.260932048394805,-0.965357170233117,6.61209317220175E-49));
#39702=DIRECTION('ref_axis',(0.965357170233117,0.260932048394805,-1.34731391844263E-65));
#39703=DIRECTION('center_axis',(0.61049597425128,0.792019359247601,-1.42637022515332E-48));
#39704=DIRECTION('ref_axis',(-0.792019359247601,0.61049597425128,4.68595517840464E-65));
#39705=DIRECTION('center_axis',(0.184386631340391,-0.982853788812427,6.81993470413385E-49));
#39706=DIRECTION('ref_axis',(0.982853788812427,0.184386631340391,-4.82159387328582E-66));
#39707=DIRECTION('center_axis',(0.670755141630908,0.741678865800894,-1.36657098320977E-48));
#39708=DIRECTION('ref_axis',(-0.741678865800894,0.670755141630908,-1.20021806126158E-65));
#39709=DIRECTION('center_axis',(0.106704409388986,-0.994290786951658,6.95579428198241E-49));
#39710=DIRECTION('ref_axis',(0.994290786951658,0.106704409388986,-5.2899598259714E-66));
#39711=DIRECTION('center_axis',(0.726878880513664,0.686765675513273,-1.30133985560118E-48));
#39712=DIRECTION('ref_axis',(-0.686765675513273,0.726878880513664,8.56568901676031E-65));
#39713=DIRECTION('center_axis',(0.0283643192708817,-0.999597651754094,7.01883428627211E-49));
#39714=DIRECTION('ref_axis',(0.999597651754094,0.0283643192708817,4.29698701010715E-68));
#46242=CARTESIAN_POINT('',(0.,0.,0.));
#46243=CARTESIAN_POINT('Origin',(30.,-1.32966554433622E-14,16.));
#46244=CARTESIAN_POINT('',(29.9999999999999,-1.50000000000001,30.25));
#46245=CARTESIAN_POINT('',(30.,-1.50000000000001,30.3125));
#46246=CARTESIAN_POINT('',(30.,-1.50000000000001,16.));
#46247=CARTESIAN_POINT('',(30.,-1.50000000000002,30.75));
#46248=CARTESIAN_POINT('Ctrl Pts',(29.9999999999999,-1.50000000000001,30.25));
#46249=CARTESIAN_POINT('Ctrl Pts',(30.1658036138247,-1.50000000000003,30.2579772300895));
#46250=CARTESIAN_POINT('Ctrl Pts',(30.3306771390814,-1.47251502213024,30.2666731828795));
#46251=CARTESIAN_POINT('Ctrl Pts',(30.6740051197163,-1.35441705513551,30.2864720571327));
#46252=CARTESIAN_POINT('Ctrl Pts',(30.8456956760641,-1.25440329321601,30.2975106829297));
#46253=CARTESIAN_POINT('Ctrl Pts',(31.1355371924707,-0.998320157723232,
30.31856910982));
#46254=CARTESIAN_POINT('Ctrl Pts',(31.2526807741055,-0.846671576374736,
30.3279626902015));
#46255=CARTESIAN_POINT('Ctrl Pts',(31.4282014939959,-0.499786966349004,
30.3472340574251));
#46256=CARTESIAN_POINT('Ctrl Pts',(31.4817951924464,-0.306278304449559,
30.3579845386417));
#46257=CARTESIAN_POINT('Ctrl Pts',(31.5101111597472,0.0860175204635018,
30.3797787511369));
#46258=CARTESIAN_POINT('Ctrl Pts',(31.4862462216493,0.280921846793951,30.3906067692664));
#46259=CARTESIAN_POINT('Ctrl Pts',(31.3664146176937,0.647698903970874,30.4109832724428));
#46260=CARTESIAN_POINT('Ctrl Pts',(31.2727727808063,0.816486916731949,30.4197772164968));
#46261=CARTESIAN_POINT('Ctrl Pts',(31.0215777110749,1.11639419547156,30.440193602667));
#46262=CARTESIAN_POINT('Ctrl Pts',(30.8638920671928,1.2424306705166,30.4512812699412));
#46263=CARTESIAN_POINT('Ctrl Pts',(30.51519869364,1.4218077371841,30.4730404839947));
#46264=CARTESIAN_POINT('Ctrl Pts',(30.3288784064271,1.47608428096084,30.4835125047644));
#46265=CARTESIAN_POINT('Ctrl Pts',(29.9417076474062,1.51169090841865,30.5031293395779));
#46266=CARTESIAN_POINT('Ctrl Pts',(29.7444133180912,1.49107258678014,30.5125449036674));
#46267=CARTESIAN_POINT('Ctrl Pts',(29.3680874803138,1.37464650826943,30.5338849467157));
#46268=CARTESIAN_POINT('Ctrl Pts',(29.192868275455,1.27964935682832,30.5449539944024));
#46269=CARTESIAN_POINT('Ctrl Pts',(28.8948089362382,1.03185947909864,30.5661774332058));
#46270=CARTESIAN_POINT('Ctrl Pts',(28.7730426891403,0.883581363472215,30.5759121464738));
#46271=CARTESIAN_POINT('Ctrl Pts',(28.5872420086988,0.541893735862482,30.5948947924521));
#46272=CARTESIAN_POINT('Ctrl Pts',(28.5279457886126,0.350092848014275,30.6055503973326));
#46273=CARTESIAN_POINT('Ctrl Pts',(28.4879441501424,-0.0417086531130522,
30.6273171473952));
#46274=CARTESIAN_POINT('Ctrl Pts',(28.5061747163527,-0.237794814766365,
30.6382108230426));
#46275=CARTESIAN_POINT('Ctrl Pts',(28.6154381406337,-0.60772707143957,30.65876261508));
#46276=CARTESIAN_POINT('Ctrl Pts',(28.7037802077497,-0.77855877037785,30.6675955620118));
#46277=CARTESIAN_POINT('Ctrl Pts',(28.9458348287961,-1.08578773838532,30.687775558397));
#46278=CARTESIAN_POINT('Ctrl Pts',(29.1002278810903,-1.21679626071423,30.6988429232091));
#46279=CARTESIAN_POINT('Ctrl Pts',(29.3881527190005,-1.37554036843891,30.7171052719799));
#46280=CARTESIAN_POINT('Ctrl Pts',(29.5080276522,-1.42282651307167,30.7241862614101));
#46281=CARTESIAN_POINT('Ctrl Pts',(29.7526687702711,-1.48465507368766,30.7376740227083));
#46282=CARTESIAN_POINT('Ctrl Pts',(29.8761199631302,-1.50000000000009,30.7440398189472));
#46283=CARTESIAN_POINT('Ctrl Pts',(30.0000000000009,-1.50000000000001,30.75));
#46284=CARTESIAN_POINT('',(30.,-1.50000000000001,30.85));
#46285=CARTESIAN_POINT('',(30.,-1.50000000000001,16.));
#46286=CARTESIAN_POINT('Origin',(30.,-1.32966554433622E-14,30.85));
#46287=CARTESIAN_POINT('',(28.9490560961666,-1.07028823734334,30.75));
#46288=CARTESIAN_POINT('Origin',(30.,-1.5916987375435E-14,30.75));
#46289=CARTESIAN_POINT('Ctrl Pts',(28.9490560961666,-1.07028823734332,30.75));
#46290=CARTESIAN_POINT('Ctrl Pts',(28.8761609488349,-0.998710593084209,
30.7445045626927));
#46291=CARTESIAN_POINT('Ctrl Pts',(28.8107674297946,-0.919873442584925,
30.7391683946938));
#46292=CARTESIAN_POINT('Ctrl Pts',(28.6983154051604,-0.752052754529888,
30.7290963583567));
#46293=CARTESIAN_POINT('Ctrl Pts',(28.6511686993163,-0.663795554008335,
30.7243775307781));
#46294=CARTESIAN_POINT('Ctrl Pts',(28.5395598759442,-0.392939439769756,
30.709329968876));
#46295=CARTESIAN_POINT('Ctrl Pts',(28.5011631241701,-0.201888114570883,
30.6987160063649));
#46296=CARTESIAN_POINT('Ctrl Pts',(28.4988436150777,0.191908857459164,30.6768383968077));
#46297=CARTESIAN_POINT('Ctrl Pts',(28.5379718270057,0.390884408078152,30.6657841995511));
#46298=CARTESIAN_POINT('Ctrl Pts',(28.6882496652404,0.752033457565058,30.6457203634686));
#46299=CARTESIAN_POINT('Ctrl Pts',(28.7941652988744,0.912256576314666,30.6368419553212));
#46300=CARTESIAN_POINT('Ctrl Pts',(29.0637866570552,1.18813740110581,30.6162064354332));
#46301=CARTESIAN_POINT('Ctrl Pts',(29.2263162356668,1.29983562680085,30.6052839989448));
#46302=CARTESIAN_POINT('Ctrl Pts',(29.5881540142218,1.45598200117754,30.5835376714189));
#46303=CARTESIAN_POINT('Ctrl Pts',(29.7845106480132,1.49769538170803,30.5729317534561));
#46304=CARTESIAN_POINT('Ctrl Pts',(30.1735918421599,1.5020241460186,30.5540918323215));
#46305=CARTESIAN_POINT('Ctrl Pts',(30.3626153088868,1.46791385953203,30.544162381137));
#46306=CARTESIAN_POINT('Ctrl Pts',(30.7246797057952,1.32812661690519,30.5228595707569));
#46307=CARTESIAN_POINT('Ctrl Pts',(30.8932233177541,1.2211620663456,30.5117792749302));
#46308=CARTESIAN_POINT('Ctrl Pts',(31.1776737025205,0.949411483501645,30.4905450221109));
#46309=CARTESIAN_POINT('Ctrl Pts',(31.2913339229655,0.787872571372875,30.4812706984095));
#46310=CARTESIAN_POINT('Ctrl Pts',(31.4489779041399,0.433069950768308,30.4615594417092));
#46311=CARTESIAN_POINT('Ctrl Pts',(31.4925441992832,0.243681023738972,30.451037834652));
#46312=CARTESIAN_POINT('Ctrl Pts',(31.5059639907605,-0.148777135728896,
30.4292346035705));
#46313=CARTESIAN_POINT('Ctrl Pts',(31.4726973264507,-0.348194823891665,
30.418155843117));
#46314=CARTESIAN_POINT('Ctrl Pts',(31.3331360295961,-0.713588890875335,
30.3978561727291));
#46315=CARTESIAN_POINT('Ctrl Pts',(31.2315888806866,-0.877298264710928,
30.3890521180742));
#46316=CARTESIAN_POINT('Ctrl Pts',(30.969887909143,-1.16071911064266,30.3685882229343));
#46317=CARTESIAN_POINT('Ctrl Pts',(30.8111118646049,-1.27673016594729,30.3577265776157));
#46318=CARTESIAN_POINT('Ctrl Pts',(30.4544959445291,-1.44324278722566,30.3359435355702));
#46319=CARTESIAN_POINT('Ctrl Pts',(30.2594138454525,-1.49071962728781,30.3252388425894));
#46320=CARTESIAN_POINT('Ctrl Pts',(30.0404799678322,-1.49959063127059,30.3144589647139));
#46321=CARTESIAN_POINT('Ctrl Pts',(30.0202329450965,-1.50000000000001,30.3134734580248));
#46322=CARTESIAN_POINT('Ctrl Pts',(30.,-1.50000000000001,30.3125));
#46323=CARTESIAN_POINT('Origin',(30.,-1.32966554433622E-14,16.));
#46324=CARTESIAN_POINT('',(30.0000000422953,-1.50000000000001,29.7500000040699));
#46325=CARTESIAN_POINT('',(30.0000000000001,-1.50000000000001,29.8125));
#46326=CARTESIAN_POINT('',(30.,-1.50000000000001,16.));
#46327=CARTESIAN_POINT('Ctrl Pts',(30.0000000423936,-1.50000000000001,29.7500000020397));
#46328=CARTESIAN_POINT('Ctrl Pts',(30.195284159332,-1.49999999448081,29.7593956136499));
#46329=CARTESIAN_POINT('Ctrl Pts',(30.3888046451199,-1.46186371850976,29.7697657133627));
#46330=CARTESIAN_POINT('Ctrl Pts',(30.7506676874449,-1.3133124636612,29.7913022808498));
#46331=CARTESIAN_POINT('Ctrl Pts',(30.9154176613495,-1.20428706546983,29.8022573009481));
#46332=CARTESIAN_POINT('Ctrl Pts',(31.18981388205,-0.933008136594988,29.8229947210741));
#46333=CARTESIAN_POINT('Ctrl Pts',(31.2983679232815,-0.774850228387389,
29.8319527650896));
#46334=CARTESIAN_POINT('Ctrl Pts',(31.4541476549185,-0.418353419581691,
29.8517581433566));
#46335=CARTESIAN_POINT('Ctrl Pts',(31.4967395542031,-0.22207441884915,29.8626625322862));
#46336=CARTESIAN_POINT('Ctrl Pts',(31.5028167108854,0.170195075492689,29.8844552819718));
#46337=CARTESIAN_POINT('Ctrl Pts',(31.4683656451658,0.362410265994727,29.8951339036664));
#46338=CARTESIAN_POINT('Ctrl Pts',(31.3284167977355,0.722950513431523,29.9151639174129));
#46339=CARTESIAN_POINT('Ctrl Pts',(31.2243440361084,0.887881539566768,29.9240904295301));
#46340=CARTESIAN_POINT('Ctrl Pts',(30.9555499935672,1.17320843290826,29.9449485359688));
#46341=CARTESIAN_POINT('Ctrl Pts',(30.7918896841479,1.28933944326239,29.9560485076758));
#46342=CARTESIAN_POINT('Ctrl Pts',(30.4356884609645,1.44801470954154,29.9775938933022));
#46343=CARTESIAN_POINT('Ctrl Pts',(30.24769400318,1.49172420709908,29.9878529335795));
#46344=CARTESIAN_POINT('Ctrl Pts',(29.8564383086953,1.50648133745832,30.007087152245));
#46345=CARTESIAN_POINT('Ctrl Pts',(29.6568006042803,1.4738887523207,30.0172375010609));
#46346=CARTESIAN_POINT('Ctrl Pts',(29.2858871639067,1.33362042993594,30.0389794245699));
#46347=CARTESIAN_POINT('Ctrl Pts',(29.1177424716204,1.22887149382963,30.049978982519));
#46348=CARTESIAN_POINT('Ctrl Pts',(28.8358984689122,0.964859074366596,30.0708728867402));
#46349=CARTESIAN_POINT('Ctrl Pts',(28.7232154667205,0.809870978335536,30.0800071678703));
#46350=CARTESIAN_POINT('Ctrl Pts',(28.5578456280088,0.457982195266601,30.0995565447074));
#46351=CARTESIAN_POINT('Ctrl Pts',(28.5099042682065,0.262965364708001,30.1103908130718));
#46352=CARTESIAN_POINT('Ctrl Pts',(28.4930631778567,-0.129475272168894,
30.1321930706761));
#46353=CARTESIAN_POINT('Ctrl Pts',(28.5224126203679,-0.323064053208287,
30.142948002956));
#46354=CARTESIAN_POINT('Ctrl Pts',(28.6526173206986,-0.686662322858743,
30.1631479068255));
#46355=CARTESIAN_POINT('Ctrl Pts',(28.7515795011674,-0.85345907766542,30.1719758706799));
#46356=CARTESIAN_POINT('Ctrl Pts',(29.0118186458561,-1.14595641051804,30.1926215582791));
#46357=CARTESIAN_POINT('Ctrl Pts',(29.172636650331,-1.26695599442051,30.2037200176798));
#46358=CARTESIAN_POINT('Ctrl Pts',(29.5253217759949,-1.43577307549295,30.2253779520631));
#46359=CARTESIAN_POINT('Ctrl Pts',(29.7125728326969,-1.48464476779679,30.2357446197376));
#46360=CARTESIAN_POINT('Ctrl Pts',(29.9359811243456,-1.49897644179293,30.2468914582366));
#46361=CARTESIAN_POINT('Ctrl Pts',(29.9680065223165,-1.50000000000001,30.2484607130873));
#46362=CARTESIAN_POINT('Ctrl Pts',(29.9999999999999,-1.50000000000001,30.25));
#46363=CARTESIAN_POINT('Ctrl Pts',(30.,-1.50000000000001,30.3125));
#46364=CARTESIAN_POINT('Ctrl Pts',(29.8305649734084,-1.50000000000001,30.3043480534823));
#46365=CARTESIAN_POINT('Ctrl Pts',(29.6621927434306,-1.471296371185,30.2954499177677));
#46366=CARTESIAN_POINT('Ctrl Pts',(29.3161242189391,-1.34950305066004,30.2754165403276));
#46367=CARTESIAN_POINT('Ctrl Pts',(29.1449154106261,-1.2480688680691,30.264361636514));
#46368=CARTESIAN_POINT('Ctrl Pts',(28.8512754656375,-0.984586302069753,
30.242914917907));
#46369=CARTESIAN_POINT('Ctrl Pts',(28.7318299827785,-0.825047829175388,
30.2333359905097));
#46370=CARTESIAN_POINT('Ctrl Pts',(28.5638630976012,-0.47370253085421,30.2138168072696));
#46371=CARTESIAN_POINT('Ctrl Pts',(28.5150825240157,-0.286153024679847,
30.2033973902599));
#46372=CARTESIAN_POINT('Ctrl Pts',(28.4904050702493,0.104624550291977,30.1816875249837));
#46373=CARTESIAN_POINT('Ctrl Pts',(28.5176966903753,0.304322584656878,30.1705931897412));
#46374=CARTESIAN_POINT('Ctrl Pts',(28.6462704703314,0.673930577459572,30.1500594123633));
#46375=CARTESIAN_POINT('Ctrl Pts',(28.7433931121189,0.841252262459088,30.141257075347));
#46376=CARTESIAN_POINT('Ctrl Pts',(28.9970706151381,1.13219704351489,30.1209702113185));
#46377=CARTESIAN_POINT('Ctrl Pts',(29.1519620886259,1.25242080149054,30.1101784429931));
#46378=CARTESIAN_POINT('Ctrl Pts',(29.5030294160994,1.42917820121841,30.0883777805545));
#46379=CARTESIAN_POINT('Ctrl Pts',(29.696654967539,1.48240812812318,30.0775833577866));
#46380=CARTESIAN_POINT('Ctrl Pts',(30.0844620336651,1.50960977413546,30.0581693803401));
#46381=CARTESIAN_POINT('Ctrl Pts',(30.2746950762916,1.48681483093204,30.0489174722834));
#46382=CARTESIAN_POINT('Ctrl Pts',(30.642872277816,1.3694262764412,30.0279427452356));
#46383=CARTESIAN_POINT('Ctrl Pts',(30.8165454300566,1.27352463490858,30.0169229573155));
#46384=CARTESIAN_POINT('Ctrl Pts',(31.1192034235311,1.01839257572982,29.9952743161713));
#46385=CARTESIAN_POINT('Ctrl Pts',(31.2444516003803,0.860842115189833,29.9853245619549));
#46386=CARTESIAN_POINT('Ctrl Pts',(31.4225185229473,0.51295924874081,29.9659977360411));
#46387=CARTESIAN_POINT('Ctrl Pts',(31.476317491186,0.327339595503408,29.9556855330835));
#46388=CARTESIAN_POINT('Ctrl Pts',(31.5118899575654,-0.0614966036299657,
29.9340835220205));
#46389=CARTESIAN_POINT('Ctrl Pts',(31.49041063713,-0.261302093346022,29.9229832170363));
#46390=CARTESIAN_POINT('Ctrl Pts',(31.3726040951777,-0.63490434793495,29.9022275362258));
#46391=CARTESIAN_POINT('Ctrl Pts',(31.2797800327084,-0.805795593106099,
29.8933569012793));
#46392=CARTESIAN_POINT('Ctrl Pts',(31.0338687856651,-1.10392432463312,29.873244137236));
#46393=CARTESIAN_POINT('Ctrl Pts',(30.8828092373533,-1.22807490132932,29.8625276541988));
#46394=CARTESIAN_POINT('Ctrl Pts',(30.5373473005298,-1.41449618106684,29.8407282401322));
#46395=CARTESIAN_POINT('Ctrl Pts',(30.3452845785499,-1.47320733373471,29.8298567527606));
#46396=CARTESIAN_POINT('Ctrl Pts',(30.0982962322989,-1.49758712755237,29.8172963039161));
#46397=CARTESIAN_POINT('Ctrl Pts',(30.0491225084885,-1.50000000000001,29.8148634077916));
#46398=CARTESIAN_POINT('Ctrl Pts',(30.0000000000002,-1.50000000000001,29.8125));
#46399=CARTESIAN_POINT('Origin',(30.,-1.32966554433622E-14,16.));
#46400=CARTESIAN_POINT('',(30.,-1.50000000000001,29.25));
#46401=CARTESIAN_POINT('',(30.,-1.50000000000001,29.3125));
#46402=CARTESIAN_POINT('',(30.,-1.50000000000001,16.));
#46403=CARTESIAN_POINT('Ctrl Pts',(30.0000000000001,-1.50000000000001,29.25));
#46404=CARTESIAN_POINT('Ctrl Pts',(30.0257058009192,-1.50000000000001,29.2512367709234));
#46405=CARTESIAN_POINT('Ctrl Pts',(30.0514327409082,-1.49933922123128,29.2524929138666));
#46406=CARTESIAN_POINT('Ctrl Pts',(30.2757518694164,-1.4877855903611,29.2636064071598));
#46407=CARTESIAN_POINT('Ctrl Pts',(30.4703136581261,-1.43816783024051,29.2743455366981));
#46408=CARTESIAN_POINT('Ctrl Pts',(30.8249043497727,-1.26783071251083,29.2961373759079));
#46409=CARTESIAN_POINT('Ctrl Pts',(30.9822510518058,-1.15024113589767,29.3069740997672));
#46410=CARTESIAN_POINT('Ctrl Pts',(31.2409808029183,-0.864020908483806,
29.3273728025942));
#46411=CARTESIAN_POINT('Ctrl Pts',(31.3408899715229,-0.698983488656709,
29.3361675839636));
#46412=CARTESIAN_POINT('Ctrl Pts',(31.4763980403227,-0.332018378933428,
29.3565545345038));
#46413=CARTESIAN_POINT('Ctrl Pts',(31.5074559153656,-0.132477013527386,
29.3676401659153));
#46414=CARTESIAN_POINT('Ctrl Pts',(31.4898677318573,0.259397054955175,29.3894109474976));
#46415=CARTESIAN_POINT('Ctrl Pts',(31.444367356687,0.448123046557066,29.3998957248088));
#46416=CARTESIAN_POINT('Ctrl Pts',(31.2829132867175,0.801659109129801,29.419536617174));
#46417=CARTESIAN_POINT('Ctrl Pts',(31.1671346623852,0.962462537199801,29.4289146111855));
#46418=CARTESIAN_POINT('Ctrl Pts',(30.8792964511142,1.23119218867364,29.4502279461232));
#46419=CARTESIAN_POINT('Ctrl Pts',(30.7097525390342,1.33613064071083,29.4613000883974));
#46420=CARTESIAN_POINT('Ctrl Pts',(30.346523773562,1.47177468007876,29.4825438305068));
#46421=CARTESIAN_POINT('Ctrl Pts',(30.1572989096959,1.50379960302192,29.4923264081504));
#46422=CARTESIAN_POINT('Ctrl Pts',(29.7684168962525,1.49529312487305,29.5112727938055));
#46423=CARTESIAN_POINT('Ctrl Pts',(29.5725063077327,1.45146676708809,29.5219159452176));
#46424=CARTESIAN_POINT('Ctrl Pts',(29.2125442219205,1.29150806105852,29.5436779265358));
#46425=CARTESIAN_POINT('Ctrl Pts',(29.051374885103,1.17821798386326,29.5545791364576));
#46426=CARTESIAN_POINT('Ctrl Pts',(28.784644635234,0.899571593555892,29.5751523790963));
#46427=CARTESIAN_POINT('Ctrl Pts',(28.6803243600253,0.738084850822973,29.5839952860653));
#46428=CARTESIAN_POINT('Ctrl Pts',(28.5339435846744,0.375376943196454,29.6041457253779));
#46429=CARTESIAN_POINT('Ctrl Pts',(28.4969501646145,0.176221200716502,29.6152099332935));
#46430=CARTESIAN_POINT('Ctrl Pts',(28.5033188891713,-0.217123692718195,
29.6370624273732));
#46431=CARTESIAN_POINT('Ctrl Pts',(28.5436046203998,-0.407585858885439,
29.6476436588269));
#46432=CARTESIAN_POINT('Ctrl Pts',(28.6948329707667,-0.764496194056087,
29.6674720107808));
#46433=CARTESIAN_POINT('Ctrl Pts',(28.8049699824855,-0.927268122072015,
29.6765948726435));
#46434=CARTESIAN_POINT('Ctrl Pts',(29.0837280295094,-1.20402609540407,29.6976943469156));
#46435=CARTESIAN_POINT('Ctrl Pts',(29.2505451199729,-1.31436112105669,29.7087851997463));
#46436=CARTESIAN_POINT('Ctrl Pts',(29.6105129505334,-1.46104267840857,29.7301786477734));
#46437=CARTESIAN_POINT('Ctrl Pts',(29.799201008928,-1.49868271487424,29.7403024627842));
#46438=CARTESIAN_POINT('Ctrl Pts',(29.9932712661576,-1.49998868274459,29.7496759492739));
#46439=CARTESIAN_POINT('Ctrl Pts',(29.9966359009771,-1.50000000009509,29.7498381447076));
#46440=CARTESIAN_POINT('Ctrl Pts',(30.0000000423936,-1.50000000000001,29.7500000020397));
#46441=CARTESIAN_POINT('Ctrl Pts',(30.0000000000002,-1.50000000000001,29.8125));
#46442=CARTESIAN_POINT('Ctrl Pts',(29.8597537134085,-1.50000000000001,29.8057523973903));
#46443=CARTESIAN_POINT('Ctrl Pts',(29.7199776172616,-1.48033650865739,29.798481208736));
#46444=CARTESIAN_POINT('Ctrl Pts',(29.396444095828,-1.38712528602054,29.7803259942996));
#46445=CARTESIAN_POINT('Ctrl Pts',(29.2206000446906,-1.29650603057681,29.7693484919046));
#46446=CARTESIAN_POINT('Ctrl Pts',(28.911420128637,-1.05097346611518,29.747652717245));
#46447=CARTESIAN_POINT('Ctrl Pts',(28.7818724475201,-0.897590413872414,
29.737366134104));
#46448=CARTESIAN_POINT('Ctrl Pts',(28.5939020851709,-0.556198210295242,
29.7183999005719));
#46449=CARTESIAN_POINT('Ctrl Pts',(28.5345980064858,-0.372882477899534,
29.7082156932166));
#46450=CARTESIAN_POINT('Ctrl Pts',(28.4870031451474,0.0134445146485481,
29.6867530825195));
#46451=CARTESIAN_POINT('Ctrl Pts',(28.502033993864,0.213177772539474,29.6756567904145));
#46452=CARTESIAN_POINT('Ctrl Pts',(28.6077791980133,0.591085049341038,29.6546619417033));
#46453=CARTESIAN_POINT('Ctrl Pts',(28.6958240597398,0.766015662165753,29.6456356480104));
#46454=CARTESIAN_POINT('Ctrl Pts',(28.9331445661562,1.07197536298372,29.6257186792435));
#46455=CARTESIAN_POINT('Ctrl Pts',(29.079894739921,1.20029258347643,29.6150937909803));
#46456=CARTESIAN_POINT('Ctrl Pts',(29.4205899711736,1.39807482372058,29.5932081329061));
#46457=CARTESIAN_POINT('Ctrl Pts',(29.6127784235583,1.46301280498413,29.5821576288666));
#46458=CARTESIAN_POINT('Ctrl Pts',(30.000882127086,1.51202551870596,29.5621235164545));
#46459=CARTESIAN_POINT('Ctrl Pts',(30.1924980276144,1.49972435337029,29.5532307774773));
#46460=CARTESIAN_POINT('Ctrl Pts',(30.565900986819,1.40283604422102,29.5325740773055));
#46461=CARTESIAN_POINT('Ctrl Pts',(30.7436552900603,1.31725598082702,29.5216446454201));
#46462=CARTESIAN_POINT('Ctrl Pts',(31.0589827795059,1.08076551025951,29.4999042647726));
#46463=CARTESIAN_POINT('Ctrl Pts',(31.1927323157941,0.931082658468895,29.4893113802134));
#46464=CARTESIAN_POINT('Ctrl Pts',(31.3898152208091,0.595521362119493,29.470508077404));
#46465=CARTESIAN_POINT('Ctrl Pts',(31.454132752542,0.414466978649508,29.4605259432583));
#46466=CARTESIAN_POINT('Ctrl Pts',(31.5126702779257,0.0306540870738048,
29.4392030048374));
#46467=CARTESIAN_POINT('Ctrl Pts',(31.5035323460368,-0.168835937693657,
29.4281202256837));
#46468=CARTESIAN_POINT('Ctrl Pts',(31.4089367798935,-0.550558804938134,
29.4069133997257));
#46469=CARTESIAN_POINT('Ctrl Pts',(31.3252882833553,-0.729258932876967,
29.3976724363492));
#46470=CARTESIAN_POINT('Ctrl Pts',(31.095809753143,-1.04226364925314,29.3779370699617));
#46471=CARTESIAN_POINT('Ctrl Pts',(30.9530486497371,-1.17422022183269,29.3674030128222));
#46472=CARTESIAN_POINT('Ctrl Pts',(30.6189939852,-1.38091973480463,29.3455891471428));
#46473=CARTESIAN_POINT('Ctrl Pts',(30.429320489981,-1.45113472826307,29.3345130603643));
#46474=CARTESIAN_POINT('Ctrl Pts',(30.1547092959792,-1.49402062264703,29.3201095482887));
#46475=CARTESIAN_POINT('Ctrl Pts',(30.0773321028638,-1.50000000000001,29.3162206425338));
#46476=CARTESIAN_POINT('Ctrl Pts',(30.,-1.50000000000001,29.3125));
#46477=CARTESIAN_POINT('Origin',(30.,-1.32966554433622E-14,16.));
#46478=CARTESIAN_POINT('',(30.0000000000001,-1.50000000000001,28.75));
#46479=CARTESIAN_POINT('',(30.,-1.50000000000001,28.8125));
#46480=CARTESIAN_POINT('',(30.,-1.50000000000001,16.));
#46481=CARTESIAN_POINT('Ctrl Pts',(30.0000000000002,-1.50000000000001,28.75));
#46482=CARTESIAN_POINT('Ctrl Pts',(30.0540853804301,-1.50000000000001,28.7526021840792));
#46483=CARTESIAN_POINT('Ctrl Pts',(30.1082259230801,-1.49707499170992,28.7552882723823));
#46484=CARTESIAN_POINT('Ctrl Pts',(30.3599293953789,-1.46969892581938,28.7681588076143));
#46485=CARTESIAN_POINT('Ctrl Pts',(30.551406195325,-1.40907643365525,28.7790551975627));
#46486=CARTESIAN_POINT('Ctrl Pts',(30.8948389562126,-1.21930777033508,28.8008499657338));
#46487=CARTESIAN_POINT('Ctrl Pts',(31.0445316684251,-1.09380802186036,28.8115381638324));
#46488=CARTESIAN_POINT('Ctrl Pts',(31.2877030940359,-0.793168713090864,
28.8315888464123));
#46489=CARTESIAN_POINT('Ctrl Pts',(31.379006293082,-0.620999590881335,28.8405000227289));
#46490=CARTESIAN_POINT('Ctrl Pts',(31.4929834420294,-0.246010850263539,
28.861332730541));
#46491=CARTESIAN_POINT('Ctrl Pts',(31.5124077516471,-0.0462064671363202,
28.872432974048));
#46492=CARTESIAN_POINT('Ctrl Pts',(31.472996504913,0.34187077296362,28.8939928207202));
#46493=CARTESIAN_POINT('Ctrl Pts',(31.4174359900152,0.526774847879437,28.9042652693267));
#46494=CARTESIAN_POINT('Ctrl Pts',(31.2357811865968,0.873408443354475,28.9235226912975));
#46495=CARTESIAN_POINT('Ctrl Pts',(31.1084372252019,1.03024288184359,28.9336214802999));
#46496=CARTESIAN_POINT('Ctrl Pts',(30.8025714917792,1.28234443647017,28.9553402732223));
#46497=CARTESIAN_POINT('Ctrl Pts',(30.6280587815183,1.37625325113107,28.9663450980946));
#46498=CARTESIAN_POINT('Ctrl Pts',(30.2588396849677,1.48965870484553,28.9872593116519));
#46499=CARTESIAN_POINT('Ctrl Pts',(30.068359262301,1.51042753130005,28.996421409812));
#46500=CARTESIAN_POINT('Ctrl Pts',(29.6808324457,1.4790834395187,29.015936971685));
#46501=CARTESIAN_POINT('Ctrl Pts',(29.4877765738488,1.42378431516532,29.0267614634377));
#46502=CARTESIAN_POINT('Ctrl Pts',(29.1387883585853,1.24336756773843,29.0485637430906));
#46503=CARTESIAN_POINT('Ctrl Pts',(28.9853282851658,1.12165139698337,29.0593280990587));
#46504=CARTESIAN_POINT('Ctrl Pts',(28.7345675292747,0.827996981331758,29.0795498986531));
#46505=CARTESIAN_POINT('Ctrl Pts',(28.6390572969471,0.659343561113025,29.0883698021604));
#46506=CARTESIAN_POINT('Ctrl Pts',(28.5145121329283,0.288224890453508,29.108987506086));
#46507=CARTESIAN_POINT('Ctrl Pts',(28.4894007489509,0.0884674237606763,
29.1200851431244));
#46508=CARTESIAN_POINT('Ctrl Pts',(28.5181714945435,-0.301617414497863,
29.1417565230277));
#46509=CARTESIAN_POINT('Ctrl Pts',(28.5688407456957,-0.488459284239858,
29.1521366269022));
#46510=CARTESIAN_POINT('Ctrl Pts',(28.7405885892344,-0.838517734954907,
29.1715843186086));
#46511=CARTESIAN_POINT('Ctrl Pts',(28.8621896492638,-0.99731625641509,29.1812936366545));
#46512=CARTESIAN_POINT('Ctrl Pts',(29.1592029920166,-1.25770358504828,29.2028166791214));
#46513=CARTESIAN_POINT('Ctrl Pts',(29.3313514615525,-1.35708034159287,29.2138596416832));
#46514=CARTESIAN_POINT('Ctrl Pts',(29.6732716198879,-1.47316539526991,29.2335348677957));
#46515=CARTESIAN_POINT('Ctrl Pts',(29.836171069295,-1.50000000000001,29.2421177768964));
#46516=CARTESIAN_POINT('Ctrl Pts',(30.0000000000001,-1.50000000000001,29.25));
#46517=CARTESIAN_POINT('Ctrl Pts',(30.,-1.50000000000001,29.3125));
#46518=CARTESIAN_POINT('Ctrl Pts',(29.8873008443269,-1.50000000000001,29.3070777593446));
#46519=CARTESIAN_POINT('Ctrl Pts',(29.7747317592542,-1.48730209620256,29.3013090571639));
#46520=CARTESIAN_POINT('Ctrl Pts',(29.4744632015876,-1.41837586794508,29.2849477619958));
#46521=CARTESIAN_POINT('Ctrl Pts',(29.294837753903,-1.33817655775596,29.2740777699983));
#46522=CARTESIAN_POINT('Ctrl Pts',(28.9731315511867,-1.11133054751215,29.2522983950411));
#46523=CARTESIAN_POINT('Ctrl Pts',(28.8350302040853,-0.965600487241644,
29.241605933651));
#46524=CARTESIAN_POINT('Ctrl Pts',(28.6283822605559,-0.636211572057215,
29.2225138877439));
#46525=CARTESIAN_POINT('Ctrl Pts',(28.5588803689078,-0.457503373167084,
29.2129168540649));
#46526=CARTESIAN_POINT('Ctrl Pts',(28.4890373687744,-0.0765943370343735,
29.1917552409464));
#46527=CARTESIAN_POINT('Ctrl Pts',(28.4920613555339,0.122462822378066,29.1806965098678));
#46528=CARTESIAN_POINT('Ctrl Pts',(28.5749385187676,0.508021327520356,29.1592765929154));
#46529=CARTESIAN_POINT('Ctrl Pts',(28.6539760022703,0.690715131611738,29.1497407450183));
#46530=CARTESIAN_POINT('Ctrl Pts',(28.8753117279029,1.01093295253508,29.1301967854836));
#46531=CARTESIAN_POINT('Ctrl Pts',(29.0138845897616,1.14650161502305,29.1197638993787));
#46532=CARTESIAN_POINT('Ctrl Pts',(29.3408853293963,1.36213850199283,29.0980411554306));
#46533=CARTESIAN_POINT('Ctrl Pts',(29.5278326261113,1.43768005817386,29.0869482728631));
#46534=CARTESIAN_POINT('Ctrl Pts',(29.9124519842907,1.50965487695232,29.0664439648431));
#46535=CARTESIAN_POINT('Ctrl Pts',(30.1057978761999,1.50848592114141,29.0576455173396));
#46536=CARTESIAN_POINT('Ctrl Pts',(30.4842893221004,1.43290905070853,29.0373359816462));
#46537=CARTESIAN_POINT('Ctrl Pts',(30.6656448486515,1.3581864320247,29.02653488151));
#46538=CARTESIAN_POINT('Ctrl Pts',(30.9934995933557,1.14126552935963,29.0047353821212));
#46539=CARTESIAN_POINT('Ctrl Pts',(31.1358790692293,0.999664672511309,28.9939517892597));
#46540=CARTESIAN_POINT('Ctrl Pts',(31.3521306759684,0.67660748989115,28.974573568351));
#46541=CARTESIAN_POINT('Ctrl Pts',(31.426848104494,0.500181082019829,28.9652878378899));
#46542=CARTESIAN_POINT('Ctrl Pts',(31.5078778462889,0.122255781263764,28.9442919878479));
#46543=CARTESIAN_POINT('Ctrl Pts',(31.5109056485428,-0.0761896933508503,
28.9332672392582));
#46544=CARTESIAN_POINT('Ctrl Pts',(31.4398008862795,-0.46541654048851,28.9116435255283));
#46545=CARTESIAN_POINT('Ctrl Pts',(31.3653977766762,-0.65214948337147,28.9017441343992));
#46546=CARTESIAN_POINT('Ctrl Pts',(31.1521444486118,-0.979425287841449,
28.8823929843003));
#46547=CARTESIAN_POINT('Ctrl Pts',(31.0177656624447,-1.1184106596764,28.8720669771632));
#46548=CARTESIAN_POINT('Ctrl Pts',(30.6979072153004,-1.34258973369453,28.8504505839492));
#46549=CARTESIAN_POINT('Ctrl Pts',(30.5137720633169,-1.42326028628083,28.8393505286358));
#46550=CARTESIAN_POINT('Ctrl Pts',(30.2141280739392,-1.48853135114915,28.8231208153399));
#46551=CARTESIAN_POINT('Ctrl Pts',(30.107104215103,-1.50000000000001,28.8176530539518));
#46552=CARTESIAN_POINT('Ctrl Pts',(30.,-1.50000000000001,28.8125));
#46553=CARTESIAN_POINT('Origin',(30.,-1.32966554433622E-14,16.));
#46554=CARTESIAN_POINT('',(30.,-1.50000000000001,28.25));
#46555=CARTESIAN_POINT('',(29.9999999999999,-1.50000000000001,28.3125));
#46556=CARTESIAN_POINT('',(30.,-1.50000000000001,16.));
#46557=CARTESIAN_POINT('Ctrl Pts',(30.,-1.50000000000001,28.25));
#46558=CARTESIAN_POINT('Ctrl Pts',(30.0829658981124,-1.50000000000001,28.2539916986341));
#46559=CARTESIAN_POINT('Ctrl Pts',(30.1659646402018,-1.49311778203419,28.258176150196));
#46560=CARTESIAN_POINT('Ctrl Pts',(30.4454386189069,-1.44623695759697,28.272924593389));
#46561=CARTESIAN_POINT('Ctrl Pts',(30.6341065114148,-1.37401296366571,28.2840081036532));
#46562=CARTESIAN_POINT('Ctrl Pts',(30.9655430066945,-1.16393488515826,28.305789851648));
#46563=CARTESIAN_POINT('Ctrl Pts',(31.1067439460802,-1.03060853555517,28.3162868947229));
#46564=CARTESIAN_POINT('Ctrl Pts',(31.3331794991128,-0.714896180931114,
28.3359510679762));
#46565=CARTESIAN_POINT('Ctrl Pts',(31.4151109522262,-0.5347128589249,28.3452937300598));
#46566=CARTESIAN_POINT('Ctrl Pts',(31.5053441166005,-0.151540941191815,
28.3665810588227));
#46567=CARTESIAN_POINT('Ctrl Pts',(31.5121960357138,0.047808853319833,28.3776560474067));
#46568=CARTESIAN_POINT('Ctrl Pts',(31.4494295470438,0.430548940590616,28.3989193855884));
#46569=CARTESIAN_POINT('Ctrl Pts',(31.3831821322801,0.610720967506089,28.4087494232854));
#46570=CARTESIAN_POINT('Ctrl Pts',(31.1825379493516,0.943999251999173,28.4276606511623));
#46571=CARTESIAN_POINT('Ctrl Pts',(31.047158086339,1.09222920702457,28.4382916166091));
#46572=CARTESIAN_POINT('Ctrl Pts',(30.7294268326579,1.32515752881874,28.4600486998403));
#46573=CARTESIAN_POINT('Ctrl Pts',(30.550958922042,1.4087432384851,28.4709570664618));
#46574=CARTESIAN_POINT('Ctrl Pts',(30.1765920486677,1.5017020595339,28.4915509905286));
#46575=CARTESIAN_POINT('Ctrl Pts',(29.9846796160604,1.51197023290498,28.5004045958464));
#46576=CARTESIAN_POINT('Ctrl Pts',(29.5971747277955,1.45876321333926,28.5205264062414));
#46577=CARTESIAN_POINT('Ctrl Pts',(29.4058997547266,1.39186434368365,28.5315874296089));
#46578=CARTESIAN_POINT('Ctrl Pts',(29.0676327101079,1.19076140439435,28.5534485031393));
#46579=CARTESIAN_POINT('Ctrl Pts',(28.9223466869136,1.06108495094317,28.5640407038963));
#46580=CARTESIAN_POINT('Ctrl Pts',(28.6879155980949,0.752518131365587,28.5838910754598));
#46581=CARTESIAN_POINT('Ctrl Pts',(28.6014862328755,0.576207606788701,28.5929884662895));
#46582=CARTESIAN_POINT('Ctrl Pts',(28.499833643426,0.196881228217823,28.6140621539879));
#46583=CARTESIAN_POINT('Ctrl Pts',(28.4869739372834,-0.00278217893022192,
28.6251545654961));
#46584=CARTESIAN_POINT('Ctrl Pts',(28.5386011115484,-0.388179803466622,
28.646565544637));
#46585=CARTESIAN_POINT('Ctrl Pts',(28.5997438056181,-0.57068109411198,28.6567045052284));
#46586=CARTESIAN_POINT('Ctrl Pts',(28.7910752661536,-0.909939730661663,
28.6755522072589));
#46587=CARTESIAN_POINT('Ctrl Pts',(28.9221594106395,-1.06198129449833,28.6859751842018));
#46588=CARTESIAN_POINT('Ctrl Pts',(29.2336502066539,-1.30423330232361,28.7076910145522));
#46589=CARTESIAN_POINT('Ctrl Pts',(29.4102115046891,-1.39300789458955,28.7186517848609));
#46590=CARTESIAN_POINT('Ctrl Pts',(29.7297304238973,-1.48169043732429,28.7364880499937));
#46591=CARTESIAN_POINT('Ctrl Pts',(29.8646679236608,-1.50000000000001,28.7434888324413));
#46592=CARTESIAN_POINT('Ctrl Pts',(30.0000000000002,-1.50000000000001,28.75));
#46593=CARTESIAN_POINT('Ctrl Pts',(30.,-1.50000000000001,28.8125));
#46594=CARTESIAN_POINT('Ctrl Pts',(29.915383015882,-1.50000000000001,28.8084288634535));
#46595=CARTESIAN_POINT('Ctrl Pts',(29.8307352254749,-1.4928411598692,28.8041573880682));
#46596=CARTESIAN_POINT('Ctrl Pts',(29.5559284168413,-1.44580747389306,28.7896292480462));
#46597=CARTESIAN_POINT('Ctrl Pts',(29.3730572440495,-1.37640415455312,28.7789029846613));
#46598=CARTESIAN_POINT('Ctrl Pts',(29.0395563050654,-1.16922544646275,28.7571024491396));
#46599=CARTESIAN_POINT('Ctrl Pts',(28.8931654598463,-1.03173520870096,28.7462400430439));
#46600=CARTESIAN_POINT('Ctrl Pts',(28.6676984257239,-0.714888535897263,
28.7265909588401));
#46601=CARTESIAN_POINT('Ctrl Pts',(28.5879546245725,-0.540586509645268,
28.7175325838691));
#46602=CARTESIAN_POINT('Ctrl Pts',(28.4963360655409,-0.165582907317607,
28.6966990504065));
#46603=CARTESIAN_POINT('Ctrl Pts',(28.4875887561367,0.032114568158461,28.6857158573245));
#46604=CARTESIAN_POINT('Ctrl Pts',(28.5470557852483,0.422500942588754,28.6640277254117));
#46605=CARTESIAN_POINT('Ctrl Pts',(28.6157998677826,0.611145026803925,28.6537877758344));
#46606=CARTESIAN_POINT('Ctrl Pts',(28.8187186237447,0.943964110383672,28.6347798680923));
#46607=CARTESIAN_POINT('Ctrl Pts',(28.9483973542157,1.08655537048085,28.6245798289275));
#46608=CARTESIAN_POINT('Ctrl Pts',(29.2601643471919,1.31985362966521,28.6030994252846));
#46609=CARTESIAN_POINT('Ctrl Pts',(29.4410566887989,1.40604402433623,28.5920020608114));
#46610=CARTESIAN_POINT('Ctrl Pts',(29.8214920682634,1.50190823479761,28.5710354603478));
#46611=CARTESIAN_POINT('Ctrl Pts',(30.0168727428654,1.5123834847247,28.5620321954671));
#46612=CARTESIAN_POINT('Ctrl Pts',(30.4002098002625,1.45848214178997,28.5420916231679));
#46613=CARTESIAN_POINT('Ctrl Pts',(30.5845472296663,1.39485738401663,28.531455330078));
#46614=CARTESIAN_POINT('Ctrl Pts',(30.9255768985555,1.19735876148644,28.5095614596354));
#46615=CARTESIAN_POINT('Ctrl Pts',(31.0774615143075,1.06275841541511,28.4985150091509));
#46616=CARTESIAN_POINT('Ctrl Pts',(31.3127681711381,0.750226996476014,28.4785123840417));
#46617=CARTESIAN_POINT('Ctrl Pts',(31.3972426471779,0.57785906771898,28.4696032815399));
#46618=CARTESIAN_POINT('Ctrl Pts',(31.4986444188222,0.205636520695856,28.4489242511497));
#46619=CARTESIAN_POINT('Ctrl Pts',(31.5126593744967,0.00877624847217685,
28.4379875693595));
#46620=CARTESIAN_POINT('Ctrl Pts',(31.4639817400215,-0.38243148199871,28.4162538065556));
#46621=CARTESIAN_POINT('Ctrl Pts',(31.4004868863224,-0.572852347631721,
28.405674869576));
#46622=CARTESIAN_POINT('Ctrl Pts',(31.2070793636249,-0.910612756316215,
28.3869104024268));
#46623=CARTESIAN_POINT('Ctrl Pts',(31.0818178721223,-1.05640050494828,28.3768711948362));
#46624=CARTESIAN_POINT('Ctrl Pts',(30.7776023551779,-1.29787423387296,28.3555270153716));
#46625=CARTESIAN_POINT('Ctrl Pts',(30.5998203088742,-1.38901510440857,28.3444417818325));
#46626=CARTESIAN_POINT('Ctrl Pts',(30.2759956104928,-1.48090471471267,28.3263092695923));
#46627=CARTESIAN_POINT('Ctrl Pts',(30.1382050521625,-1.50000000000003,28.3191493936725));
#46628=CARTESIAN_POINT('Ctrl Pts',(29.9999999999998,-1.50000000000001,28.3125));
#46629=CARTESIAN_POINT('Origin',(30.,-1.32966554433622E-14,16.));
#46630=CARTESIAN_POINT('',(30.,-1.50000000000001,27.75));
#46631=CARTESIAN_POINT('',(29.9999999999999,-1.50000000000001,27.8125));
#46632=CARTESIAN_POINT('',(30.,-1.50000000000001,16.));
#46633=CARTESIAN_POINT('Ctrl Pts',(30.,-1.50000000000001,27.75));
#46634=CARTESIAN_POINT('Ctrl Pts',(30.1124415068704,-1.50000000000002,27.7554098445216));
#46635=CARTESIAN_POINT('Ctrl Pts',(30.2247618661566,-1.48736003703784,27.7611649704098));
#46636=CARTESIAN_POINT('Ctrl Pts',(30.5287085515254,-1.41774990238772,27.7777222269793));
#46637=CARTESIAN_POINT('Ctrl Pts',(30.7117935692984,-1.3352484713228,27.7888226154224));
#46638=CARTESIAN_POINT('Ctrl Pts',(31.0290158327245,-1.10803593258209,27.810396438097));
#46639=CARTESIAN_POINT('Ctrl Pts',(31.1618575965723,-0.967846133863366,
27.8206819515156));
#46640=CARTESIAN_POINT('Ctrl Pts',(31.3721629460689,-0.6380210664967,27.8399620797878));
#46641=CARTESIAN_POINT('Ctrl Pts',(31.4448593309443,-0.449797513993593,
27.8500112492227));
#46642=CARTESIAN_POINT('Ctrl Pts',(31.5116357099559,-0.0592694964018678,
27.8717072502));
#46643=CARTESIAN_POINT('Ctrl Pts',(31.5064070816201,0.138907825669745,27.8827171014262));
#46644=CARTESIAN_POINT('Ctrl Pts',(31.4213057895144,0.515720730899333,27.9036511517167));
#46645=CARTESIAN_POINT('Ctrl Pts',(31.3446665574137,0.691326301909506,27.9128415418121));
#46646=CARTESIAN_POINT('Ctrl Pts',(31.1248857141117,1.01202109760975,27.9323239413351));
#46647=CARTESIAN_POINT('Ctrl Pts',(30.9809587395189,1.15206471718701,27.9431387316727));
#46648=CARTESIAN_POINT('Ctrl Pts',(30.6509116511972,1.36527940308072,27.964940759777));
#46649=CARTESIAN_POINT('Ctrl Pts',(30.4689587309927,1.43797198007731,27.9757142119819));
#46650=CARTESIAN_POINT('Ctrl Pts',(30.0895559298121,1.50958056680736,27.9959573651739));
#46651=CARTESIAN_POINT('Ctrl Pts',(29.8958570870542,1.50864454830606,28.0047704518936));
#46652=CARTESIAN_POINT('Ctrl Pts',(29.5119529197823,1.43233602869983,28.0253607308535));
#46653=CARTESIAN_POINT('Ctrl Pts',(29.326059536573,1.35483178794297,28.0364574259998));
#46654=CARTESIAN_POINT('Ctrl Pts',(29.0017503691465,1.13591853977073,28.058141681653));
#46655=CARTESIAN_POINT('Ctrl Pts',(28.8647633102306,0.999035130825837,28.0685347915132));
#46656=CARTESIAN_POINT('Ctrl Pts',(28.6464909172802,0.676130375169667,28.0880060034614));
#46657=CARTESIAN_POINT('Ctrl Pts',(28.5692025798653,0.491914163630282,28.097671435354));
#46658=CARTESIAN_POINT('Ctrl Pts',(28.4907708909632,0.10494838810591,28.1191695339942));
#46659=CARTESIAN_POINT('Ctrl Pts',(28.4900432259905,-0.0938982867387415,
28.1302165714856));
#46660=CARTESIAN_POINT('Ctrl Pts',(28.5641302538219,-0.473688030944453,
28.1513160017192));
#46661=CARTESIAN_POINT('Ctrl Pts',(28.6356001259049,-0.65152593371875,28.1607865563875));
#46662=CARTESIAN_POINT('Ctrl Pts',(28.845875335272,-0.978539657712538,28.1799871416705));
#46663=CARTESIAN_POINT('Ctrl Pts',(28.9856037255401,-1.12272886979256,28.1907150828729));
#46664=CARTESIAN_POINT('Ctrl Pts',(29.3096631032409,-1.34585412683097,28.2125043207586));
#46665=CARTESIAN_POINT('Ctrl Pts',(29.4899597666947,-1.42399330666579,28.2233493807965));
#46666=CARTESIAN_POINT('Ctrl Pts',(29.7854687062271,-1.48848755634025,28.2393585682142));
#46667=CARTESIAN_POINT('Ctrl Pts',(29.8926913234913,-1.50000000000001,28.2448371088943));
#46668=CARTESIAN_POINT('Ctrl Pts',(30.,-1.50000000000001,28.25));
#46669=CARTESIAN_POINT('Ctrl Pts',(29.9999999999998,-1.50000000000001,28.3125));
#46670=CARTESIAN_POINT('Ctrl Pts',(29.9436942937174,-1.50000000000001,28.3097909904434));
#46671=CARTESIAN_POINT('Ctrl Pts',(29.8873283119117,-1.49682992210333,28.3069910231599));
#46672=CARTESIAN_POINT('Ctrl Pts',(29.6396724584349,-1.46877643215582,28.2942964117443));
#46673=CARTESIAN_POINT('Ctrl Pts',(29.4541661443778,-1.41038581308707,28.2837492734071));
#46674=CARTESIAN_POINT('Ctrl Pts',(29.1087260311914,-1.22301113475657,28.2619244260365));
#46675=CARTESIAN_POINT('Ctrl Pts',(28.9535330490943,-1.09318251992373,28.250851349792));
#46676=CARTESIAN_POINT('Ctrl Pts',(28.7092889328235,-0.787692454984111,
28.2306143141317));
#46677=CARTESIAN_POINT('Ctrl Pts',(28.6196840987504,-0.61735395437333,28.2217974419096));
#46678=CARTESIAN_POINT('Ctrl Pts',(28.5078809954767,-0.248171981043882,
28.2012873322802));
#46679=CARTESIAN_POINT('Ctrl Pts',(28.4882926923279,-0.0523550997824531,
28.1904086166545));
#46680=CARTESIAN_POINT('Ctrl Pts',(28.5254878247544,0.339597077669009,28.168633495685));
#46681=CARTESIAN_POINT('Ctrl Pts',(28.5834194437059,0.531823926835376,28.1579542262869));
#46682=CARTESIAN_POINT('Ctrl Pts',(28.7667554264755,0.874769226053054,28.1389017096637));
#46683=CARTESIAN_POINT('Ctrl Pts',(28.8874031082008,1.02385470321529,28.129256101159));
#46684=CARTESIAN_POINT('Ctrl Pts',(29.1834814070674,1.27365788399194,28.1080720501192));
#46685=CARTESIAN_POINT('Ctrl Pts',(29.3578610118793,1.36987818467188,28.0970094213409));
#46686=CARTESIAN_POINT('Ctrl Pts',(29.7335617480327,1.48922788034193,28.0756182419206));
#46687=CARTESIAN_POINT('Ctrl Pts',(29.9311376367095,1.51130087803589,28.0661270552772));
#46688=CARTESIAN_POINT('Ctrl Pts',(30.3188296259211,1.47827076732948,28.0465567126743));
#46689=CARTESIAN_POINT('Ctrl Pts',(30.5053902810264,1.4253063260919,28.0361095744917));
#46690=CARTESIAN_POINT('Ctrl Pts',(30.8550820522802,1.24848731142734,28.0143733820065));
#46691=CARTESIAN_POINT('Ctrl Pts',(31.0135429189334,1.12366789185429,28.0032822239058));
#46692=CARTESIAN_POINT('Ctrl Pts',(31.2669421658592,0.825551327222966,27.9828095312695));
#46693=CARTESIAN_POINT('Ctrl Pts',(31.3618736710286,0.657250577679458,27.9740139209821));
#46694=CARTESIAN_POINT('Ctrl Pts',(31.4842407851538,0.291243414392501,27.9536801896884));
#46695=CARTESIAN_POINT('Ctrl Pts',(31.509450941646,0.0966465287303217,27.9428692515961));
#46696=CARTESIAN_POINT('Ctrl Pts',(31.4839402912682,-0.295715862316101,
27.9210713409824));
#46697=CARTESIAN_POINT('Ctrl Pts',(31.4317236332783,-0.489608696036187,
27.9102995168868));
#46698=CARTESIAN_POINT('Ctrl Pts',(31.2586786377253,-0.837725609348495,
27.8909596883695));
#46699=CARTESIAN_POINT('Ctrl Pts',(31.1426320784322,-0.99018742000189,27.8816363720611));
#46700=CARTESIAN_POINT('Ctrl Pts',(30.8547518896528,-1.24822771259633,27.8606179441152));
#46701=CARTESIAN_POINT('Ctrl Pts',(30.683921012954,-1.3494162779034,27.8495880462471));
#46702=CARTESIAN_POINT('Ctrl Pts',(30.3380948295812,-1.47125624803439,27.8295650326271));
#46703=CARTESIAN_POINT('Ctrl Pts',(30.1695563642114,-1.50000000000003,27.8206577843767));
#46704=CARTESIAN_POINT('Ctrl Pts',(29.9999999999999,-1.50000000000001,27.8125));
#46705=CARTESIAN_POINT('Origin',(30.,-1.32966554433622E-14,16.));
#46706=CARTESIAN_POINT('',(29.9999999999999,-1.50000000000001,27.25));
#46707=CARTESIAN_POINT('',(30.0000000001561,-1.50000000000001,27.312500000015));
#46708=CARTESIAN_POINT('',(30.,-1.50000000000001,16.));
#46709=CARTESIAN_POINT('Ctrl Pts',(29.9999999999998,-1.50000000000001,27.25));
#46710=CARTESIAN_POINT('Ctrl Pts',(30.1442714687728,-1.50000000000004,27.2569412642777));
#46711=CARTESIAN_POINT('Ctrl Pts',(30.2880340149987,-1.4791914741294,27.2644360576155));
#46712=CARTESIAN_POINT('Ctrl Pts',(30.6163114314673,-1.38174334274362,27.2829372047179));
#46713=CARTESIAN_POINT('Ctrl Pts',(30.7927900386128,-1.28861749288707,27.2940148648257));
#46714=CARTESIAN_POINT('Ctrl Pts',(31.0938533402203,-1.04389816914467,27.3152975386708));
#46715=CARTESIAN_POINT('Ctrl Pts',(31.2173213404585,-0.896838599044721,
27.3251756333865));
#46716=CARTESIAN_POINT('Ctrl Pts',(31.4068435879888,-0.557063752560209,
27.3440520137467));
#46717=CARTESIAN_POINT('Ctrl Pts',(31.4681965573585,-0.365925712559008,
27.3546707937468));
#46718=CARTESIAN_POINT('Ctrl Pts',(31.5124404667227,0.0256096349450533,
27.376422757497));
#46719=CARTESIAN_POINT('Ctrl Pts',(31.4962677243898,0.222085336897189,27.3873380742721));
#46720=CARTESIAN_POINT('Ctrl Pts',(31.3908461160845,0.593142920619804,27.4079523844789));
#46721=CARTESIAN_POINT('Ctrl Pts',(31.304401721973,0.764723471695272,27.4168175948822));
#46722=CARTESIAN_POINT('Ctrl Pts',(31.0656503667188,1.07455866625052,27.4369110579998));
#46723=CARTESIAN_POINT('Ctrl Pts',(30.9124772117446,1.20733392111332,27.4479688063785));
#46724=CARTESIAN_POINT('Ctrl Pts',(30.5697179509117,1.40095220523075,27.4698381046742));
#46725=CARTESIAN_POINT('Ctrl Pts',(30.3849139570494,1.46256729268532,27.4804410211816));
#46726=CARTESIAN_POINT('Ctrl Pts',(30.0007344874447,1.51254230178002,27.5003130592281));
#46727=CARTESIAN_POINT('Ctrl Pts',(29.8049569216954,1.49991645600797,27.5093863351468));
#46728=CARTESIAN_POINT('Ctrl Pts',(29.4253565109394,1.3996692288739,27.5304345136228));
#46729=CARTESIAN_POINT('Ctrl Pts',(29.245638701995,1.31157237616612,27.5415283255346));
#46730=CARTESIAN_POINT('Ctrl Pts',(28.9367683949736,1.07514318986943,27.562956332507));
#46731=CARTESIAN_POINT('Ctrl Pts',(28.8087599369318,0.93132448347984,27.5731101063824));
#46732=CARTESIAN_POINT('Ctrl Pts',(28.6094708234815,0.596592375009914,27.591996522448));
#46733=CARTESIAN_POINT('Ctrl Pts',(28.5427132787644,0.407261741609369,27.6023743476884));
#46734=CARTESIAN_POINT('Ctrl Pts',(28.4873635075659,0.0164898797776363,
27.624083895568));
#46735=CARTESIAN_POINT('Ctrl Pts',(28.4981279946982,-0.180903932406258,
27.6350502184671));
#46736=CARTESIAN_POINT('Ctrl Pts',(28.5934885065557,-0.554852956622451,
27.6558251642568));
#46737=CARTESIAN_POINT('Ctrl Pts',(28.6750314181996,-0.72841210507679,27.6648194223046));
#46738=CARTESIAN_POINT('Ctrl Pts',(28.9037835277885,-1.04301134033857,27.6845641309549));
#46739=CARTESIAN_POINT('Ctrl Pts',(29.0515807305306,-1.17900166318454,27.6954525361552));
#46740=CARTESIAN_POINT('Ctrl Pts',(29.3870321030576,-1.38265756586298,27.7172490562487));
#46741=CARTESIAN_POINT('Ctrl Pts',(29.570408592882,-1.45015060314336,27.7279465683201));
#46742=CARTESIAN_POINT('Ctrl Pts',(29.8405845073873,-1.49365112485936,27.7421537608929));
#46743=CARTESIAN_POINT('Ctrl Pts',(29.920314098353,-1.50000000000001,27.7461661102695));
#46744=CARTESIAN_POINT('Ctrl Pts',(30.,-1.50000000000001,27.75));
#46745=CARTESIAN_POINT('Ctrl Pts',(29.9999999999999,-1.50000000000001,27.8125));
#46746=CARTESIAN_POINT('Ctrl Pts',(29.9712572824709,-1.50000000000001,27.8111171153581));
#46747=CARTESIAN_POINT('Ctrl Pts',(29.9424874969812,-1.49917387170699,27.8097099804002));
#46748=CARTESIAN_POINT('Ctrl Pts',(29.7223735770152,-1.48649276547853,27.7987674915373));
#46749=CARTESIAN_POINT('Ctrl Pts',(29.5349257292356,-1.43889608772887,27.7884267728186));
#46750=CARTESIAN_POINT('Ctrl Pts',(29.1813453265204,-1.27257887490163,27.7667952051828));
#46751=CARTESIAN_POINT('Ctrl Pts',(29.0198117779222,-1.15277654761383,27.7556955762776));
#46752=CARTESIAN_POINT('Ctrl Pts',(28.7574522908629,-0.862041024530384,
27.7349968128188));
#46753=CARTESIAN_POINT('Ctrl Pts',(28.6572312223829,-0.695708343276581,
27.7261504635153));
#46754=CARTESIAN_POINT('Ctrl Pts',(28.524605736016,-0.332863036208749,27.7059923909005));
#46755=CARTESIAN_POINT('Ctrl Pts',(28.4939840388333,-0.139603136099824,
27.6952557297833));
#46756=CARTESIAN_POINT('Ctrl Pts',(28.508148989394,0.25282273238934,27.673454292645));
#46757=CARTESIAN_POINT('Ctrl Pts',(28.5547646373704,0.44816718663467,27.6626018229647));
#46758=CARTESIAN_POINT('Ctrl Pts',(28.7177569938957,0.801209312950165,27.6429883715028));
#46759=CARTESIAN_POINT('Ctrl Pts',(28.8294090431484,0.956981758536969,27.6339039237114));
#46760=CARTESIAN_POINT('Ctrl Pts',(29.1093968787388,1.22281551664853,27.6130487316321));
#46761=CARTESIAN_POINT('Ctrl Pts',(29.2767036270498,1.32864238149993,27.6020595468161));
#46762=CARTESIAN_POINT('Ctrl Pts',(29.6469534397504,1.47162694755714,27.5802741008953));
#46763=CARTESIAN_POINT('Ctrl Pts',(29.8468632228895,1.50560128622732,27.570023387908));
#46764=CARTESIAN_POINT('Ctrl Pts',(30.2385607914922,1.49319741260661,27.5508332778069));
#46765=CARTESIAN_POINT('Ctrl Pts',(30.4267058309758,1.45067195878526,27.540599882768));
#46766=CARTESIAN_POINT('Ctrl Pts',(30.7836729511717,1.29433057010809,27.5190824778378));
#46767=CARTESIAN_POINT('Ctrl Pts',(30.9479647504538,1.17932417828325,27.5079833629642));
#46768=CARTESIAN_POINT('Ctrl Pts',(31.2187102492265,0.89565657574078,27.4870774584548));
#46769=CARTESIAN_POINT('Ctrl Pts',(31.3239608540741,0.731149127851972,27.4781193959917));
#46770=CARTESIAN_POINT('Ctrl Pts',(31.4661242989034,0.37131396030254,27.4581285533501));
#46771=CARTESIAN_POINT('Ctrl Pts',(31.5017272578984,0.179429293592902,27.4474682940885));
#46772=CARTESIAN_POINT('Ctrl Pts',(31.4980926781097,-0.21275991516766,27.4256800047129));
#46773=CARTESIAN_POINT('Ctrl Pts',(31.4567210643059,-0.409304691427262,
27.4147608504762));
#46774=CARTESIAN_POINT('Ctrl Pts',(31.3031284414201,-0.766835781066652,
27.394898012163));
#46775=CARTESIAN_POINT('Ctrl Pts',(31.1955054411838,-0.925718941221814,
27.3859710339898));
#46776=CARTESIAN_POINT('Ctrl Pts',(30.9227930606553,-1.19862566676885,27.3652694110877));
#46777=CARTESIAN_POINT('Ctrl Pts',(30.75882230211,-1.30859982122977,27.354325526665));
#46778=CARTESIAN_POINT('Ctrl Pts',(30.3950972752779,-1.46060207029247,27.3326035134561));
#46779=CARTESIAN_POINT('Ctrl Pts',(30.198484714314,-1.4999999999587,27.3220496002711));
#46780=CARTESIAN_POINT('Ctrl Pts',(30.0000000003122,-1.50000000000001,27.312500000015));
#46781=CARTESIAN_POINT('Origin',(30.,-1.32966554433622E-14,16.));
#46782=CARTESIAN_POINT('',(30.,-1.50000000000001,26.75));
#46783=CARTESIAN_POINT('',(30.0000000000001,-1.50000000000001,26.8125));
#46784=CARTESIAN_POINT('',(30.,-1.50000000000001,16.));
#46785=CARTESIAN_POINT('Ctrl Pts',(29.9999999999999,-1.50000000000002,26.75));
#46786=CARTESIAN_POINT('Ctrl Pts',(30.1755630845093,-1.50000000000003,26.7584467828418));
#46787=CARTESIAN_POINT('Ctrl Pts',(30.3499584064833,-1.46918259215549,26.7676934207892));
#46788=CARTESIAN_POINT('Ctrl Pts',(30.6997034276012,-1.3412672085792,26.7880737410627));
#46789=CARTESIAN_POINT('Ctrl Pts',(30.8691431470038,-1.23821435243508,26.7990884927007));
#46790=CARTESIAN_POINT('Ctrl Pts',(31.1538803669515,-0.977054933639417,
26.8200423468827));
#46791=CARTESIAN_POINT('Ctrl Pts',(31.2681733329846,-0.823282264050392,
26.8292620964417));
#46792=CARTESIAN_POINT('Ctrl Pts',(31.4372326110993,-0.473197410553428,
26.8487112549693));
#46793=CARTESIAN_POINT('Ctrl Pts',(31.4872301101415,-0.278708237309613,
26.8595162090384));
#46794=CARTESIAN_POINT('Ctrl Pts',(31.5082331683214,0.113718878171538,26.881317715454));
#46795=CARTESIAN_POINT('Ctrl Pts',(31.4808674747884,0.307802550913579,26.8921001417175));
#46796=CARTESIAN_POINT('Ctrl Pts',(31.3544261384598,0.67256246632588,26.9123645814626));
#46797=CARTESIAN_POINT('Ctrl Pts',(31.2574072539999,0.840081862517357,26.9211719059107));
#46798=CARTESIAN_POINT('Ctrl Pts',(31.0004574791989,1.1352928844589,26.9417347138799));
#46799=CARTESIAN_POINT('Ctrl Pts',(30.8407636896231,1.25813738072432,26.9528303320317));
#46800=CARTESIAN_POINT('Ctrl Pts',(30.4894980147219,1.43081423936239,26.9745271891017));
#46801=CARTESIAN_POINT('Ctrl Pts',(30.302568408204,1.48165789304525,26.984933167702));
#46802=CARTESIAN_POINT('Ctrl Pts',(29.9140424353861,1.51051713966446,27.0044277780243));
#46803=CARTESIAN_POINT('Ctrl Pts',(29.7160053760103,1.48607476032932,27.0140505099305));
#46804=CARTESIAN_POINT('Ctrl Pts',(29.3413420123945,1.36197834203437,27.0355236321475));
#46805=CARTESIAN_POINT('Ctrl Pts',(29.1683424827117,1.26378814603618,27.0465745813446));
#46806=CARTESIAN_POINT('Ctrl Pts',(28.87548492057,1.01073104588063,27.0676940612658));
#46807=CARTESIAN_POINT('Ctrl Pts',(28.7566499301147,0.860326156686485,27.0772041024063));
#46808=CARTESIAN_POINT('Ctrl Pts',(28.5773390955292,0.515342682333064,27.0963698509815));
#46809=CARTESIAN_POINT('Ctrl Pts',(28.5216397715234,0.322442560698391,27.1070865244057));
#46810=CARTESIAN_POINT('Ctrl Pts',(28.4890218615652,-0.0697120082430973,
27.1288728893469));
#46811=CARTESIAN_POINT('Ctrl Pts',(28.510818362855,-0.265069960572926,27.1397261089208));
#46812=CARTESIAN_POINT('Ctrl Pts',(28.6267610927498,-0.633018179794785,
27.1601676766553));
#46813=CARTESIAN_POINT('Ctrl Pts',(28.7184387624141,-0.802555681667626,
27.1689674029211));
#46814=CARTESIAN_POINT('Ctrl Pts',(28.9662614123549,-1.10518359683465,27.1892971067025));
#46815=CARTESIAN_POINT('Ctrl Pts',(29.1227466839353,-1.23306866661795,27.2003783708913));
#46816=CARTESIAN_POINT('Ctrl Pts',(29.4698813680168,-1.416339226716,27.2221707450579));
#46817=CARTESIAN_POINT('Ctrl Pts',(29.6558172836666,-1.47261637710131,27.232679845148));
#46818=CARTESIAN_POINT('Ctrl Pts',(29.8981460836565,-1.49740948534734,27.2450275924248));
#46819=CARTESIAN_POINT('Ctrl Pts',(29.9491012405249,-1.5,27.247551132293));
#46820=CARTESIAN_POINT('Ctrl Pts',(29.9999999999998,-1.50000000000001,27.25));
#46821=CARTESIAN_POINT('Ctrl Pts',(30.0000000003122,-1.50000000000001,27.312500000015));
#46822=CARTESIAN_POINT('Ctrl Pts',(29.9998020603292,-1.50000000000005,27.3124904766232));
#46823=CARTESIAN_POINT('Ctrl Pts',(29.9996041185888,-1.49999996081992,27.3124809520584));
#46824=CARTESIAN_POINT('Ctrl Pts',(29.8088160951652,-1.49992443102837,27.3032995609518));
#46825=CARTESIAN_POINT('Ctrl Pts',(29.6200100906951,-1.46352575850992,27.2932045535897));
#46826=CARTESIAN_POINT('Ctrl Pts',(29.2593205849108,-1.31930644298838,27.2718447795537));
#46827=CARTESIAN_POINT('Ctrl Pts',(29.0918823606668,-1.21016636340677,27.2607572353565));
#46828=CARTESIAN_POINT('Ctrl Pts',(28.8110979291704,-0.935181294724627,
27.2396095139674));
#46829=CARTESIAN_POINT('Ctrl Pts',(28.6997118002275,-0.772848068745042,
27.2304360038192));
#46830=CARTESIAN_POINT('Ctrl Pts',(28.5461974612702,-0.416685157506792,
27.210649175417));
#46831=CARTESIAN_POINT('Ctrl Pts',(28.5047394765833,-0.226599155889903,
27.2000888419939));
#46832=CARTESIAN_POINT('Ctrl Pts',(28.4958539389935,0.166443777601294,27.1782531234666));
#46833=CARTESIAN_POINT('Ctrl Pts',(28.5315184967694,0.365700597221805,27.1671833001544));
#46834=CARTESIAN_POINT('Ctrl Pts',(28.6754701753172,0.729371435414476,27.1469793646992));
#46835=CARTESIAN_POINT('Ctrl Pts',(28.7788000491734,0.891648198610453,27.1381536711784));
#46836=CARTESIAN_POINT('Ctrl Pts',(29.0437345128306,1.17200464814443,27.1176193266989));
#46837=CARTESIAN_POINT('Ctrl Pts',(29.2040531543845,1.2862733419873,27.1067318620762));
#46838=CARTESIAN_POINT('Ctrl Pts',(29.5628324377282,1.44858368838945,27.0849614650246));
#46839=CARTESIAN_POINT('Ctrl Pts',(29.7584548095726,1.49371725552991,27.0742958690726));
#46840=CARTESIAN_POINT('Ctrl Pts',(30.1472060622831,1.50481186242553,27.055283882181));
#46841=CARTESIAN_POINT('Ctrl Pts',(30.3365600149074,1.47407427722924,27.045587089767));
#46842=CARTESIAN_POINT('Ctrl Pts',(30.7004989886168,1.34098519143669,27.0243801486806));
#46843=CARTESIAN_POINT('Ctrl Pts',(30.8706482413977,1.23730103012925,27.0133137233474));
#46844=CARTESIAN_POINT('Ctrl Pts',(31.1605713571455,0.970446090199086,26.991952153717));
#46845=CARTESIAN_POINT('Ctrl Pts',(31.2776619344983,0.810096307036669,26.9825053503909));
#46846=CARTESIAN_POINT('Ctrl Pts',(31.4414580755822,0.457344311316898,26.9629080172954));
#46847=CARTESIAN_POINT('Ctrl Pts',(31.4881418689773,0.269035150966863,26.9524463972759));
#46848=CARTESIAN_POINT('Ctrl Pts',(31.508284818313,-0.122458793694974,26.9306967336836));
#46849=CARTESIAN_POINT('Ctrl Pts',(31.478582774639,-0.322064434897177,26.9196075313946));
#46850=CARTESIAN_POINT('Ctrl Pts',(31.3455674834561,-0.689986184900448,
26.8991674341722));
#46851=CARTESIAN_POINT('Ctrl Pts',(31.246662212612,-0.855842984261559,26.8903733141072));
#46852=CARTESIAN_POINT('Ctrl Pts',(30.9897531567272,-1.14377092738595,26.8700147729728));
#46853=CARTESIAN_POINT('Ctrl Pts',(30.8332877383797,-1.26231706455743,26.8591938787678));
#46854=CARTESIAN_POINT('Ctrl Pts',(30.4799553603842,-1.43498001100993,26.8373979738484));
#46855=CARTESIAN_POINT('Ctrl Pts',(30.2857235516143,-1.48590367409306,26.8266384453951));
#46856=CARTESIAN_POINT('Ctrl Pts',(30.0581276265954,-1.49915605873645,26.8153201095514));
#46857=CARTESIAN_POINT('Ctrl Pts',(30.0290509426437,-1.50000000000001,26.8138977141296));
#46858=CARTESIAN_POINT('Ctrl Pts',(30.0000000000001,-1.50000000000001,26.8125));
#46859=CARTESIAN_POINT('Origin',(30.,-1.32966554433622E-14,16.));
#46860=CARTESIAN_POINT('',(30.,-1.50000000000001,26.25));
#46861=CARTESIAN_POINT('',(30.0000000000001,-1.50000000000001,26.3125));
#46862=CARTESIAN_POINT('',(30.,-1.50000000000001,16.));
#46863=CARTESIAN_POINT('Ctrl Pts',(30.,-1.50000000000001,26.25));
#46864=CARTESIAN_POINT('Ctrl Pts',(30.0056194401817,-1.50000000000001,26.2502703654418));
#46865=CARTESIAN_POINT('Ctrl Pts',(30.0112401600052,-1.49996842190559,26.2505416696197));
#46866=CARTESIAN_POINT('Ctrl Pts',(30.2156637559459,-1.49767029707552,26.2604408412659));
#46867=CARTESIAN_POINT('Ctrl Pts',(30.4120156853044,-1.45593401100177,26.2710471691517));
#46868=CARTESIAN_POINT('Ctrl Pts',(30.7738333695248,-1.29974623576057,26.2927936799124));
#46869=CARTESIAN_POINT('Ctrl Pts',(30.9363483004055,-1.18803068750778,26.3037158928437));
#46870=CARTESIAN_POINT('Ctrl Pts',(31.2059383925193,-0.91211987124096,26.3243507415389));
#46871=CARTESIAN_POINT('Ctrl Pts',(31.3118367658411,-0.751883140819906,
26.3332287143989));
#46872=CARTESIAN_POINT('Ctrl Pts',(31.4620725484111,-0.390717177178761,
26.3532934901568));
#46873=CARTESIAN_POINT('Ctrl Pts',(31.5011777050095,-0.191739563198423,
26.3643478020445));
#46874=CARTESIAN_POINT('Ctrl Pts',(31.4988144256802,0.202052743889533,26.3862251524383));
#46875=CARTESIAN_POINT('Ctrl Pts',(31.4603972352794,0.393097806012914,26.3968387670007));
#46876=CARTESIAN_POINT('Ctrl Pts',(31.3127984325509,0.751186708707084,26.4167325949282));
#46877=CARTESIAN_POINT('Ctrl Pts',(31.2046306350456,0.914654115967526,26.4257825736587));
#46878=CARTESIAN_POINT('Ctrl Pts',(30.929085340333,1.1942016269637,26.4468049614706));
#46879=CARTESIAN_POINT('Ctrl Pts',(30.763267624326,1.30642002708729,26.4579000478329));
#46880=CARTESIAN_POINT('Ctrl Pts',(30.4044749371868,1.4569895622401,26.479344956129));
#46881=CARTESIAN_POINT('Ctrl Pts',(30.2159899848526,1.49659297949806,26.4895135375502));
#46882=CARTESIAN_POINT('Ctrl Pts',(29.8264040657205,1.50311771775866,26.5084387415533));
#46883=CARTESIAN_POINT('Ctrl Pts',(29.6289313228251,1.46692091172634,26.5187719136178));
#46884=CARTESIAN_POINT('Ctrl Pts',(29.2622864534942,1.32066065000658,26.5404749081659));
#46885=CARTESIAN_POINT('Ctrl Pts',(29.0963152488665,1.21314636529189,26.5514467093804));
#46886=CARTESIAN_POINT('Ctrl Pts',(28.8192613253014,0.944447852152411,26.5722403200802));
#46887=CARTESIAN_POINT('Ctrl Pts',(28.7092361098565,0.787428080615722,26.5812539955214));
#46888=CARTESIAN_POINT('Ctrl Pts',(28.5500186537103,0.4325695152731,26.6009683602626));
#46889=CARTESIAN_POINT('Ctrl Pts',(28.5055087117716,0.236724815037938,26.6118486213868));
#46890=CARTESIAN_POINT('Ctrl Pts',(28.4955827399852,-0.155640049113208,
26.6336466693952));
#46891=CARTESIAN_POINT('Ctrl Pts',(28.5282144121142,-0.348361913823613,
26.6443534396569));
#46892=CARTESIAN_POINT('Ctrl Pts',(28.6646766132005,-0.710004687419899,
26.6644447048566));
#46893=CARTESIAN_POINT('Ctrl Pts',(28.7669073789545,-0.875602741749661,
26.6733284353239));
#46894=CARTESIAN_POINT('Ctrl Pts',(29.0326342692594,-1.16351957915387,26.6941109162225));
#46895=CARTESIAN_POINT('Ctrl Pts',(29.1952892767769,-1.28140768888904,26.7052113286353));
#46896=CARTESIAN_POINT('Ctrl Pts',(29.5502593863542,-1.44373597574174,26.7267989550745));
#46897=CARTESIAN_POINT('Ctrl Pts',(29.7380028348229,-1.48930167419739,26.7370974797965));
#46898=CARTESIAN_POINT('Ctrl Pts',(29.9528487018704,-1.49944465692866,26.7477160059146));
#46899=CARTESIAN_POINT('Ctrl Pts',(29.9764341399413,-1.50000000000001,26.7488661870293));
#46900=CARTESIAN_POINT('Ctrl Pts',(29.9999999999999,-1.50000000000001,26.75));
#46901=CARTESIAN_POINT('Ctrl Pts',(30.0000000000001,-1.50000000000001,26.8125));
#46902=CARTESIAN_POINT('Ctrl Pts',(29.8395800016776,-1.50000000000002,26.8047817892321));
#46903=CARTESIAN_POINT('Ctrl Pts',(29.6800130120943,-1.4742710204936,26.7963899249912));
#46904=CARTESIAN_POINT('Ctrl Pts',(29.3406580591605,-1.36160698346738,26.7769331456215));
#46905=CARTESIAN_POINT('Ctrl Pts',(29.1679496395237,-1.26348603655748,26.7658981260489));
#46906=CARTESIAN_POINT('Ctrl Pts',(28.8688888773426,-1.00499369846698,26.744329215695));
#46907=CARTESIAN_POINT('Ctrl Pts',(28.7459708502921,-0.846646295408431,
26.7345359053005));
#46908=CARTESIAN_POINT('Ctrl Pts',(28.5719299961441,-0.497373685523865,
26.7151318714181));
#46909=CARTESIAN_POINT('Ctrl Pts',(28.5201211210885,-0.310969647956289,
26.7047760915532));
#46910=CARTESIAN_POINT('Ctrl Pts',(28.4888763927518,0.078675171393689,26.6831291571448));
#46911=CARTESIAN_POINT('Ctrl Pts',(28.5126680280148,0.27845746343119,26.6720301409206));
#46912=CARTESIAN_POINT('Ctrl Pts',(28.6347687943924,0.650483449918004,26.6513620305602));
#46913=CARTESIAN_POINT('Ctrl Pts',(28.7293030467267,0.819946999855557,26.6425267967844));
#46914=CARTESIAN_POINT('Ctrl Pts',(28.9783004894773,1.11523286685495,26.62234451654));
#46915=CARTESIAN_POINT('Ctrl Pts',(29.1308905878018,1.23784103842587,26.6115972394678));
#46916=CARTESIAN_POINT('Ctrl Pts',(29.4786064716065,1.42045274911996,26.5897952036888));
#46917=CARTESIAN_POINT('Ctrl Pts',(29.671307799161,1.47699671076135,26.5789531911429));
#46918=CARTESIAN_POINT('Ctrl Pts',(30.058657983757,1.51083891985875,26.5593767353335));
#46919=CARTESIAN_POINT('Ctrl Pts',(30.2492918070221,1.49128918840572,26.5502639753537));
#46920=CARTESIAN_POINT('Ctrl Pts',(30.6191301716824,1.38027512961514,26.5293863948823));
#46921=CARTESIAN_POINT('Ctrl Pts',(30.7941362196709,1.2875659668366,26.518391157951));
#46922=CARTESIAN_POINT('Ctrl Pts',(31.1019229551517,1.03729505553015,26.4966307919773));
#46923=CARTESIAN_POINT('Ctrl Pts',(31.2305302882388,0.880892156398053,26.4864384531331));
#46924=CARTESIAN_POINT('Ctrl Pts',(31.4143329938993,0.535011347738905,26.467222852652));
#46925=CARTESIAN_POINT('Ctrl Pts',(31.4709425533457,0.350543024469619,26.4569746124704));
#46926=CARTESIAN_POINT('Ctrl Pts',(31.5126435249117,-0.0370627264893054,
26.4354409596394));
#46927=CARTESIAN_POINT('Ctrl Pts',(31.4944467514533,-0.236856679751601,
26.4243412955692));
#46928=CARTESIAN_POINT('Ctrl Pts',(31.382763240843,-0.612667143007661,26.4034629364995));
#46929=CARTESIAN_POINT('Ctrl Pts',(31.2923692914564,-0.785603738087747,
26.3945234871348));
#46930=CARTESIAN_POINT('Ctrl Pts',(31.0508333839059,-1.08773585408316,26.3745100265869));
#46931=CARTESIAN_POINT('Ctrl Pts',(30.9019600520426,-1.21403192877114,26.3638391307711));
#46932=CARTESIAN_POINT('Ctrl Pts',(30.559750929656,-1.4057831061822,26.3420481650989));
#46933=CARTESIAN_POINT('Ctrl Pts',(30.3686322762759,-1.46754077280931,26.3311374738613));
#46934=CARTESIAN_POINT('Ctrl Pts',(30.1141378164167,-1.49674664949133,26.3180818291001));
#46935=CARTESIAN_POINT('Ctrl Pts',(30.0570405412872,-1.50000000000001,26.3152443643222));
#46936=CARTESIAN_POINT('Ctrl Pts',(30.0000000000002,-1.50000000000001,26.3125));
#46937=CARTESIAN_POINT('Origin',(30.,-1.32966554433622E-14,16.));
#46938=CARTESIAN_POINT('',(30.0000000000001,-1.50000000000001,25.75));
#46939=CARTESIAN_POINT('',(30.,-1.50000000000001,25.8125));
#46940=CARTESIAN_POINT('',(30.,-1.50000000000001,16.));
#46941=CARTESIAN_POINT('Ctrl Pts',(30.0000000000002,-1.50000000000001,25.75));
#46942=CARTESIAN_POINT('Ctrl Pts',(30.0350308469701,-1.50000000000001,25.7516854224107));
#46943=CARTESIAN_POINT('Ctrl Pts',(30.0700958017757,-1.49877287551864,25.7534065726266));
#46944=CARTESIAN_POINT('Ctrl Pts',(30.3035194655511,-1.48237243734734,25.7650927416133));
#46945=CARTESIAN_POINT('Ctrl Pts',(30.4971388675202,-1.42911969045028,25.7758875024032));
#46946=CARTESIAN_POINT('Ctrl Pts',(30.848183508266,-1.2523218603483,25.7976881963921));
#46947=CARTESIAN_POINT('Ctrl Pts',(31.0030592952475,-1.13208157746957,25.8084796690252));
#46948=CARTESIAN_POINT('Ctrl Pts',(31.2567047166631,-0.841106936698577,
25.8287658189633));
#46949=CARTESIAN_POINT('Ctrl Pts',(31.3538096540821,-0.673770640691784,
25.8375682977395));
#46950=CARTESIAN_POINT('Ctrl Pts',(31.4823392304013,-0.304145984064151,
25.8581030008855));
#46951=CARTESIAN_POINT('Ctrl Pts',(31.5096068971125,-0.104447172132542,
25.8691973793261));
#46952=CARTESIAN_POINT('Ctrl Pts',(31.4848844296652,0.286323023183646,25.8909068346215));
#46953=CARTESIAN_POINT('Ctrl Pts',(31.4360830652788,0.473864860798067,25.9013258256));
#46954=CARTESIAN_POINT('Ctrl Pts',(31.2680746858178,0.825196096656156,25.9208442275921));
#46955=CARTESIAN_POINT('Ctrl Pts',(31.1486056539627,0.984726473310249,25.9304245311885));
#46956=CARTESIAN_POINT('Ctrl Pts',(30.8549287066094,1.24817526789042,25.9518720919776));
#46957=CARTESIAN_POINT('Ctrl Pts',(30.6837094772403,1.34958696185865,25.9629268724906));
#46958=CARTESIAN_POINT('Ctrl Pts',(30.3185036845909,1.47806545582453,25.9840666914365));
#46959=CARTESIAN_POINT('Ctrl Pts',(30.1289070957048,1.50647679352315,25.993618043535));
#46960=CARTESIAN_POINT('Ctrl Pts',(29.7404075656125,1.49068855536224,26.0127482980627));
#46961=CARTESIAN_POINT('Ctrl Pts',(29.545331017818,1.44318830470102,26.0234533742517));
#46962=CARTESIAN_POINT('Ctrl Pts',(29.188736991222,1.27663378618483,26.0452365267588));
#46963=CARTESIAN_POINT('Ctrl Pts',(29.0299764729631,1.16060540084053,26.056097906459));
#46964=CARTESIAN_POINT('Ctrl Pts',(28.7683079019703,0.877153943717209,26.0765610930375));
#46965=CARTESIAN_POINT('Ctrl Pts',(28.6667786145465,0.713430148276809,26.0853649917623));
#46966=CARTESIAN_POINT('Ctrl Pts',(28.5272614190292,0.348018884480366,26.1056656175288));
#46967=CARTESIAN_POINT('Ctrl Pts',(28.4940188142116,0.14859972255689,26.1167444598579));
#46968=CARTESIAN_POINT('Ctrl Pts',(28.5074840531687,-0.243852309362615,
26.1385473505201));
#46969=CARTESIAN_POINT('Ctrl Pts',(28.5510714566589,-0.433234122923729,
26.1490685623846));
#46970=CARTESIAN_POINT('Ctrl Pts',(28.7087569062828,-0.788023018123922,
26.1687790565624));
#46971=CARTESIAN_POINT('Ctrl Pts',(28.8224400778707,-0.949553940205162,
26.1780544535033));
#46972=CARTESIAN_POINT('Ctrl Pts',(29.1069273076436,-1.22127183449108,26.1992895710132));
#46973=CARTESIAN_POINT('Ctrl Pts',(29.2754819087647,-1.32821443027861,26.2103697857015));
#46974=CARTESIAN_POINT('Ctrl Pts',(29.6323103908041,-1.46593097223903,26.2313631635471));
#46975=CARTESIAN_POINT('Ctrl Pts',(29.8154198943914,-1.50000000000001,26.2411193855283));
#46976=CARTESIAN_POINT('Ctrl Pts',(30.,-1.50000000000001,26.25));
#46977=CARTESIAN_POINT('Ctrl Pts',(30.0000000000002,-1.50000000000001,26.3125));
#46978=CARTESIAN_POINT('Ctrl Pts',(29.867580258195,-1.50000000000001,26.3061289522019));
#46979=CARTESIAN_POINT('Ctrl Pts',(29.7355134428156,-1.48246999719879,26.299287940062));
#46980=CARTESIAN_POINT('Ctrl Pts',(29.4184023489971,-1.39643165750255,26.2816409715667));
#46981=CARTESIAN_POINT('Ctrl Pts',(29.2414246745114,-1.30875331188796,26.2706906196325));
#46982=CARTESIAN_POINT('Ctrl Pts',(28.9285790709285,-1.068455989113,26.2489639028796));
#46983=CARTESIAN_POINT('Ctrl Pts',(28.7965902868422,-0.917216536990246,
26.2384564742772));
#46984=CARTESIAN_POINT('Ctrl Pts',(28.6032774267936,-0.57923818308581,26.2196798990602));
#46985=CARTESIAN_POINT('Ctrl Pts',(28.5410496718181,-0.397228347537677,
26.2095682415298));
#46986=CARTESIAN_POINT('Ctrl Pts',(28.4870387262231,-0.0124011503103316,
26.1881889527949));
#46987=CARTESIAN_POINT('Ctrl Pts',(28.4986129287161,0.187210043596071,26.1770994420224));
#46988=CARTESIAN_POINT('Ctrl Pts',(28.5978341126594,0.567369358609899,26.1559794800772));
#46989=CARTESIAN_POINT('Ctrl Pts',(28.6833047820777,0.744501773375072,26.1468355900596));
#46990=CARTESIAN_POINT('Ctrl Pts',(28.9160253075989,1.05460577600707,26.1270248184819));
#46991=CARTESIAN_POINT('Ctrl Pts',(29.060441358732,1.18507685788338,26.1164524012633));
#46992=CARTESIAN_POINT('Ctrl Pts',(29.3972605323865,1.3881264388998,26.0946069150758));
#46993=CARTESIAN_POINT('Ctrl Pts',(29.5879874006837,1.45617711323181,26.0835402678372));
#46994=CARTESIAN_POINT('Ctrl Pts',(29.9751313819113,1.51185807000195,26.0633671011121));
#46995=CARTESIAN_POINT('Ctrl Pts',(30.1672228871666,1.50278877622694,26.0545319510962));
#46996=CARTESIAN_POINT('Ctrl Pts',(30.5421508905102,1.41213985662164,26.0339751935801));
#46997=CARTESIAN_POINT('Ctrl Pts',(30.7210278648892,1.32972839399854,26.0230797638426));
#46998=CARTESIAN_POINT('Ctrl Pts',(31.0401525812529,1.09890434445495,26.0013140896138));
#46999=CARTESIAN_POINT('Ctrl Pts',(31.1764827770535,0.951536572108244,25.9906613507783));
#47000=CARTESIAN_POINT('Ctrl Pts',(31.3792148041551,0.619604996410003,25.9716870800294));
#47001=CARTESIAN_POINT('Ctrl Pts',(31.4465937278795,0.439945368358781,25.9619414093531));
#47002=CARTESIAN_POINT('Ctrl Pts',(31.5118285637272,0.0578389075257285,
25.9407132726402));
#47003=CARTESIAN_POINT('Ctrl Pts',(31.5063115855957,-0.141417075009879,
25.9296434958327));
#47004=CARTESIAN_POINT('Ctrl Pts',(31.4186362556573,-0.525426994647723,
25.9083096114084));
#47005=CARTESIAN_POINT('Ctrl Pts',(31.3377111820022,-0.706481965554299,
25.8989028268757));
#47006=CARTESIAN_POINT('Ctrl Pts',(31.1130533652913,-1.0237694591265,25.8792804311414));
#47007=CARTESIAN_POINT('Ctrl Pts',(30.972766729538,-1.15788504149396,25.8688054543882));
#47008=CARTESIAN_POINT('Ctrl Pts',(30.6428698469895,-1.36991560346518,25.8470435453937));
#47009=CARTESIAN_POINT('Ctrl Pts',(30.4547968017865,-1.44330311864552,25.835956334699));
#47010=CARTESIAN_POINT('Ctrl Pts',(30.1725168697432,-1.4925627888959,25.8210068109627));
#47011=CARTESIAN_POINT('Ctrl Pts',(30.0862466800351,-1.50000000000001,25.8166495453279));
#47012=CARTESIAN_POINT('Ctrl Pts',(30.,-1.50000000000001,25.8125));
#47013=CARTESIAN_POINT('Origin',(30.,-1.32966554433622E-14,16.));
#47014=CARTESIAN_POINT('',(30.0000000000001,-1.50000000000001,25.25));
#47015=CARTESIAN_POINT('',(30.,-1.50000000000001,25.3125));
#47016=CARTESIAN_POINT('',(30.,-1.50000000000001,16.));
#47017=CARTESIAN_POINT('Ctrl Pts',(30.0000000000001,-1.50000000000001,25.25));
#47018=CARTESIAN_POINT('Ctrl Pts',(30.0627700539087,-1.50000000000001,25.2530200256268));
#47019=CARTESIAN_POINT('Ctrl Pts',(30.1255978857231,-1.49606031931736,25.2561522666689));
#47020=CARTESIAN_POINT('Ctrl Pts',(30.387395972516,-1.46296629655124,25.2696673114027));
#47021=CARTESIAN_POINT('Ctrl Pts',(30.5795743359629,-1.39800636679879,25.2807179397182));
#47022=CARTESIAN_POINT('Ctrl Pts',(30.9202426421314,-1.20018691165606,25.3026033361058));
#47023=CARTESIAN_POINT('Ctrl Pts',(31.0669765445057,-1.07185443274338,25.3132278653563));
#47024=CARTESIAN_POINT('Ctrl Pts',(31.3042648643842,-0.765865616588927,
25.3331440943071));
#47025=CARTESIAN_POINT('Ctrl Pts',(31.3922917557281,-0.59091969078094,25.3421711282901));
#47026=CARTESIAN_POINT('Ctrl Pts',(31.4979914701149,-0.212996523390812,
25.3631668598117));
#47027=CARTESIAN_POINT('Ctrl Pts',(31.5129981369395,-0.0132639168507718,
25.3742631157306));
#47028=CARTESIAN_POINT('Ctrl Pts',(31.4653583210385,0.373052959697002,25.3957251644277));
#47029=CARTESIAN_POINT('Ctrl Pts',(31.4060337226141,0.556359728684241,25.4059088738159));
#47030=CARTESIAN_POINT('Ctrl Pts',(31.2180258231604,0.89772836856045,25.4248737982534));
#47031=CARTESIAN_POINT('Ctrl Pts',(31.088460968798,1.05109657163312,25.4351618575451));
#47032=CARTESIAN_POINT('Ctrl Pts',(30.7792551558925,1.29659274113508,25.4568578671965));
#47033=CARTESIAN_POINT('Ctrl Pts',(30.6034030192283,1.3871914976091,25.4678351891908));
#47034=CARTESIAN_POINT('Ctrl Pts',(30.2324892526205,1.49400946706811,25.4886479519256));
#47035=CARTESIAN_POINT('Ctrl Pts',(30.0415773273281,1.51141487828139,25.4976825299541));
#47036=CARTESIAN_POINT('Ctrl Pts',(29.6545526771042,1.47316919187237,25.5173656422979));
#47037=CARTESIAN_POINT('Ctrl Pts',(29.4624963512885,1.41443679130397,25.5282374121534));
#47038=CARTESIAN_POINT('Ctrl Pts',(29.1170567587378,1.22797823527613,25.5500367866331));
#47039=CARTESIAN_POINT('Ctrl Pts',(28.9660123174462,1.10381260264269,25.560752961054));
#47040=CARTESIAN_POINT('Ctrl Pts',(28.7201314342041,0.805655980053721,25.5808650389699));
#47041=CARTESIAN_POINT('Ctrl Pts',(28.627324212077,0.634750626561539,25.5897360763022));
#47042=CARTESIAN_POINT('Ctrl Pts',(28.5095600205757,0.261132939276874,25.6104926144847));
#47043=CARTESIAN_POINT('Ctrl Pts',(28.4881034640454,0.0613273497745445,
25.6215929250126));
#47044=CARTESIAN_POINT('Ctrl Pts',(28.5237184917358,-0.327500650137204,
25.6431944805633));
#47045=CARTESIAN_POINT('Ctrl Pts',(28.57753700972,-0.513112472024964,25.6535062484459));
#47046=CARTESIAN_POINT('Ctrl Pts',(28.7556436240904,-0.860981573894074,
25.6728323096608));
#47047=CARTESIAN_POINT('Ctrl Pts',(28.8809148866478,-1.0185241445112,25.6827836630609));
#47048=CARTESIAN_POINT('Ctrl Pts',(29.1836083572217,-1.27362286430434,25.7044330850039));
#47049=CARTESIAN_POINT('Ctrl Pts',(29.357290902101,-1.3695025366285,25.7154527145718));
#47050=CARTESIAN_POINT('Ctrl Pts',(29.6920067607584,-1.47617903100382,25.7345199747848));
#47051=CARTESIAN_POINT('Ctrl Pts',(29.8456406050883,-1.50000000000001,25.7425733801496));
#47052=CARTESIAN_POINT('Ctrl Pts',(30.0000000000002,-1.50000000000001,25.75));
#47053=CARTESIAN_POINT('Ctrl Pts',(30.,-1.50000000000001,25.8125));
#47054=CARTESIAN_POINT('Ctrl Pts',(29.8958136711151,-1.50000000000001,25.8074873329144));
#47055=CARTESIAN_POINT('Ctrl Pts',(29.7916909834384,-1.4891476478018,25.80217627354));
#47056=CARTESIAN_POINT('Ctrl Pts',(29.4989680289332,-1.42717135574301,25.7863710701566));
#47057=CARTESIAN_POINT('Ctrl Pts',(29.3182929815531,-1.3502283271827,25.7755410315376));
#47058=CARTESIAN_POINT('Ctrl Pts',(28.9928896773701,-1.12927046795383,25.7537473394536));
#47059=CARTESIAN_POINT('Ctrl Pts',(28.8522264483536,-0.985982788210688,
25.7429994633659));
#47060=CARTESIAN_POINT('Ctrl Pts',(28.639853465626,-0.660351661724937,25.7237363544014));
#47061=CARTESIAN_POINT('Ctrl Pts',(28.5672444995779,-0.483012345456745,
25.714334019192));
#47062=CARTESIAN_POINT('Ctrl Pts',(28.4907135279836,-0.103874220197911,
25.6932707900109));
#47063=CARTESIAN_POINT('Ctrl Pts',(28.4901189594842,0.0948392876888842,
25.6822311506839));
#47064=CARTESIAN_POINT('Ctrl Pts',(28.5659791907661,0.482606924381713,25.660688504201));
#47065=CARTESIAN_POINT('Ctrl Pts',(28.6422553573453,0.667705397375409,25.6509438140946));
#47066=CARTESIAN_POINT('Ctrl Pts',(28.8587620723286,0.992152292410515,25.6315147161622));
#47067=CARTESIAN_POINT('Ctrl Pts',(28.9948328944551,1.12978254443193,25.6211449431241));
#47068=CARTESIAN_POINT('Ctrl Pts',(29.3175819275344,1.35056278988812,25.599483888434));
#47069=CARTESIAN_POINT('Ctrl Pts',(29.5028611462505,1.42918794783786,25.5883856057019));
#47070=CARTESIAN_POINT('Ctrl Pts',(29.8863465577115,1.507984767606,25.5677463546914));
#47071=CARTESIAN_POINT('Ctrl Pts',(30.0802506039983,1.51013051078303,25.5589203440921));
#47072=CARTESIAN_POINT('Ctrl Pts',(30.4601704571654,1.44079280620514,25.5387153942847));
#47073=CARTESIAN_POINT('Ctrl Pts',(30.6424548754516,1.36926262641685,25.5279582816823));
#47074=CARTESIAN_POINT('Ctrl Pts',(30.9737363815272,1.15817666999724,25.5061559940003));
#47075=CARTESIAN_POINT('Ctrl Pts',(31.118540202541,1.01903114337744,25.4953239633962));
#47076=CARTESIAN_POINT('Ctrl Pts',(31.3403349350297,0.699693252907024,25.4757823623965));
#47077=CARTESIAN_POINT('Ctrl Pts',(31.418072458882,0.524551989157358,25.4666417771753));
#47078=CARTESIAN_POINT('Ctrl Pts',(31.5054879258866,0.148377517280613,25.4457431954044));
#47079=CARTESIAN_POINT('Ctrl Pts',(31.5119666548414,-0.0496365545101339,
25.4347424136382));
#47080=CARTESIAN_POINT('Ctrl Pts',(31.4476607795272,-0.440895614279282,
25.4130057992066));
#47081=CARTESIAN_POINT('Ctrl Pts',(31.3759395541655,-0.629971074835861,
25.4028673928089));
#47082=CARTESIAN_POINT('Ctrl Pts',(31.1673112734267,-0.961240411187918,
25.383627833962));
#47083=CARTESIAN_POINT('Ctrl Pts',(31.0353453440586,-1.10210544227651,25.3733657026948));
#47084=CARTESIAN_POINT('Ctrl Pts',(30.7196295943324,-1.33102399282861,25.3518169729773));
#47085=CARTESIAN_POINT('Ctrl Pts',(30.5371475111052,-1.41455738295539,25.3407169277066));
#47086=CARTESIAN_POINT('Ctrl Pts',(30.2307882933611,-1.48667060842925,25.3239740678184));
#47087=CARTESIAN_POINT('Ctrl Pts',(30.1154677152456,-1.50000000000002,25.31805544304));
#47088=CARTESIAN_POINT('Ctrl Pts',(29.9999999999999,-1.50000000000001,25.3125));
#47089=CARTESIAN_POINT('Origin',(30.,-1.32966554433622E-14,16.));
#47090=CARTESIAN_POINT('',(30.,-1.50000000000001,24.75));
#47091=CARTESIAN_POINT('',(29.9999999999999,-1.50000000000001,24.8125));
#47092=CARTESIAN_POINT('',(30.,-1.50000000000001,16.));
#47093=CARTESIAN_POINT('Ctrl Pts',(30.,-1.50000000000001,24.75));
#47094=CARTESIAN_POINT('Ctrl Pts',(30.0924202028298,-1.50000000000002,24.7544465690819));
#47095=CARTESIAN_POINT('Ctrl Pts',(30.1848415762481,-1.49146009950343,24.759130413942));
#47096=CARTESIAN_POINT('Ctrl Pts',(30.4723479931102,-1.43762037173554,24.7744586208663));
#47097=CARTESIAN_POINT('Ctrl Pts',(30.6592834359903,-1.36205645668747,24.7855515541955));
#47098=CARTESIAN_POINT('Ctrl Pts',(30.9862537983022,-1.14638219357722,24.80727387484));
#47099=CARTESIAN_POINT('Ctrl Pts',(31.1248087259681,-1.01079850350159,24.8177063155187));
#47100=CARTESIAN_POINT('Ctrl Pts',(31.346109752526,-0.69055016576277,24.8372494532827));
#47101=CARTESIAN_POINT('Ctrl Pts',(31.4251274703691,-0.50783917665878,24.8467867124079));
#47102=CARTESIAN_POINT('Ctrl Pts',(31.5079543915197,-0.122264618516638,
24.8682075211936));
#47103=CARTESIAN_POINT('Ctrl Pts',(31.5109523526148,0.0767903025210503,
24.8792661279179));
#47104=CARTESIAN_POINT('Ctrl Pts',(31.441061251381,0.457686740875712,24.9004270411598));
#47105=CARTESIAN_POINT('Ctrl Pts',(31.3715371249325,0.636385044039808,24.9100225849775));
#47106=CARTESIAN_POINT('Ctrl Pts',(31.1648481820269,0.965747220324715,24.9291158607209));
#47107=CARTESIAN_POINT('Ctrl Pts',(31.0267283705006,1.11145999209774,24.939808730245));
#47108=CARTESIAN_POINT('Ctrl Pts',(30.7049953637051,1.33826413832451,24.9615882319247));
#47109=CARTESIAN_POINT('Ctrl Pts',(30.525362209954,1.41844022126688,24.9724579494792));
#47110=CARTESIAN_POINT('Ctrl Pts',(30.1493787440764,1.50469862427576,24.9929435291658));
#47111=CARTESIAN_POINT('Ctrl Pts',(29.9569371691124,1.5114809139774,25.00175294714));
#47112=CARTESIAN_POINT('Ctrl Pts',(29.5704977811955,1.45108059660786,25.0220233074535));
#47113=CARTESIAN_POINT('Ctrl Pts',(29.3808354910635,1.38084291684638,25.0330994853021));
#47114=CARTESIAN_POINT('Ctrl Pts',(29.0468101101847,1.17410520091496,25.0549130032641));
#47115=CARTESIAN_POINT('Ctrl Pts',(28.9040664949486,1.04213311105638,25.0654466500392));
#47116=CARTESIAN_POINT('Ctrl Pts',(28.6746221434491,0.72909790198446,25.0851812190219));
#47117=CARTESIAN_POINT('Ctrl Pts',(28.5909928953227,0.55038117737188,25.0944232679238));
#47118=CARTESIAN_POINT('Ctrl Pts',(28.496446216206,0.168641933616187,25.115631003688));
#47119=CARTESIAN_POINT('Ctrl Pts',(28.4873339658181,-0.0308466586561953,
25.1267137032587));
#47120=CARTESIAN_POINT('Ctrl Pts',(28.5459190178277,-0.414647584032544,
25.1480359768907));
#47121=CARTESIAN_POINT('Ctrl Pts',(28.6102581790788,-0.595692019972521,
25.1580163493537));
#47122=CARTESIAN_POINT('Ctrl Pts',(28.8073809961852,-0.931227827424643,
25.1768208644096));
#47123=CARTESIAN_POINT('Ctrl Pts',(28.9411488677475,-1.08089452062442,25.1874141822753));
#47124=CARTESIAN_POINT('Ctrl Pts',(29.2565034825196,-1.31734526046784,25.2091547643595));
#47125=CARTESIAN_POINT('Ctrl Pts',(29.4342658933141,-1.40290303357365,25.220083967145));
#47126=CARTESIAN_POINT('Ctrl Pts',(29.7466738861071,-1.48392560477994,25.2373653306843));
#47127=CARTESIAN_POINT('Ctrl Pts',(29.8731973879732,-1.50000000000001,25.2438992064844));
#47128=CARTESIAN_POINT('Ctrl Pts',(30.0000000000001,-1.50000000000001,25.25));
#47129=CARTESIAN_POINT('Ctrl Pts',(29.9999999999999,-1.50000000000001,25.3125));
#47130=CARTESIAN_POINT('Ctrl Pts',(29.9230963675565,-1.50000000000001,25.3087999722589));
#47131=CARTESIAN_POINT('Ctrl Pts',(29.8461434428577,-1.49408668250554,25.3049333141238));
#47132=CARTESIAN_POINT('Ctrl Pts',(29.5785997947569,-1.4525378268213,25.2909069794727));
#47133=CARTESIAN_POINT('Ctrl Pts',(29.394946779968,-1.38612426885289,25.2802261486243));
#47134=CARTESIAN_POINT('Ctrl Pts',(29.0584111434883,-1.1844646483524,25.2584329141398));
#47135=CARTESIAN_POINT('Ctrl Pts',(28.9098271705268,-1.04932739740415,25.2475303518813));
#47136=CARTESIAN_POINT('Ctrl Pts',(28.679224033866,-0.736002543967933,25.2277319851447));
#47137=CARTESIAN_POINT('Ctrl Pts',(28.5966653608253,-0.562858820299269,
25.218769934461));
#47138=CARTESIAN_POINT('Ctrl Pts',(28.4992036771274,-0.189506940379824,
25.1980281633544));
#47139=CARTESIAN_POINT('Ctrl Pts',(28.4873077258157,0.00770736323463039,
25.1870718131536));
#47140=CARTESIAN_POINT('Ctrl Pts',(28.5403428741226,0.398677937032776,25.1653512257204));
#47141=CARTESIAN_POINT('Ctrl Pts',(28.6059812891417,0.588385613614782,25.1548923783415));
#47142=CARTESIAN_POINT('Ctrl Pts',(28.8032229731553,0.924175534219124,25.1360750856002));
#47143=CARTESIAN_POINT('Ctrl Pts',(28.9302878616598,1.06867554049118,25.1259477842385));
#47144=CARTESIAN_POINT('Ctrl Pts',(29.2375170160562,1.30684882772379,25.1045502900104));
#47145=CARTESIAN_POINT('Ctrl Pts',(29.416566346389,1.39601031268743,25.0934590671725));
#47146=CARTESIAN_POINT('Ctrl Pts',(29.7956879290814,1.49872079338579,25.0723655026123));
#47147=CARTESIAN_POINT('Ctrl Pts',(29.9916913791595,1.51255777708596,25.0632485758478));
#47148=CARTESIAN_POINT('Ctrl Pts',(30.376338186137,1.46478286918679,25.0434151669436));
#47149=CARTESIAN_POINT('Ctrl Pts',(30.5613937867408,1.40429329778983,25.0328314093361));
#47150=CARTESIAN_POINT('Ctrl Pts',(30.9051019650582,1.2128519030953,25.0109769253773));
#47151=CARTESIAN_POINT('Ctrl Pts',(31.0589867932662,1.08110262857348,24.9999134360581));
#47152=CARTESIAN_POINT('Ctrl Pts',(31.2996601001576,0.7727813254929,24.9797695555402));
#47153=CARTESIAN_POINT('Ctrl Pts',(31.3872075591177,0.601637196257516,24.9709242886809));
#47154=CARTESIAN_POINT('Ctrl Pts',(31.4948659823167,0.231233394936456,24.9503462997187));
#47155=CARTESIAN_POINT('Ctrl Pts',(31.5122374051454,0.0349818838105959,
24.9394434379894));
#47156=CARTESIAN_POINT('Ctrl Pts',(31.4704629549247,-0.356714017311379,
24.9176825545938));
#47157=CARTESIAN_POINT('Ctrl Pts',(31.410306361987,-0.548240683911054,24.9070421842271));
#47158=CARTESIAN_POINT('Ctrl Pts',(31.2229499202263,-0.889130700933294,
24.8881038499482));
#47159=CARTESIAN_POINT('Ctrl Pts',(31.1004741653132,-1.03689935475768,24.8783104947773));
#47160=CARTESIAN_POINT('Ctrl Pts',(30.8011609016804,-1.28341012707365,24.8570622572132));
#47161=CARTESIAN_POINT('Ctrl Pts',(30.6254139659021,-1.37762857486559,24.8459894497178));
#47162=CARTESIAN_POINT('Ctrl Pts',(30.2947063232275,-1.4782094919839,24.8272843564766));
#47163=CARTESIAN_POINT('Ctrl Pts',(30.1476360382517,-1.50000000000004,24.8196031422022));
#47164=CARTESIAN_POINT('Ctrl Pts',(29.9999999999998,-1.50000000000001,24.8125));
#47165=CARTESIAN_POINT('Origin',(30.,-1.32966554433622E-14,16.));
#47166=CARTESIAN_POINT('',(30.,-1.50000000000001,24.25));
#47167=CARTESIAN_POINT('',(30.,-1.50000000000001,24.3125));
#47168=CARTESIAN_POINT('',(30.,-1.50000000000001,16.));
#47169=CARTESIAN_POINT('Ctrl Pts',(29.9999999999999,-1.50000000000001,24.25));
#47170=CARTESIAN_POINT('Ctrl Pts',(30.1233865336442,-1.50000000000002,24.2559364373678));
#47171=CARTESIAN_POINT('Ctrl Pts',(30.2465476489323,-1.48477988594364,24.2622848102359));
#47172=CARTESIAN_POINT('Ctrl Pts',(30.5591244259704,-1.40597165010196,24.2795127850953));
#47173=CARTESIAN_POINT('Ctrl Pts',(30.7400033595231,-1.31975922707827,24.2906101163719));
#47174=CARTESIAN_POINT('Ctrl Pts',(31.0517371878966,-1.08642473531537,24.3120899308425));
#47175=CARTESIAN_POINT('Ctrl Pts',(31.181396759577,-0.943819238764671,24.3222894436867));
#47176=CARTESIAN_POINT('Ctrl Pts',(31.3842738432636,-0.610977913754327,
24.341295964288));
#47177=CARTESIAN_POINT('Ctrl Pts',(31.4529950991553,-0.422325812949031,
24.3515374548362));
#47178=CARTESIAN_POINT('Ctrl Pts',(31.5124147536636,-0.0319347678693356,
24.3732258462295));
#47179=CARTESIAN_POINT('Ctrl Pts',(31.5036442008573,0.165759327603677,24.3842088515336));
#47180=CARTESIAN_POINT('Ctrl Pts',(31.4119825510711,0.540750850840327,24.4050417139356));
#47181=CARTESIAN_POINT('Ctrl Pts',(31.3322181025457,0.715044299742208,24.4140993016492));
#47182=CARTESIAN_POINT('Ctrl Pts',(31.106713322535,1.03186525150623,24.4337494874295));
#47183=CARTESIAN_POINT('Ctrl Pts',(30.9603062459911,1.1693383575936,24.4446121985753));
#47184=CARTESIAN_POINT('Ctrl Pts',(30.6267827077052,1.37647673516795,24.4664127011144));
#47185=CARTESIAN_POINT('Ctrl Pts',(30.4439056234701,1.4458581458551,24.47713864034));
#47186=CARTESIAN_POINT('Ctrl Pts',(30.0630400763872,1.51099956140736,24.4972725262831));
#47187=CARTESIAN_POINT('Ctrl Pts',(29.8687484810349,1.50660828894347,24.5061312780688));
#47188=CARTESIAN_POINT('Ctrl Pts',(29.4860566158504,1.4231980920111,24.526860498932));
#47189=CARTESIAN_POINT('Ctrl Pts',(29.3019333862064,1.34250650777999,24.5379605648438));
#47190=CARTESIAN_POINT('Ctrl Pts',(28.9821049580114,1.11829253966791,24.5595764830508));
#47191=CARTESIAN_POINT('Ctrl Pts',(28.8477437066725,0.979293286040407,24.5699020321484));
#47192=CARTESIAN_POINT('Ctrl Pts',(28.6345240475922,0.651988290747904,24.5892523732038));
#47193=CARTESIAN_POINT('Ctrl Pts',(28.5601403785395,0.465238374198666,24.5991534236556));
#47194=CARTESIAN_POINT('Ctrl Pts',(28.489084947481,0.0759965520384366,24.6207779693312));
#47195=CARTESIAN_POINT('Ctrl Pts',(28.4921379080883,-0.122445995567395,
24.6318025553093));
#47196=CARTESIAN_POINT('Ctrl Pts',(28.5732141775453,-0.500358663169468,
24.6527977035094));
#47197=CARTESIAN_POINT('Ctrl Pts',(28.6479534934179,-0.676775662247645,
24.662082289407));
#47198=CARTESIAN_POINT('Ctrl Pts',(28.8642453292122,-0.999806026462223,
24.6814617008812));
#47199=CARTESIAN_POINT('Ctrl Pts',(29.0066425215227,-1.1413892524153,24.6922456563782));
#47200=CARTESIAN_POINT('Ctrl Pts',(29.3345224631394,-1.35826808429126,24.7140451994209));
#47201=CARTESIAN_POINT('Ctrl Pts',(29.515884916708,-1.43296761407463,24.7248459914751));
#47202=CARTESIAN_POINT('Ctrl Pts',(29.8033393621129,-1.4903304156034,24.7402695610815));
#47203=CARTESIAN_POINT('Ctrl Pts',(29.901655948172,-1.50000000000001,24.7452684196003));
#47204=CARTESIAN_POINT('Ctrl Pts',(30.,-1.50000000000001,24.75));
#47205=CARTESIAN_POINT('Ctrl Pts',(29.9999999999998,-1.50000000000001,24.8125));
#47206=CARTESIAN_POINT('Ctrl Pts',(29.9520844763832,-1.50000000000001,24.8101946632951));
#47207=CARTESIAN_POINT('Ctrl Pts',(29.9041155058213,-1.49770423456202,24.8078229838607));
#47208=CARTESIAN_POINT('Ctrl Pts',(29.6647429412583,-1.47465918202179,24.7956660256301));
#47209=CARTESIAN_POINT('Ctrl Pts',(29.4785801635781,-1.4195491435244,24.7851784304102));
#47210=CARTESIAN_POINT('Ctrl Pts',(29.1305308217309,-1.23854895841351,24.7634051157232));
#47211=CARTESIAN_POINT('Ctrl Pts',(28.9733425780824,-1.11174127780071,24.752319957252));
#47212=CARTESIAN_POINT('Ctrl Pts',(28.7235507953419,-0.81069913235786,24.7319395626836));
#47213=CARTESIAN_POINT('Ctrl Pts',(28.6307275649839,-0.641599855569549,
24.7231444364205));
#47214=CARTESIAN_POINT('Ctrl Pts',(28.5125127288929,-0.274334472746556,
24.7027408040415));
#47215=CARTESIAN_POINT('Ctrl Pts',(28.4895069858667,-0.0792389156648355,
24.6919021619814));
#47216=CARTESIAN_POINT('Ctrl Pts',(28.5196116095794,0.313003938746328,24.6701108922919));
#47217=CARTESIAN_POINT('Ctrl Pts',(28.5740816740222,0.506262436197778,24.6593743091001));
#47218=CARTESIAN_POINT('Ctrl Pts',(28.7511791399573,0.852358280491469,24.640146762195));
#47219=CARTESIAN_POINT('Ctrl Pts',(28.8690245914396,1.00348928998653,24.630706043882));
#47220=CARTESIAN_POINT('Ctrl Pts',(29.1601188576535,1.25831795738381,24.6096221903744));
#47221=CARTESIAN_POINT('Ctrl Pts',(29.3323550489326,1.35757677634782,24.5985782833421));
#47222=CARTESIAN_POINT('Ctrl Pts',(29.7064392762191,1.4842685830248,24.577060930713));
#47223=CARTESIAN_POINT('Ctrl Pts',(29.9047304118308,1.51001063736079,24.5673617334579));
#47224=CARTESIAN_POINT('Ctrl Pts',(30.2937060245362,1.48342562743484,24.547908663068));
#47225=CARTESIAN_POINT('Ctrl Pts',(30.4808263548115,1.43373651283452,24.5375255787967));
#47226=CARTESIAN_POINT('Ctrl Pts',(30.8329282215013,1.26331849859809,24.5158512361083));
#47227=CARTESIAN_POINT('Ctrl Pts',(30.9932828024692,1.14155315563778,24.5047538020966));
#47228=CARTESIAN_POINT('Ctrl Pts',(31.2521599269974,0.847929325410954,24.4841423531291));
#47229=CARTESIAN_POINT('Ctrl Pts',(31.3503160471837,0.680833771104865,24.4753240983947));
#47230=CARTESIAN_POINT('Ctrl Pts',(31.4789636487266,0.316753550496772,24.455097419472));
#47231=CARTESIAN_POINT('Ctrl Pts',(31.5074931621648,0.122957581810777,24.4443309767673));
#47232=CARTESIAN_POINT('Ctrl Pts',(31.4889302469637,-0.269482846800126,
24.4225287307333));
#47233=CARTESIAN_POINT('Ctrl Pts',(31.4401374224707,-0.464284058469581,
24.4117064411961));
#47234=CARTESIAN_POINT('Ctrl Pts',(31.2732400969951,-0.815428064678723,
24.3921984408512));
#47235=CARTESIAN_POINT('Ctrl Pts',(31.1598920572171,-0.96991270557316,24.3830299796895));
#47236=CARTESIAN_POINT('Ctrl Pts',(30.8768520990815,-1.23274788918355,24.3621112360319));
#47237=CARTESIAN_POINT('Ctrl Pts',(30.7081704356177,-1.33679806788068,24.351105252973));
#47238=CARTESIAN_POINT('Ctrl Pts',(30.3563528915165,-1.46803396077468,24.330532982021));
#47239=CARTESIAN_POINT('Ctrl Pts',(30.1788031709794,-1.50000000000002,24.3211026715747));
#47240=CARTESIAN_POINT('Ctrl Pts',(29.9999999999999,-1.50000000000001,24.3125));
#47241=CARTESIAN_POINT('Origin',(30.,-1.32966554433622E-14,16.));
#47242=CARTESIAN_POINT('',(29.9999999999999,-1.50000000000001,23.75));
#47243=CARTESIAN_POINT('',(30.,-1.50000000000001,23.8125));
#47244=CARTESIAN_POINT('',(30.,-1.50000000000001,16.));
#47245=CARTESIAN_POINT('Ctrl Pts',(29.9999999999998,-1.50000000000001,23.75));
#47246=CARTESIAN_POINT('Ctrl Pts',(30.1539214445734,-1.50000000000004,23.7574055489549));
#47247=CARTESIAN_POINT('Ctrl Pts',(30.3071622224275,-1.47631426128188,23.7654362865035));
#47248=CARTESIAN_POINT('Ctrl Pts',(30.6423330661034,-1.36978679250727,23.7845212975935));
#47249=CARTESIAN_POINT('Ctrl Pts',(30.8166966283757,-1.27354330571266,23.7955837985834));
#47250=CARTESIAN_POINT('Ctrl Pts',(31.1127372375018,-1.02370190976136,23.8167670978074));
#47251=CARTESIAN_POINT('Ctrl Pts',(31.2333636655921,-0.874601042154043,
23.8264110532137));
#47252=CARTESIAN_POINT('Ctrl Pts',(31.4166526755054,-0.531631844802988,
23.8454648975109));
#47253=CARTESIAN_POINT('Ctrl Pts',(31.4745582697856,-0.339396978512901,
23.8561446123048));
#47254=CARTESIAN_POINT('Ctrl Pts',(31.511699941184,0.0525578729813968,23.8779198818323));
#47255=CARTESIAN_POINT('Ctrl Pts',(31.4920858025539,0.248369535334408,23.8887983075186));
#47256=CARTESIAN_POINT('Ctrl Pts',(31.3802343334373,0.617537171179423,23.909307620621));
#47257=CARTESIAN_POINT('Ctrl Pts',(31.2906053859832,0.78786629286171,23.9181242275504));
#47258=CARTESIAN_POINT('Ctrl Pts',(31.0463195284336,1.0933231170364,23.9383623481344));
#47259=CARTESIAN_POINT('Ctrl Pts',(30.8911113639651,1.22312916938911,23.9494355281055));
#47260=CARTESIAN_POINT('Ctrl Pts',(30.5456512461468,1.41045613992281,23.9712600127329));
#47261=CARTESIAN_POINT('Ctrl Pts',(30.3601397930707,1.4688221637187,23.9818067151192));
#47262=CARTESIAN_POINT('Ctrl Pts',(29.9746198000426,1.51244309002935,24.0015667468295));
#47263=CARTESIAN_POINT('Ctrl Pts',(29.7781833324316,1.4963071428617,24.0107747387592));
#47264=CARTESIAN_POINT('Ctrl Pts',(29.3999877237922,1.38893180194388,24.0319533318226));
#47265=CARTESIAN_POINT('Ctrl Pts',(29.222220687541,1.29776778429998,24.0430384861654));
#47266=CARTESIAN_POINT('Ctrl Pts',(28.9180417312452,1.05625627096343,24.0643819561719));
#47267=CARTESIAN_POINT('Ctrl Pts',(28.7928010889864,0.910453809129913,24.0744192328261));
#47268=CARTESIAN_POINT('Ctrl Pts',(28.5994385143727,0.572669994103534,24.0931850003275));
#47269=CARTESIAN_POINT('Ctrl Pts',(28.5359684061524,0.382240685005912,24.1037644063885));
#47270=CARTESIAN_POINT('Ctrl Pts',(28.4873420883061,-0.00897112678811804,
24.1254983959326));
#47271=CARTESIAN_POINT('Ctrl Pts',(28.5013820601517,-0.205827079960202,
24.1364348377755));
#47272=CARTESIAN_POINT('Ctrl Pts',(28.6028303892674,-0.578036208077185,
24.1571131226709));
#47273=CARTESIAN_POINT('Ctrl Pts',(28.6873275910153,-0.750394994115161,
24.1660216580016));
#47274=CARTESIAN_POINT('Ctrl Pts',(28.922674074919,-1.0628953635868,24.1860253368065));
#47275=CARTESIAN_POINT('Ctrl Pts',(29.0745736829203,-1.19747470970914,24.197071925274));
#47276=CARTESIAN_POINT('Ctrl Pts',(29.4156235588556,-1.39492862582615,24.2189655260838));
#47277=CARTESIAN_POINT('Ctrl Pts',(29.5999664963488,-1.45853020454807,24.2296014403193));
#47278=CARTESIAN_POINT('Ctrl Pts',(29.8606029709014,-1.49514680076604,24.2431584462207));
#47279=CARTESIAN_POINT('Ctrl Pts',(29.9303308703141,-1.50000000000001,24.2466480424351));
#47280=CARTESIAN_POINT('Ctrl Pts',(29.9999999999999,-1.50000000000001,24.25));
#47281=CARTESIAN_POINT('Ctrl Pts',(29.9999999999999,-1.50000000000001,24.3125));
#47282=CARTESIAN_POINT('Ctrl Pts',(29.9792133017942,-1.50000000000001,24.3114998995163));
#47283=CARTESIAN_POINT('Ctrl Pts',(29.9584107993835,-1.49956791710601,24.3104870363498));
#47284=CARTESIAN_POINT('Ctrl Pts',(29.7464034347025,-1.4907415866322,24.3000416514142));
#47285=CARTESIAN_POINT('Ctrl Pts',(29.5585103106211,-1.44626636462019,24.2897662164333));
#47286=CARTESIAN_POINT('Ctrl Pts',(29.2028124426411,-1.28608329400307,24.2682031650416));
#47287=CARTESIAN_POINT('Ctrl Pts',(29.0395645726164,-1.16922656097766,24.2571028778712));
#47288=CARTESIAN_POINT('Ctrl Pts',(28.7720346147835,-0.882829614311603,
24.2362758660328));
#47289=CARTESIAN_POINT('Ctrl Pts',(28.6687223598358,-0.717623891574991,
24.2273679939764));
#47290=CARTESIAN_POINT('Ctrl Pts',(28.5302095932634,-0.356628416668571,
24.2073126898149));
#47291=CARTESIAN_POINT('Ctrl Pts',(28.4965070465723,-0.164202501526158,
24.1966223611959));
#47292=CARTESIAN_POINT('Ctrl Pts',(28.504169008249,0.22811087427228,24.1748271736516));
#47293=CARTESIAN_POINT('Ctrl Pts',(28.547551398078,0.424213342298486,24.1639325920946));
#47294=CARTESIAN_POINT('Ctrl Pts',(28.7047478969298,0.780036844220854,24.1441646197656));
#47295=CARTESIAN_POINT('Ctrl Pts',(28.8139070776359,0.937725434330763,24.1351846602695));
#47296=CARTESIAN_POINT('Ctrl Pts',(29.089396967151,1.20794416549895,24.1144240709145));
#47297=CARTESIAN_POINT('Ctrl Pts',(29.2546507832928,1.31634974323744,24.10346202693));
#47298=CARTESIAN_POINT('Ctrl Pts',(29.6203184116569,1.46471395475137,24.0817476068599));
#47299=CARTESIAN_POINT('Ctrl Pts',(29.817562104219,1.50206749812624,24.0713349778568));
#47300=CARTESIAN_POINT('Ctrl Pts',(30.2070481745296,1.49784204922514,24.0524784469813));
#47301=CARTESIAN_POINT('Ctrl Pts',(30.3956551706626,1.45939464529562,24.0423361052064));
#47302=CARTESIAN_POINT('Ctrl Pts',(30.7551447714595,1.31111335433136,24.0209212289748));
#47303=CARTESIAN_POINT('Ctrl Pts',(30.9215534250012,1.20000288285394,24.0098284869129));
#47304=CARTESIAN_POINT('Ctrl Pts',(31.1989915137811,0.922095691461922,23.9887605964375));
#47305=CARTESIAN_POINT('Ctrl Pts',(31.3083178283937,0.759038041694919,23.9796687800942));
#47306=CARTESIAN_POINT('Ctrl Pts',(31.4580557742773,0.401642541393168,23.9598134745218));
#47307=CARTESIAN_POINT('Ctrl Pts',(31.4975752946798,0.210938880716583,23.9492188267065));
#47308=CARTESIAN_POINT('Ctrl Pts',(31.5023006219625,-0.182594498957542,
23.927355861169));
#47309=CARTESIAN_POINT('Ctrl Pts',(31.4644403140633,-0.381679718202,23.916295571211));
#47310=CARTESIAN_POINT('Ctrl Pts',(31.3164762945118,-0.74375638752885,23.8961802006929));
#47311=CARTESIAN_POINT('Ctrl Pts',(31.2115088567194,-0.904729197971778,
23.8873240471024));
#47312=CARTESIAN_POINT('Ctrl Pts',(30.9436055459159,-1.18225533242814,23.8667254837612));
#47313=CARTESIAN_POINT('Ctrl Pts',(30.7818828902994,-1.29490194314203,23.8558155263452));
#47314=CARTESIAN_POINT('Ctrl Pts',(30.4211554702292,-1.45331769745592,23.8340595826352));
#47315=CARTESIAN_POINT('Ctrl Pts',(30.225061216149,-1.49628795964726,23.8234313750427));
#47316=CARTESIAN_POINT('Ctrl Pts',(30.01751075903,-1.49992336974507,23.8133446154048));
#47317=CARTESIAN_POINT('Ctrl Pts',(30.0087538759465,-1.50000000000001,23.8129211710528));
#47318=CARTESIAN_POINT('Ctrl Pts',(30.,-1.50000000000001,23.8125));
#47319=CARTESIAN_POINT('Origin',(30.,-1.32966554433622E-14,16.));
#47320=CARTESIAN_POINT('',(30.,-1.50000000000001,23.25));
#47321=CARTESIAN_POINT('',(30.0000000000001,-1.50000000000001,23.3125));
#47322=CARTESIAN_POINT('',(30.,-1.50000000000001,16.));
#47323=CARTESIAN_POINT('Ctrl Pts',(30.,-1.50000000000001,23.25));
#47324=CARTESIAN_POINT('Ctrl Pts',(30.1848807806478,-1.50000000000001,23.2588950807062));
#47325=CARTESIAN_POINT('Ctrl Pts',(30.3682821495602,-1.46581977714696,23.268668433817));
#47326=CARTESIAN_POINT('Ctrl Pts',(30.7253175152828,-1.32777981441322,23.2896807492688));
#47327=CARTESIAN_POINT('Ctrl Pts',(30.8938177244611,-1.22072861570022,23.3007613637715));
#47328=CARTESIAN_POINT('Ctrl Pts',(31.17812266521,-0.948849031570725,23.3219922022812));
#47329=CARTESIAN_POINT('Ctrl Pts',(31.2916923057403,-0.787278580688064,
23.3312623010729));
#47330=CARTESIAN_POINT('Ctrl Pts',(31.4491725851422,-0.432421790169133,
23.3509765672128));
#47331=CARTESIAN_POINT('Ctrl Pts',(31.4926555401856,-0.243004803835009,
23.3614997331203));
#47332=CARTESIAN_POINT('Ctrl Pts',(31.5058959055076,0.149477495401521,23.3833043053001));
#47333=CARTESIAN_POINT('Ctrl Pts',(31.4725342594551,0.348889338242185,23.3943827410135));
#47334=CARTESIAN_POINT('Ctrl Pts',(31.3327988700423,0.714215497781599,23.4146786387656));
#47335=CARTESIAN_POINT('Ctrl Pts',(31.2311812032015,0.877867947558743,23.4234833208414));
#47336=CARTESIAN_POINT('Ctrl Pts',(30.9693523131294,1.16116792111582,23.4439500128983));
#47337=CARTESIAN_POINT('Ctrl Pts',(30.8105149834806,1.27711053175663,23.4548127055575));
#47338=CARTESIAN_POINT('Ctrl Pts',(30.4538126686857,1.44345770015622,23.4765953083576));
#47339=CARTESIAN_POINT('Ctrl Pts',(30.2587086794859,1.49084210066152,23.487298486762));
#47340=CARTESIAN_POINT('Ctrl Pts',(29.8701963712835,1.50640033026212,23.5064229669502));
#47341=CARTESIAN_POINT('Ctrl Pts',(29.6806119299331,1.47787523708767,23.5159811423084));
#47342=CARTESIAN_POINT('Ctrl Pts',(29.3158918902727,1.34932104216597,23.5370996932649));
#47343=CARTESIAN_POINT('Ctrl Pts',(29.1450773397405,1.24811033609704,23.5481294207781));
#47344=CARTESIAN_POINT('Ctrl Pts',(28.8572342555358,0.990033097118328,23.5691470898178));
#47345=CARTESIAN_POINT('Ctrl Pts',(28.741208429162,0.837555866674711,23.578469118518));
#47346=CARTESIAN_POINT('Ctrl Pts',(28.5682103547001,0.489415671302002,23.5978102404832));
#47347=CARTESIAN_POINT('Ctrl Pts',(28.5160198061383,0.295515658346084,23.6085824634252));
#47348=CARTESIAN_POINT('Ctrl Pts',(28.4905622848027,-0.0968477988030621,
23.6303804332668));
#47349=CARTESIAN_POINT('Ctrl Pts',(28.5157978904665,-0.291438773395986,
23.6411910429664));
#47350=CARTESIAN_POINT('Ctrl Pts',(28.6382130227664,-0.657431308298791,
23.6615239615721));
#47351=CARTESIAN_POINT('Ctrl Pts',(28.733169022031,-0.825722839750627,23.6703196450362));
#47352=CARTESIAN_POINT('Ctrl Pts',(28.9866100524997,-1.12380536152502,23.6907934023492));
#47353=CARTESIAN_POINT('Ctrl Pts',(29.1450855427347,-1.24860164286396,23.7018846212987));
#47354=CARTESIAN_POINT('Ctrl Pts',(29.4947960835532,-1.42537206508902,23.723620367045));
#47355=CARTESIAN_POINT('Ctrl Pts',(29.6813612118254,-1.47831159941945,23.7340670285844));
#47356=CARTESIAN_POINT('Ctrl Pts',(29.9152096611065,-1.49820471212254,23.7458706538102));
#47357=CARTESIAN_POINT('Ctrl Pts',(29.957628226374,-1.50000000000001,23.7479613870909));
#47358=CARTESIAN_POINT('Ctrl Pts',(29.9999999999998,-1.50000000000001,23.75));
#47359=CARTESIAN_POINT('Ctrl Pts',(30.,-1.50000000000001,23.8125));
#47360=CARTESIAN_POINT('Ctrl Pts',(29.8186899108673,-1.50000000000001,23.8037767142694));
#47361=CARTESIAN_POINT('Ctrl Pts',(29.6387564217711,-1.46712852254306,23.7942065636429));
#47362=CARTESIAN_POINT('Ctrl Pts',(29.284195027604,-1.33291119731626,23.7734194615783));
#47363=CARTESIAN_POINT('Ctrl Pts',(29.1150531352934,-1.22715164870581,23.762343853251));
#47364=CARTESIAN_POINT('Ctrl Pts',(28.8285848658366,-0.957196675383623,
23.7410623929517));
#47365=CARTESIAN_POINT('Ctrl Pts',(28.713664846415,-0.796095622176884,23.7317275345654));
#47366=CARTESIAN_POINT('Ctrl Pts',(28.5537507892143,-0.442046290271719,
23.7120581272374));
#47367=CARTESIAN_POINT('Ctrl Pts',(28.50903084701,-0.253050072432249,23.7015583373574));
#47368=CARTESIAN_POINT('Ctrl Pts',(28.493125704307,0.139065210502765,23.6797741549721));
#47369=CARTESIAN_POINT('Ctrl Pts',(28.5250759127101,0.338559440554235,23.6686911421915));
#47370=CARTESIAN_POINT('Ctrl Pts',(28.6622225705316,0.704891738980156,23.6483393478345));
#47371=CARTESIAN_POINT('Ctrl Pts',(28.7627930544851,0.869391639366899,23.6395420458263));
#47372=CARTESIAN_POINT('Ctrl Pts',(29.0227223626785,1.15448356589741,23.6191169709735));
#47373=CARTESIAN_POINT('Ctrl Pts',(29.1806474642266,1.27143845898823,23.6082700489523));
#47374=CARTESIAN_POINT('Ctrl Pts',(29.5360600403599,1.4402358268239,23.5864814376371));
#47375=CARTESIAN_POINT('Ctrl Pts',(29.7308346201,1.48899068833401,23.5757560395914));
#47376=CARTESIAN_POINT('Ctrl Pts',(30.1191927262396,1.50727161649964,23.5565633479378));
#47377=CARTESIAN_POINT('Ctrl Pts',(30.3089226794933,1.48009155403507,23.5470839383266));
#47378=CARTESIAN_POINT('Ctrl Pts',(30.6746275130695,1.35410584970156,23.5259893534154));
#47379=CARTESIAN_POINT('Ctrl Pts',(30.8462644331352,1.25401826984556,23.5149512576394));
#47380=CARTESIAN_POINT('Ctrl Pts',(31.1359831388577,0.997812339501797,23.4938953285128));
#47381=CARTESIAN_POINT('Ctrl Pts',(31.2530579642409,0.846112941875841,23.4845062745487));
#47382=CARTESIAN_POINT('Ctrl Pts',(31.4284239202414,0.499151075957345,23.465230615331));
#47383=CARTESIAN_POINT('Ctrl Pts',(31.4819315716114,0.305618089705,23.4544787827614));
#47384=CARTESIAN_POINT('Ctrl Pts',(31.5100720569101,-0.086682490418841,
23.4326843060879));
#47385=CARTESIAN_POINT('Ctrl Pts',(31.4861228872238,-0.281567854400411,
23.4218573414222));
#47386=CARTESIAN_POINT('Ctrl Pts',(31.3661326726942,-0.648296896097567,
23.4014835057724));
#47387=CARTESIAN_POINT('Ctrl Pts',(31.2724103712455,-0.817054396960877,
23.3926895837254));
#47388=CARTESIAN_POINT('Ctrl Pts',(31.0210775409326,-1.11685004948265,23.3722696702745));
#47389=CARTESIAN_POINT('Ctrl Pts',(30.8633432283804,-1.24281066274781,23.3611817686994));
#47390=CARTESIAN_POINT('Ctrl Pts',(30.5145869816219,-1.42202815813894,23.3394239621929));
#47391=CARTESIAN_POINT('Ctrl Pts',(30.3282514191413,-1.47622279958149,23.3289534815563));
#47392=CARTESIAN_POINT('Ctrl Pts',(30.0912045055574,-1.4979228580024,23.3169457772084));
#47393=CARTESIAN_POINT('Ctrl Pts',(30.0455768509778,-1.50000000000001,23.3146928172651));
#47394=CARTESIAN_POINT('Ctrl Pts',(30.0000000000002,-1.50000000000001,23.3125));
#47395=CARTESIAN_POINT('Origin',(30.,-1.32966554433622E-14,16.));
#47396=CARTESIAN_POINT('',(30.0000000000001,-1.50000000000001,22.75));
#47397=CARTESIAN_POINT('',(30.,-1.50000000000001,22.8125));
#47398=CARTESIAN_POINT('',(30.,-1.50000000000001,16.));
#47399=CARTESIAN_POINT('Ctrl Pts',(30.0000000000001,-1.50000000000001,22.75));
#47400=CARTESIAN_POINT('Ctrl Pts',(30.0238190927805,-1.50000000000001,22.7511459966357));
#47401=CARTESIAN_POINT('Ctrl Pts',(30.0476581179369,-1.49943265781826,22.7523087117734));
#47402=CARTESIAN_POINT('Ctrl Pts',(30.2627622738244,-1.48916810759789,22.7629430416939));
#47403=CARTESIAN_POINT('Ctrl Pts',(30.4504917710081,-1.44350305068679,22.7732436551414));
#47404=CARTESIAN_POINT('Ctrl Pts',(30.8053949324493,-1.28097942369943,22.7948334866517));
#47405=CARTESIAN_POINT('Ctrl Pts',(30.9679955997388,-1.16299746502374,22.8059338915341));
#47406=CARTESIAN_POINT('Ctrl Pts',(31.2335580340327,-0.874942371993705,
22.8267123004732));
#47407=CARTESIAN_POINT('Ctrl Pts',(31.3356903480274,-0.709308500806453,
22.8355939721774));
#47408=CARTESIAN_POINT('Ctrl Pts',(31.4719653898389,-0.347606806174152,
22.8556885107681));
#47409=CARTESIAN_POINT('Ctrl Pts',(31.5044992018676,-0.154858219876142,
22.8663967655625));
#47410=CARTESIAN_POINT('Ctrl Pts',(31.4943665307067,0.237510688978279,22.8881950382766));
#47411=CARTESIAN_POINT('Ctrl Pts',(31.4497537465181,0.433331528903234,22.899073973828));
#47412=CARTESIAN_POINT('Ctrl Pts',(31.2903519524536,0.78810181728577,22.9187834342937));
#47413=CARTESIAN_POINT('Ctrl Pts',(31.1802475750943,0.945060620681391,22.9278003293086));
#47414=CARTESIAN_POINT('Ctrl Pts',(30.9030507590494,1.21362000516214,22.948596950241));
#47415=CARTESIAN_POINT('Ctrl Pts',(30.7370141991215,1.32105257322674,22.9595696259569));
#47416=CARTESIAN_POINT('Ctrl Pts',(30.3702805499944,1.46712017353723,22.9812715402192));
#47417=CARTESIAN_POINT('Ctrl Pts',(30.1727871861063,1.50321114583692,22.991597574137));
#47418=CARTESIAN_POINT('Ctrl Pts',(29.7831928098337,1.49647610979574,23.0105290266394));
#47419=CARTESIAN_POINT('Ctrl Pts',(29.5947193673977,1.45676699750561,23.0206999902635));
#47420=CARTESIAN_POINT('Ctrl Pts',(29.2359911149794,1.30598838211349,23.0421476062271));
#47421=CARTESIAN_POINT('Ctrl Pts',(29.0702277888966,1.19366882317697,23.05324288572));
#47422=CARTESIAN_POINT('Ctrl Pts',(28.7948557226535,0.913971635465609,23.0742610967597));
#47423=CARTESIAN_POINT('Ctrl Pts',(28.686793719435,0.750466721324838,23.0833074043708));
#47424=CARTESIAN_POINT('Ctrl Pts',(28.5393908078851,0.39231449396832,23.1032047503351));
#47425=CARTESIAN_POINT('Ctrl Pts',(28.50107471408,0.201238476218244,23.1138200846545));
#47426=CARTESIAN_POINT('Ctrl Pts',(28.4989279287216,-0.192576857122968,
23.1356987142846));
#47427=CARTESIAN_POINT('Ctrl Pts',(28.5381471159066,-0.391544240809387,
23.1467524578227));
#47428=CARTESIAN_POINT('Ctrl Pts',(28.6885908974138,-0.752626531003943,
23.1668125850557));
#47429=CARTESIAN_POINT('Ctrl Pts',(28.7945746463293,-0.912795946069086,
23.1756927219105));
#47430=CARTESIAN_POINT('Ctrl Pts',(29.0643193882896,-1.1885583990927,23.1963308899987));
#47431=CARTESIAN_POINT('Ctrl Pts',(29.2269067570048,-1.30018824275338,23.2072542074138));
#47432=CARTESIAN_POINT('Ctrl Pts',(29.5888237919401,-1.45617120236401,23.228999808865));
#47433=CARTESIAN_POINT('Ctrl Pts',(29.7851989650319,-1.49779418034797,23.2396041076185));
#47434=CARTESIAN_POINT('Ctrl Pts',(29.9893352495882,-1.49997157194577,23.2494861022884));
#47435=CARTESIAN_POINT('Ctrl Pts',(29.9946682024469,-1.50000000000001,23.2497434737706));
#47436=CARTESIAN_POINT('Ctrl Pts',(30.,-1.50000000000001,23.25));
#47437=CARTESIAN_POINT('Ctrl Pts',(30.0000000000003,-1.50000000000001,23.3125));
#47438=CARTESIAN_POINT('Ctrl Pts',(29.8497176527518,-1.50000000000002,23.3052695371968));
#47439=CARTESIAN_POINT('Ctrl Pts',(29.7000480379928,-1.47742120454004,23.2974413657365));
#47440=CARTESIAN_POINT('Ctrl Pts',(29.3674490033452,-1.37435151569836,23.2785761403087));
#47441=CARTESIAN_POINT('Ctrl Pts',(29.1922818901849,-1.27927791742795,23.2675074753621));
#47442=CARTESIAN_POINT('Ctrl Pts',(28.8943459539799,-1.03136235914611,23.2462864826624));
#47443=CARTESIAN_POINT('Ctrl Pts',(28.7726494682524,-0.883034040962408,
23.2365574467202));
#47444=CARTESIAN_POINT('Ctrl Pts',(28.5870020748245,-0.541267982453404,
23.2175704434697));
#47445=CARTESIAN_POINT('Ctrl Pts',(28.5277906685824,-0.349440299767995,
23.2069133499871));
#47446=CARTESIAN_POINT('Ctrl Pts',(28.487963650694,0.0423711662580389,23.185146046319));
#47447=CARTESIAN_POINT('Ctrl Pts',(28.5062787794266,0.238440842104816,23.1742532865498));
#47448=CARTESIAN_POINT('Ctrl Pts',(28.6157002622386,0.608326552071247,23.1537040804405));
#47449=CARTESIAN_POINT('Ctrl Pts',(28.704120723826,0.779127514930934,23.1448722564411));
#47450=CARTESIAN_POINT('Ctrl Pts',(28.9463114752997,1.08624863564316,23.1246887062359));
#47451=CARTESIAN_POINT('Ctrl Pts',(29.100754465216,1.21718400346422,23.1136209708684));
#47452=CARTESIAN_POINT('Ctrl Pts',(29.4452036060534,1.40690072974557,23.0917787447896));
#47453=CARTESIAN_POINT('Ctrl Pts',(29.630453412942,1.46649956876065,23.0812103859941));
#47454=CARTESIAN_POINT('Ctrl Pts',(30.0154678344856,1.51253258675255,23.0614076760565));
#47455=CARTESIAN_POINT('Ctrl Pts',(30.2116518417758,1.49773354664468,23.052253938977));
#47456=CARTESIAN_POINT('Ctrl Pts',(30.5903886500576,1.39306917025536,23.031124612004));
#47457=CARTESIAN_POINT('Ctrl Pts',(30.7689034771477,1.3030667277533,23.0200357455338));
#47458=CARTESIAN_POINT('Ctrl Pts',(31.0748241700176,1.06351798971685,22.9986629977234));
#47459=CARTESIAN_POINT('Ctrl Pts',(31.2011381587389,0.918481956232081,22.9885569343996));
#47460=CARTESIAN_POINT('Ctrl Pts',(31.3967520547264,0.581861797904625,22.9697948964873));
#47461=CARTESIAN_POINT('Ctrl Pts',(31.4615014415134,0.391859484339943,22.9592699713522));
#47462=CARTESIAN_POINT('Ctrl Pts',(31.5127002734739,0.000740375396987882,
22.9375411319665));
#47463=CARTESIAN_POINT('Ctrl Pts',(31.4999079686113,-0.196327016676456,
22.9265929435179));
#47464=CARTESIAN_POINT('Ctrl Pts',(31.4007804390091,-0.569202940848263,
22.9058776143973));
#47465=CARTESIAN_POINT('Ctrl Pts',(31.3174135571943,-0.742018160934012,
22.8969391404085));
#47466=CARTESIAN_POINT('Ctrl Pts',(31.0853396535684,-1.05432624095891,22.8770982550692));
#47467=CARTESIAN_POINT('Ctrl Pts',(30.9361334950341,-1.18878161757634,22.8661846988469));
#47468=CARTESIAN_POINT('Ctrl Pts',(30.5987439832112,-1.38884930936682,22.8443946025078));
#47469=CARTESIAN_POINT('Ctrl Pts',(30.4148754905707,-1.45440359104526,22.8337272732621));
#47470=CARTESIAN_POINT('Ctrl Pts',(30.1494349053273,-1.49442202191131,22.8198446340705));
#47471=CARTESIAN_POINT('Ctrl Pts',(30.0746909808563,-1.50000000000001,22.816093571492));
#47472=CARTESIAN_POINT('Ctrl Pts',(30.0000000000001,-1.50000000000001,22.8125));
#47473=CARTESIAN_POINT('Origin',(30.,-1.32966554433622E-14,16.));
#47474=CARTESIAN_POINT('',(30.0000000000001,-1.50000000000001,22.25));
#47475=CARTESIAN_POINT('',(30.,-1.50000000000001,22.3125));
#47476=CARTESIAN_POINT('',(30.,-1.50000000000001,16.));
#47477=CARTESIAN_POINT('Ctrl Pts',(30.0000000000002,-1.50000000000001,22.25));
#47478=CARTESIAN_POINT('Ctrl Pts',(30.0511677444063,-1.50000000000001,22.2524618092506));
#47479=CARTESIAN_POINT('Ctrl Pts',(30.1023921263505,-1.49738203467576,22.254999064735));
#47480=CARTESIAN_POINT('Ctrl Pts',(30.3449868915282,-1.47242953219059,22.2673640358856));
#47481=CARTESIAN_POINT('Ctrl Pts',(30.5309019965201,-1.41604718249647,22.2778750569255));
#47482=CARTESIAN_POINT('Ctrl Pts',(30.8779534991821,-1.23257211766357,22.2996691097112));
#47483=CARTESIAN_POINT('Ctrl Pts',(31.0343750352224,-1.10459007945506,22.3107500009898));
#47484=CARTESIAN_POINT('Ctrl Pts',(31.2820199524192,-0.801819415517196,
22.3310751188442));
#47485=CARTESIAN_POINT('Ctrl Pts',(31.3735944009353,-0.632242273686504,
22.3398754292397));
#47486=CARTESIAN_POINT('Ctrl Pts',(31.4893318529591,-0.264232559817084,
22.3603204133435));
#47487=CARTESIAN_POINT('Ctrl Pts',(31.511019003439,-0.0688512669519718,
22.3711749296138));
#47488=CARTESIAN_POINT('Ctrl Pts',(31.4781740542578,0.32329452926424,22.3929608071814));
#47489=CARTESIAN_POINT('Ctrl Pts',(31.422363807823,0.516161881943181,22.403675660108));
#47490=CARTESIAN_POINT('Ctrl Pts',(31.2428531453717,0.861044634974944,22.4228358130542));
#47491=CARTESIAN_POINT('Ctrl Pts',(31.1239285676202,1.01138399102137,22.4323522946618));
#47492=CARTESIAN_POINT('Ctrl Pts',(30.8309115401787,1.26428053578999,22.4534749869891));
#47493=CARTESIAN_POINT('Ctrl Pts',(30.6578432463629,1.3623737449238,22.4645265505225));
#47494=CARTESIAN_POINT('Ctrl Pts',(30.2831279004866,1.48623532989505,22.4859956505893));
#47495=CARTESIAN_POINT('Ctrl Pts',(30.0851137662052,1.5105602610331,22.49561162143));
#47496=CARTESIAN_POINT('Ctrl Pts',(29.6966286981958,1.48149502237994,22.5151099857196));
#47497=CARTESIAN_POINT('Ctrl Pts',(29.5097167303907,1.43054672747056,22.5255180223776));
#47498=CARTESIAN_POINT('Ctrl Pts',(29.1585275612845,1.25766527467259,22.547216881732));
#47499=CARTESIAN_POINT('Ctrl Pts',(28.9988940242273,1.13472310971196,22.5583123140024));
#47500=CARTESIAN_POINT('Ctrl Pts',(28.7421191463059,0.839368453848379,22.5788706970727));
#47501=CARTESIAN_POINT('Ctrl Pts',(28.6452032661271,0.671810533827306,22.5876771925652));
#47502=CARTESIAN_POINT('Ctrl Pts',(28.5189623058816,0.306989072921277,22.6079450515044));
#47503=CARTESIAN_POINT('Ctrl Pts',(28.4917024287485,0.112879611784448,22.6187289104564));
#47504=CARTESIAN_POINT('Ctrl Pts',(28.5129271256702,-0.27954553838217,22.6405303076879));
#47505=CARTESIAN_POINT('Ctrl Pts',(28.5630339289139,-0.474005993650327,
22.6513336663139));
#47506=CARTESIAN_POINT('Ctrl Pts',(28.7322894218787,-0.823994430176359,
22.6707774683431));
#47507=CARTESIAN_POINT('Ctrl Pts',(28.8466683628132,-0.977702516203741,
22.680002042295));
#47508=CARTESIAN_POINT('Ctrl Pts',(29.1315598866997,-1.23870928805523,22.7009590802358));
#47509=CARTESIAN_POINT('Ctrl Pts',(29.301068288962,-1.34167114530826,22.7119746086325));
#47510=CARTESIAN_POINT('Ctrl Pts',(29.6506233621551,-1.46928601783117,22.732337442503));
#47511=CARTESIAN_POINT('Ctrl Pts',(29.8247316115896,-1.50000000000001,22.7415673957309));
#47512=CARTESIAN_POINT('Ctrl Pts',(30.0000000000001,-1.50000000000001,22.75));
#47513=CARTESIAN_POINT('Ctrl Pts',(30.0000000000001,-1.50000000000001,22.8125));
#47514=CARTESIAN_POINT('Ctrl Pts',(29.8821180181442,-1.50000000000001,22.8068284005036));
#47515=CARTESIAN_POINT('Ctrl Pts',(29.7644054408515,-1.48610745961779,22.8007790475884));
#47516=CARTESIAN_POINT('Ctrl Pts',(29.4561358619788,-1.41197523055228,22.7838881919746));
#47517=CARTESIAN_POINT('Ctrl Pts',(29.2741386603191,-1.32762177587115,22.7727886960081));
#47518=CARTESIAN_POINT('Ctrl Pts',(28.9596308471203,-1.09734948081223,22.7512604791499));
#47519=CARTESIAN_POINT('Ctrl Pts',(28.8283658665089,-0.955949757636784,
22.7410172197375));
#47520=CARTESIAN_POINT('Ctrl Pts',(28.6210784753189,-0.623528783846783,
22.7218101845402));
#47521=CARTESIAN_POINT('Ctrl Pts',(28.550139211662,-0.43377020073728,22.7115983444854));
#47522=CARTESIAN_POINT('Ctrl Pts',(28.4878128315539,-0.0419315259951405,
22.6898295292219));
#47523=CARTESIAN_POINT('Ctrl Pts',(28.4952899772074,0.155946448584049,22.678836308412));
#47524=CARTESIAN_POINT('Ctrl Pts',(28.5845546436209,0.531607574681399,22.657966245851));
#47525=CARTESIAN_POINT('Ctrl Pts',(28.6631729955745,0.706378968214403,22.6488631478995));
#47526=CARTESIAN_POINT('Ctrl Pts',(28.886581089556,1.02462509962909,22.6292742506491));
#47527=CARTESIAN_POINT('Ctrl Pts',(29.0320840520478,1.16304620087307,22.6184287055121));
#47528=CARTESIAN_POINT('Ctrl Pts',(29.3643456686259,1.37241961531272,22.5966268328521));
#47529=CARTESIAN_POINT('Ctrl Pts',(29.5468906971467,1.44301653433814,22.585883105544));
#47530=CARTESIAN_POINT('Ctrl Pts',(29.9272228832809,1.51053148619831,22.5657089493774));
#47531=CARTESIAN_POINT('Ctrl Pts',(30.1212939503538,1.50741198602448,22.5568701305933));
#47532=CARTESIAN_POINT('Ctrl Pts',(30.5044378408363,1.42661367919911,22.5361917141558));
#47533=CARTESIAN_POINT('Ctrl Pts',(30.6892182911204,1.34709011542225,22.5250924727137));
#47534=CARTESIAN_POINT('Ctrl Pts',(31.0107046879826,1.12481571216727,22.5034506622537));
#47535=CARTESIAN_POINT('Ctrl Pts',(31.1460355364563,0.986589014961116,22.4930999232927));
#47536=CARTESIAN_POINT('Ctrl Pts',(31.3611183370781,0.66090197936205,22.473704885123));
#47537=CARTESIAN_POINT('Ctrl Pts',(31.4365760335144,0.475089538086611,22.463893863227));
#47538=CARTESIAN_POINT('Ctrl Pts',(31.5103576978905,0.0866802952431828,
22.4423155719579));
#47539=CARTESIAN_POINT('Ctrl Pts',(31.5086976507443,-0.111919508747406,
22.431282249514));
#47540=CARTESIAN_POINT('Ctrl Pts',(31.4301969979147,-0.490528747223499,
22.410248402932));
#47541=CARTESIAN_POINT('Ctrl Pts',(31.3566667795852,-0.667467593155736,
22.4008985610562));
#47542=CARTESIAN_POINT('Ctrl Pts',(31.1425983489439,-0.991976419659515,
22.3815850548154));
#47543=CARTESIAN_POINT('Ctrl Pts',(31.0011829334274,-1.13452992378446,22.370821382905));
#47544=CARTESIAN_POINT('Ctrl Pts',(30.6747026750166,-1.35372782384191,22.3490247635913));
#47545=CARTESIAN_POINT('Ctrl Pts',(30.4937271061129,-1.42970164427305,22.3382071885718));
#47546=CARTESIAN_POINT('Ctrl Pts',(30.2032733713701,-1.48966742655325,22.322567010569));
#47547=CARTESIAN_POINT('Ctrl Pts',(30.1016602333963,-1.50000000000001,22.3173911302598));
#47548=CARTESIAN_POINT('Ctrl Pts',(30.,-1.50000000000001,22.3125));
#47549=CARTESIAN_POINT('Origin',(30.,-1.32966554433622E-14,16.));
#47550=CARTESIAN_POINT('',(30.,-1.50000000000001,21.75));
#47551=CARTESIAN_POINT('',(29.9999999999999,-1.50000000000001,21.8125));
#47552=CARTESIAN_POINT('',(30.,-1.50000000000001,16.));
#47553=CARTESIAN_POINT('Ctrl Pts',(30.,-1.50000000000001,21.75));
#47554=CARTESIAN_POINT('Ctrl Pts',(30.0799345840677,-1.50000000000001,21.7538458544691));
#47555=CARTESIAN_POINT('Ctrl Pts',(30.1599122998412,-1.4936114408734,21.7578712440892));
#47556=CARTESIAN_POINT('Ctrl Pts',(30.4303228176761,-1.44993500309235,21.7720946105773));
#47557=CARTESIAN_POINT('Ctrl Pts',(30.6136742893428,-1.38234553687229,21.7827935975436));
#47558=CARTESIAN_POINT('Ctrl Pts',(30.9490281775211,-1.17851150378185,21.8045903754862));
#47559=CARTESIAN_POINT('Ctrl Pts',(31.096754819913,-1.04244516916321,21.8154774972882));
#47560=CARTESIAN_POINT('Ctrl Pts',(31.3253413942278,-0.727732251316939,
21.8352173994684));
#47561=CARTESIAN_POINT('Ctrl Pts',(31.4067935410376,-0.554135842314364,
21.8442146754271));
#47562=CARTESIAN_POINT('Ctrl Pts',(31.5019658936778,-0.180133518226551,
21.8649925823208));
#47563=CARTESIAN_POINT('Ctrl Pts',(31.5126290136531,0.0172760533687308,
21.8759597807428));
#47564=CARTESIAN_POINT('Ctrl Pts',(31.457072059222,0.408029499969523,21.8976683055539));
#47565=CARTESIAN_POINT('Ctrl Pts',(31.3902144216195,0.597326073407902,21.9080390017153));
#47566=CARTESIAN_POINT('Ctrl Pts',(31.1907422817111,0.931962878929858,21.9269315763413));
#47567=CARTESIAN_POINT('Ctrl Pts',(31.0626495240423,1.07572029471252,21.9370877035676));
#47568=CARTESIAN_POINT('Ctrl Pts',(30.7536327605205,1.31199280194067,21.9585184047354));
#47569=CARTESIAN_POINT('Ctrl Pts',(30.5738554020277,1.39999410781883,21.9696124276475));
#47570=CARTESIAN_POINT('Ctrl Pts',(30.1942124641512,1.50002082255712,21.9906565268663));
#47571=CARTESIAN_POINT('Ctrl Pts',(29.9984550225415,1.51253833676667,21.9997260456303));
#47572=CARTESIAN_POINT('Ctrl Pts',(29.6143176021754,1.46236614670513,22.0196015378309));
#47573=CARTESIAN_POINT('Ctrl Pts',(29.4295365026789,1.40065016331119,22.0302061554976));
#47574=CARTESIAN_POINT('Ctrl Pts',(29.0868629977602,1.20683686352092,22.052076744962));
#47575=CARTESIAN_POINT('Ctrl Pts',(28.9337539891966,1.07396976987892,22.0631339581722));
#47576=CARTESIAN_POINT('Ctrl Pts',(28.6951751765203,0.763999003449345,22.0832228857165));
#47577=CARTESIAN_POINT('Ctrl Pts',(28.60882966791,0.592379173375639,22.0920900459236));
#47578=CARTESIAN_POINT('Ctrl Pts',(28.5036090779159,0.221263029136351,22.1127076094925));
#47579=CARTESIAN_POINT('Ctrl Pts',(28.4875441317865,0.0247675363524192,
22.1236240257582));
#47580=CARTESIAN_POINT('Ctrl Pts',(28.5320098906898,-0.36675262012417,22.1453751455625));
#47581=CARTESIAN_POINT('Ctrl Pts',(28.593470220051,-0.557855368091198,22.155991964894));
#47582=CARTESIAN_POINT('Ctrl Pts',(28.7831869687067,-0.897529793649072,
22.1748627663138));
#47583=CARTESIAN_POINT('Ctrl Pts',(28.9067443386156,-1.04452569047662,22.1847486483138));
#47584=CARTESIAN_POINT('Ctrl Pts',(29.2079650540828,-1.28908351396432,22.2060344096185));
#47585=CARTESIAN_POINT('Ctrl Pts',(29.3845091949262,-1.38211075548827,22.2171124835975));
#47586=CARTESIAN_POINT('Ctrl Pts',(29.7125665428598,-1.47927872450056,22.2355952603595));
#47587=CARTESIAN_POINT('Ctrl Pts',(29.8560312883098,-1.50000000000001,22.2430733021292));
#47588=CARTESIAN_POINT('Ctrl Pts',(30.0000000000002,-1.50000000000001,22.25));
#47589=CARTESIAN_POINT('Ctrl Pts',(30.,-1.50000000000001,22.3125));
#47590=CARTESIAN_POINT('Ctrl Pts',(29.9110895843884,-1.50000000000001,22.3082222956344));
#47591=CARTESIAN_POINT('Ctrl Pts',(29.8221645100457,-1.49209634975764,22.3037243401601));
#47592=CARTESIAN_POINT('Ctrl Pts',(29.5376207680931,-1.44087704391974,22.288611464497));
#47593=CARTESIAN_POINT('Ctrl Pts',(29.3500356587678,-1.36654835932947,22.2775215860335));
#47594=CARTESIAN_POINT('Ctrl Pts',(29.0213968226607,-1.15294073825471,22.2557763976293));
#47595=CARTESIAN_POINT('Ctrl Pts',(28.8818555948118,-1.01818896609304,22.2453196123919));
#47596=CARTESIAN_POINT('Ctrl Pts',(28.6586442869874,-0.699623440719697,
22.2257313109655));
#47597=CARTESIAN_POINT('Ctrl Pts',(28.5785399664869,-0.517856468116547,
22.2162698037842));
#47598=CARTESIAN_POINT('Ctrl Pts',(28.4929509348882,-0.133169441708886,
22.1948983023171));
#47599=CARTESIAN_POINT('Ctrl Pts',(28.4885197532221,0.0660037349236151,
22.1838331258375));
#47600=CARTESIAN_POINT('Ctrl Pts',(28.555761801385,0.44759093437612,22.1626338369791));
#47601=CARTESIAN_POINT('Ctrl Pts',(28.6240637192867,0.626835313372202,22.1529543398));
#47602=CARTESIAN_POINT('Ctrl Pts',(28.8284985352011,0.957663958533704,22.1339287805455));
#47603=CARTESIAN_POINT('Ctrl Pts',(28.9656007252824,1.10432288929781,22.1232585891618));
#47604=CARTESIAN_POINT('Ctrl Pts',(29.2858531479679,1.33342212875051,22.1014865695287));
#47605=CARTESIAN_POINT('Ctrl Pts',(29.4650586076933,1.41487321083335,22.0906020127698));
#47606=CARTESIAN_POINT('Ctrl Pts',(29.8404420905807,1.50363480947233,22.0700757665663));
#47607=CARTESIAN_POINT('Ctrl Pts',(30.0326825220108,1.51172235919918,22.0612531825154));
#47608=CARTESIAN_POINT('Ctrl Pts',(30.4195266402016,1.45401546056375,22.0410381667945));
#47609=CARTESIAN_POINT('Ctrl Pts',(30.6097995465824,1.38502427774371,22.029967235573));
#47610=CARTESIAN_POINT('Ctrl Pts',(30.9454244752463,1.18038733089544,22.0081351140291));
#47611=CARTESIAN_POINT('Ctrl Pts',(31.0891246269642,1.04926948856203,21.997579174969));
#47612=CARTESIAN_POINT('Ctrl Pts',(31.3204408508467,0.737906981306312,21.9778010094235));
#47613=CARTESIAN_POINT('Ctrl Pts',(31.4051230902783,0.560097094369773,21.9686165052427));
#47614=CARTESIAN_POINT('Ctrl Pts',(31.5023434434385,0.179258057369552,21.9474587809649));
#47615=CARTESIAN_POINT('Ctrl Pts',(31.5128623034415,-0.0203042234475934,
21.9363719875862));
#47616=CARTESIAN_POINT('Ctrl Pts',(31.4568810475112,-0.404757677376984,
21.9150134623679));
#47617=CARTESIAN_POINT('Ctrl Pts',(31.3937249627295,-0.586348141727015,
21.9049348418193));
#47618=CARTESIAN_POINT('Ctrl Pts',(31.1987850558466,-0.923274808506461,
21.8861967170992));
#47619=CARTESIAN_POINT('Ctrl Pts',(31.0660220732146,-1.07382111006007,21.8756273134093));
#47620=CARTESIAN_POINT('Ctrl Pts',(30.7521571303647,-1.31243843036869,21.8538982204082));
#47621=CARTESIAN_POINT('Ctrl Pts',(30.5748417786265,-1.39921326582906,21.8429567194739));
#47622=CARTESIAN_POINT('Ctrl Pts',(30.2597272838717,-1.48309858829145,21.8254656184301));
#47623=CARTESIAN_POINT('Ctrl Pts',(30.1300238421579,-1.50000000000003,21.8187557750226));
#47624=CARTESIAN_POINT('Ctrl Pts',(29.9999999999998,-1.50000000000001,21.8125));
#47625=CARTESIAN_POINT('Origin',(30.,-1.32966554433622E-14,16.));
#47626=CARTESIAN_POINT('',(30.,-1.50000000000001,21.25));
#47627=CARTESIAN_POINT('',(29.9999999999999,-1.50000000000001,21.3125));
#47628=CARTESIAN_POINT('',(30.,-1.50000000000001,16.));
#47629=CARTESIAN_POINT('Ctrl Pts',(30.,-1.50000000000001,21.25));
#47630=CARTESIAN_POINT('Ctrl Pts',(30.1075848726609,-1.50000000000001,21.2551761795993));
#47631=CARTESIAN_POINT('Ctrl Pts',(30.2150815962025,-1.48842822791985,21.2606695562356));
#47632=CARTESIAN_POINT('Ctrl Pts',(30.5108359622909,-1.42370950162225,21.2766967872056));
#47633=CARTESIAN_POINT('Ctrl Pts',(30.6910987866292,-1.34546461195666,21.2875431555427));
#47634=CARTESIAN_POINT('Ctrl Pts',(31.0150386063333,-1.12214805976604,21.3093319549459));
#47635=CARTESIAN_POINT('Ctrl Pts',(31.1546840327806,-0.977879417444189,
21.3200581109451));
#47636=CARTESIAN_POINT('Ctrl Pts',(31.3647735631693,-0.650743634461253,
21.3392531532717));
#47637=CARTESIAN_POINT('Ctrl Pts',(31.4361426481554,-0.472861434650035,
21.3487299202974));
#47638=CARTESIAN_POINT('Ctrl Pts',(31.5100129878737,-0.0930141634261118,
21.3698325464765));
#47639=CARTESIAN_POINT('Ctrl Pts',(31.5091680819865,0.105843895299734,21.3808802164057));
#47640=CARTESIAN_POINT('Ctrl Pts',(31.4305088048906,0.492738271362424,21.4023743484091));
#47641=CARTESIAN_POINT('Ctrl Pts',(31.3531309016418,0.676876453829759,21.4120329161916));
#47642=CARTESIAN_POINT('Ctrl Pts',(31.1347020158755,0.999644296815675,21.4315078542742));
#47643=CARTESIAN_POINT('Ctrl Pts',(30.9976338252526,1.13646112591015,21.4419030181452));
#47644=CARTESIAN_POINT('Ctrl Pts',(30.6731866853066,1.35520814296552,21.4635892944733));
#47645=CARTESIAN_POINT('Ctrl Pts',(30.4872391020676,1.43261266999426,21.474685827494));
#47646=CARTESIAN_POINT('Ctrl Pts',(30.1032980730075,1.50870030742653,21.4952717443516));
#47647=CARTESIAN_POINT('Ctrl Pts',(29.9096173130592,1.50952898426713,21.5040838450456));
#47648=CARTESIAN_POINT('Ctrl Pts',(29.5302606487566,1.43771855687004,21.5243303851611));
#47649=CARTESIAN_POINT('Ctrl Pts',(29.3483375586665,1.36492268311026,21.5351052715185));
#47650=CARTESIAN_POINT('Ctrl Pts',(29.0184009025148,1.15151905747937,21.5569072347786));
#47651=CARTESIAN_POINT('Ctrl Pts',(28.8745521744234,1.01139585435745,21.5677204711336));
#47652=CARTESIAN_POINT('Ctrl Pts',(28.6549505368779,0.690580628714703,21.5871975938919));
#47653=CARTESIAN_POINT('Ctrl Pts',(28.5784089748082,0.514933598952509,21.596392577836));
#47654=CARTESIAN_POINT('Ctrl Pts',(28.4935139297613,0.138064010695691,21.6173297771836));
#47655=CARTESIAN_POINT('Ctrl Pts',(28.4883967455728,-0.0601274794615553,
21.6283404155257));
#47656=CARTESIAN_POINT('Ctrl Pts',(28.5553929405263,-0.450590041266374,
21.6500327800704));
#47657=CARTESIAN_POINT('Ctrl Pts',(28.6281760530356,-0.63873783180513,21.6600741404618));
#47658=CARTESIAN_POINT('Ctrl Pts',(28.8386308155265,-0.968434016466414,
21.6793578772949));
#47659=CARTESIAN_POINT('Ctrl Pts',(28.9715505605447,-1.10856330761102,21.6896454618184));
#47660=CARTESIAN_POINT('Ctrl Pts',(29.2889068065357,-1.33562316156644,21.7112214894881));
#47661=CARTESIAN_POINT('Ctrl Pts',(29.4720453487169,-1.41803231498314,21.7223218898575));
#47662=CARTESIAN_POINT('Ctrl Pts',(29.7757758521236,-1.48742065117207,21.7388625842992));
#47663=CARTESIAN_POINT('Ctrl Pts',(29.8878284604463,-1.50000000000001,21.7446031442869));
#47664=CARTESIAN_POINT('Ctrl Pts',(30.,-1.50000000000001,21.75));
#47665=CARTESIAN_POINT('Ctrl Pts',(29.9999999999998,-1.50000000000001,21.8125));
#47666=CARTESIAN_POINT('Ctrl Pts',(29.9405204451645,-1.50000000000001,21.8096382885837));
#47667=CARTESIAN_POINT('Ctrl Pts',(29.8809833669271,-1.49646250510709,21.8066755458243));
#47668=CARTESIAN_POINT('Ctrl Pts',(29.6241950912386,-1.46572084178495,21.7934668790576));
#47669=CARTESIAN_POINT('Ctrl Pts',(29.4333772164259,-1.40302797833686,21.782544681346));
#47670=CARTESIAN_POINT('Ctrl Pts',(29.0921865820648,-1.20964665656295,21.760757435914));
#47671=CARTESIAN_POINT('Ctrl Pts',(28.9439925649252,-1.08269733302756,21.7501010778418));
#47672=CARTESIAN_POINT('Ctrl Pts',(28.7038088414644,-0.77933430694382,21.7301184823344));
#47673=CARTESIAN_POINT('Ctrl Pts',(28.6141674942217,-0.605760578772268,
21.7211533654873));
#47674=CARTESIAN_POINT('Ctrl Pts',(28.5043846389733,-0.22927416638246,21.7002374536878));
#47675=CARTESIAN_POINT('Ctrl Pts',(28.4872031236976,-0.0294943674923172,
21.6891385759717));
#47676=CARTESIAN_POINT('Ctrl Pts',(28.5307959749546,0.357711165892058,21.6676271574504));
#47677=CARTESIAN_POINT('Ctrl Pts',(28.588271358922,0.541814389624386,21.6573992005764));
#47678=CARTESIAN_POINT('Ctrl Pts',(28.7738533380075,0.887068805374046,21.6382183997014));
#47679=CARTESIAN_POINT('Ctrl Pts',(28.903512180976,1.043112470525,21.6279461150529));
#47680=CARTESIAN_POINT('Ctrl Pts',(29.2128905056455,1.29185751769652,21.6061515588234));
#47681=CARTESIAN_POINT('Ctrl Pts',(29.3882998946744,1.38356922217579,21.5951646233122));
#47682=CARTESIAN_POINT('Ctrl Pts',(29.7586487303438,1.49259838475184,21.5743176187989));
#47683=CARTESIAN_POINT('Ctrl Pts',(29.9494126813103,1.51113463524617,21.5652431789286));
#47684=CARTESIAN_POINT('Ctrl Pts',(30.3366113826679,1.4752126287187,21.5456162392091));
#47685=CARTESIAN_POINT('Ctrl Pts',(30.5290112502297,1.41763409463152,21.5347599925404));
#47686=CARTESIAN_POINT('Ctrl Pts',(30.8756573292315,1.23320190987312,21.512958859045));
#47687=CARTESIAN_POINT('Ctrl Pts',(31.0275193143428,1.10985575574539,21.5022261138206));
#47688=CARTESIAN_POINT('Ctrl Pts',(31.2750461098143,0.813213213668382,21.4820769047076));
#47689=CARTESIAN_POINT('Ctrl Pts',(31.3687657636095,0.643070885011216,21.4732261602783));
#47690=CARTESIAN_POINT('Ctrl Pts',(31.4888227697242,0.270291882918073,21.4525162157176));
#47691=CARTESIAN_POINT('Ctrl Pts',(31.5115128952941,0.0704953149593227,
21.4414164063865));
#47692=CARTESIAN_POINT('Ctrl Pts',(31.4782054807328,-0.318770290439176,
21.4197905394199));
#47693=CARTESIAN_POINT('Ctrl Pts',(31.4254475382382,-0.504803416717179,
21.4094553657378));
#47694=CARTESIAN_POINT('Ctrl Pts',(31.2494901966584,-0.853416070021567,
21.3900879961098));
#47695=CARTESIAN_POINT('Ctrl Pts',(31.1254658116588,-1.01138492328729,21.3802216401301));
#47696=CARTESIAN_POINT('Ctrl Pts',(30.8246930412984,-1.26828298434064,21.3586146462176));
#47697=CARTESIAN_POINT('Ctrl Pts',(30.6515224369356,-1.36534975789868,21.347586672365));
#47698=CARTESIAN_POINT('Ctrl Pts',(30.3143398429227,-1.47517879246933,21.3283131607309));
#47699=CARTESIAN_POINT('Ctrl Pts',(30.1575657374829,-1.50000000000003,21.3200808850792));
#47700=CARTESIAN_POINT('Ctrl Pts',(29.9999999999998,-1.50000000000001,21.3125));
#47701=CARTESIAN_POINT('Origin',(30.,-1.32966554433622E-14,16.));
#47702=CARTESIAN_POINT('',(29.9999999999999,-1.50000000000001,20.75));
#47703=CARTESIAN_POINT('',(30.0000000238974,-1.50000000000001,20.8125000022995));
#47704=CARTESIAN_POINT('',(30.,-1.50000000000001,16.));
#47705=CARTESIAN_POINT('Ctrl Pts',(29.9999999999998,-1.50000000000001,20.75));
#47706=CARTESIAN_POINT('Ctrl Pts',(30.1355873378723,-1.50000000000003,20.7565234488349));
#47707=CARTESIAN_POINT('Ctrl Pts',(30.2707763371628,-1.48162130053548,20.7635382520255));
#47708=CARTESIAN_POINT('Ctrl Pts',(30.5905052894202,-1.39270558594719,20.7813910993741));
#47709=CARTESIAN_POINT('Ctrl Pts',(30.767029784006,-1.30383501600373,20.7923527650226));
#47710=CARTESIAN_POINT('Ctrl Pts',(31.0784013127494,-1.06141205266722,20.8140676058879));
#47711=CARTESIAN_POINT('Ctrl Pts',(31.2094059572181,-0.909300433903993,
20.8244833092276));
#47712=CARTESIAN_POINT('Ctrl Pts',(31.4005633760122,-0.569930140644686,
20.8433372144086));
#47713=CARTESIAN_POINT('Ctrl Pts',(31.4616108021312,-0.387386085525011,
20.8534785508042));
#47714=CARTESIAN_POINT('Ctrl Pts',(31.5130288281118,-0.00193915990322278,
20.8748922688942));
#47715=CARTESIAN_POINT('Ctrl Pts',(31.5000564049022,0.197728440072968,20.8859849133374));
#47716=CARTESIAN_POINT('Ctrl Pts',(31.3981909189968,0.576981524645895,20.907054529147));
#47717=CARTESIAN_POINT('Ctrl Pts',(31.3116775745975,0.753220156722293,20.9161479987326));
#47718=CARTESIAN_POINT('Ctrl Pts',(31.0770964939546,1.06165196611475,20.9360018364982));
#47719=CARTESIAN_POINT('Ctrl Pts',(30.9317342971964,1.19125838532521,20.946595756762));
#47720=CARTESIAN_POINT('Ctrl Pts',(30.5933406580028,1.39218994814601,20.9684581606193));
#47721=CARTESIAN_POINT('Ctrl Pts',(30.4020178812766,1.458987498605,20.9795186695191));
#47722=CARTESIAN_POINT('Ctrl Pts',(30.0144815741343,1.51197726610397,20.999635956776));
#47723=CARTESIAN_POINT('Ctrl Pts',(29.8225847199203,1.50160380579917,21.0084913464817));
#47724=CARTESIAN_POINT('Ctrl Pts',(29.4482673839794,1.40844186112423,21.0290885295006));
#47725=CARTESIAN_POINT('Ctrl Pts',(29.2698358143887,1.32475295725216,21.0399980141694));
#47726=CARTESIAN_POINT('Ctrl Pts',(28.9522277915389,1.09163995424434,21.0617542984881));
#47727=CARTESIAN_POINT('Ctrl Pts',(28.8169317835683,0.943334467611102,21.0723833275575));
#47728=CARTESIAN_POINT('Ctrl Pts',(28.6164713965323,0.609937924996611,21.0912889974983));
#47729=CARTESIAN_POINT('Ctrl Pts',(28.5503235834348,0.429720618453307,21.1011266323083));
#47730=CARTESIAN_POINT('Ctrl Pts',(28.4877747716401,0.0469249157698905,
21.1223930602351));
#47731=CARTESIAN_POINT('Ctrl Pts',(28.4947443957624,-0.152432728065059,
21.1334684848926));
#47732=CARTESIAN_POINT('Ctrl Pts',(28.585202717896,-0.535530466260377,21.1547516925701));
#47733=CARTESIAN_POINT('Ctrl Pts',(28.6672227696192,-0.715637129073743,
21.1640888680802));
#47734=CARTESIAN_POINT('Ctrl Pts',(28.8938150388557,-1.03121039122832,21.1837567176656));
#47735=CARTESIAN_POINT('Ctrl Pts',(29.0350964807726,-1.16446677665445,21.1942556904709));
#47736=CARTESIAN_POINT('Ctrl Pts',(29.3666683501557,-1.37437197910307,21.2160391495426));
#47737=CARTESIAN_POINT('Ctrl Pts',(29.5553884234738,-1.44649304249621,21.2271223111757));
#47738=CARTESIAN_POINT('Ctrl Pts',(29.8346137979128,-1.49316573714005,21.2418530120072));
#47739=CARTESIAN_POINT('Ctrl Pts',(29.917323692752,-1.50000000000001,21.2460222343129));
#47740=CARTESIAN_POINT('Ctrl Pts',(30.,-1.50000000000001,21.25));
#47741=CARTESIAN_POINT('Ctrl Pts',(29.9999999999998,-1.50000000000001,21.3125));
#47742=CARTESIAN_POINT('Ctrl Pts',(29.9681380540405,-1.50000000000001,21.3109670414103));
#47743=CARTESIAN_POINT('Ctrl Pts',(29.9362464291016,-1.4989848402199,21.3094044560071));
#47744=CARTESIAN_POINT('Ctrl Pts',(29.7059061051266,-1.48427038685078,21.2979134671869));
#47745=CARTESIAN_POINT('Ctrl Pts',(29.5119585810338,-1.43225099507769,21.2871371794785));
#47746=CARTESIAN_POINT('Ctrl Pts',(29.1596955105172,-1.25764065487782,21.2653386273684));
#47747=CARTESIAN_POINT('Ctrl Pts',(29.0039750821709,-1.13829559847059,21.2545313843106));
#47748=CARTESIAN_POINT('Ctrl Pts',(28.7485987477413,-0.848934521932683,
21.2342067770101));
#47749=CARTESIAN_POINT('Ctrl Pts',(28.6505388148689,-0.682384621723858,
21.2254102567623));
#47750=CARTESIAN_POINT('Ctrl Pts',(28.5196273945211,-0.313661198442873,
21.2049256221356));
#47751=CARTESIAN_POINT('Ctrl Pts',(28.4910680085409,-0.114008266472331,
21.1938337925817));
#47752=CARTESIAN_POINT('Ctrl Pts',(28.5133617159534,0.277152561451723,21.1721026354748));
#47753=CARTESIAN_POINT('Ctrl Pts',(28.5610406223868,0.465104578293146,21.1616608567614));
#47754=CARTESIAN_POINT('Ctrl Pts',(28.7268127368948,0.817191792877632,21.1421004559512));
#47755=CARTESIAN_POINT('Ctrl Pts',(28.8450160186508,0.977157792197407,21.1325925873729));
#47756=CARTESIAN_POINT('Ctrl Pts',(29.1366994431696,1.24242044599111,21.1111905550177));
#47757=CARTESIAN_POINT('Ctrl Pts',(29.3073536529405,1.34504122266248,21.1001293733922));
#47758=CARTESIAN_POINT('Ctrl Pts',(29.6718885684984,1.47596994041667,21.0789537702634));
#47759=CARTESIAN_POINT('Ctrl Pts',(29.8613546451375,1.5056180641301,21.0693266350828));
#47760=CARTESIAN_POINT('Ctrl Pts',(30.2499905035945,1.49232790599687,21.0502592125655));
#47761=CARTESIAN_POINT('Ctrl Pts',(30.4453612619354,1.44608660162569,21.0395749518952));
#47762=CARTESIAN_POINT('Ctrl Pts',(30.8031247707546,1.28178759217525,21.017798185678));
#47763=CARTESIAN_POINT('Ctrl Pts',(30.9627170127615,1.16669332668992,21.0069227374242));
#47764=CARTESIAN_POINT('Ctrl Pts',(31.2261252563514,0.884888124749317,20.9864215801195));
#47765=CARTESIAN_POINT('Ctrl Pts',(31.3286136134484,0.721936793997485,20.9776075996665));
#47766=CARTESIAN_POINT('Ctrl Pts',(31.4704956794702,0.357450862099888,20.9573583812278));
#47767=CARTESIAN_POINT('Ctrl Pts',(31.5050292215643,0.158114714869949,20.9462841508261));
#47768=CARTESIAN_POINT('Ctrl Pts',(31.4940038450927,-0.234658795010768,
20.9244634002772));
#47769=CARTESIAN_POINT('Ctrl Pts',(31.4515503117875,-0.4244189406881,20.9139211699618));
#47770=CARTESIAN_POINT('Ctrl Pts',(31.2960889353342,-0.779942120592769,
20.8941698821893));
#47771=CARTESIAN_POINT('Ctrl Pts',(31.1836334516182,-0.941901166431575,
20.8849503363697));
#47772=CARTESIAN_POINT('Ctrl Pts',(30.9011214218994,-1.21536636315781,20.8637617145378));
#47773=CARTESIAN_POINT('Ctrl Pts',(30.7331593249481,-1.323483412269,20.8526773830162));
#47774=CARTESIAN_POINT('Ctrl Pts',(30.374104697925,-1.46471715060753,20.8314791998208));
#47775=CARTESIAN_POINT('Ctrl Pts',(30.1878361111775,-1.49999999700053,20.821537269196));
#47776=CARTESIAN_POINT('Ctrl Pts',(30.0000000239529,-1.50000000000001,20.8125000011524));
#47777=CARTESIAN_POINT('Origin',(30.,-1.32966554433622E-14,16.));
#47778=CARTESIAN_POINT('',(29.9999999999999,-1.50000000000001,20.25));
#47779=CARTESIAN_POINT('',(30.0000000000001,-1.50000000000001,20.3125));
#47780=CARTESIAN_POINT('',(30.,-1.50000000000001,16.));
#47781=CARTESIAN_POINT('Ctrl Pts',(29.9999999999999,-1.50000000000001,20.25));
#47782=CARTESIAN_POINT('Ctrl Pts',(30.1641246040904,-1.50000000000003,20.257896448696));
#47783=CARTESIAN_POINT('Ctrl Pts',(30.3273129308388,-1.47306839847894,20.2664959507697));
#47784=CARTESIAN_POINT('Ctrl Pts',(30.6694540696788,-1.35668483193177,20.2861901008358));
#47785=CARTESIAN_POINT('Ctrl Pts',(30.8415535621189,-1.25719932144175,20.2972337279289));
#47786=CARTESIAN_POINT('Ctrl Pts',(31.1383891848058,-0.996648092240175,
20.3187527726287));
#47787=CARTESIAN_POINT('Ctrl Pts',(31.2598762410215,-0.837810488997904,
20.3284549728335));
#47788=CARTESIAN_POINT('Ctrl Pts',(31.4314249865634,-0.487683998530185,
20.3479064445261));
#47789=CARTESIAN_POINT('Ctrl Pts',(31.4819950779928,-0.300804420279551,
20.3582886433178));
#47790=CARTESIAN_POINT('Ctrl Pts',(31.5105507066295,0.0893179172321859,
20.3799621065129));
#47791=CARTESIAN_POINT('Ctrl Pts',(31.4853246402279,0.289072829407564,20.3910596016338));
#47792=CARTESIAN_POINT('Ctrl Pts',(31.3605672791737,0.660112394093701,20.411672910783));
#47793=CARTESIAN_POINT('Ctrl Pts',(31.2649722312571,0.828695575895264,20.4204916500332));
#47794=CARTESIAN_POINT('Ctrl Pts',(31.0140581775355,1.12220790918685,20.4407168784407));
#47795=CARTESIAN_POINT('Ctrl Pts',(30.8605226301063,1.24384616367647,20.4514827013131));
#47796=CARTESIAN_POINT('Ctrl Pts',(30.5114243415045,1.42407146100134,20.4732849588136));
#47797=CARTESIAN_POINT('Ctrl Pts',(30.3183380047095,1.47926213924964,20.4841079039198));
#47798=CARTESIAN_POINT('Ctrl Pts',(29.9307960888716,1.51038882263748,20.5036181531332));
#47799=CARTESIAN_POINT('Ctrl Pts',(29.7403288665302,1.48951380456358,20.5127847164407));
#47800=CARTESIAN_POINT('Ctrl Pts',(29.3711639835748,1.37589985350485,20.5337021132381));
#47801=CARTESIAN_POINT('Ctrl Pts',(29.1966946677341,1.28188655628153,20.5447077525887));
#47802=CARTESIAN_POINT('Ctrl Pts',(28.8909965958092,1.02962579258236,20.5664229013678));
#47803=CARTESIAN_POINT('Ctrl Pts',(28.7637626025144,0.872753791453066,20.5765136782526));
#47804=CARTESIAN_POINT('Ctrl Pts',(28.582295287402,0.526054660802727,20.5957747410665));
#47805=CARTESIAN_POINT('Ctrl Pts',(28.5268265400693,0.341112810094873,20.6060492883281));
#47806=CARTESIAN_POINT('Ctrl Pts',(28.4876154625531,-0.0470049788678421,
20.6276113877149));
#47807=CARTESIAN_POINT('Ctrl Pts',(28.5071470207889,-0.246809925970759,
20.6387116625539));
#47808=CARTESIAN_POINT('Ctrl Pts',(28.6213243381125,-0.621726643029005,
20.6595403690571));
#47809=CARTESIAN_POINT('Ctrl Pts',(28.7127069454602,-0.793828860292424,
20.6684492190444));
#47810=CARTESIAN_POINT('Ctrl Pts',(28.9560213000323,-1.09433750409046,20.6885031487146));
#47811=CARTESIAN_POINT('Ctrl Pts',(29.1057854975977,-1.21976733917156,20.6991928441151));
#47812=CARTESIAN_POINT('Ctrl Pts',(29.4493247586543,-1.40936219023255,20.7209879081598));
#47813=CARTESIAN_POINT('Ctrl Pts',(29.6408325610402,-1.46988527163767,20.7318830283038));
#47814=CARTESIAN_POINT('Ctrl Pts',(29.8922912775479,-1.4971028845898,20.7447373862468));
#47815=CARTESIAN_POINT('Ctrl Pts',(29.9461731363168,-1.50000000000001,20.7474102538136));
#47816=CARTESIAN_POINT('Ctrl Pts',(29.9999999999998,-1.50000000000001,20.75));
#47817=CARTESIAN_POINT('Ctrl Pts',(30.0000000239529,-1.50000000000001,20.8125000011524));
#47818=CARTESIAN_POINT('Ctrl Pts',(29.9974904007656,-1.50000000004009,20.8123792568517));
#47819=CARTESIAN_POINT('Ctrl Pts',(29.994980514477,-1.49999370187214,20.8122583249421));
#47820=CARTESIAN_POINT('Ctrl Pts',(29.7936662704942,-1.49898314378545,20.8025445178046));
#47821=CARTESIAN_POINT('Ctrl Pts',(29.5970666373285,-1.45847246315053,20.7919603168594));
#47822=CARTESIAN_POINT('Ctrl Pts',(29.2341811004286,-1.30450218441903,20.7702240261379));
#47823=CARTESIAN_POINT('Ctrl Pts',(29.0708854167951,-1.19371554978206,20.7592900523783));
#47824=CARTESIAN_POINT('Ctrl Pts',(28.7996246113049,-0.919409908918738,
20.738619409654));
#47825=CARTESIAN_POINT('Ctrl Pts',(28.6928036628702,-0.759898893507146,
20.7297166051949));
#47826=CARTESIAN_POINT('Ctrl Pts',(28.540323338491,-0.399638425423168,20.7097021347457));
#47827=CARTESIAN_POINT('Ctrl Pts',(28.4999872115666,-0.200774562873281,
20.6986541423819));
#47828=CARTESIAN_POINT('Ctrl Pts',(28.5000123038317,0.193260173251348,20.6767633237083));
#47829=CARTESIAN_POINT('Ctrl Pts',(28.5373370740434,0.384636586987589,20.6661313007229));
#47830=CARTESIAN_POINT('Ctrl Pts',(28.6828216865171,0.743407395273799,20.6461995891515));
#47831=CARTESIAN_POINT('Ctrl Pts',(28.7898502936129,0.90727948583588,20.637187813622));
#47832=CARTESIAN_POINT('Ctrl Pts',(29.0635269308615,1.18843769395866,20.6162105900475));
#47833=CARTESIAN_POINT('Ctrl Pts',(29.228755223573,1.30174519776628,20.6051136094466));
#47834=CARTESIAN_POINT('Ctrl Pts',(29.5868470804747,1.45456710532649,20.5836398539607));
#47835=CARTESIAN_POINT('Ctrl Pts',(29.7752048690842,1.49530975495507,20.5734457453635));
#47836=CARTESIAN_POINT('Ctrl Pts',(30.1648759814307,1.50410182396658,20.5544534610902));
#47837=CARTESIAN_POINT('Ctrl Pts',(30.3625681263815,1.46904639647318,20.544196110566));
#47838=CARTESIAN_POINT('Ctrl Pts',(30.7301648562918,1.32486538129436,20.5225050764527));
#47839=CARTESIAN_POINT('Ctrl Pts',(30.8968384149473,1.21823387618242,20.5115240048699));
#47840=CARTESIAN_POINT('Ctrl Pts',(31.1754315899033,0.951036194862134,20.4906980266758));
#47841=CARTESIAN_POINT('Ctrl Pts',(31.2863099173977,0.794671992670377,20.4816484440372));
#47842=CARTESIAN_POINT('Ctrl Pts',(31.4475104523221,0.440765387920731,20.4619869659956));
#47843=CARTESIAN_POINT('Ctrl Pts',(31.4931266838049,0.245180433281527,20.4511211351823));
#47844=CARTESIAN_POINT('Ctrl Pts',(31.505277935416,-0.147222207316758,20.4293209884824));
#47845=CARTESIAN_POINT('Ctrl Pts',(31.4737006088925,-0.340229130529765,
20.4185983816372));
#47846=CARTESIAN_POINT('Ctrl Pts',(31.339252899941,-0.702504700740186,20.39847196107));
#47847=CARTESIAN_POINT('Ctrl Pts',(31.2380795698328,-0.868488363198902,
20.3896091209879));
#47848=CARTESIAN_POINT('Ctrl Pts',(30.9741217873874,-1.15788922779948,20.3688705333532));
#47849=CARTESIAN_POINT('Ctrl Pts',(30.8120536546578,-1.27678494801521,20.3577703677868));
#47850=CARTESIAN_POINT('Ctrl Pts',(30.4578087067642,-1.44121172280179,20.3361593393739));
#47851=CARTESIAN_POINT('Ctrl Pts',(30.2702179556352,-1.48784534045563,20.3258384968839));
#47852=CARTESIAN_POINT('Ctrl Pts',(30.052598998323,-1.49930896382792,20.3150498659359));
#47853=CARTESIAN_POINT('Ctrl Pts',(30.0262877690999,-1.50000000000001,20.3137647708805));
#47854=CARTESIAN_POINT('Ctrl Pts',(30.0000000000001,-1.50000000000001,20.3125));
#47855=CARTESIAN_POINT('Origin',(30.,-1.32966554433622E-14,16.));
#47856=CARTESIAN_POINT('',(29.9999999508795,-1.50000000000001,19.7499999952734));
#47857=CARTESIAN_POINT('',(30.0000000000001,-1.50000000000001,19.8125));
#47858=CARTESIAN_POINT('',(30.,-1.50000000000001,16.));
#47859=CARTESIAN_POINT('Ctrl Pts',(29.9999999507652,-1.50000000000001,19.7499999976312));
#47860=CARTESIAN_POINT('Ctrl Pts',(30.0036354883629,-1.50000000011934,19.7501749125187));
#47861=CARTESIAN_POINT('Ctrl Pts',(30.007271600744,-1.4999867831078,19.7503502221899));
#47862=CARTESIAN_POINT('Ctrl Pts',(30.201622915749,-1.49857339489822,19.7597402149765));
#47863=CARTESIAN_POINT('Ctrl Pts',(30.3903004853368,-1.46082693625102,19.769866481516));
#47864=CARTESIAN_POINT('Ctrl Pts',(30.7502056783764,-1.31393443624912,19.7912627754119));
#47865=CARTESIAN_POINT('Ctrl Pts',(30.9169691324023,-1.2034971179945,19.8023538891195));
#47866=CARTESIAN_POINT('Ctrl Pts',(31.1955532827852,-0.926587489668503,
19.8234492094243));
#47867=CARTESIAN_POINT('Ctrl Pts',(31.305583357368,-0.763777918932018,19.8325678933928));
#47868=CARTESIAN_POINT('Ctrl Pts',(31.4566154175894,-0.406803589900389,
19.8523998005612));
#47869=CARTESIAN_POINT('Ctrl Pts',(31.4968003232487,-0.216309448389897,
19.8629828084229));
#47870=CARTESIAN_POINT('Ctrl Pts',(31.5029527191874,0.177060648076386,19.884836702671));
#47871=CARTESIAN_POINT('Ctrl Pts',(31.4658451495388,0.376207311237188,19.8959004061799));
#47872=CARTESIAN_POINT('Ctrl Pts',(31.3192558360179,0.738832237635632,19.9160462354243));
#47873=CARTESIAN_POINT('Ctrl Pts',(31.2148503942445,0.900251242918639,19.9248907954582));
#47874=CARTESIAN_POINT('Ctrl Pts',(30.9479657510409,1.17875033469753,19.9454673747239));
#47875=CARTESIAN_POINT('Ctrl Pts',(30.7867234803792,1.29195591113542,19.9563697464337));
#47876=CARTESIAN_POINT('Ctrl Pts',(30.4266603329508,1.45171184585212,19.9781309575447));
#47877=CARTESIAN_POINT('Ctrl Pts',(30.2307253625385,1.49542562590392,19.9887721548721));
#47878=CARTESIAN_POINT('Ctrl Pts',(29.8418323593176,1.50370934578551,20.0077128815434));
#47879=CARTESIAN_POINT('Ctrl Pts',(29.6526184508184,1.47157346290215,20.0175030286082));
#47880=CARTESIAN_POINT('Ctrl Pts',(29.2894512067405,1.33570909972092,20.038749930874));
#47881=CARTESIAN_POINT('Ctrl Pts',(29.1199599079427,1.2306626568369,20.0498225415362));
#47882=CARTESIAN_POINT('Ctrl Pts',(28.8323016398048,0.961771765690436,20.0711316978356));
#47883=CARTESIAN_POINT('Ctrl Pts',(28.7166359490173,0.80092922531751,20.0805039319268));
#47884=CARTESIAN_POINT('Ctrl Pts',(28.5553841103709,0.447325657819572,20.1001485745656));
#47885=CARTESIAN_POINT('Ctrl Pts',(28.5099861175222,0.258564005548656,20.1106353330251));
#47886=CARTESIAN_POINT('Ctrl Pts',(28.4926188058233,-0.133342134639988,
20.1324078963689));
#47887=CARTESIAN_POINT('Ctrl Pts',(28.5237938243712,-0.332877530953282,
20.1434931961641));
#47888=CARTESIAN_POINT('Ctrl Pts',(28.6595170927538,-0.699759711689848,
20.1638755395383));
#47889=CARTESIAN_POINT('Ctrl Pts',(28.759513047986,-0.864726488741114,20.1726705572702));
#47890=CARTESIAN_POINT('Ctrl Pts',(29.0184002150316,-1.15079879551533,20.1930727248681));
#47891=CARTESIAN_POINT('Ctrl Pts',(29.1758229214277,-1.26830528519454,20.2039107975187));
#47892=CARTESIAN_POINT('Ctrl Pts',(29.5305217931358,-1.4384406773805,20.2257022380569));
#47893=CARTESIAN_POINT('Ctrl Pts',(29.7251117157194,-1.4879453135066,20.2364395788536));
#47894=CARTESIAN_POINT('Ctrl Pts',(29.9491466954872,-1.49935402178859,20.2475353754067));
#47895=CARTESIAN_POINT('Ctrl Pts',(29.9745837219083,-1.50000000000001,20.2487771587502));
#47896=CARTESIAN_POINT('Ctrl Pts',(29.9999999999999,-1.50000000000001,20.25));
#47897=CARTESIAN_POINT('Ctrl Pts',(30.0000000000001,-1.50000000000001,20.3125));
#47898=CARTESIAN_POINT('Ctrl Pts',(29.8275998140085,-1.50000000000001,20.3042053921841));
#47899=CARTESIAN_POINT('Ctrl Pts',(29.6562870357889,-1.47028352574469,20.2951376446808));
#47900=CARTESIAN_POINT('Ctrl Pts',(29.3085931862514,-1.34558031058123,20.2749452383464));
#47901=CARTESIAN_POINT('Ctrl Pts',(29.1384186293223,-1.24350663328035,20.2639223312337));
#47902=CARTESIAN_POINT('Ctrl Pts',(28.8520258822514,-0.983987574399218,
20.242934391019));
#47903=CARTESIAN_POINT('Ctrl Pts',(28.7368098691781,-0.830906588856551,
20.2336614771587));
#47904=CARTESIAN_POINT('Ctrl Pts',(28.5656483010559,-0.481857271883387,
20.214269848438));
#47905=CARTESIAN_POINT('Ctrl Pts',(28.5144799811963,-0.287679235979695,
20.2034821797766));
#47906=CARTESIAN_POINT('Ctrl Pts',(28.4911007681834,0.104720249591022,20.181682208356));
#47907=CARTESIAN_POINT('Ctrl Pts',(28.5173310962609,0.299077411990059,20.1708845882228));
#47908=CARTESIAN_POINT('Ctrl Pts',(28.6416246239434,0.664496311411631,20.1505835382549));
#47909=CARTESIAN_POINT('Ctrl Pts',(28.7375408574377,0.832427515421977,20.1417837739438));
#47910=CARTESIAN_POINT('Ctrl Pts',(28.9926175512114,1.12917452204563,20.1212684183864));
#47911=CARTESIAN_POINT('Ctrl Pts',(29.1516633795811,1.2530630770023,20.1101749736523));
#47912=CARTESIAN_POINT('Ctrl Pts',(29.5021040725661,1.42792836972927,20.0884570187074));
#47913=CARTESIAN_POINT('Ctrl Pts',(29.6888418601191,1.47989191267207,20.0780291609664));
#47914=CARTESIAN_POINT('Ctrl Pts',(30.0769287467939,1.5109546306831,20.0584944686474));
#47915=CARTESIAN_POINT('Ctrl Pts',(30.2747213678695,1.48776626200004,20.0489426359701));
#47916=CARTESIAN_POINT('Ctrl Pts',(30.6499367323256,1.36617967610523,20.027512673167));
#47917=CARTESIAN_POINT('Ctrl Pts',(30.8236685705517,1.26902858360925,20.0164553547449));
#47918=CARTESIAN_POINT('Ctrl Pts',(31.1182297704941,1.01768973269335,19.9953016376572));
#47919=CARTESIAN_POINT('Ctrl Pts',(31.2380227260335,0.867983838688731,19.9857213243715));
#47920=CARTESIAN_POINT('Ctrl Pts',(31.4194655172301,0.52407745893419,19.9666154143852));
#47921=CARTESIAN_POINT('Ctrl Pts',(31.4763477416476,0.331530482038543,19.9559183601132));
#47922=CARTESIAN_POINT('Ctrl Pts',(31.5113890098208,-0.0605236259430762,
19.9341375763365));
#47923=CARTESIAN_POINT('Ctrl Pts',(31.4907606610887,-0.256127601642152,
19.9232706887976));
#47924=CARTESIAN_POINT('Ctrl Pts',(31.3770092904839,-0.62473058770716,19.9027927451274));
#47925=CARTESIAN_POINT('Ctrl Pts',(31.2864311739689,-0.794691675228615,
19.8939853466257));
#47926=CARTESIAN_POINT('Ctrl Pts',(31.0405043429371,-1.09883901947073,19.8737046491109));
#47927=CARTESIAN_POINT('Ctrl Pts',(30.8847013390568,-1.22775605549742,19.8626275448131));
#47928=CARTESIAN_POINT('Ctrl Pts',(30.5384592288504,-1.41320441242881,19.8408176202706));
#47929=CARTESIAN_POINT('Ctrl Pts',(30.3527481344157,-1.47060245170435,19.8302882010938));
#47930=CARTESIAN_POINT('Ctrl Pts',(30.1075898199807,-1.49710947656403,19.8177567099449));
#47931=CARTESIAN_POINT('Ctrl Pts',(30.0537655536404,-1.50000000000001,19.8150867964056));
#47932=CARTESIAN_POINT('Ctrl Pts',(30.0000000000003,-1.50000000000001,19.8125));
#47933=CARTESIAN_POINT('Origin',(30.,-1.32966554433622E-14,16.));
#47934=CARTESIAN_POINT('',(30.0000000000001,-1.50000000000001,19.25));
#47935=CARTESIAN_POINT('',(30.,-1.50000000000001,19.3125));
#47936=CARTESIAN_POINT('',(30.,-1.50000000000001,16.));
#47937=CARTESIAN_POINT('Ctrl Pts',(30.0000000000001,-1.50000000000001,19.25));
#47938=CARTESIAN_POINT('Ctrl Pts',(30.0322695745912,-1.50000000000001,19.2515525706314));
#47939=CARTESIAN_POINT('Ctrl Pts',(30.0645714825038,-1.49895869986435,19.2531356219044));
#47940=CARTESIAN_POINT('Ctrl Pts',(30.2882590679586,-1.48448482383795,19.2642998479893));
#47941=CARTESIAN_POINT('Ctrl Pts',(30.4754930135539,-1.43550485550641,19.2746687000727));
#47942=CARTESIAN_POINT('Ctrl Pts',(30.8281012978914,-1.26647563555772,19.2963288301724));
#47943=CARTESIAN_POINT('Ctrl Pts',(30.9888581275123,-1.14537453755813,19.3074271661326));
#47944=CARTESIAN_POINT('Ctrl Pts',(31.2489169787693,-0.852727854965852,
19.328068327964));
#47945=CARTESIAN_POINT('Ctrl Pts',(31.3477723438117,-0.685891580063111,
19.3368949122188));
#47946=CARTESIAN_POINT('Ctrl Pts',(31.4777710225729,-0.322229436301838,
19.35709836465));
#47947=CARTESIAN_POINT('Ctrl Pts',(31.5070120496637,-0.128613045958812,
19.3678548307802));
#47948=CARTESIAN_POINT('Ctrl Pts',(31.4899431617665,0.263827999699887,19.3896571110945));
#47949=CARTESIAN_POINT('Ctrl Pts',(31.4418890858574,0.458816520684437,19.4004898067048));
#47950=CARTESIAN_POINT('Ctrl Pts',(31.2763170645903,0.810606892156535,19.420033716231));
#47951=CARTESIAN_POINT('Ctrl Pts',(31.1635461572557,0.965528328551652,19.4291724240899));
#47952=CARTESIAN_POINT('Ctrl Pts',(30.8815440072885,1.22938524433353,19.4500696176279));
#47953=CARTESIAN_POINT('Ctrl Pts',(30.713328176096,1.33404197013925,19.4610700368521));
#47954=CARTESIAN_POINT('Ctrl Pts',(30.3423586225268,1.47407873960012,19.4828082280827));
#47955=CARTESIAN_POINT('Ctrl Pts',(30.1427440803289,1.50655371354715,19.4929501746347));
#47956=CARTESIAN_POINT('Ctrl Pts',(29.7515262729803,1.4915957790601,19.5121881483469));
#47957=CARTESIAN_POINT('Ctrl Pts',(29.563545020268,1.44778515274356,19.522449362427));
#47958=CARTESIAN_POINT('Ctrl Pts',(29.2074099124303,1.28891068317319,19.5439971005021));
#47959=CARTESIAN_POINT('Ctrl Pts',(29.0438038910602,1.17268375630169,19.5550971246218));
#47960=CARTESIAN_POINT('Ctrl Pts',(28.7751767012687,0.88721540741588,19.5759511326745));
#47961=CARTESIAN_POINT('Ctrl Pts',(28.6712044325382,0.722248138115754,19.5848751034381));
#47962=CARTESIAN_POINT('Ctrl Pts',(28.5314450700553,0.361647735614998,19.6049084591326));
#47963=CARTESIAN_POINT('Ctrl Pts',(28.4970926988021,0.169404578017586,19.6155886345547));
#47964=CARTESIAN_POINT('Ctrl Pts',(28.5033789257342,-0.222871075081128,
19.6373817263935));
#47965=CARTESIAN_POINT('Ctrl Pts',(28.5460751647458,-0.419126971559099,
19.6482848317533));
#47966=CARTESIAN_POINT('Ctrl Pts',(28.7020419000445,-0.77553505760853,19.6680852809783));
#47967=CARTESIAN_POINT('Ctrl Pts',(28.8106757232385,-0.933630997355151,
19.6770461367592));
#47968=CARTESIAN_POINT('Ctrl Pts',(29.0852161697017,-1.20477024704427,19.697786615973));
#47969=CARTESIAN_POINT('Ctrl Pts',(29.2500326897204,-1.31371406923191,19.7087425717726));
#47970=CARTESIAN_POINT('Ctrl Pts',(29.611734771314,-1.46197087611401,19.7302632159228));
#47971=CARTESIAN_POINT('Ctrl Pts',(29.8049901134984,-1.49999999359916,19.7406175822833));
#47972=CARTESIAN_POINT('Ctrl Pts',(29.9999999507652,-1.50000000000001,19.7499999976312));
#47973=CARTESIAN_POINT('Ctrl Pts',(30.0000000000003,-1.50000000000001,19.8125));
#47974=CARTESIAN_POINT('Ctrl Pts',(29.8589500630315,-1.50000000000001,19.8057137317435));
#47975=CARTESIAN_POINT('Ctrl Pts',(29.7183576297039,-1.48011045726929,19.7983969878431));
#47976=CARTESIAN_POINT('Ctrl Pts',(29.392433533781,-1.38562863633522,19.7800914624408));
#47977=CARTESIAN_POINT('Ctrl Pts',(29.2152602016442,-1.29355450601908,19.7690095917929));
#47978=CARTESIAN_POINT('Ctrl Pts',(28.9125224323809,-1.05055621120639,19.7476941614444));
#47979=CARTESIAN_POINT('Ctrl Pts',(28.7881027470448,-0.904173072558181,
19.7377318373643));
#47980=CARTESIAN_POINT('Ctrl Pts',(28.5965141205021,-0.565467385757126,
19.7189148547643));
#47981=CARTESIAN_POINT('Ctrl Pts',(28.5340212729776,-0.374707579896709,
19.708317087772));
#47982=CARTESIAN_POINT('Ctrl Pts',(28.4874198303467,0.0166598622973653,
19.6865744520946));
#47983=CARTESIAN_POINT('Ctrl Pts',(28.5024461232084,0.213342923270549,19.6756476153738));
#47984=CARTESIAN_POINT('Ctrl Pts',(28.605730933148,0.585021358101511,19.6549988134388));
#47985=CARTESIAN_POINT('Ctrl Pts',(28.6911262279336,0.757019946925095,19.6461115535275));
#47986=CARTESIAN_POINT('Ctrl Pts',(28.9280450078188,1.06829223859541,19.6260663408692));
#47987=CARTESIAN_POINT('Ctrl Pts',(29.0805347242822,1.20204064727676,19.6150144423906));
#47988=CARTESIAN_POINT('Ctrl Pts',(29.4223784266326,1.3977266885599,19.5931317562239));
#47989=CARTESIAN_POINT('Ctrl Pts',(29.6069366918152,1.46041214264913,19.5825109299366));
#47990=CARTESIAN_POINT('Ctrl Pts',(29.9906687655378,1.51247863508202,19.562602320475));
#47991=CARTESIAN_POINT('Ctrl Pts',(30.1862339040192,1.50100007477566,19.55356759697));
#47992=CARTESIAN_POINT('Ctrl Pts',(30.5662821795392,1.40308967236277,19.5325627823883));
#47993=CARTESIAN_POINT('Ctrl Pts',(30.7466285872712,1.31600734425417,19.5214669082421));
#47994=CARTESIAN_POINT('Ctrl Pts',(31.0570470506688,1.08124306107491,19.5000106628701));
#47995=CARTESIAN_POINT('Ctrl Pts',(31.185947420448,0.938076365153711,19.4898320882731));
#47996=CARTESIAN_POINT('Ctrl Pts',(31.387173884418,0.604359282145194,19.4708806565388));
#47997=CARTESIAN_POINT('Ctrl Pts',(31.4549913450499,0.415392173173207,19.460577342954));
#47998=CARTESIAN_POINT('Ctrl Pts',(31.5125364736871,0.0248207245632997,
19.4388789291423));
#47999=CARTESIAN_POINT('Ctrl Pts',(31.5028468405333,-0.172737498474235,
19.4279034723069));
#48000=CARTESIAN_POINT('Ctrl Pts',(31.4094808313587,-0.547250043493136,
19.4070972198059));
#48001=CARTESIAN_POINT('Ctrl Pts',(31.3288984144444,-0.721204660777261,
19.3980698586427));
#48002=CARTESIAN_POINT('Ctrl Pts',(31.1018991125715,-1.03700530321776,19.3783761095713));
#48003=CARTESIAN_POINT('Ctrl Pts',(30.9548507096631,-1.17379817492847,19.3675014379958));
#48004=CARTESIAN_POINT('Ctrl Pts',(30.6204358823266,-1.37933694163779,19.3457024869274));
#48005=CARTESIAN_POINT('Ctrl Pts',(30.4373267027344,-1.44785012953098,19.3349894983086));
#48006=CARTESIAN_POINT('Ctrl Pts',(30.1646733538461,-1.49322482781476,19.3206110496582));
#48007=CARTESIAN_POINT('Ctrl Pts',(30.0823180279059,-1.50000000000001,19.3164605279642));
#48008=CARTESIAN_POINT('Ctrl Pts',(30.,-1.50000000000001,19.3125));
#48009=CARTESIAN_POINT('Origin',(30.,-1.32966554433622E-14,16.));
#48010=CARTESIAN_POINT('',(30.0000000000001,-1.50000000000001,18.75));
#48011=CARTESIAN_POINT('',(30.,-1.50000000000001,18.8125));
#48012=CARTESIAN_POINT('',(30.,-1.50000000000001,16.));
#48013=CARTESIAN_POINT('Ctrl Pts',(30.0000000000002,-1.50000000000001,18.75));
#48014=CARTESIAN_POINT('Ctrl Pts',(30.0598815861698,-1.50000000000001,18.7528810541579));
#48015=CARTESIAN_POINT('Ctrl Pts',(30.1198247627216,-1.4964145214846,18.7558646682098));
#48016=CARTESIAN_POINT('Ctrl Pts',(30.3709807388755,-1.46613984657296,18.7687893789386));
#48017=CARTESIAN_POINT('Ctrl Pts',(30.5561899070999,-1.40635296128044,18.7793610060131));
#48018=CARTESIAN_POINT('Ctrl Pts',(30.9004833554958,-1.21627199481911,18.8012058591186));
#48019=CARTESIAN_POINT('Ctrl Pts',(31.054808880873,-1.08516465668695,18.8122727199239));
#48020=CARTESIAN_POINT('Ctrl Pts',(31.2966795386424,-0.777790002612556,
18.832447912207));
#48021=CARTESIAN_POINT('Ctrl Pts',(31.3849156897549,-0.606916752329299,
18.8412824026485));
#48022=CARTESIAN_POINT('Ctrl Pts',(31.4939654845851,-0.236921615045211,
18.8618376880532));
#48023=CARTESIAN_POINT('Ctrl Pts',(31.5120817444602,-0.0408132290769898,
18.8727325983848));
#48024=CARTESIAN_POINT('Ctrl Pts',(31.4718441015158,0.350974679810523,18.8944985933229));
#48025=CARTESIAN_POINT('Ctrl Pts',(31.4124332725198,0.54273929222595,18.9051521829016));
#48026=CARTESIAN_POINT('Ctrl Pts',(31.2264254338517,0.884320880490274,18.9241289378051));
#48027=CARTESIAN_POINT('Ctrl Pts',(31.1045648671413,1.03253115218655,18.9338713522791));
#48028=CARTESIAN_POINT('Ctrl Pts',(30.8063387149155,1.2801510812434,18.9550980960807));
#48029=CARTESIAN_POINT('Ctrl Pts',(30.6310491381331,1.37504484021148,18.9661676575249));
#48030=CARTESIAN_POINT('Ctrl Pts',(30.2546711108962,1.4912245976519,18.9875033692879));
#48031=CARTESIAN_POINT('Ctrl Pts',(30.05740041095,1.51172051693628,18.9969127515258));
#48032=CARTESIAN_POINT('Ctrl Pts',(29.6702738320324,1.47589654334487,19.0165334981157));
#48033=CARTESIAN_POINT('Ctrl Pts',(29.4839742576828,1.42150925053353,19.0270075986994));
#48034=CARTESIAN_POINT('Ctrl Pts',(29.1353660189379,1.24191643228194,19.048768709802));
#48035=CARTESIAN_POINT('Ctrl Pts',(28.9777462443354,1.1157773991078,19.059856056776));
#48036=CARTESIAN_POINT('Ctrl Pts',(28.7267374929236,0.815719209989595,19.0802676706567));
#48037=CARTESIAN_POINT('Ctrl Pts',(28.6332044534767,0.64688991790973,19.0890616712273));
#48038=CARTESIAN_POINT('Ctrl Pts',(28.5135873974093,0.280047942578678,19.109441780968));
#48039=CARTESIAN_POINT('Ctrl Pts',(28.4898364137009,0.0851180238092936,
19.1202712208996));
#48040=CARTESIAN_POINT('Ctrl Pts',(28.5183897482981,-0.307171243363851,
19.1420650690759));
#48041=CARTESIAN_POINT('Ctrl Pts',(28.5720998196786,-0.500646940480604,
19.1528137189157));
#48042=CARTESIAN_POINT('Ctrl Pts',(28.747829861517,-0.847427013151625,19.1720792785085));
#48043=CARTESIAN_POINT('Ctrl Pts',(28.8650664758991,-0.999006868470888,
19.1814790094866));
#48044=CARTESIAN_POINT('Ctrl Pts',(29.1550741400796,-1.25492382568339,19.2025408141021));
#48045=CARTESIAN_POINT('Ctrl Pts',(29.3268372187205,-1.35483766663846,19.2135801535473));
#48046=CARTESIAN_POINT('Ctrl Pts',(29.6699517271029,-1.47262040644266,19.2333600008011));
#48047=CARTESIAN_POINT('Ctrl Pts',(29.8345144389513,-1.50000000000001,19.2420380722318));
#48048=CARTESIAN_POINT('Ctrl Pts',(30.0000000000001,-1.50000000000001,19.25));
#48049=CARTESIAN_POINT('Ctrl Pts',(30.,-1.50000000000001,19.3125));
#48050=CARTESIAN_POINT('Ctrl Pts',(29.8904115959066,-1.50000000000001,19.3072274254497));
#48051=CARTESIAN_POINT('Ctrl Pts',(29.7809217474217,-1.48799325955223,19.3016260720903));
#48052=CARTESIAN_POINT('Ctrl Pts',(29.479267613868,-1.42071467340943,19.2852438812078));
#48053=CARTESIAN_POINT('Ctrl Pts',(29.2956191224553,-1.33919024824593,19.2741435216794));
#48054=CARTESIAN_POINT('Ctrl Pts',(28.9769843310201,-1.11359538988626,19.2525466742853));
#48055=CARTESIAN_POINT('Ctrl Pts',(28.8433197059369,-0.97404728751911,19.2422393958357));
#48056=CARTESIAN_POINT('Ctrl Pts',(28.6314369352188,-0.64558462894177,19.2229212185382));
#48057=CARTESIAN_POINT('Ctrl Pts',(28.5578261508896,-0.458159789494097,
19.2129533216385));
#48058=CARTESIAN_POINT('Ctrl Pts',(28.4887314396478,-0.0683254796838233,
19.1912958599824));
#48059=CARTESIAN_POINT('Ctrl Pts',(28.4927829468086,0.129998312926432,19.180277871504));
#48060=CARTESIAN_POINT('Ctrl Pts',(28.5757061903925,0.507408017565263,19.1593106656908));
#48061=CARTESIAN_POINT('Ctrl Pts',(28.6513157241137,0.683452060166118,19.1500704896955));
#48062=CARTESIAN_POINT('Ctrl Pts',(28.8692063981292,1.00541452618758,19.1306438179201));
#48063=CARTESIAN_POINT('Ctrl Pts',(29.0123062748592,1.14629480240063,19.119845580885));
#48064=CARTESIAN_POINT('Ctrl Pts',(29.3411837772215,1.36149831072911,19.0980445794436));
#48065=CARTESIAN_POINT('Ctrl Pts',(29.5228193452006,1.43527924918368,19.0872561635921));
#48066=CARTESIAN_POINT('Ctrl Pts',(29.9017346505858,1.50901487689319,19.0669773805809));
#48067=CARTESIAN_POINT('Ctrl Pts',(30.095243866884,1.50920856983617,19.0581733709244));
#48068=CARTESIAN_POINT('Ctrl Pts',(30.4795337547919,1.43522535350299,19.0376291257293));
#48069=CARTESIAN_POINT('Ctrl Pts',(30.6659951148259,1.35877256279477,19.0265343107311));
#48070=CARTESIAN_POINT('Ctrl Pts',(30.9917525251624,1.14161337833726,19.0048291004505));
#48071=CARTESIAN_POINT('Ctrl Pts',(31.12959203788,1.00543319777699,18.9944145110095));
#48072=CARTESIAN_POINT('Ctrl Pts',(31.3495099297643,0.683969951441068,18.9749041718824));
#48073=CARTESIAN_POINT('Ctrl Pts',(31.4277388995994,0.500572833869038,18.9653096018815));
#48074=CARTESIAN_POINT('Ctrl Pts',(31.5085610210805,0.114360476914036,18.9438533598284));
#48075=CARTESIAN_POINT('Ctrl Pts',(31.510521839189,-0.0846024989690804,
18.9327998611683));
#48076=CARTESIAN_POINT('Ctrl Pts',(31.4387139095947,-0.464995267712227,
18.9116669295714));
#48077=CARTESIAN_POINT('Ctrl Pts',(31.3683024334794,-0.643299822803022,
18.9021297086694));
#48078=CARTESIAN_POINT('Ctrl Pts',(31.1599775839064,-0.97159308723095,18.8829874173259));
#48079=CARTESIAN_POINT('Ctrl Pts',(31.021122395481,-1.11661364586043,18.8722783951071));
#48080=CARTESIAN_POINT('Ctrl Pts',(30.6983237124874,-1.34174379218127,18.8504941210548));
#48081=CARTESIAN_POINT('Ctrl Pts',(30.5183853004494,-1.42099198981035,18.8396354913461));
#48082=CARTESIAN_POINT('Ctrl Pts',(30.220307982392,-1.48785706899676,18.8234368763837));
#48083=CARTESIAN_POINT('Ctrl Pts',(30.1102084329115,-1.50000000000001,18.8178024057007));
#48084=CARTESIAN_POINT('Ctrl Pts',(30.,-1.50000000000001,18.8125));
#48085=CARTESIAN_POINT('Origin',(30.,-1.32966554433622E-14,16.));
#48086=CARTESIAN_POINT('',(30.,-1.50000000000001,18.25));
#48087=CARTESIAN_POINT('',(29.9999999999999,-1.50000000000001,18.3125));
#48088=CARTESIAN_POINT('',(30.,-1.50000000000001,16.));
#48089=CARTESIAN_POINT('Ctrl Pts',(30.,-1.50000000000001,18.25));
#48090=CARTESIAN_POINT('Ctrl Pts',(30.0882156275205,-1.50000000000001,18.254244276358));
#48091=CARTESIAN_POINT('Ctrl Pts',(30.1764501130872,-1.49221937550789,18.2587055884823));
#48092=CARTESIAN_POINT('Ctrl Pts',(30.4546079281867,-1.44254775409159,18.2734682298626));
#48093=CARTESIAN_POINT('Ctrl Pts',(30.6370980720641,-1.37175281599007,18.2842148170619));
#48094=CARTESIAN_POINT('Ctrl Pts',(30.9691525442989,-1.16201577961996,18.3060168240942));
#48095=CARTESIAN_POINT('Ctrl Pts',(31.1145075241426,-1.02344071977941,18.3168595260404));
#48096=CARTESIAN_POINT('Ctrl Pts',(31.3375735551139,-0.704962761586156,
18.3364384054093));
#48097=CARTESIAN_POINT('Ctrl Pts',(31.4160050795816,-0.530113102524481,
18.345549272082));
#48098=CARTESIAN_POINT('Ctrl Pts',(31.5048780292219,-0.154342998497877,
18.3664253889724));
#48099=CARTESIAN_POINT('Ctrl Pts',(31.5121437205665,0.0435642244476196,
18.3774202346916));
#48100=CARTESIAN_POINT('Ctrl Pts',(31.4493976248982,0.435280459623824,18.3991822477569));
#48101=CARTESIAN_POINT('Ctrl Pts',(31.3782925123276,0.624894161678516,18.4093783750732));
#48102=CARTESIAN_POINT('Ctrl Pts',(31.1707210215853,0.957071364942045,18.428592307613));
#48103=CARTESIAN_POINT('Ctrl Pts',(31.0393074800838,1.09835818528463,18.4388395784748));
#48104=CARTESIAN_POINT('Ctrl Pts',(30.7245434883219,1.32834442072559,18.4603721746294));
#48105=CARTESIAN_POINT('Ctrl Pts',(30.5424433469957,1.41252449906513,18.4714718072734));
#48106=CARTESIAN_POINT('Ctrl Pts',(30.1611576166725,1.50380428740964,18.492351975203));
#48107=CARTESIAN_POINT('Ctrl Pts',(29.9661847612145,1.51203572283979,18.5012926108002));
#48108=CARTESIAN_POINT('Ctrl Pts',(29.583743920727,1.45401144673963,18.5213045897645));
#48109=CARTESIAN_POINT('Ctrl Pts',(29.3999206687447,1.38827539073469,18.5319747916547));
#48110=CARTESIAN_POINT('Ctrl Pts',(29.0627111089636,1.18787072518152,18.5537655904295));
#48111=CARTESIAN_POINT('Ctrl Pts',(28.9136362676481,1.05327089433686,18.5646768412665));
#48112=CARTESIAN_POINT('Ctrl Pts',(28.6818733006966,0.740747545450625,18.5845087463487));
#48113=CARTESIAN_POINT('Ctrl Pts',(28.5986773683508,0.567862991064222,18.593452056052));
#48114=CARTESIAN_POINT('Ctrl Pts',(28.4999017481138,0.194886335563048,18.6141729813576));
#48115=CARTESIAN_POINT('Ctrl Pts',(28.4872987443723,-0.0022124298529334,
18.6251229127696));
#48116=CARTESIAN_POINT('Ctrl Pts',(28.538885584329,-0.393300822235859,18.6468500456797));
#48117=CARTESIAN_POINT('Ctrl Pts',(28.6038229043615,-0.583241208522858,
18.6573608761808));
#48118=CARTESIAN_POINT('Ctrl Pts',(28.7997809979745,-0.919686600601166,
18.6761346196911));
#48119=CARTESIAN_POINT('Ctrl Pts',(28.9262538190534,-1.06460970419426,18.6862451878989));
#48120=CARTESIAN_POINT('Ctrl Pts',(29.2324514589516,-1.30386842227857,18.7076232042196));
#48121=CARTESIAN_POINT('Ctrl Pts',(29.4110795308611,-1.39369344460164,18.7187125908454));
#48122=CARTESIAN_POINT('Ctrl Pts',(29.7319270119205,-1.48199126728517,18.7366020897721));
#48123=CARTESIAN_POINT('Ctrl Pts',(29.8657845574029,-1.50000000000001,18.7435425565073));
#48124=CARTESIAN_POINT('Ctrl Pts',(30.0000000000002,-1.50000000000001,18.75));
#48125=CARTESIAN_POINT('Ctrl Pts',(30.,-1.50000000000001,18.8125));
#48126=CARTESIAN_POINT('Ctrl Pts',(29.9200694828282,-1.50000000000001,18.8086543411995));
#48127=CARTESIAN_POINT('Ctrl Pts',(29.8400989517173,-1.4936120985387,18.8046293155201));
#48128=CARTESIAN_POINT('Ctrl Pts',(29.5632380932733,-1.44889785862683,18.7900667790378));
#48129=CARTESIAN_POINT('Ctrl Pts',(29.3740258977232,-1.377754564609,18.7789871004233));
#48130=CARTESIAN_POINT('Ctrl Pts',(29.041174726881,-1.16949277461302,18.7571877412774));
#48131=CARTESIAN_POINT('Ctrl Pts',(28.8991316339595,-1.03690216726548,18.7466706173565));
#48132=CARTESIAN_POINT('Ctrl Pts',(28.6710550609186,-0.722648191218263,
18.7269680010074));
#48133=CARTESIAN_POINT('Ctrl Pts',(28.5881967902834,-0.543266122771758,
18.717681451265));
#48134=CARTESIAN_POINT('Ctrl Pts',(28.4956085723343,-0.160873384602161,
18.6964374102556));
#48135=CARTESIAN_POINT('Ctrl Pts',(28.4875239735192,0.0385552236194734,
18.6853580431322));
#48136=CARTESIAN_POINT('Ctrl Pts',(28.5480104653806,0.421875716785893,18.6640624601785));
#48137=CARTESIAN_POINT('Ctrl Pts',(28.6132160700899,0.602522755625134,18.6541515963916));
#48138=CARTESIAN_POINT('Ctrl Pts',(28.8119377533085,0.937035677616922,18.635298569339));
#48139=CARTESIAN_POINT('Ctrl Pts',(28.9464389491764,1.08605274148643,18.6246880146503));
#48140=CARTESIAN_POINT('Ctrl Pts',(29.2628767471001,1.32090830831045,18.6029396282541));
#48141=CARTESIAN_POINT('Ctrl Pts',(29.4409618987283,1.40557199772365,18.5920197332512));
#48142=CARTESIAN_POINT('Ctrl Pts',(29.814809484317,1.50065373381321,18.5713918235674));
#48143=CARTESIAN_POINT('Ctrl Pts',(30.0065604479866,1.51202122412194,18.5625182831912));
#48144=CARTESIAN_POINT('Ctrl Pts',(30.3943911928229,1.4610824148403,18.5424438008558));
#48145=CARTESIAN_POINT('Ctrl Pts',(30.58616263238,1.39524271133166,18.5313883125152));
#48146=CARTESIAN_POINT('Ctrl Pts',(30.9257469654151,1.19593240245758,18.5095136562056));
#48147=CARTESIAN_POINT('Ctrl Pts',(31.0718264769195,1.06698913560375,18.4989036450188));
#48148=CARTESIAN_POINT('Ctrl Pts',(31.3078217753803,0.759832047419874,18.4790171745892));
#48149=CARTESIAN_POINT('Ctrl Pts',(31.3951262846915,0.584269865007977,18.4699594369449));
#48150=CARTESIAN_POINT('Ctrl Pts',(31.4989966927882,0.205709858638526,18.4489283254799));
#48151=CARTESIAN_POINT('Ctrl Pts',(31.5130318328004,0.00600577899638372,
18.4378336543887));
#48152=CARTESIAN_POINT('Ctrl Pts',(31.4635867359632,-0.379900299649008,
18.4163944277973));
#48153=CARTESIAN_POINT('Ctrl Pts',(31.4034385131977,-0.562844950250642,
18.4062308360972));
#48154=CARTESIAN_POINT('Ctrl Pts',(31.213924427377,-0.903263174389702,18.387318712534));
#48155=CARTESIAN_POINT('Ctrl Pts',(31.0836707542498,-1.05603307941032,18.3769705479341));
#48156=CARTESIAN_POINT('Ctrl Pts',(30.7734274797909,-1.30006438227702,18.3552653141303));
#48157=CARTESIAN_POINT('Ctrl Pts',(30.5972523067208,-1.389838711312,18.3442953508018));
#48158=CARTESIAN_POINT('Ctrl Pts',(30.27555179434,-1.4809632576453,18.3262862902852));
#48159=CARTESIAN_POINT('Ctrl Pts',(30.1379932399681,-1.50000000000003,18.3191392028535));
#48160=CARTESIAN_POINT('Ctrl Pts',(29.9999999999998,-1.50000000000001,18.3125));
#48161=CARTESIAN_POINT('Origin',(30.,-1.32966554433622E-14,16.));
#48162=CARTESIAN_POINT('',(30.,-1.50000000000001,17.75));
#48163=CARTESIAN_POINT('',(30.,-1.50000000000001,17.8125));
#48164=CARTESIAN_POINT('',(30.,-1.50000000000001,16.));
#48165=CARTESIAN_POINT('Ctrl Pts',(30.,-1.50000000000001,17.75));
#48166=CARTESIAN_POINT('Ctrl Pts',(30.1165214576707,-1.50000000000002,17.755606141246));
#48167=CARTESIAN_POINT('Ctrl Pts',(30.2328774102524,-1.48642630258387,17.7615813667753));
#48168=CARTESIAN_POINT('Ctrl Pts',(30.5364815251301,-1.41429282343802,17.778192234317));
#48169=CARTESIAN_POINT('Ctrl Pts',(30.7156172892318,-1.33263663661631,17.7890791351975));
#48170=CARTESIAN_POINT('Ctrl Pts',(31.0356297737271,-1.1031687507031,17.8108498509785));
#48171=CARTESIAN_POINT('Ctrl Pts',(31.1725674881258,-0.956358157459637,
17.8215163418689));
#48172=CARTESIAN_POINT('Ctrl Pts',(31.376639002963,-0.625293846242278,17.8405309680715));
#48173=CARTESIAN_POINT('Ctrl Pts',(31.4447439774106,-0.445961069817197,
17.8502243850103));
#48174=CARTESIAN_POINT('Ctrl Pts',(31.5115582160321,-0.0642628969545898,
17.8714298390582));
#48175=CARTESIAN_POINT('Ctrl Pts',(31.5068955968845,0.134928419608339,17.8824960233117));
#48176=CARTESIAN_POINT('Ctrl Pts',(31.4208614242251,0.519471460613856,17.9038595255897));
#48177=CARTESIAN_POINT('Ctrl Pts',(31.3405819882652,0.701086441059189,17.9133091757132));
#48178=CARTESIAN_POINT('Ctrl Pts',(31.1170623100669,1.01937978501502,17.9329047530211));
#48179=CARTESIAN_POINT('Ctrl Pts',(30.9773620677606,1.15399638378434,17.9433654340287));
#48180=CARTESIAN_POINT('Ctrl Pts',(30.6484546459992,1.36726868066811,17.9651142302054));
#48181=CARTESIAN_POINT('Ctrl Pts',(30.4607652253454,1.44139714446346,17.9762035656613));
#48182=CARTESIAN_POINT('Ctrl Pts',(30.0756449322311,1.51026934438856,17.9966457910675));
#48183=CARTESIAN_POINT('Ctrl Pts',(29.8825476840369,1.50759466650969,18.005439964228));
#48184=CARTESIAN_POINT('Ctrl Pts',(29.5047175214704,1.42916638864856,18.025796889674));
#48185=CARTESIAN_POINT('Ctrl Pts',(29.323805468645,1.35298625851431,18.0366171395998));
#48186=CARTESIAN_POINT('Ctrl Pts',(28.9975535579724,1.13341344377778,18.0584131868245));
#48187=CARTESIAN_POINT('Ctrl Pts',(28.8562978602342,0.990703384015885,18.0691735230773));
#48188=CARTESIAN_POINT('Ctrl Pts',(28.6425900107442,0.665955504210131,18.088476321219));
#48189=CARTESIAN_POINT('Ctrl Pts',(28.5692557712623,0.488931672930093,18.0978371292817));
#48190=CARTESIAN_POINT('Ctrl Pts',(28.4911736103312,0.110209786397706,18.118877234089));
#48191=CARTESIAN_POINT('Ctrl Pts',(28.4897399259643,-0.0884146511275797,
18.1299119250627));
#48192=CARTESIAN_POINT('Ctrl Pts',(28.563963673652,-0.476687925939349,18.1514826625522));
#48193=CARTESIAN_POINT('Ctrl Pts',(28.6395954743022,-0.662348456736596,
18.1612794083161));
#48194=CARTESIAN_POINT('Ctrl Pts',(28.8549808751967,-0.987772207975308,
18.1806816918938));
#48195=CARTESIAN_POINT('Ctrl Pts',(28.9904690556508,-1.12587258901724,18.1910364917109));
#48196=CARTESIAN_POINT('Ctrl Pts',(29.3122241078786,-1.34783032180127,18.2126824314563));
#48197=CARTESIAN_POINT('Ctrl Pts',(29.4971108100191,-1.42716337813628,18.2237814930698));
#48198=CARTESIAN_POINT('Ctrl Pts',(29.7935943795659,-1.48934588454492,18.2397733573052));
#48199=CARTESIAN_POINT('Ctrl Pts',(29.8967698772032,-1.50000000000001,18.2450333384012));
#48200=CARTESIAN_POINT('Ctrl Pts',(30.,-1.50000000000001,18.25));
#48201=CARTESIAN_POINT('Ctrl Pts',(29.9999999999998,-1.50000000000001,18.3125));
#48202=CARTESIAN_POINT('Ctrl Pts',(29.9486057940186,-1.50000000000001,18.3100272951118));
#48203=CARTESIAN_POINT('Ctrl Pts',(29.8971583803719,-1.4973588143077,18.3074786639994));
#48204=CARTESIAN_POINT('Ctrl Pts',(29.6480074739756,-1.47161947014145,18.294776403644));
#48205=CARTESIAN_POINT('Ctrl Pts',(29.4562105276991,-1.41203266981329,18.2838933798658));
#48206=CARTESIAN_POINT('Ctrl Pts',(29.1116733937691,-1.22407639141983,18.2620958215476));
#48207=CARTESIAN_POINT('Ctrl Pts',(28.9612380534891,-1.09930641465076,18.2513921651757));
#48208=CARTESIAN_POINT('Ctrl Pts',(28.7165798694464,-0.800027931931824,
18.231307751621));
#48209=CARTESIAN_POINT('Ctrl Pts',(28.6244510402799,-0.628553460673264,
18.2224196367041));
#48210=CARTESIAN_POINT('Ctrl Pts',(28.5083938755392,-0.254315567480426,
18.2016286426378));
#48211=CARTESIAN_POINT('Ctrl Pts',(28.4878541874048,-0.054508044740069,
18.1905282247078));
#48212=CARTESIAN_POINT('Ctrl Pts',(28.5251827599344,0.333985841156563,18.1689452310469));
#48213=CARTESIAN_POINT('Ctrl Pts',(28.5797880070138,0.519280463308488,18.1586510853718));
#48214=CARTESIAN_POINT('Ctrl Pts',(28.7594942565881,0.866593796413574,18.1393559001993));
#48215=CARTESIAN_POINT('Ctrl Pts',(28.8856977548396,1.02381782162173,18.1293391744996));
#48216=CARTESIAN_POINT('Ctrl Pts',(29.1898211855382,1.2775694571787,18.1076583725746));
#48217=CARTESIAN_POINT('Ctrl Pts',(29.3638803222543,1.37256230066096,18.096645258358));
#48218=CARTESIAN_POINT('Ctrl Pts',(29.732534735318,1.48813273455022,18.0756980748094));
#48219=CARTESIAN_POINT('Ctrl Pts',(29.9228794435952,1.51000349618475,18.066488339394));
#48220=CARTESIAN_POINT('Ctrl Pts',(30.3105607244676,1.48091384388274,18.0470279691741));
#48221=CARTESIAN_POINT('Ctrl Pts',(30.5039294602603,1.4267400893485,18.0362196850207));
#48222=CARTESIAN_POINT('Ctrl Pts',(30.8540539626656,1.24831186951753,18.0144179726049));
#48223=CARTESIAN_POINT('Ctrl Pts',(31.0082947964679,1.12740587313612,18.0036385571291));
#48224=CARTESIAN_POINT('Ctrl Pts',(31.2606439376435,0.835225571389926,17.9833812839205));
#48225=CARTESIAN_POINT('Ctrl Pts',(31.3570327509323,0.667298431844612,17.9745721351024));
#48226=CARTESIAN_POINT('Ctrl Pts',(31.4837741625619,0.297001147228916,17.9540000637349));
#48227=CARTESIAN_POINT('Ctrl Pts',(31.5100733842477,0.0972732161684081,
17.9429040675649));
#48228=CARTESIAN_POINT('Ctrl Pts',(31.4835317838137,-0.293194316444828,
17.9212114268642));
#48229=CARTESIAN_POINT('Ctrl Pts',(31.4338905957024,-0.480424140062753,
17.9108097699965));
#48230=CARTESIAN_POINT('Ctrl Pts',(31.2642037542022,-0.83118542637216,17.8913230318682));
#48231=CARTESIAN_POINT('Ctrl Pts',(31.14378015867,-0.99038786521744,17.8816860411746));
#48232=CARTESIAN_POINT('Ctrl Pts',(30.8486060826855,-1.25246692848107,17.8602044978428));
#48233=CARTESIAN_POINT('Ctrl Pts',(30.6769673305094,-1.35296725332812,17.8491548488382));
#48234=CARTESIAN_POINT('Ctrl Pts',(30.3327732686651,-1.47215364288648,17.8292840712733));
#48235=CARTESIAN_POINT('Ctrl Pts',(30.1668871533766,-1.50000000000002,17.8205293619105));
#48236=CARTESIAN_POINT('Ctrl Pts',(29.9999999999999,-1.50000000000001,17.8125));
#48237=CARTESIAN_POINT('Origin',(30.,-1.32966554433622E-14,16.));
#48238=CARTESIAN_POINT('',(29.9999999999999,-1.50000000000001,17.25));
#48239=CARTESIAN_POINT('',(30.,-1.50000000000001,17.3125));
#48240=CARTESIAN_POINT('',(30.,-1.50000000000001,16.));
#48241=CARTESIAN_POINT('Ctrl Pts',(29.9999999999998,-1.50000000000001,17.25));
#48242=CARTESIAN_POINT('Ctrl Pts',(30.1437406795734,-1.50000000000003,17.2569157266704));
#48243=CARTESIAN_POINT('Ctrl Pts',(30.2869532673798,-1.47934432155244,17.2643798143597));
#48244=CARTESIAN_POINT('Ctrl Pts',(30.6133040117111,-1.38286217393555,17.2827614315232));
#48245=CARTESIAN_POINT('Ctrl Pts',(30.7886268831202,-1.29093521604786,17.2937501837148));
#48246=CARTESIAN_POINT('Ctrl Pts',(31.0976621700988,-1.04186059007729,17.3155373905022));
#48247=CARTESIAN_POINT('Ctrl Pts',(31.2270940102629,-0.885739363684009,
17.3257922575731));
#48248=CARTESIAN_POINT('Ctrl Pts',(31.4122925189225,-0.540349731904653,
17.3449805704497));
#48249=CARTESIAN_POINT('Ctrl Pts',(31.4695815451721,-0.356167506723217,
17.3552129162933));
#48250=CARTESIAN_POINT('Ctrl Pts',(31.5127670349393,0.0311250181831806,
17.376729167677));
#48251=CARTESIAN_POINT('Ctrl Pts',(31.4953668358477,0.230908289106308,17.3878282382838));
#48252=CARTESIAN_POINT('Ctrl Pts',(31.3851742993692,0.607249385403804,17.408736076967));
#48253=CARTESIAN_POINT('Ctrl Pts',(31.2953707932844,0.78068569360338,17.4176954906944));
#48254=CARTESIAN_POINT('Ctrl Pts',(31.054895847731,1.08378386704463,17.4376847406135));
#48255=CARTESIAN_POINT('Ctrl Pts',(30.9065553840191,1.21059289157644,17.4483442474051));
#48256=CARTESIAN_POINT('Ctrl Pts',(30.5651448786952,1.40362381134034,17.4701323379946));
#48257=CARTESIAN_POINT('Ctrl Pts',(30.3742618691092,1.46611551598061,17.4810520817598));
#48258=CARTESIAN_POINT('Ctrl Pts',(29.9878426931301,1.51196372025337,17.5009172442622));
#48259=CARTESIAN_POINT('Ctrl Pts',(29.7964276873605,1.49824842026232,17.5098430324513));
#48260=CARTESIAN_POINT('Ctrl Pts',(29.423704438961,1.39861791618851,17.5305432021031));
#48261=CARTESIAN_POINT('Ctrl Pts',(29.2464613140656,1.31164870813791,17.5414866272603));
#48262=CARTESIAN_POINT('Ctrl Pts',(28.9327465597656,1.07261781027188,17.5632199825769));
#48263=CARTESIAN_POINT('Ctrl Pts',(28.8001758891987,0.921899105215767,17.5737833830436));
#48264=CARTESIAN_POINT('Ctrl Pts',(28.6055876448106,0.584753731199478,17.5925136816001));
#48265=CARTESIAN_POINT('Ctrl Pts',(28.5426610065469,0.403064732761888,17.6026075148466));
#48266=CARTESIAN_POINT('Ctrl Pts',(28.487113056257,0.0186136653436067,17.623965907481));
#48267=CARTESIAN_POINT('Ctrl Pts',(28.4978576022209,-0.180959534499292,
17.6350533074722));
#48268=CARTESIAN_POINT('Ctrl Pts',(28.5955062015491,-0.561653522812593,
17.6562029734896));
#48269=CARTESIAN_POINT('Ctrl Pts',(28.6803571582567,-0.739318323214391,
17.6653786075964));
#48270=CARTESIAN_POINT('Ctrl Pts',(28.9119736981394,-1.05041195534416,17.6851637533487));
#48271=CARTESIAN_POINT('Ctrl Pts',(29.0558270731865,-1.1813919096406,17.6957232341464));
#48272=CARTESIAN_POINT('Ctrl Pts',(29.3917078154049,-1.38569020760041,17.7175582566121));
#48273=CARTESIAN_POINT('Ctrl Pts',(29.5820781032457,-1.45448064464283,17.7286282968298));
#48274=CARTESIAN_POINT('Ctrl Pts',(29.8532284268276,-1.49461899708891,17.7427889770903));
#48275=CARTESIAN_POINT('Ctrl Pts',(29.9266397495672,-1.50000000000001,17.7464704533054));
#48276=CARTESIAN_POINT('Ctrl Pts',(30.,-1.50000000000001,17.75));
#48277=CARTESIAN_POINT('Ctrl Pts',(29.9999999999999,-1.50000000000001,17.8125));
#48278=CARTESIAN_POINT('Ctrl Pts',(29.9772840745252,-1.50000000000001,17.811407079526));
#48279=CARTESIAN_POINT('Ctrl Pts',(29.9545509622526,-1.49948399224778,17.8102989986031));
#48280=CARTESIAN_POINT('Ctrl Pts',(29.7331702393738,-1.48941079200354,17.7993680024896));
#48281=CARTESIAN_POINT('Ctrl Pts',(29.5383211874472,-1.44096198242896,17.7886475228419));
#48282=CARTESIAN_POINT('Ctrl Pts',(29.1826189299973,-1.27271128807371,17.7668601596023));
#48283=CARTESIAN_POINT('Ctrl Pts',(29.0244894301944,-1.15598200374574,17.7560096703756));
#48284=CARTESIAN_POINT('Ctrl Pts',(28.764135320164,-0.871290254073719,17.7355752732588));
#48285=CARTESIAN_POINT('Ctrl Pts',(28.6633306533142,-0.706980266162622,
17.7267766814534));
#48286=CARTESIAN_POINT('Ctrl Pts',(28.5256044330412,-0.340872542641299,
17.70643736348));
#48287=CARTESIAN_POINT('Ctrl Pts',(28.4933384090279,-0.141395913779689,
17.6953553285433));
#48288=CARTESIAN_POINT('Ctrl Pts',(28.5086475773052,0.250803035896437,17.6735664980057));
#48289=CARTESIAN_POINT('Ctrl Pts',(28.5530910089168,0.439894111123241,17.6630614382709));
#48290=CARTESIAN_POINT('Ctrl Pts',(28.7124602775381,0.794124581104987,17.6433819677164));
#48291=CARTESIAN_POINT('Ctrl Pts',(28.8270773285161,0.955330804312479,17.6340619682235));
#48292=CARTESIAN_POINT('Ctrl Pts',(29.1130611662184,1.22571784831621,17.6127918131944));
#48293=CARTESIAN_POINT('Ctrl Pts',(29.2820600929988,1.33176716482588,17.6017150341911));
#48294=CARTESIAN_POINT('Ctrl Pts',(29.6446531268203,1.46968030941703,17.5804388480344));
#48295=CARTESIAN_POINT('Ctrl Pts',(29.8337664889299,1.50284763615596,17.5705770145346));
#48296=CARTESIAN_POINT('Ctrl Pts',(30.2227595353817,1.49663210693258,17.5516889242716));
#48297=CARTESIAN_POINT('Ctrl Pts',(30.4189176611452,1.45396403183943,17.5410660377374));
#48298=CARTESIAN_POINT('Ctrl Pts',(30.7799134803451,1.29609345193241,17.5193123244018));
#48299=CARTESIAN_POINT('Ctrl Pts',(30.9418307309724,1.18367445855365,17.5083993272327));
#48300=CARTESIAN_POINT('Ctrl Pts',(31.2101475557693,0.906543829758461,17.4877918549585));
#48301=CARTESIAN_POINT('Ctrl Pts',(31.3153431699375,0.745751786456619,17.478930654803));
#48302=CARTESIAN_POINT('Ctrl Pts',(31.463864637894,0.383898047749162,17.4588276693193));
#48303=CARTESIAN_POINT('Ctrl Pts',(31.5020303054666,0.184838532612863,17.4477688073673));
#48304=CARTESIAN_POINT('Ctrl Pts',(31.4978841524782,-0.208759642694536,
17.4259022420724));
#48305=CARTESIAN_POINT('Ctrl Pts',(31.4586348080642,-0.399547636290809,
17.4153029090948));
#48306=CARTESIAN_POINT('Ctrl Pts',(31.3094217036004,-0.757113584921528,
17.3954381341709));
#48307=CARTESIAN_POINT('Ctrl Pts',(31.200380183046,-0.920271802442848,17.3863568795276));
#48308=CARTESIAN_POINT('Ctrl Pts',(30.923406682912,-1.19858244148629,17.3653001347046));
#48309=CARTESIAN_POINT('Ctrl Pts',(30.7571425046312,-1.30996529750999,17.3542067774745));
#48310=CARTESIAN_POINT('Ctrl Pts',(30.3978227489156,-1.45880886920802,17.3327844540089));
#48311=CARTESIAN_POINT('Ctrl Pts',(30.2092450764931,-1.49754020852369,17.3226356359777));
#48312=CARTESIAN_POINT('Ctrl Pts',(30.0122952852091,-1.49996221637769,17.3130926067305));
#48313=CARTESIAN_POINT('Ctrl Pts',(30.0061468402235,-1.50000000000001,17.3127957399881));
#48314=CARTESIAN_POINT('Ctrl Pts',(30.,-1.50000000000001,17.3125));
#48315=CARTESIAN_POINT('Origin',(30.,-1.32966554433622E-14,16.));
#48316=CARTESIAN_POINT('',(30.,-1.50000000000001,16.75));
#48317=CARTESIAN_POINT('',(30.0000000000001,-1.50000000000001,16.8125));
#48318=CARTESIAN_POINT('',(30.,-1.50000000000001,16.));
#48319=CARTESIAN_POINT('Ctrl Pts',(30.,-1.50000000000001,16.75));
#48320=CARTESIAN_POINT('Ctrl Pts',(30.1733135774153,-1.50000000000002,16.7583385533812));
#48321=CARTESIAN_POINT('Ctrl Pts',(30.3454665850143,-1.46996630625128,16.767455538092));
#48322=CARTESIAN_POINT('Ctrl Pts',(30.6943533649566,-1.34416445320596,16.7877358570363));
#48323=CARTESIAN_POINT('Ctrl Pts',(30.8648984846931,-1.24131259552183,16.7987982089822));
#48324=CARTESIAN_POINT('Ctrl Pts',(31.1561999433551,-0.975703692756434,
16.8201914820235));
#48325=CARTESIAN_POINT('Ctrl Pts',(31.2741613882488,-0.815654351280513,
16.8296858693734));
#48326=CARTESIAN_POINT('Ctrl Pts',(31.4395048489934,-0.463422668720622,
16.8492542961822));
#48327=CARTESIAN_POINT('Ctrl Pts',(31.4869681438372,-0.275392752547583,
16.8597004026363));
#48328=CARTESIAN_POINT('Ctrl Pts',(31.5087956503657,0.115841301406496,16.881435627856));
#48329=CARTESIAN_POINT('Ctrl Pts',(31.4799884843839,0.315484512989904,16.8925269173884));
#48330=CARTESIAN_POINT('Ctrl Pts',(31.3486206066034,0.684034451059388,16.9130019139478));
#48331=CARTESIAN_POINT('Ctrl Pts',(31.2503774147184,0.850433854559545,16.9217976845453));
#48332=CARTESIAN_POINT('Ctrl Pts',(30.994668844219,1.13948462780369,16.9421296570253));
#48333=CARTESIAN_POINT('Ctrl Pts',(30.8387866934565,1.25865700214481,16.9529398842324));
#48334=CARTESIAN_POINT('Ctrl Pts',(30.4862910667067,1.43284604521895,16.9747379225116));
#48335=CARTESIAN_POINT('Ctrl Pts',(30.2922814189341,1.48462820882751,16.9855106094757));
#48336=CARTESIAN_POINT('Ctrl Pts',(29.904287970164,1.50893843055208,17.0048532369201));
#48337=CARTESIAN_POINT('Ctrl Pts',(29.714222422622,1.48472560659638,17.014173768808));
#48338=CARTESIAN_POINT('Ctrl Pts',(29.3467837907597,1.36454370703768,17.0351905543248));
#48339=CARTESIAN_POINT('Ctrl Pts',(29.1737126610206,1.26724866527873,17.0462200829857));
#48340=CARTESIAN_POINT('Ctrl Pts',(28.8733100927186,1.01000510192613,17.0678188628294));
#48341=CARTESIAN_POINT('Ctrl Pts',(28.7495253450837,0.851954282658887,17.0776692065189));
#48342=CARTESIAN_POINT('Ctrl Pts',(28.5739823591041,0.503198698880474,17.0970445167289));
#48343=CARTESIAN_POINT('Ctrl Pts',(28.5214293436323,0.317084997718663,17.1073841667934));
#48344=CARTESIAN_POINT('Ctrl Pts',(28.4885674976081,-0.0722634762162506,
17.1290146375676));
#48345=CARTESIAN_POINT('Ctrl Pts',(28.5114956545415,-0.272057456078969,
17.1401143031155));
#48346=CARTESIAN_POINT('Ctrl Pts',(28.6319945909535,-0.644674063533988,
17.1608152257519));
#48347=CARTESIAN_POINT('Ctrl Pts',(28.7258902835189,-0.814669507709904,
17.1696624095652));
#48348=CARTESIAN_POINT('Ctrl Pts',(28.9737348011573,-1.1110192567928,17.1898187719544));
#48349=CARTESIAN_POINT('Ctrl Pts',(29.1257542814876,-1.2342064357884,17.2005546786951));
#48350=CARTESIAN_POINT('Ctrl Pts',(29.4726321438156,-1.41824610841819,17.2223560607564));
#48351=CARTESIAN_POINT('Ctrl Pts',(29.6650975807577,-1.47560141498182,17.2332092613688));
#48352=CARTESIAN_POINT('Ctrl Pts',(29.9087297050291,-1.49791971441829,17.2455509701752));
#48353=CARTESIAN_POINT('Ctrl Pts',(29.9543886563371,-1.50000000000001,17.2478055232048));
#48354=CARTESIAN_POINT('Ctrl Pts',(29.9999999999998,-1.50000000000001,17.25));
#48355=CARTESIAN_POINT('Ctrl Pts',(30.,-1.50000000000001,17.3125));
#48356=CARTESIAN_POINT('Ctrl Pts',(29.8075276745562,-1.50000000000001,17.3032396709245));
#48357=CARTESIAN_POINT('Ctrl Pts',(29.6167265402445,-1.46295509134636,17.2930307218294));
#48358=CARTESIAN_POINT('Ctrl Pts',(29.2565239800332,-1.31741270776536,17.2716576240826));
#48359=CARTESIAN_POINT('Ctrl Pts',(29.0910935230227,-1.20922562866616,17.2606931508671));
#48360=CARTESIAN_POINT('Ctrl Pts',(28.8152192771185,-0.939380042859163,
17.2399244343056));
#48361=CARTESIAN_POINT('Ctrl Pts',(28.7058473428781,-0.781856067083356,
17.2309364481713));
#48362=CARTESIAN_POINT('Ctrl Pts',(28.5481536416827,-0.426269472803969,
17.211181637378));
#48363=CARTESIAN_POINT('Ctrl Pts',(28.5044938401357,-0.230229772369996,
17.2002905429095));
#48364=CARTESIAN_POINT('Ctrl Pts',(28.4962752409133,0.162097483734217,17.178494584237));
#48365=CARTESIAN_POINT('Ctrl Pts',(28.5297146688179,0.3545967167103,17.167800182405));
#48366=CARTESIAN_POINT('Ctrl Pts',(28.6677231734513,0.715751667501951,17.1477360184722));
#48367=CARTESIAN_POINT('Ctrl Pts',(28.7707689938353,0.881053857184024,17.1388343527704));
#48368=CARTESIAN_POINT('Ctrl Pts',(29.0378553430027,1.16782543883526,17.1180182775366));
#48369=CARTESIAN_POINT('Ctrl Pts',(29.2009578477084,1.28493633443696,17.1069179241867));
#48370=CARTESIAN_POINT('Ctrl Pts',(29.5564777297123,1.44564779283652,17.0853487587108));
#48371=CARTESIAN_POINT('Ctrl Pts',(29.7443345881639,1.49039149544099,17.0750676107666));
#48372=CARTESIAN_POINT('Ctrl Pts',(30.1352017346056,1.50720082969336,17.0557950804638));
#48373=CARTESIAN_POINT('Ctrl Pts',(30.3346031531762,1.47580805773789,17.0457293998907));
#48374=CARTESIAN_POINT('Ctrl Pts',(30.7060862860091,1.33790450333634,17.02402575504));
#48375=CARTESIAN_POINT('Ctrl Pts',(30.8749553104054,1.23409963004519,17.0130175716131));
#48376=CARTESIAN_POINT('Ctrl Pts',(31.1584137835032,0.971677105747927,16.9920901549037));
#48377=CARTESIAN_POINT('Ctrl Pts',(31.271994699923,0.817368296550736,16.9829093498084));
#48378=CARTESIAN_POINT('Ctrl Pts',(31.4394257557863,0.466485221859018,16.9634158456588));
#48379=CARTESIAN_POINT('Ctrl Pts',(31.488516036617,0.271760297088586,16.9525977942827));
#48380=CARTESIAN_POINT('Ctrl Pts',(31.5076810248584,-0.120678265071266,
16.9307956519405));
#48381=CARTESIAN_POINT('Ctrl Pts',(31.4794384691607,-0.314545865899112,
16.9200252296723));
#48382=CARTESIAN_POINT('Ctrl Pts',(31.3513352758344,-0.678794152386266,
16.8997892137563));
#48383=CARTESIAN_POINT('Ctrl Pts',(31.2534603041453,-0.845994238167287,
16.890973963719));
#48384=CARTESIAN_POINT('Ctrl Pts',(30.9950590391717,-1.14001068930543,16.8703745034186));
#48385=CARTESIAN_POINT('Ctrl Pts',(30.8348670617779,-1.26204295887652,16.8592774780469));
#48386=CARTESIAN_POINT('Ctrl Pts',(30.4829704713108,-1.43301939771413,16.8375974999208));
#48387=CARTESIAN_POINT('Ctrl Pts',(30.2958966065637,-1.48299380376918,16.8272087264607));
#48388=CARTESIAN_POINT('Ctrl Pts',(30.0696474084832,-1.49878860163674,16.8158845624575));
#48389=CARTESIAN_POINT('Ctrl Pts',(30.0348056486057,-1.50000000000001,16.8141745875493));
#48390=CARTESIAN_POINT('Ctrl Pts',(30.0000000000002,-1.50000000000001,16.8125));
#48391=CARTESIAN_POINT('Origin',(30.,-1.32966554433622E-14,16.));
#48392=CARTESIAN_POINT('',(30.0000000000023,1.33373412263454,16.1584936490537));
#48393=CARTESIAN_POINT('',(30.,1.1752404735808,16.));
#48394=CARTESIAN_POINT('',(30.,1.17524047358083,16.));
#48395=CARTESIAN_POINT('',(30.,-1.17524047358085,16.));
#48396=CARTESIAN_POINT('Ctrl Pts',(30.,-1.17524047358083,16.));
#48397=CARTESIAN_POINT('Ctrl Pts',(30.0938726776238,-1.17889502189498,16.0036545483141));
#48398=CARTESIAN_POINT('Ctrl Pts',(30.2222715669962,-1.17292308708929,16.0088746896198));
#48399=CARTESIAN_POINT('Ctrl Pts',(30.4821758748939,-1.10061359842964,16.0205734257761));
#48400=CARTESIAN_POINT('Ctrl Pts',(30.5904809486724,-1.05245648363552,16.0257840816621));
#48401=CARTESIAN_POINT('Ctrl Pts',(30.8133642274912,-0.91102859460423,16.0372929849601));
#48402=CARTESIAN_POINT('Ctrl Pts',(30.9213977318432,-0.810903247446717,
16.0434573291476));
#48403=CARTESIAN_POINT('Ctrl Pts',(31.1067869536601,-0.562636269482013,
16.0555173993883));
#48404=CARTESIAN_POINT('Ctrl Pts',(31.1779495349821,-0.411557996758087,
16.0617064115579));
#48405=CARTESIAN_POINT('Ctrl Pts',(31.2569648094213,-0.0966670523057213,
16.075198195417));
#48406=CARTESIAN_POINT('Ctrl Pts',(31.2657685184509,0.0650399419384585,
16.0820144838088));
#48407=CARTESIAN_POINT('Ctrl Pts',(31.2286447980599,0.334175553677255,16.0931820826379));
#48408=CARTESIAN_POINT('Ctrl Pts',(31.1927617340632,0.495209878479218,16.0995752755442));
#48409=CARTESIAN_POINT('Ctrl Pts',(31.0046982036223,0.825162649859306,16.1133508913014));
#48410=CARTESIAN_POINT('Ctrl Pts',(30.8901527526008,0.956864086379422,16.1201881413696));
#48411=CARTESIAN_POINT('Ctrl Pts',(30.6234294043457,1.16264469041258,16.1337830625282));
#48412=CARTESIAN_POINT('Ctrl Pts',(30.4758334589096,1.2374906559331,16.1404068749596));
#48413=CARTESIAN_POINT('Ctrl Pts',(30.2026344427889,1.31649705751482,16.1513204506313));
#48414=CARTESIAN_POINT('Ctrl Pts',(30.094862299376,1.33047991225226,16.1552394386714));
#48415=CARTESIAN_POINT('Ctrl Pts',(30.0000000000046,1.33373412263454,16.1584936490537));
#48416=CARTESIAN_POINT('Origin',(30.,-1.32966554433622E-14,16.));
#48417=CARTESIAN_POINT('Origin',(30.,-1.21864324187371E-14,15.78125));
#48418=CARTESIAN_POINT('',(30.0000000000002,-1.17524047358085,16.0625));
#48419=CARTESIAN_POINT('',(30.,-1.17524047358085,15.78125));
#48420=CARTESIAN_POINT('',(29.1765921258349,-0.838564036615843,16.));
#48421=CARTESIAN_POINT('Ctrl Pts',(30.0000000000004,-1.17524047358085,16.0625));
#48422=CARTESIAN_POINT('Ctrl Pts',(29.8936372832897,-1.17524047358089,16.0559685129868));
#48423=CARTESIAN_POINT('Ctrl Pts',(29.7875857388152,-1.16080842474563,16.0489444642731));
#48424=CARTESIAN_POINT('Ctrl Pts',(29.5893382840682,-1.10559796441283,16.034813132098));
#48425=CARTESIAN_POINT('Ctrl Pts',(29.4977179176601,-1.06709869274158,16.0278219954706));
#48426=CARTESIAN_POINT('Ctrl Pts',(29.3263212626278,-0.968061456605931,
16.0137856854629));
#48427=CARTESIAN_POINT('Ctrl Pts',(29.2472234502441,-0.90791877416947,16.0067961899552));
#48428=CARTESIAN_POINT('Ctrl Pts',(29.176592125834,-0.838564036614912,15.9999999999999));
#48429=CARTESIAN_POINT('Origin',(30.,-1.32966554433622E-14,16.));
#48430=CARTESIAN_POINT('Origin',(30.,-1.21864324187371E-14,15.78125));
#48431=CARTESIAN_POINT('',(30.0000000000002,-1.17524047358085,16.5625));
#48432=CARTESIAN_POINT('',(30.,-1.17524047358085,16.5));
#48433=CARTESIAN_POINT('',(30.,-1.17524047358085,15.78125));
#48434=CARTESIAN_POINT('Ctrl Pts',(30.0000000000004,-1.17524047358085,16.5625));
#48435=CARTESIAN_POINT('Ctrl Pts',(29.8712710011335,-1.17524047358089,16.5545950516279));
#48436=CARTESIAN_POINT('Ctrl Pts',(29.7432544697015,-1.15409887958747,16.5459843057103));
#48437=CARTESIAN_POINT('Ctrl Pts',(29.4749058017838,-1.06268366571272,16.5262646272929));
#48438=CARTESIAN_POINT('Ctrl Pts',(29.3400104190766,-0.984598569044377,
16.515212607152));
#48439=CARTESIAN_POINT('Ctrl Pts',(29.1121607207208,-0.784303734398693,
16.4941196868072));
#48440=CARTESIAN_POINT('Ctrl Pts',(29.0200231478196,-0.665589512335134,
16.4846952710458));
#48441=CARTESIAN_POINT('Ctrl Pts',(28.8817974975863,-0.393869611486594,
16.465428299239));
#48442=CARTESIAN_POINT('Ctrl Pts',(28.83947486215,-0.242215228858268,16.4546748700446));
#48443=CARTESIAN_POINT('Ctrl Pts',(28.8167032491755,0.0653802904577292,
16.4328640487538));
#48444=CARTESIAN_POINT('Ctrl Pts',(28.8351718353917,0.218291541824621,16.422021498172));
#48445=CARTESIAN_POINT('Ctrl Pts',(28.9287391651494,0.506051914833821,16.4016171370023));
#48446=CARTESIAN_POINT('Ctrl Pts',(29.0019741006921,0.638460005621421,16.3928173224174));
#48447=CARTESIAN_POINT('Ctrl Pts',(29.1986594960153,0.873851822283252,16.3723938102577));
#48448=CARTESIAN_POINT('Ctrl Pts',(29.3222166226463,0.972810188230982,16.3612980106481));
#48449=CARTESIAN_POINT('Ctrl Pts',(29.5955374213776,1.11370354874836,16.3395188200451));
#48450=CARTESIAN_POINT('Ctrl Pts',(29.7416409158841,1.1563714827732,16.3290342066007));
#48451=CARTESIAN_POINT('Ctrl Pts',(30.0452139523297,1.18442751027465,16.309397801581));
#48452=CARTESIAN_POINT('Ctrl Pts',(30.1998697024494,1.16832333055968,16.2999812279383));
#48453=CARTESIAN_POINT('Ctrl Pts',(30.4949641982123,1.07710916023858,16.2786262781941));
#48454=CARTESIAN_POINT('Ctrl Pts',(30.6323783558426,1.00262103976947,16.2675471121926));
#48455=CARTESIAN_POINT('Ctrl Pts',(30.8661146099677,0.80826573510396,16.246303290685));
#48456=CARTESIAN_POINT('Ctrl Pts',(30.9615634972897,0.691955855651338,16.2365648418493));
#48457=CARTESIAN_POINT('Ctrl Pts',(31.1071384709944,0.423965303495795,16.217562308738));
#48458=CARTESIAN_POINT('Ctrl Pts',(31.153539286677,0.273539680121433,16.2068960077584));
#48459=CARTESIAN_POINT('Ctrl Pts',(31.1846742020807,-0.0336925499575308,
16.1851109463897));
#48460=CARTESIAN_POINT('Ctrl Pts',(31.1702391074247,-0.187447361382806,
16.174208581095));
#48461=CARTESIAN_POINT('Ctrl Pts',(31.0842361864784,-0.477469105777865,
16.1536438717926));
#48462=CARTESIAN_POINT('Ctrl Pts',(31.0147909316618,-0.611342914691707,
16.1448082262658));
#48463=CARTESIAN_POINT('Ctrl Pts',(30.8246452237759,-0.851973319529638,
16.1246005735716));
#48464=CARTESIAN_POINT('Ctrl Pts',(30.7034471847234,-0.954486386541281,
16.1135236126058));
#48465=CARTESIAN_POINT('Ctrl Pts',(30.4332129266933,-1.10289061678379,16.0916676708875));
#48466=CARTESIAN_POINT('Ctrl Pts',(30.2878849143487,-1.14942616400118,16.0810935566577));
#48467=CARTESIAN_POINT('Ctrl Pts',(30.0919105154022,-1.17254804866719,16.0682394674743));
#48468=CARTESIAN_POINT('Ctrl Pts',(30.0459321343385,-1.17524047358084,16.0653205855228));
#48469=CARTESIAN_POINT('Ctrl Pts',(30.0000000000004,-1.17524047358085,16.0625));
#48470=CARTESIAN_POINT('Ctrl Pts',(29.9999999999986,-1.17524047358085,15.9999999999999));
#48471=CARTESIAN_POINT('Ctrl Pts',(30.1214028111116,-1.17524047358099,16.0074550642242));
#48472=CARTESIAN_POINT('Ctrl Pts',(30.2421537204218,-1.15643017464734,16.0155369920666));
#48473=CARTESIAN_POINT('Ctrl Pts',(30.4776301337898,-1.08113291233427,16.0326666201836));
#48474=CARTESIAN_POINT('Ctrl Pts',(30.5903997908,-1.02391620718435,16.0416200885134));
#48475=CARTESIAN_POINT('Ctrl Pts',(30.8179173133188,-0.858187726048923,
16.0614671043063));
#48476=CARTESIAN_POINT('Ctrl Pts',(30.9244135286053,-0.742266950950034,
16.0721166138301));
#48477=CARTESIAN_POINT('Ctrl Pts',(31.0824458543846,-0.481384401141323,
16.0910702726526));
#48478=CARTESIAN_POINT('Ctrl Pts',(31.1347636661213,-0.340257482296023,
16.1008732014181));
#48479=CARTESIAN_POINT('Ctrl Pts',(31.1847167047507,-0.0402726429290417,
16.1221443686182));
#48480=CARTESIAN_POINT('Ctrl Pts',(31.1797095913038,0.116033015525934,16.1332276080324));
#48481=CARTESIAN_POINT('Ctrl Pts',(31.1096057651028,0.416692954381308,16.1545466448319));
#48482=CARTESIAN_POINT('Ctrl Pts',(31.0456145958404,0.558153128413804,16.1639131875247));
#48483=CARTESIAN_POINT('Ctrl Pts',(30.868452148125,0.806074678480504,16.1835820667589));
#48484=CARTESIAN_POINT('Ctrl Pts',(30.7578944192075,0.910792535772415,16.1940837990854));
#48485=CARTESIAN_POINT('Ctrl Pts',(30.4982839285527,1.07586594639843,16.2158783446996));
#48486=CARTESIAN_POINT('Ctrl Pts',(30.350445183185,1.13268560339106,16.2269712473271));
#48487=CARTESIAN_POINT('Ctrl Pts',(30.0480054721768,1.18378716120051,16.2473551076386));
#48488=CARTESIAN_POINT('Ctrl Pts',(29.8968386090012,1.18026105605562,16.2561569026374));
#48489=CARTESIAN_POINT('Ctrl Pts',(29.6011798659176,1.11599305250821,16.276591159187));
#48490=CARTESIAN_POINT('Ctrl Pts',(29.4597499374869,1.05480717934155,16.2874453099545));
#48491=CARTESIAN_POINT('Ctrl Pts',(29.2055652972218,0.87997645163687,16.3092526000714));
#48492=CARTESIAN_POINT('Ctrl Pts',(29.0959568884663,0.766951615708884,16.3199905502909));
#48493=CARTESIAN_POINT('Ctrl Pts',(28.9310246543964,0.510549118020342,16.3392090818415));
#48494=CARTESIAN_POINT('Ctrl Pts',(28.8749728808886,0.371095429589151,16.348686560472));
#48495=CARTESIAN_POINT('Ctrl Pts',(28.8169184420094,0.0732292943615943,
16.3698074957134));
#48496=CARTESIAN_POINT('Ctrl Pts',(28.817543647408,-0.0827153411142831,
16.3808651359001));
#48497=CARTESIAN_POINT('Ctrl Pts',(28.8792006517981,-0.386085589929172,
16.4023763539327));
#48498=CARTESIAN_POINT('Ctrl Pts',(28.9398691853048,-0.530428612710414,
16.4120388426041));
#48499=CARTESIAN_POINT('Ctrl Pts',(29.1111806434797,-0.783487027051828,
16.4315305472161));
#48500=CARTESIAN_POINT('Ctrl Pts',(29.2187204550675,-0.890749010718532,
16.441937155047));
#48501=CARTESIAN_POINT('Ctrl Pts',(29.4732317621912,-1.06214794881238,16.4636428352494));
#48502=CARTESIAN_POINT('Ctrl Pts',(29.6190899112583,-1.1227476098516,16.4747481293347));
#48503=CARTESIAN_POINT('Ctrl Pts',(29.8476395120001,-1.16783357420714,16.490381294589));
#48504=CARTESIAN_POINT('Ctrl Pts',(29.9238084968367,-1.17524047358085,16.4953212570267));
#48505=CARTESIAN_POINT('Ctrl Pts',(30.,-1.17524047358085,16.5));
#48506=CARTESIAN_POINT('Origin',(30.,-1.21864324187371E-14,15.78125));
#48507=CARTESIAN_POINT('',(30.,-1.17524047358085,17.0625));
#48508=CARTESIAN_POINT('',(30.0000000000001,-1.17524047358085,17.));
#48509=CARTESIAN_POINT('',(30.,-1.17524047358085,15.78125));
#48510=CARTESIAN_POINT('Ctrl Pts',(30.,-1.17524047358085,17.0625));
#48511=CARTESIAN_POINT('Ctrl Pts',(29.8500434788821,-1.17524047358086,17.0532915188657));
#48512=CARTESIAN_POINT('Ctrl Pts',(29.7013448813168,-1.14654165820119,17.0431428036379));
#48513=CARTESIAN_POINT('Ctrl Pts',(29.4194581258723,-1.03331719487298,17.0218185633632));
#48514=CARTESIAN_POINT('Ctrl Pts',(29.2895397758247,-0.948696042884902,
17.0108404436342));
#48515=CARTESIAN_POINT('Ctrl Pts',(29.0728347660888,-0.737413048700427,
16.9900423213744));
#48516=CARTESIAN_POINT('Ctrl Pts',(28.9869014388118,-0.614031092098323,
16.9810393937031));
#48517=CARTESIAN_POINT('Ctrl Pts',(28.8628735458866,-0.335358890642938,
16.9612794518217));
#48518=CARTESIAN_POINT('Ctrl Pts',(28.82846267168,-0.181667965469806,16.9503816165397));
#48519=CARTESIAN_POINT('Ctrl Pts',(28.8217124648996,0.125982959524893,16.9285668665722));
#48520=CARTESIAN_POINT('Ctrl Pts',(28.8478169965895,0.276986540894418,16.9178595840512));
#48521=CARTESIAN_POINT('Ctrl Pts',(28.9558731518301,0.560261316962501,16.89777328523));
#48522=CARTESIAN_POINT('Ctrl Pts',(29.0365906245512,0.68988311408331,16.8888684608487));
#48523=CARTESIAN_POINT('Ctrl Pts',(29.2459337687842,0.914815990147539,16.868038474302));
#48524=CARTESIAN_POINT('Ctrl Pts',(29.3738173058995,1.00667300394252,16.8569287693601));
#48525=CARTESIAN_POINT('Ctrl Pts',(29.6525904034611,1.13269913332434,16.8353418646716));
#48526=CARTESIAN_POINT('Ctrl Pts',(29.7999172965718,1.16777128086699,16.825051424181));
#48527=CARTESIAN_POINT('Ctrl Pts',(30.1064062467105,1.18085135988937,16.8057669130232));
#48528=CARTESIAN_POINT('Ctrl Pts',(30.2627337376109,1.15617395633467,16.7956901530542));
#48529=CARTESIAN_POINT('Ctrl Pts',(30.5539694020395,1.04785975388265,16.7739659051239));
#48530=CARTESIAN_POINT('Ctrl Pts',(30.6863296582614,0.96635719030164,16.7629483992302));
#48531=CARTESIAN_POINT('Ctrl Pts',(30.9084297587183,0.760352988428474,16.7420061299136));
#48532=CARTESIAN_POINT('Ctrl Pts',(30.9973576321623,0.639251123876904,16.7328276824508));
#48533=CARTESIAN_POINT('Ctrl Pts',(31.1283061935881,0.363925745860841,16.7133050553655));
#48534=CARTESIAN_POINT('Ctrl Pts',(31.1665770325591,0.21117202309341,16.7024736747387));
#48535=CARTESIAN_POINT('Ctrl Pts',(31.1811107740607,-0.0965571386816749,
16.6806533771987));
#48536=CARTESIAN_POINT('Ctrl Pts',(31.1587010998539,-0.248535347285279,
16.6698769863224));
#48537=CARTESIAN_POINT('Ctrl Pts',(31.0576874952353,-0.534014859537023,
16.6496343552276));
#48538=CARTESIAN_POINT('Ctrl Pts',(30.9806443499075,-0.664990212129755,
16.6408093669374));
#48539=CARTESIAN_POINT('Ctrl Pts',(30.7774744062741,-0.895077677115282,
16.6201757128395));
#48540=CARTESIAN_POINT('Ctrl Pts',(30.6516599935628,-0.990433515302137,
16.6090690216144));
#48541=CARTESIAN_POINT('Ctrl Pts',(30.3754577665479,-1.12376244747141,16.5873810764564));
#48542=CARTESIAN_POINT('Ctrl Pts',(30.2286809422177,-1.16255586785604,16.5769924813814));
#48543=CARTESIAN_POINT('Ctrl Pts',(30.0523684587312,-1.17436628643519,16.5657468184328));
#48544=CARTESIAN_POINT('Ctrl Pts',(30.0261713894288,-1.17524047358084,16.5641071241452));
#48545=CARTESIAN_POINT('Ctrl Pts',(30.0000000000004,-1.17524047358085,16.5625));
#48546=CARTESIAN_POINT('Ctrl Pts',(30.,-1.17524047358085,16.5));
#48547=CARTESIAN_POINT('Ctrl Pts',(30.073608323754,-1.17524047358085,16.5045201159347));
#48548=CARTESIAN_POINT('Ctrl Pts',(30.1472072638744,-1.16832718018639,16.5092847577281));
#48549=CARTESIAN_POINT('Ctrl Pts',(30.369441082132,-1.12600740446215,16.5244320137475));
#48550=CARTESIAN_POINT('Ctrl Pts',(30.5120596783037,-1.06872004059094,16.5352209411127));
#48551=CARTESIAN_POINT('Ctrl Pts',(30.770540092832,-0.900978381413799,16.5570406907631));
#48552=CARTESIAN_POINT('Ctrl Pts',(30.8831588051698,-0.790914789141215,
16.5678585095693));
#48553=CARTESIAN_POINT('Ctrl Pts',(31.0548992370084,-0.539025681589464,
16.5873351001607));
#48554=CARTESIAN_POINT('Ctrl Pts',(31.1146464335618,-0.40117702528207,16.5965535505072));
#48555=CARTESIAN_POINT('Ctrl Pts',(31.1805926646682,-0.105443065986663,
16.6175232985392));
#48556=CARTESIAN_POINT('Ctrl Pts',(31.1842348048322,0.0500317177053629,
16.6285476227227));
#48557=CARTESIAN_POINT('Ctrl Pts',(31.1309192517252,0.355959076743607,16.650240158982));
#48558=CARTESIAN_POINT('Ctrl Pts',(31.0735350939833,0.503164977113694,16.6602491192277));
#48559=CARTESIAN_POINT('Ctrl Pts',(30.9079406905516,0.761174069707616,16.6795652728517));
#48560=CARTESIAN_POINT('Ctrl Pts',(30.8033709986449,0.870813111599809,16.6898737681392));
#48561=CARTESIAN_POINT('Ctrl Pts',(30.5539282192807,1.04817985026245,16.7114797826742));
#48562=CARTESIAN_POINT('Ctrl Pts',(30.4100715847777,1.1123704677318,16.7225894812308));
#48563=CARTESIAN_POINT('Ctrl Pts',(30.1103488398163,1.179778360742,16.7433846194973));
#48564=CARTESIAN_POINT('Ctrl Pts',(29.957856215253,1.1841771173115,16.7522711143702));
#48565=CARTESIAN_POINT('Ctrl Pts',(29.6587896018035,1.13483145500942,16.7723855875496));
#48566=CARTESIAN_POINT('Ctrl Pts',(29.5151366653971,1.08127741557342,16.7831056710399));
#48567=CARTESIAN_POINT('Ctrl Pts',(29.252747940286,0.920389087589127,16.80492244475));
#48568=CARTESIAN_POINT('Ctrl Pts',(29.137337166046,0.813224513877345,16.8158089365411));
#48569=CARTESIAN_POINT('Ctrl Pts',(28.9591466935998,0.565701034789473,16.8355268312788));
#48570=CARTESIAN_POINT('Ctrl Pts',(28.8958814901205,0.429333298679841,16.8445570602832));
#48571=CARTESIAN_POINT('Ctrl Pts',(28.8225467136217,0.135655218439199,16.8653810311245));
#48572=CARTESIAN_POINT('Ctrl Pts',(28.8149165149687,-0.0192736957647923,
16.8763666490815));
#48573=CARTESIAN_POINT('Ctrl Pts',(28.8600359901893,-0.325574492875678,
16.8980856648912));
#48574=CARTESIAN_POINT('Ctrl Pts',(28.9132427466147,-0.473736863683124,
16.908393840582));
#48575=CARTESIAN_POINT('Ctrl Pts',(29.0711075417097,-0.735375844223955,
16.9273640300312));
#48576=CARTESIAN_POINT('Ctrl Pts',(29.1722563389189,-0.847605887640186,
16.9375543168196));
#48577=CARTESIAN_POINT('Ctrl Pts',(29.4158032201734,-1.03154789820323,16.9590313959273));
#48578=CARTESIAN_POINT('Ctrl Pts',(29.5572939812199,-1.09972494823153,16.97013714563));
#48579=CARTESIAN_POINT('Ctrl Pts',(29.8035947514828,-1.1629117021743,16.9875021095456));
#48580=CARTESIAN_POINT('Ctrl Pts',(29.9016938547886,-1.17524047358087,16.9939632483014));
#48581=CARTESIAN_POINT('Ctrl Pts',(30.0000000000002,-1.17524047358085,17.));
#48582=CARTESIAN_POINT('Origin',(30.,-1.21864324187371E-14,15.78125));
#48583=CARTESIAN_POINT('',(30.,-1.17524047358085,17.5625));
#48584=CARTESIAN_POINT('',(30.0000000000003,-1.17524047358085,17.5));
#48585=CARTESIAN_POINT('',(30.,-1.17524047358085,15.78125));
#48586=CARTESIAN_POINT('Ctrl Pts',(29.9999999999999,-1.17524047358085,17.5625));
#48587=CARTESIAN_POINT('Ctrl Pts',(29.9853039952848,-1.17524047358085,17.5615975525362));
#48588=CARTESIAN_POINT('Ctrl Pts',(29.9705988101993,-1.17496482223763,17.560684768457));
#48589=CARTESIAN_POINT('Ctrl Pts',(29.8000675583885,-1.16856010727206,17.5499857698916));
#48590=CARTESIAN_POINT('Ctrl Pts',(29.6469974366404,-1.13175546252589,17.53928122759));
#48591=CARTESIAN_POINT('Ctrl Pts',(29.3669883306193,-1.00191414640604,17.51748315987));
#48592=CARTESIAN_POINT('Ctrl Pts',(29.2422159979844,-0.911212372037981,
17.5066054643129));
#48593=CARTESIAN_POINT('Ctrl Pts',(29.0365009193432,-0.689398438610156,
17.4861088470066));
#48594=CARTESIAN_POINT('Ctrl Pts',(28.9566358845376,-0.561238966410083,
17.477296037423));
#48595=CARTESIAN_POINT('Ctrl Pts',(28.8466374529962,-0.274946499836391,
17.4569957617908));
#48596=CARTESIAN_POINT('Ctrl Pts',(28.8202715815142,-0.118602529031394,
17.4459098057446));
#48597=CARTESIAN_POINT('Ctrl Pts',(28.8303001790337,0.189193535952347,17.4240847642671));
#48598=CARTESIAN_POINT('Ctrl Pts',(28.8642598713376,0.337792935402822,17.413547956213));
#48599=CARTESIAN_POINT('Ctrl Pts',(28.9875332190235,0.616132121834573,17.3938116275857));
#48600=CARTESIAN_POINT('Ctrl Pts',(29.0764632180064,0.742831294355827,17.3845427667776));
#48601=CARTESIAN_POINT('Ctrl Pts',(29.2992557500629,0.956131495581886,17.3632993064049));
#48602=CARTESIAN_POINT('Ctrl Pts',(29.431365525465,1.04013508414132,17.3522085112739));
#48603=CARTESIAN_POINT('Ctrl Pts',(29.7152659077079,1.14996876403328,17.3308808348058));
#48604=CARTESIAN_POINT('Ctrl Pts',(29.8634965281812,1.17678287245723,17.3209370444755));
#48605=CARTESIAN_POINT('Ctrl Pts',(30.1685869462377,1.17348866615416,17.3020853596773));
#48606=CARTESIAN_POINT('Ctrl Pts',(30.3225567032231,1.14080144678595,17.291471550985));
#48607=CARTESIAN_POINT('Ctrl Pts',(30.6062809135034,1.01837161133764,17.269708112041));
#48608=CARTESIAN_POINT('Ctrl Pts',(30.7337302229979,0.930754504232001,17.2587753925441));
#48609=CARTESIAN_POINT('Ctrl Pts',(30.9451039338725,0.714326579760782,17.2381222459404));
#48610=CARTESIAN_POINT('Ctrl Pts',(31.0280898505948,0.588650269560749,17.2292397036887));
#48611=CARTESIAN_POINT('Ctrl Pts',(31.1457356989614,0.305390771140385,17.209154488167));
#48612=CARTESIAN_POINT('Ctrl Pts',(31.1762844162632,0.149369866697047,17.1980914399405));
#48613=CARTESIAN_POINT('Ctrl Pts',(31.1741828829317,-0.159374372954329,
17.1761991657924));
#48614=CARTESIAN_POINT('Ctrl Pts',(31.1439148549186,-0.309160960295119,
17.1655781772438));
#48615=CARTESIAN_POINT('Ctrl Pts',(31.0278391895685,-0.589863984020037,
17.1456742348851));
#48616=CARTESIAN_POINT('Ctrl Pts',(30.9428415818715,-0.717947604052165,
17.1366104494432));
#48617=CARTESIAN_POINT('Ctrl Pts',(30.7264277284841,-0.936836489561928,
17.1155605491468));
#48618=CARTESIAN_POINT('Ctrl Pts',(30.5962729133073,-1.02460346942682,17.10445637729));
#48619=CARTESIAN_POINT('Ctrl Pts',(30.3147671476396,-1.1421454095557,17.0830024620243));
#48620=CARTESIAN_POINT('Ctrl Pts',(30.1669216238945,-1.17291749944691,17.0728326267459));
#48621=CARTESIAN_POINT('Ctrl Pts',(30.0114948569556,-1.17519832475422,17.06320736676));
#48622=CARTESIAN_POINT('Ctrl Pts',(30.0057465951805,-1.17524047358085,17.0628528850424));
#48623=CARTESIAN_POINT('Ctrl Pts',(30.,-1.17524047358085,17.0625));
#48624=CARTESIAN_POINT('Ctrl Pts',(30.0000000000002,-1.17524047358085,17.));
#48625=CARTESIAN_POINT('Ctrl Pts',(30.0532026451947,-1.17524047358084,17.0032670506819));
#48626=CARTESIAN_POINT('Ctrl Pts',(30.1064500803375,-1.17162840402792,17.0066649131742));
#48627=CARTESIAN_POINT('Ctrl Pts',(30.3094843531048,-1.14383638948677,17.0201181063427));
#48628=CARTESIAN_POINT('Ctrl Pts',(30.4541770343026,-1.0944632219883,17.0307538106078));
#48629=CARTESIAN_POINT('Ctrl Pts',(30.7220117324143,-0.94057404805184,17.0526568626846));
#48630=CARTESIAN_POINT('Ctrl Pts',(30.8414109395085,-0.835479490322757,
17.0637148850572));
#48631=CARTESIAN_POINT('Ctrl Pts',(31.0267110546809,-0.591037021798696,
17.0837601330781));
#48632=CARTESIAN_POINT('Ctrl Pts',(31.0933788874677,-0.456058910657645,
17.0926620146465));
#48633=CARTESIAN_POINT('Ctrl Pts',(31.1737387540124,-0.16438811954927,17.1133436536858));
#48634=CARTESIAN_POINT('Ctrl Pts',(31.1851490819135,-0.0100732318962758,
17.1242857325711));
#48635=CARTESIAN_POINT('Ctrl Pts',(31.1477867853133,0.296739304676255,17.1460410345334));
#48636=CARTESIAN_POINT('Ctrl Pts',(31.0983725298423,0.446176311422578,17.156637235205));
#48637=CARTESIAN_POINT('Ctrl Pts',(30.9473434585081,0.711342976495719,17.1754395336164));
#48638=CARTESIAN_POINT('Ctrl Pts',(30.8493881217234,0.825870653120103,17.1854545855523));
#48639=CARTESIAN_POINT('Ctrl Pts',(30.6112318646727,1.01569990967513,17.2068093638384));
#48640=CARTESIAN_POINT('Ctrl Pts',(30.4719800604887,1.0874234537732,17.2179033608764));
#48641=CARTESIAN_POINT('Ctrl Pts',(30.1755334231398,1.17210985582506,17.2391099087106));
#48642=CARTESIAN_POINT('Ctrl Pts',(30.0214941231326,1.18498177307235,17.2483347304275));
#48643=CARTESIAN_POINT('Ctrl Pts',(29.7191034448427,1.1511421779865,17.2681035786673));
#48644=CARTESIAN_POINT('Ctrl Pts',(29.5735822533488,1.10552321949792,17.2786570590835));
#48645=CARTESIAN_POINT('Ctrl Pts',(29.3025973986068,0.958895356196027,17.3004961143537));
#48646=CARTESIAN_POINT('Ctrl Pts',(29.1808306521913,0.85722095928387,17.3115782643265));
#48647=CARTESIAN_POINT('Ctrl Pts',(28.9891285746956,0.617827320312939,17.3318376420863));
#48648=CARTESIAN_POINT('Ctrl Pts',(28.918785924397,0.484304768960115,17.3406591721831));
#48649=CARTESIAN_POINT('Ctrl Pts',(28.8309775509286,0.194817478373176,17.361185984716));
#48650=CARTESIAN_POINT('Ctrl Pts',(28.8155773691905,0.0412543792472424,
17.3720747561758));
#48651=CARTESIAN_POINT('Ctrl Pts',(28.8447173912596,-0.266085346871024,
17.3938674398171));
#48652=CARTESIAN_POINT('Ctrl Pts',(28.8901486797617,-0.416814366578493,
17.4045552538642));
#48653=CARTESIAN_POINT('Ctrl Pts',(29.0339735284972,-0.685700945089528,
17.423621321941));
#48654=CARTESIAN_POINT('Ctrl Pts',(29.1286271803726,-0.802582950507819,
17.4332789203108));
#48655=CARTESIAN_POINT('Ctrl Pts',(29.3609543925255,-0.998368963070605,
17.45448693977));
#48656=CARTESIAN_POINT('Ctrl Pts',(29.4977729352126,-1.07372697749091,17.4655603714348));
#48657=CARTESIAN_POINT('Ctrl Pts',(29.7602131749374,-1.15682002764215,17.484622175217));
#48658=CARTESIAN_POINT('Ctrl Pts',(29.879837116137,-1.1752404735809,17.4926210768238));
#48659=CARTESIAN_POINT('Ctrl Pts',(30.0000000000005,-1.17524047358085,17.5));
#48660=CARTESIAN_POINT('Origin',(30.,-1.21864324187371E-14,15.78125));
#48661=CARTESIAN_POINT('',(29.9999999999998,-1.17524047358085,18.0625));
#48662=CARTESIAN_POINT('',(30.,-1.17524047358085,18.));
#48663=CARTESIAN_POINT('',(30.,-1.17524047358085,15.78125));
#48664=CARTESIAN_POINT('Ctrl Pts',(29.9999999999995,-1.17524047358085,18.0625));
#48665=CARTESIAN_POINT('Ctrl Pts',(29.9645254254169,-1.17524047358085,18.0603215888955));
#48666=CARTESIAN_POINT('Ctrl Pts',(29.929015100466,-1.17363438891304,18.0580840407407));
#48667=CARTESIAN_POINT('Ctrl Pts',(29.7382382629168,-1.15628718990462,18.0457538558988));
#48668=CARTESIAN_POINT('Ctrl Pts',(29.5872914572777,-1.11138228831714,18.0348925171245));
#48669=CARTESIAN_POINT('Ctrl Pts',(29.315235711072,-0.96715790012321,18.0130729130751));
#48670=CARTESIAN_POINT('Ctrl Pts',(29.1959940490486,-0.870565282945587,
18.0023259907432));
#48671=CARTESIAN_POINT('Ctrl Pts',(29.0016396885941,-0.638155310236294,
17.9821513395236));
#48672=CARTESIAN_POINT('Ctrl Pts',(28.9280461950896,-0.504858426874225,
17.9732982357813));
#48673=CARTESIAN_POINT('Ctrl Pts',(28.8336569152641,-0.212647772939916,
17.9525783164326));
#48674=CARTESIAN_POINT('Ctrl Pts',(28.8157570812338,-0.0559802507924535,
17.9414694181781));
#48675=CARTESIAN_POINT('Ctrl Pts',(28.841716723376,0.249283949869151,17.9198239048041));
#48676=CARTESIAN_POINT('Ctrl Pts',(28.8830393993721,0.395199804389445,17.9094773801424));
#48677=CARTESIAN_POINT('Ctrl Pts',(29.0209639808548,0.668562290928518,17.8900939367334));
#48678=CARTESIAN_POINT('Ctrl Pts',(29.1181759703235,0.792402282110926,17.8802238069267));
#48679=CARTESIAN_POINT('Ctrl Pts',(29.3540263292146,0.993822233016871,17.8585996950535));
#48680=CARTESIAN_POINT('Ctrl Pts',(29.4898462594122,1.06991069869815,17.8475616886318));
#48681=CARTESIAN_POINT('Ctrl Pts',(29.7781387158762,1.16368326761588,17.8265337315072));
#48682=CARTESIAN_POINT('Ctrl Pts',(29.9272121099849,1.18239624377936,17.817223433802));
#48683=CARTESIAN_POINT('Ctrl Pts',(30.231427568808,1.16273575019751,17.7978452321702));
#48684=CARTESIAN_POINT('Ctrl Pts',(30.3834744853667,1.1218012564522,17.7870571039388));
#48685=CARTESIAN_POINT('Ctrl Pts',(30.6595367886018,0.984593855649311,17.7652402449678));
#48686=CARTESIAN_POINT('Ctrl Pts',(30.78153371397,0.890859052478792,17.7544254485094));
#48687=CARTESIAN_POINT('Ctrl Pts',(30.9814968973686,0.663646825098318,17.7340906520159));
#48688=CARTESIAN_POINT('Ctrl Pts',(31.0581916579204,0.532910080900297,17.7252873077101));
#48689=CARTESIAN_POINT('Ctrl Pts',(31.1603311881744,0.243593094566313,17.7047725710215));
#48690=CARTESIAN_POINT('Ctrl Pts',(31.1824208985569,0.0870303935487086,
17.6936711053685));
#48691=CARTESIAN_POINT('Ctrl Pts',(31.1643265939555,-0.219589452433675,
17.6719294666093));
#48692=CARTESIAN_POINT('Ctrl Pts',(31.126629625228,-0.366880394031282,17.6614854379963));
#48693=CARTESIAN_POINT('Ctrl Pts',(30.9959732548856,-0.642739672382233,
17.6419249533869));
#48694=CARTESIAN_POINT('Ctrl Pts',(30.9029171297163,-0.76800751067264,17.6323839709445));
#48695=CARTESIAN_POINT('Ctrl Pts',(30.6735549835348,-0.97540763183831,17.6109462657373));
#48696=CARTESIAN_POINT('Ctrl Pts',(30.5395284406378,-1.05546393695081,17.5998777123224));
#48697=CARTESIAN_POINT('Ctrl Pts',(30.2672665806154,-1.15230702152505,17.5797252955804));
#48698=CARTESIAN_POINT('Ctrl Pts',(30.1340643685791,-1.17524047358085,17.5707325810151));
#48699=CARTESIAN_POINT('Ctrl Pts',(29.9999999999999,-1.17524047358085,17.5625));
#48700=CARTESIAN_POINT('Ctrl Pts',(30.0000000000005,-1.17524047358085,17.5));
#48701=CARTESIAN_POINT('Ctrl Pts',(30.033668671514,-1.17524047358084,17.5020675147979));
#48702=CARTESIAN_POINT('Ctrl Pts',(30.0673733741507,-1.17379373295066,17.504188534545));
#48703=CARTESIAN_POINT('Ctrl Pts',(30.2512194694897,-1.15793171152857,17.5160404635345));
#48704=CARTESIAN_POINT('Ctrl Pts',(30.3974945854731,-1.11619705184184,17.5265025277916));
#48705=CARTESIAN_POINT('Ctrl Pts',(30.6715286389123,-0.977122112696594,
17.5482610478741));
#48706=CARTESIAN_POINT('Ctrl Pts',(30.7956391457863,-0.8790277241657,17.559360198049));
#48707=CARTESIAN_POINT('Ctrl Pts',(30.9938921656194,-0.644908297614295,
17.579834863399));
#48708=CARTESIAN_POINT('Ctrl Pts',(31.0680432549382,-0.51284781086492,17.5886352571811));
#48709=CARTESIAN_POINT('Ctrl Pts',(31.1634155774875,-0.225635628704456,
17.6090007475224));
#48710=CARTESIAN_POINT('Ctrl Pts',(31.1828424433655,-0.0729412614644995,
17.6198279193986));
#48711=CARTESIAN_POINT('Ctrl Pts',(31.1620678214981,0.234707081573543,17.6416424862861));
#48712=CARTESIAN_POINT('Ctrl Pts',(31.120724241081,0.386638085314584,17.6524155299848));
#48713=CARTESIAN_POINT('Ctrl Pts',(30.9842587758127,0.659238100700609,17.6717449084903));
#48714=CARTESIAN_POINT('Ctrl Pts',(30.8929036275603,0.778529076192667,17.6811039637465));
#48715=CARTESIAN_POINT('Ctrl Pts',(30.6664518626416,0.98022024209091,17.7021605454119));
#48716=CARTESIAN_POINT('Ctrl Pts',(30.5321662358965,1.05914504613978,17.7132048926221));
#48717=CARTESIAN_POINT('Ctrl Pts',(30.2394356343315,1.16107865610412,17.7347947253164));
#48718=CARTESIAN_POINT('Ctrl Pts',(30.0837395746803,1.18253750639866,17.7445990404306));
#48719=CARTESIAN_POINT('Ctrl Pts',(29.7783085058998,1.16389753061854,17.7640157086725));
#48720=CARTESIAN_POINT('Ctrl Pts',(29.6313883618284,1.12601470121935,17.7743808208261));
#48721=CARTESIAN_POINT('Ctrl Pts',(29.3545393068819,0.994469365010162,17.7960452510406));
#48722=CARTESIAN_POINT('Ctrl Pts',(29.2282096618696,0.899966183720928,17.8071533516094));
#48723=CARTESIAN_POINT('Ctrl Pts',(29.0235241701317,0.671134004766118,17.8278355674102));
#48724=CARTESIAN_POINT('Ctrl Pts',(28.9455840780504,0.540492245953914,17.8366750601186));
#48725=CARTESIAN_POINT('Ctrl Pts',(28.8428376707835,0.255550540540784,17.8568795566889));
#48726=CARTESIAN_POINT('Ctrl Pts',(28.819515816648,0.103803872119581,17.8676395296357));
#48727=CARTESIAN_POINT('Ctrl Pts',(28.8321334408652,-0.203924479248023,
17.8894597697118));
#48728=CARTESIAN_POINT('Ctrl Pts',(28.8694569005926,-0.356918085677502,
17.9003081598831));
#48729=CARTESIAN_POINT('Ctrl Pts',(28.9987062002081,-0.633072693900888,
17.9198895855878));
#48730=CARTESIAN_POINT('Ctrl Pts',(29.0868937988439,-0.754733453808526,
17.9290197269592));
#48731=CARTESIAN_POINT('Ctrl Pts',(29.3076626510103,-0.962047131353844,
17.9499266732212));
#48732=CARTESIAN_POINT('Ctrl Pts',(29.439425880769,-1.04432722335896,17.9609350833968));
#48733=CARTESIAN_POINT('Ctrl Pts',(29.7165797609128,-1.14942800619046,17.981680673977));
#48734=CARTESIAN_POINT('Ctrl Pts',(29.857771536572,-1.17524047358086,17.9912660809114));
#48735=CARTESIAN_POINT('Ctrl Pts',(30.0000000000001,-1.17524047358085,18.));
#48736=CARTESIAN_POINT('Origin',(30.,-1.21864324187371E-14,15.78125));
#48737=CARTESIAN_POINT('',(29.9999999999999,-1.17524047358085,18.5625));
#48738=CARTESIAN_POINT('',(30.,-1.17524047358085,18.5));
#48739=CARTESIAN_POINT('',(30.,-1.17524047358085,15.78125));
#48740=CARTESIAN_POINT('Ctrl Pts',(29.9999999999998,-1.17524047358085,18.5625));
#48741=CARTESIAN_POINT('Ctrl Pts',(29.9448799883238,-1.17524047358085,18.5591152083026));
#48742=CARTESIAN_POINT('Ctrl Pts',(29.8897199177939,-1.17136342891428,18.5555905009623));
#48743=CARTESIAN_POINT('Ctrl Pts',(29.6792216999803,-1.14149919812993,18.5416054964814));
#48744=CARTESIAN_POINT('Ctrl Pts',(29.5295600411529,-1.08838822549331,18.5305321396985));
#48745=CARTESIAN_POINT('Ctrl Pts',(29.2651715824486,-0.929562358041593,
18.5086656889335));
#48746=CARTESIAN_POINT('Ctrl Pts',(29.1517563578462,-0.827380506823195,
18.4980783953365));
#48747=CARTESIAN_POINT('Ctrl Pts',(28.9690035888602,-0.584433789122884,
18.4782426038757));
#48748=CARTESIAN_POINT('Ctrl Pts',(28.9018681826973,-0.445680079983302,
18.4691020486872));
#48749=CARTESIAN_POINT('Ctrl Pts',(28.8237798560613,-0.147691887525462,
18.4479724586759));
#48750=CARTESIAN_POINT('Ctrl Pts',(28.8145788645707,0.00884554058040183,
18.4368727850612));
#48751=CARTESIAN_POINT('Ctrl Pts',(28.8567482751501,0.310649796974269,18.4154726075955));
#48752=CARTESIAN_POINT('Ctrl Pts',(28.9054833559201,0.453415390787842,18.4053494599629));
#48753=CARTESIAN_POINT('Ctrl Pts',(29.0569965845258,0.718468314308288,18.3865552266777));
#48754=CARTESIAN_POINT('Ctrl Pts',(29.1604683184012,0.83707730034545,18.3760428358642));
#48755=CARTESIAN_POINT('Ctrl Pts',(29.4058248734932,1.0255154952049,18.3542952223602));
#48756=CARTESIAN_POINT('Ctrl Pts',(29.544631443668,1.0942445155017,18.3433347331662));
#48757=CARTESIAN_POINT('Ctrl Pts',(29.8366929775619,1.17335763361873,18.3225950580774));
#48758=CARTESIAN_POINT('Ctrl Pts',(29.986714530993,1.18458952273488,18.3136472884771));
#48759=CARTESIAN_POINT('Ctrl Pts',(30.2898186404183,1.14957783224746,18.2937930749288));
#48760=CARTESIAN_POINT('Ctrl Pts',(30.4396462258347,1.10100720458506,18.2828705011767));
#48761=CARTESIAN_POINT('Ctrl Pts',(30.7078144176317,0.95036138884417,18.2610619591969));
#48762=CARTESIAN_POINT('Ctrl Pts',(30.8244348872713,0.851181456147988,18.250384268188));
#48763=CARTESIAN_POINT('Ctrl Pts',(31.0135314789776,0.613960284599869,18.2303619093383));
#48764=CARTESIAN_POINT('Ctrl Pts',(31.0842069749077,0.478217809229905,18.2214092168781));
#48765=CARTESIAN_POINT('Ctrl Pts',(31.1712537448649,0.183351777827692,18.2005010114207));
#48766=CARTESIAN_POINT('Ctrl Pts',(31.1852144107931,0.026684835425868,18.1893921542744));
#48767=CARTESIAN_POINT('Ctrl Pts',(31.151894218573,-0.277120859310672,18.1678500598715));
#48768=CARTESIAN_POINT('Ctrl Pts',(31.1071955868466,-0.421659698179358,
18.1576011759113));
#48769=CARTESIAN_POINT('Ctrl Pts',(30.9623980704004,-0.692609521716023,
18.1383888083414));
#48770=CARTESIAN_POINT('Ctrl Pts',(30.8611688824271,-0.815074867780112,
18.1281515944925));
#48771=CARTESIAN_POINT('Ctrl Pts',(30.6191698348665,-1.010677278137,18.1063561595037));
#48772=CARTESIAN_POINT('Ctrl Pts',(30.481744547401,-1.08294295672688,18.0953551039148));
#48773=CARTESIAN_POINT('Ctrl Pts',(30.2255864017037,-1.15894806928573,18.0769303627887));
#48774=CARTESIAN_POINT('Ctrl Pts',(30.1130100641695,-1.17524047358085,18.0694396851576));
#48775=CARTESIAN_POINT('Ctrl Pts',(29.9999999999995,-1.17524047358085,18.0625));
#48776=CARTESIAN_POINT('Ctrl Pts',(30.0000000000001,-1.17524047358085,18.));
#48777=CARTESIAN_POINT('Ctrl Pts',(30.0145244311397,-1.17524047358085,18.0008919115297));
#48778=CARTESIAN_POINT('Ctrl Pts',(30.0290585224951,-1.1749712210064,18.0017939622806));
#48779=CARTESIAN_POINT('Ctrl Pts',(30.1935181174434,-1.16886648233729,18.0121094792412));
#48780=CARTESIAN_POINT('Ctrl Pts',(30.3409577753235,-1.13464684718278,18.022376619604));
#48781=CARTESIAN_POINT('Ctrl Pts',(30.6202928748417,-1.01029888563142,18.0439385382044));
#48782=CARTESIAN_POINT('Ctrl Pts',(30.7486368752819,-0.919248747112441,
18.055047912384));
#48783=CARTESIAN_POINT('Ctrl Pts',(30.9593869332128,-0.695506306327382,
18.0759220888488));
#48784=CARTESIAN_POINT('Ctrl Pts',(31.0409497614259,-0.566191331080132,
18.084852802908));
#48785=CARTESIAN_POINT('Ctrl Pts',(31.1506054030915,-0.283424289026694,
18.1049030995926));
#48786=CARTESIAN_POINT('Ctrl Pts',(31.1775442736485,-0.132654402671248,
18.1155938113905));
#48787=CARTESIAN_POINT('Ctrl Pts',(31.1725598607287,0.174951078257229,18.1374053390341));
#48788=CARTESIAN_POINT('Ctrl Pts',(31.1390289434739,0.328840847644919,18.148317273857));
#48789=CARTESIAN_POINT('Ctrl Pts',(31.0165781905916,0.608264397522364,18.1681304919571));
#48790=CARTESIAN_POINT('Ctrl Pts',(30.9313199722933,0.732167484063905,18.1771012136858));
#48791=CARTESIAN_POINT('Ctrl Pts',(30.7158345492886,0.944633593585631,18.1978663898215));
#48792=CARTESIAN_POINT('Ctrl Pts',(30.5864762504196,1.02994768568734,18.208834685427));
#48793=CARTESIAN_POINT('Ctrl Pts',(30.3000115977578,1.14695518635867,18.2305741665317));
#48794=CARTESIAN_POINT('Ctrl Pts',(30.1454149851266,1.17656763909288,18.2410233510493));
#48795=CARTESIAN_POINT('Ctrl Pts',(29.8400425266379,1.17387642244061,18.2598709770579));
#48796=CARTESIAN_POINT('Ctrl Pts',(29.6921041520777,1.14400535739554,18.2700145693908));
#48797=CARTESIAN_POINT('Ctrl Pts',(29.4100579886469,1.02824734385133,18.2914384223622));
#48798=CARTESIAN_POINT('Ctrl Pts',(29.2794434337127,0.941343746808855,18.3025402156205));
#48799=CARTESIAN_POINT('Ctrl Pts',(29.061555804029,0.723734320476339,18.3236352554819));
#48800=CARTESIAN_POINT('Ctrl Pts',(28.9756558249342,0.595970538008072,18.3327412345668));
#48801=CARTESIAN_POINT('Ctrl Pts',(28.8579142725366,0.315809924655313,18.3526067159761));
#48802=CARTESIAN_POINT('Ctrl Pts',(28.8267878271973,0.166290213657428,18.3632087809973));
#48803=CARTESIAN_POINT('Ctrl Pts',(28.8228465258246,-0.142252171918218,
18.3850867421828));
#48804=CARTESIAN_POINT('Ctrl Pts',(28.8524261916584,-0.298357527348321,
18.3961557786154));
#48805=CARTESIAN_POINT('Ctrl Pts',(28.9683032793772,-0.582326286319503,
18.4162912860112));
#48806=CARTESIAN_POINT('Ctrl Pts',(29.0505638845767,-0.708574806470949,
18.4251522948912));
#48807=CARTESIAN_POINT('Ctrl Pts',(29.2606233813178,-0.926260402003281,
18.4457693278011));
#48808=CARTESIAN_POINT('Ctrl Pts',(29.3874559625716,-1.01460273580079,18.4566898874478));
#48809=CARTESIAN_POINT('Ctrl Pts',(29.670332667393,-1.13876808411125,18.4784628134696));
#48810=CARTESIAN_POINT('Ctrl Pts',(29.8241031351402,-1.17241612945781,18.4890984491449));
#48811=CARTESIAN_POINT('Ctrl Pts',(29.9866645216768,-1.17518374723239,18.4991790881359));
#48812=CARTESIAN_POINT('Ctrl Pts',(29.9933333092278,-1.17524047358085,18.4995906140276));
#48813=CARTESIAN_POINT('Ctrl Pts',(30.,-1.17524047358085,18.5));
#48814=CARTESIAN_POINT('Origin',(30.,-1.21864324187371E-14,15.78125));
#48815=CARTESIAN_POINT('',(30.,-1.17524047358085,19.0625));
#48816=CARTESIAN_POINT('',(29.9999999999998,-1.17524047358085,18.9999999999999));
#48817=CARTESIAN_POINT('',(30.,-1.17524047358085,15.78125));
#48818=CARTESIAN_POINT('Ctrl Pts',(30.,-1.17524047358085,19.0625));
#48819=CARTESIAN_POINT('Ctrl Pts',(29.9235115354988,-1.17524047358085,19.0578030213218));
#48820=CARTESIAN_POINT('Ctrl Pts',(29.84704716558,-1.16777574293408,19.0528428696387));
#48821=CARTESIAN_POINT('Ctrl Pts',(29.6182505756017,-1.12246086107485,19.0371864213689));
#48822=CARTESIAN_POINT('Ctrl Pts',(29.4724485773796,-1.06175746863862,19.0260808977107));
#48823=CARTESIAN_POINT('Ctrl Pts',(29.2180805672544,-0.890185564352666,
19.0043778847458));
#48824=CARTESIAN_POINT('Ctrl Pts',(29.1106251205818,-0.782854361416016,
18.9939740034863));
#48825=CARTESIAN_POINT('Ctrl Pts',(28.9394765622835,-0.529653947083613,
18.9744872677464));
#48826=CARTESIAN_POINT('Ctrl Pts',(28.8789010658566,-0.385229961133875,
18.9648156834562));
#48827=CARTESIAN_POINT('Ctrl Pts',(28.8174805423046,-0.0817855742350542,
18.9432992084794));
#48828=CARTESIAN_POINT('Ctrl Pts',(28.8169771571136,0.0741472763924911,
18.9322424039265));
#48829=CARTESIAN_POINT('Ctrl Pts',(28.8752567923883,0.371953492557534,18.9111257173945));
#48830=CARTESIAN_POINT('Ctrl Pts',(28.9314131886074,0.511361040736907,18.9016564371649));
#48831=CARTESIAN_POINT('Ctrl Pts',(29.0965385184593,0.767636822695621,18.8824305405978));
#48832=CARTESIAN_POINT('Ctrl Pts',(29.2062331582591,0.880579083863968,18.8716902227143));
#48833=CARTESIAN_POINT('Ctrl Pts',(29.4605419802015,1.05521085002794,18.8498823608196));
#48834=CARTESIAN_POINT('Ctrl Pts',(29.6020069692685,1.11628678080371,18.8390299549287));
#48835=CARTESIAN_POINT('Ctrl Pts',(29.8977163387384,1.18033932535056,18.8186002283572));
#48836=CARTESIAN_POINT('Ctrl Pts',(30.0489012110254,1.18375239923791,18.8097988699583));
#48837=CARTESIAN_POINT('Ctrl Pts',(30.351304458352,1.13241772416719,18.7894089839185));
#48838=CARTESIAN_POINT('Ctrl Pts',(30.4990888608278,1.07549105419273,18.7783156243515));
#48839=CARTESIAN_POINT('Ctrl Pts',(30.7585582244441,0.910237971254531,18.7565233749656));
#48840=CARTESIAN_POINT('Ctrl Pts',(30.869032001546,0.80544751578808,18.7460242240482));
#48841=CARTESIAN_POINT('Ctrl Pts',(31.0460310070461,0.557381504027199,18.7263602597134));
#48842=CARTESIAN_POINT('Ctrl Pts',(31.1099298338315,0.41584148204013,18.7169862690792));
#48843=CARTESIAN_POINT('Ctrl Pts',(31.1797989523814,0.115104609901925,18.6956617771348));
#48844=CARTESIAN_POINT('Ctrl Pts',(31.1846835245906,-0.0411926090939851,
18.6845791361414));
#48845=CARTESIAN_POINT('Ctrl Pts',(31.134503841219,-0.341119161052378,18.6633121019541));
#48846=CARTESIAN_POINT('Ctrl Pts',(31.082082323541,-0.482198917475646,18.6535190714213));
#48847=CARTESIAN_POINT('Ctrl Pts',(30.9238582069445,-0.74295817680152,18.6345580062792));
#48848=CARTESIAN_POINT('Ctrl Pts',(30.8172746962663,-0.85879990158245,18.6239059387776));
#48849=CARTESIAN_POINT('Ctrl Pts',(30.5674863902569,-1.04046451233651,18.6021263306283));
#48850=CARTESIAN_POINT('Ctrl Pts',(30.4273223446806,-1.10544579712631,18.5912153532567));
#48851=CARTESIAN_POINT('Ctrl Pts',(30.1872213612661,-1.164041447155,18.5743938756203));
#48852=CARTESIAN_POINT('Ctrl Pts',(30.0936931422672,-1.17524047358085,18.5682534779185));
#48853=CARTESIAN_POINT('Ctrl Pts',(29.9999999999998,-1.17524047358085,18.5625));
#48854=CARTESIAN_POINT('Ctrl Pts',(30.,-1.17524047358085,18.5));
#48855=CARTESIAN_POINT('Ctrl Pts',(30.1423690472132,-1.17524047358085,18.5087425520117));
#48856=CARTESIAN_POINT('Ctrl Pts',(30.2836710124158,-1.14937338085773,18.5183366621019));
#48857=CARTESIAN_POINT('Ctrl Pts',(30.561858730089,-1.04379601878612,18.5391626347549));
#48858=CARTESIAN_POINT('Ctrl Pts',(30.6944274791866,-0.96071277520592,18.550248984724));
#48859=CARTESIAN_POINT('Ctrl Pts',(30.9187624839086,-0.748784365111015,
18.5715385296331));
#48860=CARTESIAN_POINT('Ctrl Pts',(31.0086541273172,-0.622420436396325,
18.5808657390843));
#48861=CARTESIAN_POINT('Ctrl Pts',(31.1336634286392,-0.344659292163419,
18.6005610801994));
#48862=CARTESIAN_POINT('Ctrl Pts',(31.1685065373813,-0.196359387070609,
18.6110766518651));
#48863=CARTESIAN_POINT('Ctrl Pts',(31.1804379609257,0.111178530247992,18.6328833887437));
#48864=CARTESIAN_POINT('Ctrl Pts',(31.1550790566304,0.267584160665563,18.6439737169172));
#48865=CARTESIAN_POINT('Ctrl Pts',(31.0469271232095,0.554595748580105,18.6643249836272));
#48866=CARTESIAN_POINT('Ctrl Pts',(30.9678100781097,0.68335841703765,18.6731299773448));
#48867=CARTESIAN_POINT('Ctrl Pts',(30.763452167876,0.90645295543942,18.6935886563282));
#48868=CARTESIAN_POINT('Ctrl Pts',(30.6393299618342,0.997879761179756,18.7044521341951));
#48869=CARTESIAN_POINT('Ctrl Pts',(30.3602369836734,1.12947461105548,18.7262561139589));
#48870=CARTESIAN_POINT('Ctrl Pts',(30.207398548302,1.16725893034935,18.7369811620628));
#48871=CARTESIAN_POINT('Ctrl Pts',(29.9028111520737,1.18064726329168,18.7561598319717));
#48872=CARTESIAN_POINT('Ctrl Pts',(29.7540809815473,1.15884794274813,18.7656824913455));
#48873=CARTESIAN_POINT('Ctrl Pts',(29.4674235177593,1.05897426017317,18.7868263546523));
#48874=CARTESIAN_POINT('Ctrl Pts',(29.332959967187,0.979858413005439,18.7978884009434));
#48875=CARTESIAN_POINT('Ctrl Pts',(29.1020498086111,0.773870883761844,18.8193710843283));
#48876=CARTESIAN_POINT('Ctrl Pts',(29.0080096312967,0.648942084974305,18.8289851559772));
#48877=CARTESIAN_POINT('Ctrl Pts',(28.8756172989166,0.373674108747255,18.8485037128466));
#48878=CARTESIAN_POINT('Ctrl Pts',(28.8370493704244,0.226703861544607,18.85892500183));
#48879=CARTESIAN_POINT('Ctrl Pts',(28.8170693542027,-0.0796098764074361,
18.8806449352421));
#48880=CARTESIAN_POINT('Ctrl Pts',(28.838156352639,-0.236207536581086,18.8917488797605));
#48881=CARTESIAN_POINT('Ctrl Pts',(28.9384458248014,-0.526222673597261,
18.9123131205504));
#48882=CARTESIAN_POINT('Ctrl Pts',(29.0143989785152,-0.657569956199922,
18.921123179589));
#48883=CARTESIAN_POINT('Ctrl Pts',(29.2130173163762,-0.886033452067211,
18.9414197543903));
#48884=CARTESIAN_POINT('Ctrl Pts',(29.3343580168877,-0.980462303689547,
18.9522188602181));
#48885=CARTESIAN_POINT('Ctrl Pts',(29.609473809437,-1.11936682716347,18.9740377655105));
#48886=CARTESIAN_POINT('Ctrl Pts',(29.7612660994758,-1.16125829944545,18.9848441861849));
#48887=CARTESIAN_POINT('Ctrl Pts',(29.9445511530895,-1.1742603871282,18.9965602675684));
#48888=CARTESIAN_POINT('Ctrl Pts',(29.9722886221142,-1.17524047358085,18.998298308746));
#48889=CARTESIAN_POINT('Ctrl Pts',(29.9999999999996,-1.17524047358085,18.9999999999999));
#48890=CARTESIAN_POINT('Origin',(30.,-1.21864324187371E-14,15.78125));
#48891=CARTESIAN_POINT('',(30.0000000000001,-1.17524047358085,19.5625));
#48892=CARTESIAN_POINT('',(29.9999999999998,-1.17524047358085,19.4999999999999));
#48893=CARTESIAN_POINT('',(30.,-1.17524047358085,15.78125));
#48894=CARTESIAN_POINT('Ctrl Pts',(30.0000000000003,-1.17524047358085,19.5625));
#48895=CARTESIAN_POINT('Ctrl Pts',(29.9013941092948,-1.17524047358088,19.5564448416279));
#48896=CARTESIAN_POINT('Ctrl Pts',(29.8029987638489,-1.16283641906691,19.549962842264));
#48897=CARTESIAN_POINT('Ctrl Pts',(29.5564668004839,-1.09938994466242,19.5325744732568));
#48898=CARTESIAN_POINT('Ctrl Pts',(29.415037771559,-1.03111229808663,19.5214689478566));
#48899=CARTESIAN_POINT('Ctrl Pts',(29.1716434679328,-0.847005065425004,
19.4999953804452));
#48900=CARTESIAN_POINT('Ctrl Pts',(29.0705827398005,-0.734710314058229,
19.4898082076353));
#48901=CARTESIAN_POINT('Ctrl Pts',(28.9129094963582,-0.472970867922037,
19.4708462190468));
#48902=CARTESIAN_POINT('Ctrl Pts',(28.8598073237114,-0.32477237703938,19.4605287888834));
#48903=CARTESIAN_POINT('Ctrl Pts',(28.8149047814539,-0.0184511328725056,
19.4388083232246));
#48904=CARTESIAN_POINT('Ctrl Pts',(28.8226412643137,0.136461808695805,19.4278238378469));
#48905=CARTESIAN_POINT('Ctrl Pts',(28.8961732267534,0.430084241574931,19.4070038128194));
#48906=CARTESIAN_POINT('Ctrl Pts',(28.9595331463533,0.5664127336681,19.3979778677293));
#48907=CARTESIAN_POINT('Ctrl Pts',(29.137896746023,0.813817787616469,19.3782535402653));
#48908=CARTESIAN_POINT('Ctrl Pts',(29.2533816215898,0.92090330809607,19.3673653008166));
#48909=CARTESIAN_POINT('Ctrl Pts',(29.5158730245192,1.08160589182486,19.3455488072285));
#48910=CARTESIAN_POINT('Ctrl Pts',(29.6595524720356,1.13505921849913,19.3348306663965));
#48911=CARTESIAN_POINT('Ctrl Pts',(29.9586626554596,1.18420822106571,19.3147204900089));
#48912=CARTESIAN_POINT('Ctrl Pts',(30.1111738123977,1.17970362181747,19.305831310076));
#48913=CARTESIAN_POINT('Ctrl Pts',(30.4108580361143,1.11207867833533,19.2850308420592));
#48914=CARTESIAN_POINT('Ctrl Pts',(30.5546592354692,1.0477915906526,19.2739211274165));
#48915=CARTESIAN_POINT('Ctrl Pts',(30.8039627363725,0.870265103601911,19.2523180019705));
#48916=CARTESIAN_POINT('Ctrl Pts',(30.9084512058835,0.760562755820576,19.242012249931));
#48917=CARTESIAN_POINT('Ctrl Pts',(31.0738897348627,0.502419631313023,19.2227009162624));
#48918=CARTESIAN_POINT('Ctrl Pts',(31.1311837638208,0.355135076925594,19.2126817312365));
#48919=CARTESIAN_POINT('Ctrl Pts',(31.1842706831827,0.04913932312708,19.1909843452775));
#48920=CARTESIAN_POINT('Ctrl Pts',(31.1805124566442,-0.106321035688241,
19.1799610439256));
#48921=CARTESIAN_POINT('Ctrl Pts',(31.1143513914742,-0.401996025434437,
19.1589954772754));
#48922=CARTESIAN_POINT('Ctrl Pts',(31.0545027280943,-0.539801328735837,
19.1497832518808));
#48923=CARTESIAN_POINT('Ctrl Pts',(30.8825757787308,-0.791565442014421,
19.1302996391962));
#48924=CARTESIAN_POINT('Ctrl Pts',(30.7698754890686,-0.90154647307845,19.1194797380197));
#48925=CARTESIAN_POINT('Ctrl Pts',(30.5112798180774,-1.06909180183037,19.0976598713853));
#48926=CARTESIAN_POINT('Ctrl Pts',(30.3686300461772,-1.12627173763864,19.0868728383175));
#48927=CARTESIAN_POINT('Ctrl Pts',(30.146651557919,-1.16837939048486,19.071748782068));
#48928=CARTESIAN_POINT('Ctrl Pts',(30.0733297917687,-1.17524047358085,19.0670030119334));
#48929=CARTESIAN_POINT('Ctrl Pts',(30.,-1.17524047358085,19.0625));
#48930=CARTESIAN_POINT('Ctrl Pts',(29.9999999999996,-1.17524047358085,18.9999999999999));
#48931=CARTESIAN_POINT('Ctrl Pts',(30.1208018343283,-1.17524047358085,19.0074181596379));
#48932=CARTESIAN_POINT('Ctrl Pts',(30.2410273417982,-1.15662316578329,19.0154609815185));
#48933=CARTESIAN_POINT('Ctrl Pts',(30.5033214237856,-1.07312795539109,19.0345280681775));
#48934=CARTESIAN_POINT('Ctrl Pts',(30.6395388198866,-0.997960158889978,
19.0455578408927));
#48935=CARTESIAN_POINT('Ctrl Pts',(30.876878941369,-0.797935916319293,19.067223952545));
#48936=CARTESIAN_POINT('Ctrl Pts',(30.9750570407496,-0.674426741281125,
19.0771781033725));
#48937=CARTESIAN_POINT('Ctrl Pts',(31.1146479426385,-0.401644540658674,
19.0965204001729));
#48938=CARTESIAN_POINT('Ctrl Pts',(31.1567939343853,-0.256055794064216,
19.1068437304378));
#48939=CARTESIAN_POINT('Ctrl Pts',(31.1845453028865,0.0488704061743495,
19.1284652770555));
#48940=CARTESIAN_POINT('Ctrl Pts',(31.1676027188842,0.205546638234067,19.1395747929079));
#48941=CARTESIAN_POINT('Ctrl Pts',(31.0749923240704,0.498408501569657,19.1603408878703));
#48942=CARTESIAN_POINT('Ctrl Pts',(31.0021074917097,0.632295920687204,19.1692134966416));
#48943=CARTESIAN_POINT('Ctrl Pts',(30.8090318381138,0.865881565613648,19.1893513074212));
#48944=CARTESIAN_POINT('Ctrl Pts',(30.6904244547157,0.963111668252584,19.2000818814201));
#48945=CARTESIAN_POINT('Ctrl Pts',(30.419302827982,1.10891198567697,19.2218999959461));
#48946=CARTESIAN_POINT('Ctrl Pts',(30.2686205389783,1.15471361101177,19.232776883577));
#48947=CARTESIAN_POINT('Ctrl Pts',(29.9650775926592,1.18413115670169,19.2524597117397));
#48948=CARTESIAN_POINT('Ctrl Pts',(29.8154193388389,1.17018311968912,19.2615139711268));
#48949=CARTESIAN_POINT('Ctrl Pts',(29.5246945745281,1.08577187830739,19.2823593965739));
#48950=CARTESIAN_POINT('Ctrl Pts',(29.3869225275025,1.01437069769904,19.2933510961767));
#48951=CARTESIAN_POINT('Ctrl Pts',(29.1449076103833,0.821179121928182,19.3150620325829));
#48952=CARTESIAN_POINT('Ctrl Pts',(29.0436548787038,0.700625409307818,19.3253204220004));
#48953=CARTESIAN_POINT('Ctrl Pts',(28.8969987915807,0.43246305184088,19.3443351373923));
#48954=CARTESIAN_POINT('Ctrl Pts',(28.8509250755758,0.288512534702925,19.3545423049446));
#48955=CARTESIAN_POINT('Ctrl Pts',(28.8145962917767,-0.0146433580687103,
19.3760383235316));
#48956=CARTESIAN_POINT('Ctrl Pts',(28.8269416915671,-0.171282191603316,
19.3871451875491));
#48957=CARTESIAN_POINT('Ctrl Pts',(28.9109596159865,-0.467218400914038,
19.4081292766188));
#48958=CARTESIAN_POINT('Ctrl Pts',(28.9804361831083,-0.603975745967944,
19.4171374882925));
#48959=CARTESIAN_POINT('Ctrl Pts',(29.167379298401,-0.843150163563664,19.4370968570367));
#48960=CARTESIAN_POINT('Ctrl Pts',(29.2829166096857,-0.943363871775425,
19.447744685016));
#48961=CARTESIAN_POINT('Ctrl Pts',(29.5508199561077,-1.09737775425148,19.4696563740096));
#48962=CARTESIAN_POINT('Ctrl Pts',(29.7018004358378,-1.14764798506443,19.4807100016028));
#48963=CARTESIAN_POINT('Ctrl Pts',(29.9053565213586,-1.17238533019257,19.4940869386326));
#48964=CARTESIAN_POINT('Ctrl Pts',(29.9526999581129,-1.17524047358085,19.4970954144566));
#48965=CARTESIAN_POINT('Ctrl Pts',(29.9999999999997,-1.17524047358085,19.4999999999999));
#48966=CARTESIAN_POINT('Origin',(30.,-1.21864324187371E-14,15.78125));
#48967=CARTESIAN_POINT('',(30.0000000000003,-1.17524047358085,20.0625));
#48968=CARTESIAN_POINT('',(30.,-1.17524047358085,20.));
#48969=CARTESIAN_POINT('',(30.,-1.17524047358085,15.78125));
#48970=CARTESIAN_POINT('Ctrl Pts',(30.0000000000005,-1.17524047358085,20.0625));
#48971=CARTESIAN_POINT('Ctrl Pts',(29.8795085612599,-1.17524047358091,20.0551009010331));
#48972=CARTESIAN_POINT('Ctrl Pts',(29.7595622632698,-1.15671912815303,20.0470786269818));
#48973=CARTESIAN_POINT('Ctrl Pts',(29.4968909328774,-1.07331217196907,20.0279915033172));
#48974=CARTESIAN_POINT('Ctrl Pts',(29.3601452160293,-0.997848639613717,
20.0169188027128));
#48975=CARTESIAN_POINT('Ctrl Pts',(29.1279895360134,-0.801888849412877,
19.9957151555763));
#48976=CARTESIAN_POINT('Ctrl Pts',(29.0334325756294,-0.684937055319331,
19.9860671564471));
#48977=CARTESIAN_POINT('Ctrl Pts',(28.8898211655935,-0.415941538872162,
19.9669933638564));
#48978=CARTESIAN_POINT('Ctrl Pts',(28.8445081931777,-0.265175978908636,
19.956302958832));
#48979=CARTESIAN_POINT('Ctrl Pts',(28.8156113317766,0.0421759568632406,
19.934509409435));
#48980=CARTESIAN_POINT('Ctrl Pts',(28.8311290214712,0.195715280521655,19.9236223238335));
#48981=CARTESIAN_POINT('Ctrl Pts',(28.9191574051752,0.485137216573778,19.9031001454256));
#48982=CARTESIAN_POINT('Ctrl Pts',(28.9896097101006,0.618617028321211,19.8942800985803));
#48983=CARTESIAN_POINT('Ctrl Pts',(29.1815016413357,0.8578593810217,19.8740144260076));
#48984=CARTESIAN_POINT('Ctrl Pts',(29.3033374545183,0.95943115864218,19.8629316730427));
#48985=CARTESIAN_POINT('Ctrl Pts',(29.5744131919249,1.10584185120943,19.8410947363937));
#48986=CARTESIAN_POINT('Ctrl Pts',(29.7199575824398,1.1513488317962,19.8305438014147));
#48987=CARTESIAN_POINT('Ctrl Pts',(30.0223936436952,1.18496921575338,19.8107799381662));
#48988=CARTESIAN_POINT('Ctrl Pts',(30.17645595477,1.17197553997772,19.8015484961906));
#48989=CARTESIAN_POINT('Ctrl Pts',(30.4728526803367,1.08704252391974,19.7803362699347));
#48990=CARTESIAN_POINT('Ctrl Pts',(30.6120360120599,1.01521369720442,19.7692427449689));
#48991=CARTESIAN_POINT('Ctrl Pts',(30.8500255075595,0.825212607475584,19.7478921149936));
#48992=CARTESIAN_POINT('Ctrl Pts',(30.9478859340228,0.710618012755788,19.7378881282691));
#48993=CARTESIAN_POINT('Ctrl Pts',(31.0987101974267,0.445344450081356,19.7190782500187));
#48994=CARTESIAN_POINT('Ctrl Pts',(31.148011535677,0.295869142851177,19.7084793335565));
#48995=CARTESIAN_POINT('Ctrl Pts',(31.1851397417262,-0.0109614779842622,
19.6867227492848));
#48996=CARTESIAN_POINT('Ctrl Pts',(31.1736153786499,-0.165256365490512,
19.6757820885594));
#48997=CARTESIAN_POINT('Ctrl Pts',(31.093043155488,-0.456865689692268,19.6551048079831));
#48998=CARTESIAN_POINT('Ctrl Pts',(31.0262715370984,-0.591802059151614,
19.6462060198927));
#48999=CARTESIAN_POINT('Ctrl Pts',(30.8407896047275,-0.836102523209368,
19.6261546414896));
#49000=CARTESIAN_POINT('Ctrl Pts',(30.7213221432726,-0.941101033293042,
19.6150958330235));
#49001=CARTESIAN_POINT('Ctrl Pts',(30.4533957183897,-1.09478566221008,19.5931944001043));
#49002=CARTESIAN_POINT('Ctrl Pts',(30.3086782810935,-1.14405280540599,19.5825609345826));
#49003=CARTESIAN_POINT('Ctrl Pts',(30.1059062370161,-1.17166523878134,19.5691302110914));
#49004=CARTESIAN_POINT('Ctrl Pts',(30.0529306288365,-1.17524047358084,19.5657503467901));
#49005=CARTESIAN_POINT('Ctrl Pts',(30.0000000000003,-1.17524047358085,19.5625));
#49006=CARTESIAN_POINT('Ctrl Pts',(29.9999999999997,-1.17524047358085,19.4999999999999));
#49007=CARTESIAN_POINT('Ctrl Pts',(30.1013134091967,-1.17524047358085,19.5062214207844));
#49008=CARTESIAN_POINT('Ctrl Pts',(30.2023703512557,-1.16214610944681,19.5128913366607));
#49009=CARTESIAN_POINT('Ctrl Pts',(30.4489451189351,-1.0968832859302,19.530346730545));
#49010=CARTESIAN_POINT('Ctrl Pts',(30.5880725807912,-1.02901377075515,19.5412964522821));
#49011=CARTESIAN_POINT('Ctrl Pts',(30.8343712795547,-0.842194481571482,
19.5630445243813));
#49012=CARTESIAN_POINT('Ctrl Pts',(30.9385897374703,-0.724253666071193,
19.5736257801046));
#49013=CARTESIAN_POINT('Ctrl Pts',(31.0916505061583,-0.460199205120922,
19.5923866032744));
#49014=CARTESIAN_POINT('Ctrl Pts',(31.1412805360793,-0.317836464065441,
19.6024630191855));
#49015=CARTESIAN_POINT('Ctrl Pts',(31.1853286010408,-0.0163533735884271,
19.6238404235873));
#49016=CARTESIAN_POINT('Ctrl Pts',(31.1771308821554,0.140138676220234,19.6349368795415));
#49017=CARTESIAN_POINT('Ctrl Pts',(31.1009443941398,0.438772825443172,19.6561122727154));
#49018=CARTESIAN_POINT('Ctrl Pts',(31.0345585763112,0.578169376036336,19.6653017627446));
#49019=CARTESIAN_POINT('Ctrl Pts',(30.8531427469532,0.82231181712456,19.6850978487155));
#49020=CARTESIAN_POINT('Ctrl Pts',(30.7404083067898,0.925109501957493,19.6956651705268));
#49021=CARTESIAN_POINT('Ctrl Pts',(30.4771535858122,1.08544747135218,19.7175156107599));
#49022=CARTESIAN_POINT('Ctrl Pts',(30.3279214291812,1.13945389596675,19.7285943399309));
#49023=CARTESIAN_POINT('Ctrl Pts',(30.0245530133835,1.1844610145353,19.7488191591971));
#49024=CARTESIAN_POINT('Ctrl Pts',(29.8738446796079,1.17798106878653,19.7576497404222));
#49025=CARTESIAN_POINT('Ctrl Pts',(29.5795308296296,1.10805786067705,19.7782019083499));
#49026=CARTESIAN_POINT('Ctrl Pts',(29.4390520876789,1.04399036655414,19.7890998131999));
#49027=CARTESIAN_POINT('Ctrl Pts',(29.1881857877585,0.86396490371117,19.8108875045287));
#49028=CARTESIAN_POINT('Ctrl Pts',(29.0808654270878,0.748795351686304,19.8215609892382));
#49029=CARTESIAN_POINT('Ctrl Pts',(28.9210185508111,0.489082061917269,19.8405846207479));
#49030=CARTESIAN_POINT('Ctrl Pts',(28.8677194354805,0.348399842158546,19.8502958472478));
#49031=CARTESIAN_POINT('Ctrl Pts',(28.8156254684423,0.0489678765559477,
19.8715278115659));
#49032=CARTESIAN_POINT('Ctrl Pts',(28.8194748723048,-0.107254256712007,
19.88260512842));
#49033=CARTESIAN_POINT('Ctrl Pts',(28.8873579337553,-0.408638429267571,
19.9039755188019));
#49034=CARTESIAN_POINT('Ctrl Pts',(28.9504754704978,-0.550854728104584,
19.9134143320288));
#49035=CARTESIAN_POINT('Ctrl Pts',(29.1260934520651,-0.800139160205639,
19.9330366884507));
#49036=CARTESIAN_POINT('Ctrl Pts',(29.2358570179041,-0.905539531949709,
19.9435138507578));
#49037=CARTESIAN_POINT('Ctrl Pts',(29.4941308064619,-1.07230397107708,19.9652862658853));
#49038=CARTESIAN_POINT('Ctrl Pts',(29.6414537313008,-1.13013161490591,19.9763832300743));
#49039=CARTESIAN_POINT('Ctrl Pts',(29.8633704190017,-1.16928660340085,19.9913988083098));
#49040=CARTESIAN_POINT('Ctrl Pts',(29.9316910379181,-1.17524047358085,19.9958053055382));
#49041=CARTESIAN_POINT('Ctrl Pts',(30.,-1.17524047358085,20.));
#49042=CARTESIAN_POINT('Origin',(30.,-1.21864324187371E-14,15.78125));
#49043=CARTESIAN_POINT('',(30.,-1.17524047358085,20.5625));
#49044=CARTESIAN_POINT('',(30.,-1.17524047358085,20.5));
#49045=CARTESIAN_POINT('',(30.,-1.17524047358085,15.78125));
#49046=CARTESIAN_POINT('Ctrl Pts',(30.0000000000001,-1.17524047358085,20.5625));
#49047=CARTESIAN_POINT('Ctrl Pts',(29.857466677664,-1.17524047358086,20.5537473602351));
#49048=CARTESIAN_POINT('Ctrl Pts',(29.7159780885029,-1.14931710991913,20.5441397949867));
#49049=CARTESIAN_POINT('Ctrl Pts',(29.4386327044728,-1.04389937724848,20.5233712075421));
#49050=CARTESIAN_POINT('Ctrl Pts',(29.3069416102485,-0.961526015490682,
20.5123639202805));
#49051=CARTESIAN_POINT('Ctrl Pts',(29.086333053172,-0.75405497378,20.4914612382194));
#49052=CARTESIAN_POINT('Ctrl Pts',(28.998234525789,-0.632326756560098,20.4823366930552));
#49053=CARTESIAN_POINT('Ctrl Pts',(28.8691902031313,-0.356072447869899,
20.4627481978422));
#49054=CARTESIAN_POINT('Ctrl Pts',(28.8319810448841,-0.203050335093991,
20.4518977863579));
#49055=CARTESIAN_POINT('Ctrl Pts',(28.8195943462911,0.104677105391675,20.4300776108702));
#49056=CARTESIAN_POINT('Ctrl Pts',(28.8430260194231,0.256395499280261,20.419319642799));
#49057=CARTESIAN_POINT('Ctrl Pts',(28.9459812899286,0.541272174450661,20.399119757359));
#49058=CARTESIAN_POINT('Ctrl Pts',(29.0240298052411,0.671873753047622,20.3902782906932));
#49059=CARTESIAN_POINT('Ctrl Pts',(29.2288981247322,0.900554058537053,20.3695902323474));
#49060=CARTESIAN_POINT('Ctrl Pts',(29.3552896087803,0.99495410007641,20.3584819910769));
#49061=CARTESIAN_POINT('Ctrl Pts',(29.6322160097862,1.12628386030684,20.3368204541948));
#49062=CARTESIAN_POINT('Ctrl Pts',(29.7791530812878,1.16405670631925,20.3264582018892));
#49063=CARTESIAN_POINT('Ctrl Pts',(30.0846260087116,1.18247957174534,20.3070466605788));
#49064=CARTESIAN_POINT('Ctrl Pts',(30.2403465146444,1.16089584876694,20.297232309072));
#49065=CARTESIAN_POINT('Ctrl Pts',(30.5330201521523,1.05871377596515,20.2756371654718));
#49066=CARTESIAN_POINT('Ctrl Pts',(30.6672316693715,0.979687699230499,20.2645937786601));
#49067=CARTESIAN_POINT('Ctrl Pts',(30.8935142020877,0.777827856358351,20.2435416089216));
#49068=CARTESIAN_POINT('Ctrl Pts',(30.9847747247484,0.658466900361099,20.2341902246224));
#49069=CARTESIAN_POINT('Ctrl Pts',(31.1210267097183,0.385760488516485,20.2148533018128));
#49070=CARTESIAN_POINT('Ctrl Pts',(31.1622514979646,0.233796400148884,20.2040779121667));
#49071=CARTESIAN_POINT('Ctrl Pts',(31.1827840987885,-0.0738574566284658,
20.1822629543138));
#49072=CARTESIAN_POINT('Ctrl Pts',(31.1632412224874,-0.226525134572718,
20.1714376749082));
#49073=CARTESIAN_POINT('Ctrl Pts',(31.0676501608268,-0.513670659031922,
20.1510769110961));
#49074=CARTESIAN_POINT('Ctrl Pts',(30.9933877261944,-0.645689071009633,
20.1422762056128));
#49075=CARTESIAN_POINT('Ctrl Pts',(30.7949445520148,-0.879653706050947,
20.1217953512642));
#49076=CARTESIAN_POINT('Ctrl Pts',(30.670767244765,-0.977642983856647,20.1106958256016));
#49077=CARTESIAN_POINT('Ctrl Pts',(30.3966473841018,-1.11649688166864,20.0889398730384));
#49078=CARTESIAN_POINT('Ctrl Pts',(30.2503518300705,-1.15811817698529,20.0784805729189));
#49079=CARTESIAN_POINT('Ctrl Pts',(30.0667947188483,-1.17381847353791,20.0666521235228));
#49080=CARTESIAN_POINT('Ctrl Pts',(30.0333795266192,-1.17524047358084,20.0645497590825));
#49081=CARTESIAN_POINT('Ctrl Pts',(30.0000000000005,-1.17524047358085,20.0625));
#49082=CARTESIAN_POINT('Ctrl Pts',(30.,-1.17524047358085,20.));
#49083=CARTESIAN_POINT('Ctrl Pts',(30.0810461612404,-1.17524047358085,20.0049768562329));
#49084=CARTESIAN_POINT('Ctrl Pts',(30.1620390634994,-1.16685998246121,20.0102475616837));
#49085=CARTESIAN_POINT('Ctrl Pts',(30.3910188268312,-1.11873616439623,20.0260148454886));
#49086=CARTESIAN_POINT('Ctrl Pts',(30.5327757448135,-1.05858684074315,20.0368523263699));
#49087=CARTESIAN_POINT('Ctrl Pts',(30.7881241531233,-0.885634167315425,
20.0586644967329));
#49088=CARTESIAN_POINT('Ctrl Pts',(30.8985424642913,-0.773390023616368,
20.0694245027186));
#49089=CARTESIAN_POINT('Ctrl Pts',(31.0652926267422,-0.518183463935382,
20.0887122685505));
#49090=CARTESIAN_POINT('Ctrl Pts',(31.1223297618129,-0.379162720763723,
20.0981145292327));
#49091=CARTESIAN_POINT('Ctrl Pts',(31.182501138976,-0.0818619977066759,
20.1191953725253));
#49092=CARTESIAN_POINT('Ctrl Pts',(31.1830210318339,0.0739680814447177,
20.1302448898124));
#49093=CARTESIAN_POINT('Ctrl Pts',(31.1235906320717,0.378032609170699,20.1518053374088));
#49094=CARTESIAN_POINT('Ctrl Pts',(31.0637982215859,0.523138441463073,20.1615551718639));
#49095=CARTESIAN_POINT('Ctrl Pts',(30.8940186419568,0.777530022608243,20.1810000731231));
#49096=CARTESIAN_POINT('Ctrl Pts',(30.7872728375238,0.885439479392022,20.1913808781633));
#49097=CARTESIAN_POINT('Ctrl Pts',(30.5341117586616,1.05845819784869,20.2130610712561));
#49098=CARTESIAN_POINT('Ctrl Pts',(30.3887837233288,1.12003007025227,20.2241682808161));
#49099=CARTESIAN_POINT('Ctrl Pts',(30.0880464072922,1.18158358213937,20.2448181618436));
#49100=CARTESIAN_POINT('Ctrl Pts',(29.9360438868879,1.18313176496437,20.2536476203627));
#49101=CARTESIAN_POINT('Ctrl Pts',(29.6381705506099,1.1284628410545,20.2738775466838));
#49102=CARTESIAN_POINT('Ctrl Pts',(29.4952627894061,1.07218329111658,20.2846485002308));
#49103=CARTESIAN_POINT('Ctrl Pts',(29.2357076507194,0.906285518142771,20.3064688735353));
#49104=CARTESIAN_POINT('Ctrl Pts',(29.1223265216238,0.796998466553187,20.3173059793119));
#49105=CARTESIAN_POINT('Ctrl Pts',(28.94883850375,0.546283376626024,20.3368482617845));
#49106=CARTESIAN_POINT('Ctrl Pts',(28.8881400415123,0.408839661433748,20.3460102123335));
#49107=CARTESIAN_POINT('Ctrl Pts',(28.8201837019616,0.113659356458156,20.3669407021362));
#49108=CARTESIAN_POINT('Ctrl Pts',(28.8154556440784,-0.0416770716817043,
20.377955215877));
#49109=CARTESIAN_POINT('Ctrl Pts',(28.8666287496698,-0.348241759389233,
20.3996929435023));
#49110=CARTESIAN_POINT('Ctrl Pts',(28.923168044506,-0.496185032937023,20.4097992015263));
#49111=CARTESIAN_POINT('Ctrl Pts',(29.0873034963183,-0.755446668555585,
20.4290701716561));
#49112=CARTESIAN_POINT('Ctrl Pts',(29.1911125253156,-0.865675121623956,
20.4393528532326));
#49113=CARTESIAN_POINT('Ctrl Pts',(29.4392495659902,-1.04453090441881,20.4609314775711));
#49114=CARTESIAN_POINT('Ctrl Pts',(29.5825856119781,-1.10962145963742,20.4720411141544));
#49115=CARTESIAN_POINT('Ctrl Pts',(29.8217321396476,-1.16509155071327,20.4886931681386));
#49116=CARTESIAN_POINT('Ctrl Pts',(29.9108091908387,-1.17524047358086,20.4945229998842));
#49117=CARTESIAN_POINT('Ctrl Pts',(30.0000000000001,-1.17524047358085,20.5));
#49118=CARTESIAN_POINT('Origin',(30.,-1.21864324187371E-14,15.78125));
#49119=CARTESIAN_POINT('',(30.,-1.17524047358085,21.0625));
#49120=CARTESIAN_POINT('',(30.0000000000003,-1.17524047358085,21.));
#49121=CARTESIAN_POINT('',(30.,-1.17524047358085,15.78125));
#49122=CARTESIAN_POINT('Ctrl Pts',(30.,-1.17524047358085,21.0625));
#49123=CARTESIAN_POINT('Ctrl Pts',(29.9930425354756,-1.17524047358085,21.062072758288));
#49124=CARTESIAN_POINT('Ctrl Pts',(29.9860827950433,-1.17517869098314,21.0616431863938));
#49125=CARTESIAN_POINT('Ctrl Pts',(29.8232316065342,-1.17228514735699,21.0515402867957));
#49126=CARTESIAN_POINT('Ctrl Pts',(29.6694853244495,-1.13852257202281,21.0409020757897));
#49127=CARTESIAN_POINT('Ctrl Pts',(29.3867104280309,-1.01415059452875,21.0191280758083));
#49128=CARTESIAN_POINT('Ctrl Pts',(29.2599516823908,-0.925722033008617,
21.0082089931399));
#49129=CARTESIAN_POINT('Ctrl Pts',(29.0500490851207,-0.707886564567504,
20.9875962815068));
#49130=CARTESIAN_POINT('Ctrl Pts',(28.9678750474644,-0.58156955059427,20.9787376277926));
#49131=CARTESIAN_POINT('Ctrl Pts',(28.852209421352,-0.297516308143681,20.9585961298867));
#49132=CARTESIAN_POINT('Ctrl Pts',(28.8227455494544,-0.141401249035421,
20.9475264053908));
#49133=CARTESIAN_POINT('Ctrl Pts',(28.8269065561122,0.16711629798966,20.9256502054441));
#49134=CARTESIAN_POINT('Ctrl Pts',(28.8581354481118,0.316603790040456,20.915050424987));
#49135=CARTESIAN_POINT('Ctrl Pts',(28.9760761175465,0.596699382404322,20.8951895540518));
#49136=CARTESIAN_POINT('Ctrl Pts',(29.0620842641545,0.724424918144287,20.8860783197069));
#49137=CARTESIAN_POINT('Ctrl Pts',(29.2801481558297,0.941880855388224,20.8649778977684));
#49138=CARTESIAN_POINT('Ctrl Pts',(29.4108173740059,1.02868094436595,20.8538764175153));
#49139=CARTESIAN_POINT('Ctrl Pts',(29.6929274853784,1.14422525088517,20.8324562143623));
#49140=CARTESIAN_POINT('Ctrl Pts',(29.8408766090356,1.17398844910975,20.8223157862342));
#49141=CARTESIAN_POINT('Ctrl Pts',(30.146238089068,1.17646530253954,20.8034764343644));
#49142=CARTESIAN_POINT('Ctrl Pts',(30.3008127704194,1.14674523024735,20.7930175246536));
#49143=CARTESIAN_POINT('Ctrl Pts',(30.5871854304481,1.02954198948055,20.7712767528846));
#49144=CARTESIAN_POINT('Ctrl Pts',(30.7164764357369,0.944145175747713,20.7603096568304));
#49145=CARTESIAN_POINT('Ctrl Pts',(30.9318157386174,0.731537563311469,20.7395484367846));
#49146=CARTESIAN_POINT('Ctrl Pts',(31.0169931096024,0.607571893797524,20.7305813882675));
#49147=CARTESIAN_POINT('Ctrl Pts',(31.1392545858023,0.328058458126713,20.7107617965928));
#49148=CARTESIAN_POINT('Ctrl Pts',(31.1726798971535,0.174145191638854,20.6998481956499));
#49149=CARTESIAN_POINT('Ctrl Pts',(31.177452605602,-0.133454152417299,20.6780371031564));
#49150=CARTESIAN_POINT('Ctrl Pts',(31.1504138008343,-0.284195707834949,
20.6673484002337));
#49151=CARTESIAN_POINT('Ctrl Pts',(31.0405663350578,-0.566901684154618,
20.647302433566));
#49152=CARTESIAN_POINT('Ctrl Pts',(30.9589018497076,-0.696179869646961,
20.6383684206626));
#49153=CARTESIAN_POINT('Ctrl Pts',(30.7479829469593,-0.919779045347213,
20.6174889551129));
#49154=CARTESIAN_POINT('Ctrl Pts',(30.6195839675717,-1.0107321163549,20.6063796462101));
#49155=CARTESIAN_POINT('Ctrl Pts',(30.3401820261614,-1.13487834149049,20.5848207753144));
#49156=CARTESIAN_POINT('Ctrl Pts',(30.1927291526794,-1.16899555973842,20.5745564544744));
#49157=CARTESIAN_POINT('Ctrl Pts',(30.02853673898,-1.17498080122699,20.5642615811144));
#49158=CARTESIAN_POINT('Ctrl Pts',(30.0142636931895,-1.17524047358085,20.5633759002187));
#49159=CARTESIAN_POINT('Ctrl Pts',(30.0000000000001,-1.17524047358085,20.5625));
#49160=CARTESIAN_POINT('Ctrl Pts',(30.0000000000001,-1.17524047358085,20.5));
#49161=CARTESIAN_POINT('Ctrl Pts',(30.0615320920417,-1.17524047358085,20.5037785426368));
#49162=CARTESIAN_POINT('Ctrl Pts',(30.1230970944725,-1.17040913175211,20.5077303953467));
#49163=CARTESIAN_POINT('Ctrl Pts',(30.3340845761439,-1.13693724894346,20.5218733491291));
#49164=CARTESIAN_POINT('Ctrl Pts',(30.4779822284686,-1.08432359797014,20.5325751197693));
#49165=CARTESIAN_POINT('Ctrl Pts',(30.7413240882277,-0.925171378815601,
20.5543888717152));
#49166=CARTESIAN_POINT('Ctrl Pts',(30.8574242886598,-0.818746672756081,
20.5652914684918));
#49167=CARTESIAN_POINT('Ctrl Pts',(31.0372296037246,-0.572330389441825,
20.5850692727305));
#49168=CARTESIAN_POINT('Ctrl Pts',(31.1013789298939,-0.436327710632643,
20.5940611041994));
#49169=CARTESIAN_POINT('Ctrl Pts',(31.1765507195451,-0.143169609179877,
20.6148482046583));
#49170=CARTESIAN_POINT('Ctrl Pts',(31.1851707108535,0.0116076749541518,
20.6258230709101));
#49171=CARTESIAN_POINT('Ctrl Pts',(31.1420730921553,0.318093458162843,20.6475552036167));
#49172=CARTESIAN_POINT('Ctrl Pts',(31.0898417933348,0.466589648702242,20.6579510306787));
#49173=CARTESIAN_POINT('Ctrl Pts',(30.9337645237733,0.729159361106415,20.6768444502657));
#49174=CARTESIAN_POINT('Ctrl Pts',(30.8334379992983,0.84198975683026,20.6870055279311));
#49175=CARTESIAN_POINT('Ctrl Pts',(30.591317195237,1.02746666327729,20.7084494527507));
#49176=CARTESIAN_POINT('Ctrl Pts',(30.4504043784541,1.09657907803444,20.7195528744157));
#49177=CARTESIAN_POINT('Ctrl Pts',(30.1527579068286,1.17519666342875,20.7406179390521));
#49178=CARTESIAN_POINT('Ctrl Pts',(29.9992772327099,1.18508027808452,20.7496955256169));
#49179=CARTESIAN_POINT('Ctrl Pts',(29.6980213394833,1.14582802600215,20.7695865882633));
#49180=CARTESIAN_POINT('Ctrl Pts',(29.5531012936116,1.09744171629364,20.7802012666676));
#49181=CARTESIAN_POINT('Ctrl Pts',(29.2844190436536,0.945457598499347,20.8020888235724));
#49182=CARTESIAN_POINT('Ctrl Pts',(29.1643876737344,0.84125826030012,20.8131539267157));
#49183=CARTESIAN_POINT('Ctrl Pts',(28.9773975743441,0.59813879267389,20.8332560474103));
#49184=CARTESIAN_POINT('Ctrl Pts',(28.9097638018428,0.463547729800393,20.8421310013978));
#49185=CARTESIAN_POINT('Ctrl Pts',(28.8274319674294,0.172449502758382,20.8627720413655));
#49186=CARTESIAN_POINT('Ctrl Pts',(28.8149632933605,0.0183235810432114,
20.8737007211534));
#49187=CARTESIAN_POINT('Ctrl Pts',(28.850150967155,-0.288650006351519,20.8954674428227));
#49188=CARTESIAN_POINT('Ctrl Pts',(28.898515176706,-0.438439388541448,20.906088629547));
#49189=CARTESIAN_POINT('Ctrl Pts',(29.047641063206,-0.704596833168998,20.9249611816339));
#49190=CARTESIAN_POINT('Ctrl Pts',(29.1447168471359,-0.819746341645053,
20.9348754556746));
#49191=CARTESIAN_POINT('Ctrl Pts',(29.381325819526,-1.01116668011756,20.9561916286088));
#49192=CARTESIAN_POINT('Ctrl Pts',(29.5199396968772,-1.08386414625954,20.96728098122));
#49193=CARTESIAN_POINT('Ctrl Pts',(29.7764916553148,-1.15925176815251,20.9857080131187));
#49194=CARTESIAN_POINT('Ctrl Pts',(29.8880479255875,-1.1752404735809,20.9931252835322));
#49195=CARTESIAN_POINT('Ctrl Pts',(30.0000000000005,-1.17524047358085,21.));
#49196=CARTESIAN_POINT('Origin',(30.,-1.21864324187371E-14,15.78125));
#49197=CARTESIAN_POINT('',(29.9999999999998,-1.17524047358085,21.5625));
#49198=CARTESIAN_POINT('',(30.0000000000001,-1.17524047358085,21.5));
#49199=CARTESIAN_POINT('',(30.,-1.17524047358085,15.78125));
#49200=CARTESIAN_POINT('Ctrl Pts',(29.9999999999996,-1.17524047358085,21.5625));
#49201=CARTESIAN_POINT('Ctrl Pts',(29.9719988088573,-1.17524047358085,21.5607805119881));
#49202=CARTESIAN_POINT('Ctrl Pts',(29.9439711363572,-1.17423978092491,21.5590239195234));
#49203=CARTESIAN_POINT('Ctrl Pts',(29.7604047377572,-1.16108096387714,21.547285004757));
#49204=CARTESIAN_POINT('Ctrl Pts',(29.6086428973266,-1.11907669828182,21.5364764549777));
#49205=CARTESIAN_POINT('Ctrl Pts',(29.3336394628651,-0.979972388454951,
21.5146573661612));
#49206=CARTESIAN_POINT('Ctrl Pts',(29.2123764352237,-0.885461951955829,
21.503860137555));
#49207=CARTESIAN_POINT('Ctrl Pts',(29.0139169118187,-0.656850944948416,
21.4835680853588));
#49208=CARTESIAN_POINT('Ctrl Pts',(28.9380513713638,-0.525431379870783,
21.4747570119112));
#49209=CARTESIAN_POINT('Ctrl Pts',(28.8379806985326,-0.235334014126339,
21.4541869404899));
#49210=CARTESIAN_POINT('Ctrl Pts',(28.81701218115,-0.0787326333033737,21.4430827321496));
#49211=CARTESIAN_POINT('Ctrl Pts',(28.8372148732154,0.227544173701852,21.4213654174177));
#49212=CARTESIAN_POINT('Ctrl Pts',(28.8758855793473,0.374476178993786,21.4109468400715));
#49213=CARTESIAN_POINT('Ctrl Pts',(29.008483168462,0.64967403277934,21.3914332554072));
#49214=CARTESIAN_POINT('Ctrl Pts',(29.1026400510551,0.774562668949264,21.3818103125428));
#49215=CARTESIAN_POINT('Ctrl Pts',(29.3337333173752,0.980382528955385,21.3603223294383));
#49216=CARTESIAN_POINT('Ctrl Pts',(29.4682481852686,1.05938687455618,21.3492610850172));
#49217=CARTESIAN_POINT('Ctrl Pts',(29.7549668128984,1.15903498567807,21.3281214631321));
#49218=CARTESIAN_POINT('Ctrl Pts',(29.9037091563498,1.1807204220266,21.3186072813687));
#49219=CARTESIAN_POINT('Ctrl Pts',(30.2082836909242,1.16710140483065,21.2994212226452));
#49220=CARTESIAN_POINT('Ctrl Pts',(30.3610942123922,1.12920096767185,21.2886937718569));
#49221=CARTESIAN_POINT('Ctrl Pts',(30.6400777787282,0.99739853025376,21.2668891510646));
#49222=CARTESIAN_POINT('Ctrl Pts',(30.7641225887122,0.905886016702667,21.2560273872475));
#49223=CARTESIAN_POINT('Ctrl Pts',(30.9683193471767,0.682639701404097,21.2355732231612));
#49224=CARTESIAN_POINT('Ctrl Pts',(31.0473475790777,0.553805208866279,21.2267689284532));
#49225=CARTESIAN_POINT('Ctrl Pts',(31.1552799375254,0.266708452111841,21.2064116226359));
#49226=CARTESIAN_POINT('Ctrl Pts',(31.1805191858716,0.110295910456217,21.195320804404));
#49227=CARTESIAN_POINT('Ctrl Pts',(31.1683617956532,-0.197210560675315,
21.173516297295));
#49228=CARTESIAN_POINT('Ctrl Pts',(31.1334138492448,-0.345474524238407,
21.1630032741523));
#49229=CARTESIAN_POINT('Ctrl Pts',(31.0081981695942,-0.623166742222595,
21.1433128204234));
#49230=CARTESIAN_POINT('Ctrl Pts',(30.9181918552343,-0.749490769431124,
21.1339784439808));
#49231=CARTESIAN_POINT('Ctrl Pts',(30.6936733778382,-0.961255467276285,
21.1126834366527));
#49232=CARTESIAN_POINT('Ctrl Pts',(30.5610503971428,-1.04422897430134,21.1015976470182));
#49233=CARTESIAN_POINT('Ctrl Pts',(30.283074075588,-1.14948332004627,21.080796107845));
#49234=CARTESIAN_POINT('Ctrl Pts',(30.1420666819575,-1.17524047358085,21.0712239844648));
#49235=CARTESIAN_POINT('Ctrl Pts',(30.,-1.17524047358085,21.0625));
#49236=CARTESIAN_POINT('Ctrl Pts',(30.0000000000005,-1.17524047358085,21.));
#49237=CARTESIAN_POINT('Ctrl Pts',(30.0409368563611,-1.17524047358083,21.0025138371222));
#49238=CARTESIAN_POINT('Ctrl Pts',(30.0819173014533,-1.17310176285816,21.0051061762144));
#49239=CARTESIAN_POINT('Ctrl Pts',(30.2729829235624,-1.15303120950392,21.0175506477331));
#49240=CARTESIAN_POINT('Ctrl Pts',(30.4187156327833,-1.10844931428969,21.0280803491923));
#49241=CARTESIAN_POINT('Ctrl Pts',(30.6905353954506,-0.963834030798816,
21.0498993207407));
#49242=CARTESIAN_POINT('Ctrl Pts',(30.8129383742835,-0.863111359129209,
21.0609867980498));
#49243=CARTESIAN_POINT('Ctrl Pts',(31.0063964161767,-0.625120486728277,
21.0813042721815));
#49244=CARTESIAN_POINT('Ctrl Pts',(31.0777548462909,-0.49199236060375,21.0901140644785));
#49245=CARTESIAN_POINT('Ctrl Pts',(31.1675962416571,-0.203110857145286,
21.1105979221763));
#49246=CARTESIAN_POINT('Ctrl Pts',(31.1840814343856,-0.0497708726068158,
21.1214708731443));
#49247=CARTESIAN_POINT('Ctrl Pts',(31.1571888276141,0.257674311285982,21.14327103453));
#49248=CARTESIAN_POINT('Ctrl Pts',(31.1128522255693,0.408737402730974,21.1539825367601));
#49249=CARTESIAN_POINT('Ctrl Pts',(30.9710010878299,0.678628541040232,21.1731198356347));
#49250=CARTESIAN_POINT('Ctrl Pts',(30.8772391714915,0.796156039182743,21.1826908232652));
#49251=CARTESIAN_POINT('Ctrl Pts',(30.6464955823919,0.993543206250726,21.2038583630273));
#49252=CARTESIAN_POINT('Ctrl Pts',(30.5103519798164,1.06987223749504,21.214924774365));
#49253=CARTESIAN_POINT('Ctrl Pts',(30.2162079552513,1.16549604568273,21.2363776960251));
#49254=CARTESIAN_POINT('Ctrl Pts',(30.061127965963,1.18379547472913,21.2459429670447));
#49255=CARTESIAN_POINT('Ctrl Pts',(29.7567781749822,1.15962478754955,21.2654893209196));
#49256=CARTESIAN_POINT('Ctrl Pts',(29.6103180879013,1.11893466526318,21.2759257110673));
#49257=CARTESIAN_POINT('Ctrl Pts',(29.3355002124366,0.981897695520532,21.2976601102058));
#49258=CARTESIAN_POINT('Ctrl Pts',(29.2107776319456,0.884773136393355,21.3087624623211));
#49259=CARTESIAN_POINT('Ctrl Pts',(29.0107746609087,0.652081932742376,21.3292939522647));
#49260=CARTESIAN_POINT('Ctrl Pts',(28.9355970901093,0.52040794626517,21.3380991870768));
#49261=CARTESIAN_POINT('Ctrl Pts',(28.8382134265824,0.233810524699486,21.3584210862971));
#49262=CARTESIAN_POINT('Ctrl Pts',(28.8177208295725,0.0813648692728661,
21.3692306226469));
#49263=CARTESIAN_POINT('Ctrl Pts',(28.8362699803681,-0.22632694032349,21.3910482716382));
#49264=CARTESIAN_POINT('Ctrl Pts',(28.8765201026755,-0.378558584509325,
21.4018426329915));
#49265=CARTESIAN_POINT('Ctrl Pts',(29.0110211856253,-0.652134791815677,
21.4212412308003));
#49266=CARTESIAN_POINT('Ctrl Pts',(29.1015077791443,-0.772069972681635,
21.4305317818752));
#49267=CARTESIAN_POINT('Ctrl Pts',(29.3264048767426,-0.975307798634206,
21.4515477299157));
#49268=CARTESIAN_POINT('Ctrl Pts',(29.4600073333855,-1.05515984377402,21.4625829994009));
#49269=CARTESIAN_POINT('Ctrl Pts',(29.7321091399909,-1.15220558787994,21.4827327726726));
#49270=CARTESIAN_POINT('Ctrl Pts',(29.8656344449969,-1.17524047358088,21.4917489238272));
#49271=CARTESIAN_POINT('Ctrl Pts',(30.0000000000003,-1.17524047358085,21.5));
#49272=CARTESIAN_POINT('Origin',(30.,-1.21864324187371E-14,15.78125));
#49273=CARTESIAN_POINT('',(29.9999999999998,-1.17524047358085,22.0625));
#49274=CARTESIAN_POINT('',(30.000000003784,-1.17524047358085,22.0000000004647));
#49275=CARTESIAN_POINT('',(30.,-1.17524047358085,15.78125));
#49276=CARTESIAN_POINT('Ctrl Pts',(29.9999999999997,-1.17524047358085,22.0625));
#49277=CARTESIAN_POINT('Ctrl Pts',(29.9524010211782,-1.17524047358085,22.0595770574349));
#49278=CARTESIAN_POINT('Ctrl Pts',(29.9047586284152,-1.17234913259513,22.0565489400777));
#49279=CARTESIAN_POINT('Ctrl Pts',(29.7009349924679,-1.1474210952591,22.0431488126472));
#49280=CARTESIAN_POINT('Ctrl Pts',(29.5500039838267,-1.09704169086814,22.0320943523472));
#49281=CARTESIAN_POINT('Ctrl Pts',(29.2822334508411,-0.942842462410207,
22.01018424791));
#49282=CARTESIAN_POINT('Ctrl Pts',(29.1667766500969,-0.842552714869588,
21.9995386680174));
#49283=CARTESIAN_POINT('Ctrl Pts',(28.9799931885339,-0.603233884932394,
21.9795839832802));
#49284=CARTESIAN_POINT('Ctrl Pts',(28.910605612196,-0.466400997640195,21.9705713166174));
#49285=CARTESIAN_POINT('Ctrl Pts',(28.8268127379948,-0.170385863417145,
21.9495816311816));
#49286=CARTESIAN_POINT('Ctrl Pts',(28.8145871174915,-0.0137497615287427,
21.9384749608582));
#49287=CARTESIAN_POINT('Ctrl Pts',(28.85113877829,0.289356743861303,21.9169824442057));
#49288=CARTESIAN_POINT('Ctrl Pts',(28.8973142483913,0.433263084581444,21.9067784090915));
#49289=CARTESIAN_POINT('Ctrl Pts',(29.0441562961032,0.701308793511537,21.8877719649526));
#49290=CARTESIAN_POINT('Ctrl Pts',(29.145494108998,0.821789237943167,21.8775043861745));
#49291=CARTESIAN_POINT('Ctrl Pts',(29.3876377187977,1.01480099788269,21.8557919221934));
#49292=CARTESIAN_POINT('Ctrl Pts',(29.5254500415353,1.08610079854932,21.8448013436507));
#49293=CARTESIAN_POINT('Ctrl Pts',(29.8162261597603,1.17031056565349,21.8239599076952));
#49294=CARTESIAN_POINT('Ctrl Pts',(29.965897796871,1.18415559330363,21.814910211276));
#49295=CARTESIAN_POINT('Ctrl Pts',(30.2694248477664,1.15452627142302,21.7952208509568));
#49296=CARTESIAN_POINT('Ctrl Pts',(30.4200757340443,1.10861951539323,21.7843421644183));
#49297=CARTESIAN_POINT('Ctrl Pts',(30.6910871340011,0.962634653497324,21.762524275871));
#49298=CARTESIAN_POINT('Ctrl Pts',(30.8096198631452,0.865330005993902,21.7517956433222));
#49299=CARTESIAN_POINT('Ctrl Pts',(31.0025452942337,0.631606479581076,21.7316621689435));
#49300=CARTESIAN_POINT('Ctrl Pts',(31.075346835895,0.497649504779323,21.7227870693252));
#49301=CARTESIAN_POINT('Ctrl Pts',(31.1677479593254,0.204711362167963,21.7020155655921));
#49302=CARTESIAN_POINT('Ctrl Pts',(31.1845780485819,0.0480344792828584,
21.6909060035913));
#49303=CARTESIAN_POINT('Ctrl Pts',(31.1566162472742,-0.256851307753155,
21.6692873225717));
#49304=CARTESIAN_POINT('Ctrl Pts',(31.1143736239456,-0.402401296420415,
21.6589667405334));
#49305=CARTESIAN_POINT('Ctrl Pts',(30.9745867433069,-0.675115053903835,
21.6396292968631));
#49306=CARTESIAN_POINT('Ctrl Pts',(30.8762946890393,-0.798585224220405,
21.6296650545771));
#49307=CARTESIAN_POINT('Ctrl Pts',(30.6387793080734,-0.998444700485959,
21.6079940222289));
#49308=CARTESIAN_POINT('Ctrl Pts',(30.5025155082578,-1.07350395293815,21.5969652482617));
#49309=CARTESIAN_POINT('Ctrl Pts',(30.2404480736925,-1.15671325182863,21.5779222161248));
#49310=CARTESIAN_POINT('Ctrl Pts',(30.1205093503255,-1.17524047358085,21.5699001988757));
#49311=CARTESIAN_POINT('Ctrl Pts',(29.9999999999996,-1.17524047358085,21.5625));
#49312=CARTESIAN_POINT('Ctrl Pts',(30.0000000000003,-1.17524047358085,21.5));
#49313=CARTESIAN_POINT('Ctrl Pts',(30.0212839202784,-1.17524047358085,21.5013069960338));
#49314=CARTESIAN_POINT('Ctrl Pts',(30.0425864419315,-1.17466229796956,21.5026356328208));
#49315=CARTESIAN_POINT('Ctrl Pts',(30.2139454930837,-1.16533366693515,21.5134891283695));
#49316=CARTESIAN_POINT('Ctrl Pts',(30.3610177391346,-1.12845915530085,21.523827832119));
#49317=CARTESIAN_POINT('Ctrl Pts',(30.6385696146112,-0.998891400827412,
21.5454653082446));
#49318=CARTESIAN_POINT('Ctrl Pts',(30.7654630357173,-0.905335035089088,
21.5565744608423));
#49319=CARTESIAN_POINT('Ctrl Pts',(30.9718229035628,-0.677897335355307,
21.5773100566854));
#49320=CARTESIAN_POINT('Ctrl Pts',(31.0507577571561,-0.547623084998762,
21.5861694304673));
#49321=CARTESIAN_POINT('Ctrl Pts',(31.1570604439752,-0.258809326298121,
21.6066484845527));
#49322=CARTESIAN_POINT('Ctrl Pts',(31.1812214838473,-0.102338491331391,
21.6177434360859));
#49323=CARTESIAN_POINT('Ctrl Pts',(31.1670292938221,0.204877234262332,21.6395273271632));
#49324=CARTESIAN_POINT('Ctrl Pts',(31.1311379778152,0.352813947812694,21.6500171458341));
#49325=CARTESIAN_POINT('Ctrl Pts',(31.0040616369159,0.629882761963365,21.6696633955718));
#49326=CARTESIAN_POINT('Ctrl Pts',(30.9130181373807,0.755846555951633,21.6790645983814));
#49327=CARTESIAN_POINT('Ctrl Pts',(30.6868446220844,0.966129203413541,21.7004086935125));
#49328=CARTESIAN_POINT('Ctrl Pts',(30.553735937256,1.0481102897547,21.711489124086));
#49329=CARTESIAN_POINT('Ctrl Pts',(30.2686762405413,1.15380487275931,21.7327412449065));
#49330=CARTESIAN_POINT('Ctrl Pts',(30.1202468756007,1.17853792824007,21.7424990119962));
#49331=CARTESIAN_POINT('Ctrl Pts',(29.8153503696085,1.17107054155024,21.7614867439455));
#49332=CARTESIAN_POINT('Ctrl Pts',(29.661826921183,1.13627251461424,21.7721479818837));
#49333=CARTESIAN_POINT('Ctrl Pts',(29.3799800833098,1.01003478165367,21.7939311399523));
#49334=CARTESIAN_POINT('Ctrl Pts',(29.253891997555,0.920828765085568,21.8048366026441));
#49335=CARTESIAN_POINT('Ctrl Pts',(29.0454103417907,0.701638656512355,21.8254100846196));
#49336=CARTESIAN_POINT('Ctrl Pts',(28.9640200854668,0.5746995746724,21.8342495048467));
#49337=CARTESIAN_POINT('Ctrl Pts',(28.8502724171258,0.289883112959693,21.8544451207025));
#49338=CARTESIAN_POINT('Ctrl Pts',(28.8218581810328,0.133683866085342,21.8655208147403));
#49339=CARTESIAN_POINT('Ctrl Pts',(28.8280094580603,-0.174601530686287,
21.8873805534988));
#49340=CARTESIAN_POINT('Ctrl Pts',(28.8601657562679,-0.323793761637004,
21.8979593977371));
#49341=CARTESIAN_POINT('Ctrl Pts',(28.9799119697649,-0.603297917389521,
21.9177783313962));
#49342=CARTESIAN_POINT('Ctrl Pts',(29.0669039974813,-0.730676428244075,
21.9269392883002));
#49343=CARTESIAN_POINT('Ctrl Pts',(29.2865672059309,-0.946735069741176,
21.9480883812055));
#49344=CARTESIAN_POINT('Ctrl Pts',(29.4177292577255,-1.03259356038437,21.9591867420451));
#49345=CARTESIAN_POINT('Ctrl Pts',(29.7004129009365,-1.14619538664958,21.98057329627));
#49346=CARTESIAN_POINT('Ctrl Pts',(29.8484560704769,-1.17497884076058,21.9906847639469));
#49347=CARTESIAN_POINT('Ctrl Pts',(29.9986381885534,-1.17523988185415,21.9999163533479));
#49348=CARTESIAN_POINT('Ctrl Pts',(29.9993191103818,-1.17524047358524,21.9999581881525));
#49349=CARTESIAN_POINT('Ctrl Pts',(30.0000000075681,-1.17524047358085,22.0000000004647));
#49350=CARTESIAN_POINT('Origin',(30.,-1.21864324187371E-14,15.78125));
#49351=CARTESIAN_POINT('',(30.,-1.17524047358085,22.5625));
#49352=CARTESIAN_POINT('',(29.9999999999999,-1.17524047358085,22.4999999999999));
#49353=CARTESIAN_POINT('',(30.,-1.17524047358085,15.78125));
#49354=CARTESIAN_POINT('Ctrl Pts',(30.,-1.17524047358085,22.5625));
#49355=CARTESIAN_POINT('Ctrl Pts',(29.9313687068489,-1.17524047358085,22.5582855119371));
#49356=CARTESIAN_POINT('Ctrl Pts',(29.8627268799626,-1.16923029327301,22.55385729367));
#49357=CARTESIAN_POINT('Ctrl Pts',(29.6405360439417,-1.12983827415446,22.5388164770024));
#49358=CARTESIAN_POINT('Ctrl Pts',(29.4932720438495,-1.07189657475161,22.5277190875488));
#49359=CARTESIAN_POINT('Ctrl Pts',(29.2351505504649,-0.904940984815958,
22.505949247503));
#49360=CARTESIAN_POINT('Ctrl Pts',(29.125477326134,-0.799463570556349,22.4954749014128));
#49361=CARTESIAN_POINT('Ctrl Pts',(28.9500348086396,-0.550024618450246,
22.4758578415198));
#49362=CARTESIAN_POINT('Ctrl Pts',(28.8870166724079,-0.407722193677489,
22.4664105508506));
#49363=CARTESIAN_POINT('Ctrl Pts',(28.8193863135494,-0.106256134735224,
22.4450343541119));
#49364=CARTESIAN_POINT('Ctrl Pts',(28.8156683957017,0.0499559751614321,
22.4339577479897));
#49365=CARTESIAN_POINT('Ctrl Pts',(28.8680054797788,0.349324836623415,22.4127302582268));
#49366=CARTESIAN_POINT('Ctrl Pts',(28.9214162690158,0.489956671932254,22.4030291896045));
#49367=CARTESIAN_POINT('Ctrl Pts',(29.0814696037689,0.749536525817022,22.3839976107609));
#49368=CARTESIAN_POINT('Ctrl Pts',(29.1888834831425,0.864620134172483,22.3733214303097));
#49369=CARTESIAN_POINT('Ctrl Pts',(29.4398862783311,1.04443640573476,22.3515327737366));
#49370=CARTESIAN_POINT('Ctrl Pts',(29.5804046735503,1.10838743829029,22.3406365628695));
#49371=CARTESIAN_POINT('Ctrl Pts',(29.874773559948,1.17808176091705,22.320089130129));
#49372=CARTESIAN_POINT('Ctrl Pts',(30.0254999210416,1.18444262102585,22.3112603596819));
#49373=CARTESIAN_POINT('Ctrl Pts',(30.3288317944626,1.13918974891494,22.2910290715165));
#49374=CARTESIAN_POINT('Ctrl Pts',(30.4780087858284,1.08506931516396,22.2799496878662));
#49375=CARTESIAN_POINT('Ctrl Pts',(30.7411182596149,0.924538989516088,22.2581013471772));
#49376=CARTESIAN_POINT('Ctrl Pts',(30.8537656083098,0.82166305580017,22.2475365992352));
#49377=CARTESIAN_POINT('Ctrl Pts',(31.0350106463268,0.577368135111118,22.2277455951917));
#49378=CARTESIAN_POINT('Ctrl Pts',(31.1013006049905,0.437889260334813,22.2185496213456));
#49379=CARTESIAN_POINT('Ctrl Pts',(31.1772437890897,0.139172903087767,22.1973683990083));
#49380=CARTESIAN_POINT('Ctrl Pts',(31.185313349087,-0.0173128950364053,
22.1862723863453));
#49381=CARTESIAN_POINT('Ctrl Pts',(31.1410279217834,-0.318736522964712,
22.1648991982826));
#49382=CARTESIAN_POINT('Ctrl Pts',(31.0912903592309,-0.461049327500964,
22.1548343474741));
#49383=CARTESIAN_POINT('Ctrl Pts',(30.9380306919572,-0.724977765907907,
22.136065778375));
#49384=CARTESIAN_POINT('Ctrl Pts',(30.8337205687989,-0.842838844072579,
22.1254817206889));
#49385=CARTESIAN_POINT('Ctrl Pts',(30.5872857957992,-1.02946130111843,22.1037322710222));
#49386=CARTESIAN_POINT('Ctrl Pts',(30.4481174203718,-1.09722011431045,22.0927839616769));
#49387=CARTESIAN_POINT('Ctrl Pts',(30.2017882631029,-1.16222172164091,22.0753529112466));
#49388=CARTESIAN_POINT('Ctrl Pts',(30.1010204315162,-1.17524047358085,22.0687034297066));
#49389=CARTESIAN_POINT('Ctrl Pts',(29.9999999999997,-1.17524047358085,22.0625));
#49390=CARTESIAN_POINT('Ctrl Pts',(30.0000000075681,-1.17524047358085,22.0000000004647));
#49391=CARTESIAN_POINT('Ctrl Pts',(30.1550617076756,-1.17524047258231,22.0095219788006));
#49392=CARTESIAN_POINT('Ctrl Pts',(30.3087125624576,-1.14455036320512,22.020045399438));
#49393=CARTESIAN_POINT('Ctrl Pts',(30.5936146237504,-1.02583437646268,22.0417494976575));
#49394=CARTESIAN_POINT('Ctrl Pts',(30.7222919834293,-0.9396884903777,22.0527054685765));
#49395=CARTESIAN_POINT('Ctrl Pts',(30.9363028934711,-0.725796874489648,
22.0734306378289));
#49396=CARTESIAN_POINT('Ctrl Pts',(31.0207456221836,-0.60126080890756,22.0823661148205));
#49397=CARTESIAN_POINT('Ctrl Pts',(31.1412832329984,-0.320931550152795,
22.1022435544492));
#49398=CARTESIAN_POINT('Ctrl Pts',(31.1737467539974,-0.166807893544759,
22.1131720736242));
#49399=CARTESIAN_POINT('Ctrl Pts',(31.1765934878998,0.140728845238564,22.1349787269359));
#49400=CARTESIAN_POINT('Ctrl Pts',(31.148646481366,0.291209583454888,22.1456489359696));
#49401=CARTESIAN_POINT('Ctrl Pts',(31.0370532707971,0.573358102978206,22.165655374784));
#49402=CARTESIAN_POINT('Ctrl Pts',(30.9544609034821,0.702301510156061,22.1746213225474));
#49403=CARTESIAN_POINT('Ctrl Pts',(30.7420042686145,0.924591934894812,22.1955488165371));
#49404=CARTESIAN_POINT('Ctrl Pts',(30.6131073712558,1.01465868002552,22.2066572778597));
#49405=CARTESIAN_POINT('Ctrl Pts',(30.3331026676289,1.1369643062698,22.228187906872));
#49406=CARTESIAN_POINT('Ctrl Pts',(30.1855325771707,1.17014774287538,22.2384263196851));
#49407=CARTESIAN_POINT('Ctrl Pts',(29.8783465649041,1.17947691083341,22.2576206519922));
#49408=CARTESIAN_POINT('Ctrl Pts',(29.7215875906434,1.15260328305267,22.2678992314176));
#49409=CARTESIAN_POINT('Ctrl Pts',(29.4314038660401,1.03996407151785,22.2897122199048));
#49410=CARTESIAN_POINT('Ctrl Pts',(29.3003745517226,0.9567417174806,22.3007089687507));
#49411=CARTESIAN_POINT('Ctrl Pts',(29.0812311411824,0.747835374300097,22.3215725663721));
#49412=CARTESIAN_POINT('Ctrl Pts',(28.9939461402353,0.625488946274541,22.3306481587999));
#49413=CARTESIAN_POINT('Ctrl Pts',(28.866779072646,0.34832483100282,22.3503011660994));
#49414=CARTESIAN_POINT('Ctrl Pts',(28.8306169080572,0.195045951299282,22.3611697842779));
#49415=CARTESIAN_POINT('Ctrl Pts',(28.8203429359976,-0.112665031360941,
22.3829887927828));
#49416=CARTESIAN_POINT('Ctrl Pts',(28.844778193878,-0.264121048518041,22.3937281563827));
#49417=CARTESIAN_POINT('Ctrl Pts',(28.9496447173484,-0.548400594969454,
22.4138857009336));
#49418=CARTESIAN_POINT('Ctrl Pts',(29.0286885091485,-0.678634752036216,
22.4227474921567));
#49419=CARTESIAN_POINT('Ctrl Pts',(29.2352313232766,-0.905919594975383,
22.4434889029608));
#49420=CARTESIAN_POINT('Ctrl Pts',(29.3621859947411,-0.999372204838993,
22.454598138267));
#49421=CARTESIAN_POINT('Ctrl Pts',(29.6398139077013,-1.12872343697434,22.4762326071516));
#49422=CARTESIAN_POINT('Ctrl Pts',(29.7869023742936,-1.1654876328242,22.4865683958599));
#49423=CARTESIAN_POINT('Ctrl Pts',(29.9579757834663,-1.17467745886044,22.4973994296432));
#49424=CARTESIAN_POINT('Ctrl Pts',(29.9789969929607,-1.17524047358085,22.4987102541947));
#49425=CARTESIAN_POINT('Ctrl Pts',(29.9999999999997,-1.17524047358085,22.4999999999999));
#49426=CARTESIAN_POINT('Origin',(30.,-1.21864324187371E-14,15.78125));
#49427=CARTESIAN_POINT('',(30.,-1.17524047358085,23.0625));
#49428=CARTESIAN_POINT('',(29.9999999999997,-1.17524047358085,22.9999999999999));
#49429=CARTESIAN_POINT('',(30.,-1.17524047358085,15.78125));
#49430=CARTESIAN_POINT('Ctrl Pts',(30.0000000000001,-1.17524047358085,23.0625));
#49431=CARTESIAN_POINT('Ctrl Pts',(29.9105144759955,-1.17524047358086,23.0570049021313));
#49432=CARTESIAN_POINT('Ctrl Pts',(29.8211453329131,-1.16502438899623,23.0511547525684));
#49433=CARTESIAN_POINT('Ctrl Pts',(29.5817638222111,-1.10931034878277,23.0344796199141));
#49434=CARTESIAN_POINT('Ctrl Pts',(29.4384864599594,-1.04411918186912,23.0233700199021));
#49435=CARTESIAN_POINT('Ctrl Pts',(29.1904963016638,-0.865097093142698,
23.001794519102));
#49436=CARTESIAN_POINT('Ctrl Pts',(29.0867727283959,-0.754802905276228,
22.9915147546188));
#49437=CARTESIAN_POINT('Ctrl Pts',(28.9228010666229,-0.495400927229172,
22.9722488667908));
#49438=CARTESIAN_POINT('Ctrl Pts',(28.8663568012591,-0.347374707529959,
22.9621314630453));
#49439=CARTESIAN_POINT('Ctrl Pts',(28.8154245654916,-0.0407388679671123,
22.9403886902216));
#49440=CARTESIAN_POINT('Ctrl Pts',(28.820274444704,0.114581560721945,22.9293753109615));
#49441=CARTESIAN_POINT('Ctrl Pts',(28.8884563534747,0.409699470717337,22.9084492454292));
#49442=CARTESIAN_POINT('Ctrl Pts',(28.9492618301764,0.547097841052301,22.8992933904858));
#49443=CARTESIAN_POINT('Ctrl Pts',(29.1229462954904,0.797680554149997,22.8797437378863));
#49444=CARTESIAN_POINT('Ctrl Pts',(29.2364128570735,0.906879897838648,22.8689044954722));
#49445=CARTESIAN_POINT('Ctrl Pts',(29.4960880788397,1.07256979024568,22.8470841182882));
#49446=CARTESIAN_POINT('Ctrl Pts',(29.6390279331417,1.12873587584898,22.8363152167134));
#49447=CARTESIAN_POINT('Ctrl Pts',(29.9369514995214,1.18318311725145,22.8160900653519));
#49448=CARTESIAN_POINT('Ctrl Pts',(30.0889739777062,1.18151676550276,22.8072588330028));
#49449=CARTESIAN_POINT('Ctrl Pts',(30.3896701123462,1.11972025811827,22.7866028657307));
#49450=CARTESIAN_POINT('Ctrl Pts',(30.5349379950004,1.05803905954289,22.7754954739854));
#49451=CARTESIAN_POINT('Ctrl Pts',(30.7879462278465,0.88483838172195,22.7538182156715));
#49452=CARTESIAN_POINT('Ctrl Pts',(30.894602280459,0.776856295524231,22.7434403470977));
#49453=CARTESIAN_POINT('Ctrl Pts',(31.0642088755634,0.522314474535101,22.7240007418519));
#49454=CARTESIAN_POINT('Ctrl Pts',(31.1239021773863,0.377122301428262,22.7142407897863));
#49455=CARTESIAN_POINT('Ctrl Pts',(31.1830807507881,0.07297978420699,22.6926748121518));
#49456=CARTESIAN_POINT('Ctrl Pts',(31.1824316194307,-0.0828368341019099,
22.681626249339));
#49457=CARTESIAN_POINT('Ctrl Pts',(31.1220212984731,-0.380073436416841,
22.6605499526862));
#49458=CARTESIAN_POINT('Ctrl Pts',(31.0648726782981,-0.5190454232441,22.6511559208149));
#49459=CARTESIAN_POINT('Ctrl Pts',(30.897916936256,-0.774116322820778,22.6318603404761));
#49460=CARTESIAN_POINT('Ctrl Pts',(30.7874073117601,-0.886271721025917,
22.6210978735108));
#49461=CARTESIAN_POINT('Ctrl Pts',(30.5319280571356,-1.05901132752472,22.5992852221989));
#49462=CARTESIAN_POINT('Ctrl Pts',(30.390134598554,-1.11904322637321,22.5884496605924));
#49463=CARTESIAN_POINT('Ctrl Pts',(30.1614293865023,-1.16692310230727,22.5727078850032));
#49464=CARTESIAN_POINT('Ctrl Pts',(30.0807402688424,-1.17524047358085,22.5674580720923));
#49465=CARTESIAN_POINT('Ctrl Pts',(30.,-1.17524047358085,22.5625));
#49466=CARTESIAN_POINT('Ctrl Pts',(29.9999999999997,-1.17524047358085,22.4999999999999));
#49467=CARTESIAN_POINT('Ctrl Pts',(30.1346907701741,-1.17524047358085,22.5082710468799));
#49468=CARTESIAN_POINT('Ctrl Pts',(30.2685335864829,-1.15209385827977,22.5173106568969));
#49469=CARTESIAN_POINT('Ctrl Pts',(30.5408486178537,-1.05471955701661,22.5374851723845));
#49470=CARTESIAN_POINT('Ctrl Pts',(30.6743758210798,-0.974766233245233,
22.5485194114384));
#49471=CARTESIAN_POINT('Ctrl Pts',(30.8991023951896,-0.771359157149707,
22.5695308885782));
#49472=CARTESIAN_POINT('Ctrl Pts',(30.9894938192057,-0.651353133995038,
22.5788141945814));
#49473=CARTESIAN_POINT('Ctrl Pts',(31.1237789969096,-0.377670022359416,
22.598220372706));
#49474=CARTESIAN_POINT('Ctrl Pts',(31.1639088895479,-0.225405854113982,
22.6090170402582));
#49475=CARTESIAN_POINT('Ctrl Pts',(31.1822136536976,0.0822897394418652,
22.6308349575606));
#49476=CARTESIAN_POINT('Ctrl Pts',(31.1616041653703,0.234707632570292,22.6416425253559));
#49477=CARTESIAN_POINT('Ctrl Pts',(31.0639996311159,0.521237294982461,22.6619596199458));
#49478=CARTESIAN_POINT('Ctrl Pts',(30.9887089758802,0.652868889710107,22.6707656569643));
#49479=CARTESIAN_POINT('Ctrl Pts',(30.7885136410845,0.885402585167096,22.6913033752648));
#49480=CARTESIAN_POINT('Ctrl Pts',(30.6637241461389,0.982420191755087,22.7024060445739));
#49481=CARTESIAN_POINT('Ctrl Pts',(30.38882091141,1.11923262290395,22.724137724694));
#49482=CARTESIAN_POINT('Ctrl Pts',(30.2423409189137,1.15980775171446,22.7345712602384));
#49483=CARTESIAN_POINT('Ctrl Pts',(29.9379463484727,1.1837522744206,22.75411234554));
#49484=CARTESIAN_POINT('Ctrl Pts',(29.7828414350779,1.1653244529442,22.7636867623073));
#49485=CARTESIAN_POINT('Ctrl Pts',(29.4887538037787,1.06944336967731,22.7851453423512));
#49486=CARTESIAN_POINT('Ctrl Pts',(29.3526850446683,0.993007607592932,22.7962109417328));
#49487=CARTESIAN_POINT('Ctrl Pts',(29.1221162292212,0.795444169323972,22.8173739985243));
#49488=CARTESIAN_POINT('Ctrl Pts',(29.0284526004007,0.677845266859518,22.8269357043589));
#49489=CARTESIAN_POINT('Ctrl Pts',(28.8868197290406,0.407843425299078,22.8460808529214));
#49490=CARTESIAN_POINT('Ctrl Pts',(28.8426042638403,0.256743916657897,22.8567949374029));
#49491=CARTESIAN_POINT('Ctrl Pts',(28.8159600292804,-0.0507119050410385,
22.8785958530886));
#49492=CARTESIAN_POINT('Ctrl Pts',(28.8325649861531,-0.204026768591548,
22.8894670227908));
#49493=CARTESIAN_POINT('Ctrl Pts',(28.9226310063267,-0.492841082076786,
22.9099461162173));
#49494=CARTESIAN_POINT('Ctrl Pts',(28.994102015515,-0.625925698199416,22.918754883105));
#49495=CARTESIAN_POINT('Ctrl Pts',(29.1877542901984,-0.863760919482141,
22.9390787662067));
#49496=CARTESIAN_POINT('Ctrl Pts',(29.3102272892874,-0.964377961033194,
22.9501667983144));
#49497=CARTESIAN_POINT('Ctrl Pts',(29.5821386201159,-1.10877008329771,22.9719834809511));
#49498=CARTESIAN_POINT('Ctrl Pts',(29.7278943046296,-1.1532370774207,22.9825105195965));
#49499=CARTESIAN_POINT('Ctrl Pts',(29.9186700556686,-1.17313232338821,22.9949309755051));
#49500=CARTESIAN_POINT('Ctrl Pts',(29.9593567068785,-1.17524047358085,22.9975041899134));
#49501=CARTESIAN_POINT('Ctrl Pts',(29.9999999999995,-1.17524047358085,22.9999999999999));
#49502=CARTESIAN_POINT('Origin',(30.,-1.21864324187371E-14,15.78125));
#49503=CARTESIAN_POINT('',(30.0000000000003,-1.17524047358085,23.5625));
#49504=CARTESIAN_POINT('',(30.,-1.17524047358085,23.5));
#49505=CARTESIAN_POINT('',(30.,-1.17524047358085,15.78125));
#49506=CARTESIAN_POINT('Ctrl Pts',(30.0000000000005,-1.17524047358085,23.5625));
#49507=CARTESIAN_POINT('Ctrl Pts',(29.8877180837681,-1.1752404735809,23.5556050287134));
#49508=CARTESIAN_POINT('Ctrl Pts',(29.7758372881673,-1.15915740880452,23.548164484563));
#49509=CARTESIAN_POINT('Ctrl Pts',(29.5190446425994,-1.08346545175016,23.5297118828087));
#49510=CARTESIAN_POINT('Ctrl Pts',(29.3805019669677,-1.01066023747548,23.5186230824555));
#49511=CARTESIAN_POINT('Ctrl Pts',(29.1440648218203,-0.81906365611398,23.4973112125635));
#49512=CARTESIAN_POINT('Ctrl Pts',(29.0470865676084,-0.703844960553528,
23.4874078682461));
#49513=CARTESIAN_POINT('Ctrl Pts',(28.8981724330839,-0.43757763652763,23.4685275248886));
#49514=CARTESIAN_POINT('Ctrl Pts',(28.8499251562346,-0.287749538271772,
23.4579035929059));
#49515=CARTESIAN_POINT('Ctrl Pts',(28.8149793372208,0.0192409990811535,
23.4361356693579));
#49516=CARTESIAN_POINT('Ctrl Pts',(28.8275655785823,0.173345465604893,23.4252085109033));
#49517=CARTESIAN_POINT('Ctrl Pts',(28.9101166290744,0.46437979734691,23.4045720015899));
#49518=CARTESIAN_POINT('Ctrl Pts',(28.9778580847147,0.598927911512345,23.3956997913279));
#49519=CARTESIAN_POINT('Ctrl Pts',(29.1650362747697,0.841899704480849,23.3755913560416));
#49520=CARTESIAN_POINT('Ctrl Pts',(29.2851376881026,0.945999066866448,23.3645254962114));
#49521=CARTESIAN_POINT('Ctrl Pts',(29.5539135664443,1.09777062977422,23.3426397256705));
#49522=CARTESIAN_POINT('Ctrl Pts',(29.6988585362439,1.14604691671332,23.3320274174642));
#49523=CARTESIAN_POINT('Ctrl Pts',(30.0001600354305,1.18508412542801,23.3121411783529));
#49524=CARTESIAN_POINT('Ctrl Pts',(30.1536625413848,1.17508243739145,23.3030583378086));
#49525=CARTESIAN_POINT('Ctrl Pts',(30.4512625228178,1.09622449574564,23.2819876064994));
#49526=CARTESIAN_POINT('Ctrl Pts',(30.592110439614,1.02700793469459,23.2708844778163));
#49527=CARTESIAN_POINT('Ctrl Pts',(30.8340714315268,0.841360319080231,23.2494443144111));
#49528=CARTESIAN_POINT('Ctrl Pts',(30.9343059293982,0.728463261371192,23.2392865244689));
#49529=CARTESIAN_POINT('Ctrl Pts',(31.0901832738534,0.465790392750319,23.2204017245443));
#49530=CARTESIAN_POINT('Ctrl Pts',(31.1423055420081,0.317257314781848,23.2099959148018));
#49531=CARTESIAN_POINT('Ctrl Pts',(31.1851773743111,0.010751647338072,23.1882623721543));
#49532=CARTESIAN_POINT('Ctrl Pts',(31.1764469607209,-0.144008319910697,
23.1772887337992));
#49533=CARTESIAN_POINT('Ctrl Pts',(31.1010701340243,-0.437108167734962,
23.1565057639579));
#49534=CARTESIAN_POINT('Ctrl Pts',(31.0368218842674,-0.573070176242618,
23.1475180074206));
#49535=CARTESIAN_POINT('Ctrl Pts',(30.8568360573785,-0.819362332337596,
23.1277335191445));
#49536=CARTESIAN_POINT('Ctrl Pts',(30.7406590361852,-0.925703986430565,
23.1168291494862));
#49537=CARTESIAN_POINT('Ctrl Pts',(30.477211273408,-1.08466164141258,23.0950157923094));
#49538=CARTESIAN_POINT('Ctrl Pts',(30.3332866239118,-1.13717003604433,23.0843160955662));
#49539=CARTESIAN_POINT('Ctrl Pts',(30.1225555529996,-1.17045159552602,23.0701956350453));
#49540=CARTESIAN_POINT('Ctrl Pts',(30.0612610274847,-1.17524047358085,23.066261897193));
#49541=CARTESIAN_POINT('Ctrl Pts',(30.0000000000001,-1.17524047358085,23.0625));
#49542=CARTESIAN_POINT('Ctrl Pts',(29.9999999999995,-1.17524047358085,22.9999999999999));
#49543=CARTESIAN_POINT('Ctrl Pts',(30.1122819160637,-1.17524047358085,23.0068949712763));
#49544=CARTESIAN_POINT('Ctrl Pts',(30.2241627114991,-1.15915740885253,23.0143355154149));
#49545=CARTESIAN_POINT('Ctrl Pts',(30.4809553569443,-1.08346545195345,23.0327881171562));
#49546=CARTESIAN_POINT('Ctrl Pts',(30.6194980326123,-1.01066023773368,23.0438769175097));
#49547=CARTESIAN_POINT('Ctrl Pts',(30.8559351778473,-0.819063656461988,
23.0651887874038));
#49548=CARTESIAN_POINT('Ctrl Pts',(30.952913432109,-0.703844960936813,23.0750921317269));
#49549=CARTESIAN_POINT('Ctrl Pts',(31.1018275667414,-0.437577636966923,
23.0939724750804));
#49550=CARTESIAN_POINT('Ctrl Pts',(31.1500748436503,-0.287749538730812,
23.1045964070617));
#49551=CARTESIAN_POINT('Ctrl Pts',(31.1850206627874,0.0192409986134863,
23.126364330609));
#49552=CARTESIAN_POINT('Ctrl Pts',(31.1724344214858,0.173345465148191,23.1372914890643));
#49553=CARTESIAN_POINT('Ctrl Pts',(31.0898833711054,0.464379796922714,23.15792799838));
#49554=CARTESIAN_POINT('Ctrl Pts',(31.0221419155201,0.598927911110121,23.1668002086434));
#49555=CARTESIAN_POINT('Ctrl Pts',(30.8349637255609,0.841899704153978,23.1869086439265));
#49556=CARTESIAN_POINT('Ctrl Pts',(30.7148623122637,0.945999066590532,23.1979745037564));
#49557=CARTESIAN_POINT('Ctrl Pts',(30.4460864339697,1.09777062960664,23.2198602742982));
#49558=CARTESIAN_POINT('Ctrl Pts',(30.3011414641827,1.1460469166018,23.2304725825058));
#49559=CARTESIAN_POINT('Ctrl Pts',(29.9998399650194,1.18508412542607,23.2503588216195));
#49560=CARTESIAN_POINT('Ctrl Pts',(29.8463374590763,1.17508243744973,23.2594416621611));
#49561=CARTESIAN_POINT('Ctrl Pts',(29.5487374776195,1.09622449592641,23.2805123934674));
#49562=CARTESIAN_POINT('Ctrl Pts',(29.4078895607902,1.02700793492841,23.2916155221506));
#49563=CARTESIAN_POINT('Ctrl Pts',(29.1659285687959,0.841360319401014,23.3130556855578));
#49564=CARTESIAN_POINT('Ctrl Pts',(29.0656940708777,0.72846326172594,23.3232134755017));
#49565=CARTESIAN_POINT('Ctrl Pts',(28.9098167263205,0.465790393157422,23.3420982754308));
#49566=CARTESIAN_POINT('Ctrl Pts',(28.8576944581104,0.317257315207477,23.3525040851682));
#49567=CARTESIAN_POINT('Ctrl Pts',(28.8148226256923,0.0107516477743395,
23.3742376278149));
#49568=CARTESIAN_POINT('Ctrl Pts',(28.8235530392262,-0.144008319483296,
23.3852112661707));
#49569=CARTESIAN_POINT('Ctrl Pts',(28.8989298658185,-0.437108167337535,
23.4059942360141));
#49570=CARTESIAN_POINT('Ctrl Pts',(28.9631781155251,-0.573070175865714,
23.4149819925535));
#49571=CARTESIAN_POINT('Ctrl Pts',(29.1431639423218,-0.819362332023802,
23.4347664808262));
#49572=CARTESIAN_POINT('Ctrl Pts',(29.2593409634759,-0.925703986159073,
23.4456708504836));
#49573=CARTESIAN_POINT('Ctrl Pts',(29.5227887261992,-1.08466164124026,23.4674842076606));
#49574=CARTESIAN_POINT('Ctrl Pts',(29.6667133756817,-1.13717003592563,23.4781839044047));
#49575=CARTESIAN_POINT('Ctrl Pts',(29.8774444467245,-1.17045159550418,23.4923043649371));
#49576=CARTESIAN_POINT('Ctrl Pts',(29.9387389723772,-1.17524047358085,23.4962381027985));
#49577=CARTESIAN_POINT('Ctrl Pts',(29.9999999999999,-1.17524047358085,23.5));
#49578=CARTESIAN_POINT('Origin',(30.,-1.21864324187371E-14,15.78125));
#49579=CARTESIAN_POINT('',(30.0000000000001,-1.17524047358085,24.0625));
#49580=CARTESIAN_POINT('',(30.,-1.17524047358085,24.));
#49581=CARTESIAN_POINT('',(30.,-1.17524047358085,15.78125));
#49582=CARTESIAN_POINT('Ctrl Pts',(30.0000000000002,-1.17524047358085,24.0625));
#49583=CARTESIAN_POINT('Ctrl Pts',(29.8653092296601,-1.17524047358088,24.0542289531099));
#49584=CARTESIAN_POINT('Ctrl Pts',(29.7314664131893,-1.15209385822287,24.045189343081));
#49585=CARTESIAN_POINT('Ctrl Pts',(29.4591513817099,-1.05471955679206,24.0250148275808));
#49586=CARTESIAN_POINT('Ctrl Pts',(29.3256241785221,-0.974766232969058,
24.0139805885274));
#49587=CARTESIAN_POINT('Ctrl Pts',(29.1008976044993,-0.771359156787199,
23.99296911139));
#49588=CARTESIAN_POINT('Ctrl Pts',(29.0105061805318,-0.651353133596405,
23.9836858053905));
#49589=CARTESIAN_POINT('Ctrl Pts',(28.876221002938,-0.377670021906335,23.9642796272619));
#49590=CARTESIAN_POINT('Ctrl Pts',(28.8360911103609,-0.225405853644338,
23.9534829597086));
#49591=CARTESIAN_POINT('Ctrl Pts',(28.8177863463358,0.0822897399134218,
23.931665042406));
#49592=CARTESIAN_POINT('Ctrl Pts',(28.8383958347227,0.234707633027682,23.9208574746117));
#49593=CARTESIAN_POINT('Ctrl Pts',(28.9360003690899,0.521237295405437,23.9005403800242));
#49594=CARTESIAN_POINT('Ctrl Pts',(29.0112910243832,0.652868890111379,23.8917343430053));
#49595=CARTESIAN_POINT('Ctrl Pts',(29.211486359277,0.885402585487968,23.8711966247017));
#49596=CARTESIAN_POINT('Ctrl Pts',(29.3362758542566,0.98242019202142,23.8600939553924));
#49597=CARTESIAN_POINT('Ctrl Pts',(29.611179089029,1.11923262305578,23.8383622752737));
#49598=CARTESIAN_POINT('Ctrl Pts',(29.7576590815354,1.15980775180767,23.8279287397307));
#49599=CARTESIAN_POINT('Ctrl Pts',(30.0620536519992,1.1837522743985,23.8083876544318));
#49600=CARTESIAN_POINT('Ctrl Pts',(30.2171585654068,1.16532445285658,23.7988132376599));
#49601=CARTESIAN_POINT('Ctrl Pts',(30.5112461966771,1.06944336945855,23.7773546576131));
#49602=CARTESIAN_POINT('Ctrl Pts',(30.6473149557494,0.993007607319778,23.7662890582319));
#49603=CARTESIAN_POINT('Ctrl Pts',(30.8778837711073,0.795444168961031,23.7451260014428));
#49604=CARTESIAN_POINT('Ctrl Pts',(30.9715473998777,0.67784526646015,23.735564295613));
#49605=CARTESIAN_POINT('Ctrl Pts',(31.1131802711266,0.407843424843195,23.7164191470464));
#49606=CARTESIAN_POINT('Ctrl Pts',(31.1573957362652,0.25674391618342,23.7057050625635));
#49607=CARTESIAN_POINT('Ctrl Pts',(31.1840399706984,-0.0507119055208601,
23.6839041468775));
#49608=CARTESIAN_POINT('Ctrl Pts',(31.1674350137646,-0.204026769058537,
23.6730329771762));
#49609=CARTESIAN_POINT('Ctrl Pts',(31.0773689934766,-0.492841082509219,
23.6525538837521));
#49610=CARTESIAN_POINT('Ctrl Pts',(31.0058979842309,-0.625925698609867,
23.643745116865));
#49611=CARTESIAN_POINT('Ctrl Pts',(30.8122457094484,-0.863760919813326,
23.62342123376));
#49612=CARTESIAN_POINT('Ctrl Pts',(30.6897727103237,-0.964377961310509,
23.612333201652));
#49613=CARTESIAN_POINT('Ctrl Pts',(30.4178613794486,-1.10877008346121,23.5905165190165));
#49614=CARTESIAN_POINT('Ctrl Pts',(30.2721056949232,-1.15323707752562,23.5799894803724));
#49615=CARTESIAN_POINT('Ctrl Pts',(30.081329944032,-1.17313232340388,23.5675690244761));
#49616=CARTESIAN_POINT('Ctrl Pts',(30.0406432929718,-1.17524047358083,23.5649958100773));
#49617=CARTESIAN_POINT('Ctrl Pts',(30.0000000000005,-1.17524047358085,23.5625));
#49618=CARTESIAN_POINT('Ctrl Pts',(29.9999999999999,-1.17524047358085,23.5));
#49619=CARTESIAN_POINT('Ctrl Pts',(30.0894855238544,-1.17524047358085,23.5054950978594));
#49620=CARTESIAN_POINT('Ctrl Pts',(30.178854666788,-1.16502438903023,23.5113452474122));
#49621=CARTESIAN_POINT('Ctrl Pts',(30.4182361773703,-1.10931034894115,23.5280203800546));
#49622=CARTESIAN_POINT('Ctrl Pts',(30.5615135396518,-1.04411918207875,23.5391299800668));
#49623=CARTESIAN_POINT('Ctrl Pts',(30.8095036980223,-0.865097093436967,
23.5607054808684));
#49624=CARTESIAN_POINT('Ctrl Pts',(30.9132272713337,-0.75480290560396,23.5709852453531));
#49625=CARTESIAN_POINT('Ctrl Pts',(31.0771989331901,-0.495400927628404,
23.5902511331837));
#49626=CARTESIAN_POINT('Ctrl Pts',(31.1336431986023,-0.347374707971562,
23.6003685369235));
#49627=CARTESIAN_POINT('Ctrl Pts',(31.1845754344926,-0.0407388684447008,
23.6221113097446));
#49628=CARTESIAN_POINT('Ctrl Pts',(31.1797255553422,0.114581560252514,23.6331246890053));
#49629=CARTESIAN_POINT('Ctrl Pts',(31.1115436466863,0.409699470279596,23.6540507545398));
#49630=CARTESIAN_POINT('Ctrl Pts',(31.0507381700391,0.547097840637693,23.6632066094863));
#49631=CARTESIAN_POINT('Ctrl Pts',(30.877053704825,0.797680553802843,23.6827562620821));
#49632=CARTESIAN_POINT('Ctrl Pts',(30.7635871432854,0.906879897536129,23.6935955044951));
#49633=CARTESIAN_POINT('Ctrl Pts',(30.5039119215803,1.07256979004896,23.7154158816792));
#49634=CARTESIAN_POINT('Ctrl Pts',(30.3609720672946,1.12873587571,23.726184783255));
#49635=CARTESIAN_POINT('Ctrl Pts',(30.0630485009405,1.18318311722529,23.7464099346189));
#49636=CARTESIAN_POINT('Ctrl Pts',(29.9110260227659,1.18151676553675,23.755241166967));
#49637=CARTESIAN_POINT('Ctrl Pts',(29.6103298881048,1.1197202582759,23.7758971342361));
#49638=CARTESIAN_POINT('Ctrl Pts',(29.46506200542,1.05803905975613,23.7870045259814));
#49639=CARTESIAN_POINT('Ctrl Pts',(29.2120537724961,0.884838382027716,23.8086817842968));
#49640=CARTESIAN_POINT('Ctrl Pts',(29.1053977198379,0.776856295866943,23.8190596528721));
#49641=CARTESIAN_POINT('Ctrl Pts',(28.9357911246459,0.52231447495466,23.8384992581206));
#49642=CARTESIAN_POINT('Ctrl Pts',(28.8760978227722,0.377122301892393,23.8482592101808));
#49643=CARTESIAN_POINT('Ctrl Pts',(28.816919249242,0.0729797847098555,23.8698251878126));
#49644=CARTESIAN_POINT('Ctrl Pts',(28.8175683805337,-0.0828368336059415,
23.8808737506258));
#49645=CARTESIAN_POINT('Ctrl Pts',(28.8779787013698,-0.380073435953635,
23.9019500472809));
#49646=CARTESIAN_POINT('Ctrl Pts',(28.9351273214881,-0.519045422805617,
23.9113440791565));
#49647=CARTESIAN_POINT('Ctrl Pts',(29.1020830634255,-0.774116322451291,
23.9306396594913));
#49648=CARTESIAN_POINT('Ctrl Pts',(29.212592687875,-0.88627172070161,23.9414021264554));
#49649=CARTESIAN_POINT('Ctrl Pts',(29.4680719424329,-1.05901132730886,23.963214777767));
#49650=CARTESIAN_POINT('Ctrl Pts',(29.609865400996,-1.11904322621712,23.9740503393744));
#49651=CARTESIAN_POINT('Ctrl Pts',(29.8385706131875,-1.1669231022752,23.9897921149766));
#49652=CARTESIAN_POINT('Ctrl Pts',(29.9192597310019,-1.17524047358085,23.9950419278981));
#49653=CARTESIAN_POINT('Ctrl Pts',(30.,-1.17524047358085,24.));
#49654=CARTESIAN_POINT('Origin',(30.,-1.21864324187371E-14,15.78125));
#49655=CARTESIAN_POINT('',(29.9999999962159,-1.17524047358085,24.5624999995353));
#49656=CARTESIAN_POINT('',(30.0000000000002,-1.17524047358085,24.5));
#49657=CARTESIAN_POINT('',(30.,-1.17524047358085,15.78125));
#49658=CARTESIAN_POINT('Ctrl Pts',(29.9999999924319,-1.17524047358085,24.5624999995353));
#49659=CARTESIAN_POINT('Ctrl Pts',(29.8449382921852,-1.17524047258231,24.5529780211908));
#49660=CARTESIAN_POINT('Ctrl Pts',(29.6912874372683,-1.14455036315003,24.5424546005433));
#49661=CARTESIAN_POINT('Ctrl Pts',(29.4063853758944,-1.0258343762565,24.5207505023134));
#49662=CARTESIAN_POINT('Ctrl Pts',(29.2777080162496,-0.939688490130196,
24.5097945313951));
#49663=CARTESIAN_POINT('Ctrl Pts',(29.0636971062813,-0.72579687417109,24.4890693621447));
#49664=CARTESIAN_POINT('Ctrl Pts',(28.9792543776096,-0.601260808557374,
24.4801338851547));
#49665=CARTESIAN_POINT('Ctrl Pts',(28.8587167668904,-0.3209315497576,24.4602564455228));
#49666=CARTESIAN_POINT('Ctrl Pts',(28.8262532459446,-0.166807893138082,
24.449327926347));
#49667=CARTESIAN_POINT('Ctrl Pts',(28.823406512149,0.140728845641508,24.4275212730356));
#49668=CARTESIAN_POINT('Ctrl Pts',(28.851353518733,0.291209583843224,24.4168510640028));
#49669=CARTESIAN_POINT('Ctrl Pts',(28.9629467293987,0.573358103335639,24.3968446251906));
#49670=CARTESIAN_POINT('Ctrl Pts',(29.0455390967654,0.702301510494977,24.3878786774254));
#49671=CARTESIAN_POINT('Ctrl Pts',(29.2579957317181,0.924591935160839,24.3669511834331));
#49672=CARTESIAN_POINT('Ctrl Pts',(29.3868926291043,1.01465868024229,24.3558427221105));
#49673=CARTESIAN_POINT('Ctrl Pts',(29.6668973327643,1.13696430638437,24.3343120930999));
#49674=CARTESIAN_POINT('Ctrl Pts',(29.8144674232288,1.17014774293813,24.3240736802882));
#49675=CARTESIAN_POINT('Ctrl Pts',(30.1216534355145,1.17947691079308,24.3048793479835));
#49676=CARTESIAN_POINT('Ctrl Pts',(30.2784124097871,1.15260328295164,24.2946007685524));
#49677=CARTESIAN_POINT('Ctrl Pts',(30.5685961343608,1.03996407129779,24.2727877800628));
#49678=CARTESIAN_POINT('Ctrl Pts',(30.6996254486415,0.956741717213513,24.2617910312175));
#49679=CARTESIAN_POINT('Ctrl Pts',(30.9187688591,0.747835373953449,24.2409274335984));
#49680=CARTESIAN_POINT('Ctrl Pts',(31.006053860002,0.625488945893405,24.2318518411732));
#49681=CARTESIAN_POINT('Ctrl Pts',(31.1332209274868,0.348324830571042,24.2121988338701));
#49682=CARTESIAN_POINT('Ctrl Pts',(31.1693830920172,0.195045950853365,24.2013302156905));
#49683=CARTESIAN_POINT('Ctrl Pts',(31.1796570639592,-0.112665031805443,
24.1795112071857));
#49684=CARTESIAN_POINT('Ctrl Pts',(31.1552218060231,-0.264121048947789,
24.1687718435869));
#49685=CARTESIAN_POINT('Ctrl Pts',(31.0503552824464,-0.548400595365726,
24.1486142990383));
#49686=CARTESIAN_POINT('Ctrl Pts',(30.9713114905908,-0.678634752411996,
24.1397525078141));
#49687=CARTESIAN_POINT('Ctrl Pts',(30.7647686763693,-0.905919595273436,
24.119011097007));
#49688=CARTESIAN_POINT('Ctrl Pts',(30.6378140048735,-0.999372205084128,
24.1079018617007));
#49689=CARTESIAN_POINT('Ctrl Pts',(30.3601860918747,-1.12872343710904,24.0862673928177));
#49690=CARTESIAN_POINT('Ctrl Pts',(30.2130976252741,-1.16548763290266,24.0759316041108));
#49691=CARTESIAN_POINT('Ctrl Pts',(30.042024216247,-1.17467745886824,24.065100570339));
#49692=CARTESIAN_POINT('Ctrl Pts',(30.021003006896,-1.17524047358085,24.0637897457965));
#49693=CARTESIAN_POINT('Ctrl Pts',(30.0000000000002,-1.17524047358085,24.0625));
#49694=CARTESIAN_POINT('Ctrl Pts',(30.,-1.17524047358085,24.));
#49695=CARTESIAN_POINT('Ctrl Pts',(30.068631292987,-1.17524047358085,24.0042144880528));
#49696=CARTESIAN_POINT('Ctrl Pts',(30.1372731197099,-1.16923029330172,24.0086427063088));
#49697=CARTESIAN_POINT('Ctrl Pts',(30.3594639555913,-1.12983827430394,24.0236835229636));
#49698=CARTESIAN_POINT('Ctrl Pts',(30.5067279557135,-1.07189657495913,24.034780912417));
#49699=CARTESIAN_POINT('Ctrl Pts',(30.7648494491756,-0.904940985120749,
24.0565507524641));
#49700=CARTESIAN_POINT('Ctrl Pts',(30.8745226735525,-0.799463570900332,
24.0670250985558));
#49701=CARTESIAN_POINT('Ctrl Pts',(31.0499651911362,-0.550024618872908,
24.0866421584515));
#49702=CARTESIAN_POINT('Ctrl Pts',(31.1129833274185,-0.407722194144101,
24.0960894491163));
#49703=CARTESIAN_POINT('Ctrl Pts',(31.1806136864057,-0.106256135243321,
24.117465645852));
#49704=CARTESIAN_POINT('Ctrl Pts',(31.1843316043204,0.0499559746584703,
24.1285422519746));
#49705=CARTESIAN_POINT('Ctrl Pts',(31.131994520367,0.349324836152535,24.1497697417397));
#49706=CARTESIAN_POINT('Ctrl Pts',(31.0785837311869,0.489956671487056,24.1594708103671));
#49707=CARTESIAN_POINT('Ctrl Pts',(30.9185303965388,0.749536525439823,24.1785023892068));
#49708=CARTESIAN_POINT('Ctrl Pts',(30.8111165172128,0.864620133839068,24.1891785696567));
#49709=CARTESIAN_POINT('Ctrl Pts',(30.5601137220937,1.04443640550787,24.2109672262292));
#49710=CARTESIAN_POINT('Ctrl Pts',(30.4195953268947,1.10838743812269,24.2218634370972));
#49711=CARTESIAN_POINT('Ctrl Pts',(30.125226440525,1.17808176086598,24.2424108698401));
#49712=CARTESIAN_POINT('Ctrl Pts',(29.9745000794406,1.18444262103543,24.2512396402881));
#49713=CARTESIAN_POINT('Ctrl Pts',(29.671168206001,1.13918974904968,24.2714709284502));
#49714=CARTESIAN_POINT('Ctrl Pts',(29.5219912146071,1.08506931535676,24.2825503121002));
#49715=CARTESIAN_POINT('Ctrl Pts',(29.2588817407465,0.924538989806815,24.3043986527903));
#49716=CARTESIAN_POINT('Ctrl Pts',(29.1462343920073,0.821663056130735,24.3149634007337));
#49717=CARTESIAN_POINT('Ctrl Pts',(28.9649893539032,0.577368135519195,24.3347544047798));
#49718=CARTESIAN_POINT('Ctrl Pts',(28.8986993951907,0.437889260784583,24.3439503786226));
#49719=CARTESIAN_POINT('Ctrl Pts',(28.8227562109677,0.139172903579825,24.3651316009568));
#49720=CARTESIAN_POINT('Ctrl Pts',(28.814686650905,-0.0173128945475468,
24.3762276136201));
#49721=CARTESIAN_POINT('Ctrl Pts',(28.8589720780878,-0.318736522506238,
24.3976008016849));
#49722=CARTESIAN_POINT('Ctrl Pts',(28.9087096405855,-0.46104932706788,24.4076656524993));
#49723=CARTESIAN_POINT('Ctrl Pts',(29.0619693077579,-0.724977765539007,
24.4264342215945));
#49724=CARTESIAN_POINT('Ctrl Pts',(29.1662794308695,-0.84283884374432,24.4370182792792));
#49725=CARTESIAN_POINT('Ctrl Pts',(29.4127142037999,-1.0294613008905,24.4587677289451));
#49726=CARTESIAN_POINT('Ctrl Pts',(29.5518825792064,-1.09722011413893,24.4697160382912));
#49727=CARTESIAN_POINT('Ctrl Pts',(29.7982117366005,-1.1622217216024,24.4871470887339));
#49728=CARTESIAN_POINT('Ctrl Pts',(29.8989795683345,-1.17524047358088,24.4937965702842));
#49729=CARTESIAN_POINT('Ctrl Pts',(30.0000000000003,-1.17524047358085,24.5));
#49730=CARTESIAN_POINT('Origin',(30.,-1.21864324187371E-14,15.78125));
#49731=CARTESIAN_POINT('',(29.9999999999999,-1.17524047358085,25.0625));
#49732=CARTESIAN_POINT('',(30.0000000000002,-1.17524047358085,25.));
#49733=CARTESIAN_POINT('',(30.,-1.17524047358085,15.78125));
#49734=CARTESIAN_POINT('Ctrl Pts',(29.9999999999998,-1.17524047358085,25.0625));
#49735=CARTESIAN_POINT('Ctrl Pts',(29.9787160795735,-1.17524047358085,25.0611930039571));
#49736=CARTESIAN_POINT('Ctrl Pts',(29.9574135577721,-1.17466229796152,25.0598643671606));
#49737=CARTESIAN_POINT('Ctrl Pts',(29.7860545064693,-1.16533366685381,25.0490108716001));
#49738=CARTESIAN_POINT('Ctrl Pts',(29.638982260427,-1.12845915516134,25.0386721678491));
#49739=CARTESIAN_POINT('Ctrl Pts',(29.3614303849904,-0.998891400573746,
25.0170346917219));
#49740=CARTESIAN_POINT('Ctrl Pts',(29.2345369639167,-0.905335034780717,
25.0059255391243));
#49741=CARTESIAN_POINT('Ctrl Pts',(29.0281770961676,-0.677897334966365,
24.9851899432843));
#49742=CARTESIAN_POINT('Ctrl Pts',(28.9492422426318,-0.547623084588669,
24.9763305695037));
#49743=CARTESIAN_POINT('Ctrl Pts',(28.8429395559285,-0.25880932586385,24.9558515154165));
#49744=CARTESIAN_POINT('Ctrl Pts',(28.8187785161156,-0.102338490894112,
24.9447565638831));
#49745=CARTESIAN_POINT('Ctrl Pts',(28.8329707062525,0.20487723468326,24.9229726728069));
#49746=CARTESIAN_POINT('Ctrl Pts',(28.8688620223111,0.352813948215486,24.9124828541373));
#49747=CARTESIAN_POINT('Ctrl Pts',(28.9959383633127,0.629882762331914,24.8928366044019));
#49748=CARTESIAN_POINT('Ctrl Pts',(29.0869818629053,0.755846556300386,24.8834354015886));
#49749=CARTESIAN_POINT('Ctrl Pts',(29.3131553782924,0.966129203680405,24.8620913064548));
#49750=CARTESIAN_POINT('Ctrl Pts',(29.4462640631474,1.04811028996687,24.8510108758816));
#49751=CARTESIAN_POINT('Ctrl Pts',(29.731323759893,1.1538048728599,24.8297587550632));
#49752=CARTESIAN_POINT('Ctrl Pts',(29.8797531248391,1.17853792828451,24.8200009879783));
#49753=CARTESIAN_POINT('Ctrl Pts',(30.1846496308258,1.17107054148177,24.8010132560253));
#49754=CARTESIAN_POINT('Ctrl Pts',(30.3381730792388,1.13627251448872,24.7903520180859));
#49755=CARTESIAN_POINT('Ctrl Pts',(30.6200199170605,1.01003478142549,24.7685688600169));
#49756=CARTESIAN_POINT('Ctrl Pts',(30.7461080027782,0.920828764814659,24.7576633973259));
#49757=CARTESIAN_POINT('Ctrl Pts',(30.954589658464,0.701638656166971,24.7370899153526));
#49758=CARTESIAN_POINT('Ctrl Pts',(31.0359799147447,0.574699574292555,24.7282504951265));
#49759=CARTESIAN_POINT('Ctrl Pts',(31.1497275829798,0.289883112537678,24.7080548792676));
#49760=CARTESIAN_POINT('Ctrl Pts',(31.1781418190148,0.133683865658838,24.6969791852295));
#49761=CARTESIAN_POINT('Ctrl Pts',(31.1719905418774,-0.174601531099527,
24.6751194464719));
#49762=CARTESIAN_POINT('Ctrl Pts',(31.1398342436188,-0.323793762033814,
24.6645406022347));
#49763=CARTESIAN_POINT('Ctrl Pts',(31.020088030022,-0.603297917753395,24.644721668578));
#49764=CARTESIAN_POINT('Ctrl Pts',(30.9330960022514,-0.730676428588708,
24.6355607116713));
#49765=CARTESIAN_POINT('Ctrl Pts',(30.7134327937131,-0.946735070008641,
24.6144116187632));
#49766=CARTESIAN_POINT('Ctrl Pts',(30.5822707418913,-1.03259356059966,24.6033132579239));
#49767=CARTESIAN_POINT('Ctrl Pts',(30.299587098649,-1.14619538675731,24.5819267037008));
#49768=CARTESIAN_POINT('Ctrl Pts',(30.1515439291036,-1.17497884081411,24.5718152360255));
#49769=CARTESIAN_POINT('Ctrl Pts',(30.0013618111703,-1.17523988185447,24.5625836466351));
#49770=CARTESIAN_POINT('Ctrl Pts',(30.0006808894801,-1.17524047358524,24.5625418118389));
#49771=CARTESIAN_POINT('Ctrl Pts',(29.9999999924319,-1.17524047358085,24.5624999995353));
#49772=CARTESIAN_POINT('Ctrl Pts',(30.0000000000003,-1.17524047358085,24.5));
#49773=CARTESIAN_POINT('Ctrl Pts',(30.0475989786694,-1.17524047358084,24.5029229425557));
#49774=CARTESIAN_POINT('Ctrl Pts',(30.0952413712801,-1.17234913261358,24.5059510599029));
#49775=CARTESIAN_POINT('Ctrl Pts',(30.2990650070911,-1.14742109537484,24.5193511873216));
#49776=CARTESIAN_POINT('Ctrl Pts',(30.4499960157575,-1.0970416910395,24.5304056476212));
#49777=CARTESIAN_POINT('Ctrl Pts',(30.7177665488108,-0.942842462676014,
24.5523157520592));
#49778=CARTESIAN_POINT('Ctrl Pts',(30.833223349596,-0.842552715174129,24.5629613319529));
#49779=CARTESIAN_POINT('Ctrl Pts',(31.0200068112404,-0.603233885310555,
24.5829160166926));
#49780=CARTESIAN_POINT('Ctrl Pts',(31.0893943876237,-0.466400998056969,
24.591928683353));
#49781=CARTESIAN_POINT('Ctrl Pts',(31.1731872619397,-0.170385863873932,
24.612918368786));
#49782=CARTESIAN_POINT('Ctrl Pts',(31.185412882504,-0.0137497619841131,
24.6240250391094));
#49783=CARTESIAN_POINT('Ctrl Pts',(31.1488612218191,0.289356743431089,24.6455175557638));
#49784=CARTESIAN_POINT('Ctrl Pts',(31.1026857517696,0.433263084173784,24.6557215908795));
#49785=CARTESIAN_POINT('Ctrl Pts',(30.9558437041525,0.701308793163264,24.6747280350226));
#49786=CARTESIAN_POINT('Ctrl Pts',(30.8545058913013,0.821789237632239,24.6849956137961));
#49787=CARTESIAN_POINT('Ctrl Pts',(30.6123622815668,1.01480099766359,24.7067080777764));
#49788=CARTESIAN_POINT('Ctrl Pts',(30.4745499588497,1.08610079838188,24.7176986563197));
#49789=CARTESIAN_POINT('Ctrl Pts',(30.1837738406509,1.17031056558872,24.7385400922772));
#49790=CARTESIAN_POINT('Ctrl Pts',(30.0341022035471,1.18415559329136,24.7475897886987));
#49791=CARTESIAN_POINT('Ctrl Pts',(29.7305751526436,1.15452627151871,24.7672791490145));
#49792=CARTESIAN_POINT('Ctrl Pts',(29.5799242663497,1.10861951554252,24.7781578355522));
#49793=CARTESIAN_POINT('Ctrl Pts',(29.3089128663366,0.962634653740643,24.7999757240996));
#49794=CARTESIAN_POINT('Ctrl Pts',(29.1903801371545,0.865330006275208,24.8107043566494));
#49795=CARTESIAN_POINT('Ctrl Pts',(28.9974547059893,0.631606479932577,24.8308378310304));
#49796=CARTESIAN_POINT('Ctrl Pts',(28.9246531642855,0.497649505166107,24.8397129306474));
#49797=CARTESIAN_POINT('Ctrl Pts',(28.8322520407485,0.204711362593916,24.8604844343777));
#49798=CARTESIAN_POINT('Ctrl Pts',(28.8154219514347,0.0480344797090969,
24.8715939963785));
#49799=CARTESIAN_POINT('Ctrl Pts',(28.8433837526351,-0.256851307347509,
24.8932126773996));
#49800=CARTESIAN_POINT('Ctrl Pts',(28.8856263759144,-0.402401296034548,
24.9035332594392));
#49801=CARTESIAN_POINT('Ctrl Pts',(29.0254132564532,-0.675115053553108,
24.9228707031121));
#49802=CARTESIAN_POINT('Ctrl Pts',(29.1237053106631,-0.798585223889617,
24.932834945393));
#49803=CARTESIAN_POINT('Ctrl Pts',(29.3612206915393,-0.998444700238917,
24.9545059777387));
#49804=CARTESIAN_POINT('Ctrl Pts',(29.4974844913312,-1.07350395274647,24.9655347517064));
#49805=CARTESIAN_POINT('Ctrl Pts',(29.7595519260122,-1.15671325178265,24.9845777838555));
#49806=CARTESIAN_POINT('Ctrl Pts',(29.8794906495254,-1.17524047358089,24.9925998011151));
#49807=CARTESIAN_POINT('Ctrl Pts',(30.0000000000004,-1.17524047358085,25.));
#49808=CARTESIAN_POINT('Origin',(30.,-1.21864324187371E-14,15.78125));
#49809=CARTESIAN_POINT('',(29.9999999999997,-1.17524047358085,25.5625));
#49810=CARTESIAN_POINT('',(30.,-1.17524047358085,25.5));
#49811=CARTESIAN_POINT('',(30.,-1.17524047358085,15.78125));
#49812=CARTESIAN_POINT('Ctrl Pts',(29.9999999999995,-1.17524047358085,25.5625));
#49813=CARTESIAN_POINT('Ctrl Pts',(29.9590631434842,-1.17524047358085,25.5599861628683));
#49814=CARTESIAN_POINT('Ctrl Pts',(29.9180826982373,-1.17310176284205,25.557393823766));
#49815=CARTESIAN_POINT('Ctrl Pts',(29.7270170759755,-1.15303120939534,25.5449493522346));
#49816=CARTESIAN_POINT('Ctrl Pts',(29.5812843667667,-1.10844931412058,25.534419650774));
#49817=CARTESIAN_POINT('Ctrl Pts',(29.3094646041477,-0.963834030512161,
25.5126006792245));
#49818=CARTESIAN_POINT('Ctrl Pts',(29.1870616253517,-0.863111358786919,
25.5015132019157));
#49819=CARTESIAN_POINT('Ctrl Pts',(28.9936035835609,-0.625120486304078,
25.4811957277874));
#49820=CARTESIAN_POINT('Ctrl Pts',(28.922245153506,-0.491992360156719,25.4723859354899));
#49821=CARTESIAN_POINT('Ctrl Pts',(28.8324037582581,-0.203110856662721,
25.4519020777895));
#49822=CARTESIAN_POINT('Ctrl Pts',(28.8159185655927,-0.0497708721110285,
25.4410291268206));
#49823=CARTESIAN_POINT('Ctrl Pts',(28.8428111724951,0.257674311776114,25.4192289654353));
#49824=CARTESIAN_POINT('Ctrl Pts',(28.8871477746036,0.408737403201897,25.4085174632064));
#49825=CARTESIAN_POINT('Ctrl Pts',(29.028998912458,0.678628541452795,25.389380164336));
#49826=CARTESIAN_POINT('Ctrl Pts',(29.1227608288482,0.796156039557689,25.3798091767006));
#49827=CARTESIAN_POINT('Ctrl Pts',(29.3535044180399,0.99354320653279,25.3586416369362));
#49828=CARTESIAN_POINT('Ctrl Pts',(29.4896480206548,1.06987223772086,25.3475752255981));
#49829=CARTESIAN_POINT('Ctrl Pts',(29.7837920452496,1.16549604577304,25.326122303941));
#49830=CARTESIAN_POINT('Ctrl Pts',(29.9388720345248,1.18379547475176,25.3165570329261));
#49831=CARTESIAN_POINT('Ctrl Pts',(30.243221825482,1.15962478745302,25.2970106790485));
#49832=CARTESIAN_POINT('Ctrl Pts',(30.3896819125524,1.11893466510606,25.2865742888993));
#49833=CARTESIAN_POINT('Ctrl Pts',(30.664499787972,0.981897695245122,25.2648398897594));
#49834=CARTESIAN_POINT('Ctrl Pts',(30.7892223684277,0.884773136061606,25.2537375376443));
#49835=CARTESIAN_POINT('Ctrl Pts',(30.9892253393634,0.652081932327525,25.233206047704));
#49836=CARTESIAN_POINT('Ctrl Pts',(31.0644029101032,0.520407945827758,25.2244008128923));
#49837=CARTESIAN_POINT('Ctrl Pts',(31.1617865735135,0.233810524226684,25.2040789136694));
#49838=CARTESIAN_POINT('Ctrl Pts',(31.1822791704619,0.0813648687854731,
25.1932693773186));
#49839=CARTESIAN_POINT('Ctrl Pts',(31.1637300195375,-0.226326940808914,
25.1714517283273));
#49840=CARTESIAN_POINT('Ctrl Pts',(31.1234798971667,-0.378558584977568,
25.1606573669753));
#49841=CARTESIAN_POINT('Ctrl Pts',(30.9889788141031,-0.652134792227603,
25.1412587691706));
#49842=CARTESIAN_POINT('Ctrl Pts',(30.8984922205339,-0.772069973056249,
25.1319682180917));
#49843=CARTESIAN_POINT('Ctrl Pts',(30.6735951228457,-0.975307798919531,
25.1109522700489));
#49844=CARTESIAN_POINT('Ctrl Pts',(30.5399926661631,-1.05515984400593,25.0999170005632));
#49845=CARTESIAN_POINT('Ctrl Pts',(30.2678908596704,-1.15220558793873,25.0797672273045));
#49846=CARTESIAN_POINT('Ctrl Pts',(30.1343655548317,-1.17524047358085,25.0707510761622));
#49847=CARTESIAN_POINT('Ctrl Pts',(29.9999999999998,-1.17524047358085,25.0625));
#49848=CARTESIAN_POINT('Ctrl Pts',(30.0000000000004,-1.17524047358085,25.));
#49849=CARTESIAN_POINT('Ctrl Pts',(30.0280011909949,-1.17524047358084,25.0017194880028));
#49850=CARTESIAN_POINT('Ctrl Pts',(30.056028863347,-1.17423978093536,25.0034760804581));
#49851=CARTESIAN_POINT('Ctrl Pts',(30.2395952618035,-1.16108096396762,25.0152149952129));
#49852=CARTESIAN_POINT('Ctrl Pts',(30.3913571022497,-1.11907669842983,25.0260235449911));
#49853=CARTESIAN_POINT('Ctrl Pts',(30.6663605367685,-0.979972388704826,
25.0478426338075));
#49854=CARTESIAN_POINT('Ctrl Pts',(30.7876235644496,-0.885461952247295,
25.0586398624147));
#49855=CARTESIAN_POINT('Ctrl Pts',(30.9860830879355,-0.656850945315206,
25.0789319146131));
#49856=CARTESIAN_POINT('Ctrl Pts',(31.0619486284351,-0.525431380274417,
25.0877429880603));
#49857=CARTESIAN_POINT('Ctrl Pts',(31.162019301378,-0.235334014571736,25.1083130594786));
#49858=CARTESIAN_POINT('Ctrl Pts',(31.182987818821,-0.0787326337506094,
25.1194172678187));
#49859=CARTESIAN_POINT('Ctrl Pts',(31.162785126869,0.227544173273347,25.1411345825519));
#49860=CARTESIAN_POINT('Ctrl Pts',(31.1241144207896,0.374476178584838,25.1515531598995));
#49861=CARTESIAN_POINT('Ctrl Pts',(30.9915168317796,0.649674032406111,25.1710667445663));
#49862=CARTESIAN_POINT('Ctrl Pts',(30.8973599492461,0.774562668596496,25.1806896874262));
#49863=CARTESIAN_POINT('Ctrl Pts',(30.6662666830193,0.980382528688255,25.202177670528));
#49864=CARTESIAN_POINT('Ctrl Pts',(30.531751815152,1.05938687434591,25.2132389149495));
#49865=CARTESIAN_POINT('Ctrl Pts',(30.2450331875533,1.15903498558282,25.2343785368368));
#49866=CARTESIAN_POINT('Ctrl Pts',(30.0962908441082,1.18072042198942,25.2438927186044));
#49867=CARTESIAN_POINT('Ctrl Pts',(29.7917163095273,1.16710140491111,25.2630787773242));
#49868=CARTESIAN_POINT('Ctrl Pts',(29.638905788045,1.12920096781154,25.2738062281113));
#49869=CARTESIAN_POINT('Ctrl Pts',(29.3599222216531,0.997398530499289,25.2956108489033));
#49870=CARTESIAN_POINT('Ctrl Pts',(29.2358774116296,0.905886016991888,25.3064726127214));
#49871=CARTESIAN_POINT('Ctrl Pts',(29.0316806530828,0.682639701770527,25.32692677681));
#49872=CARTESIAN_POINT('Ctrl Pts',(28.9526524211366,0.553805209269406,25.3357310715183));
#49873=CARTESIAN_POINT('Ctrl Pts',(28.844720062577,0.266708452558536,25.3560883773325));
#49874=CARTESIAN_POINT('Ctrl Pts',(28.8194808141697,0.110295910906438,25.3671791955642));
#49875=CARTESIAN_POINT('Ctrl Pts',(28.8316382042729,-0.197210560241239,
25.3889837026743));
#49876=CARTESIAN_POINT('Ctrl Pts',(28.8665861506279,-0.345474523822663,
25.3994967258182));
#49877=CARTESIAN_POINT('Ctrl Pts',(28.9918018301732,-0.623166741842213,
25.4191871795497));
#49878=CARTESIAN_POINT('Ctrl Pts',(29.081808144475,-0.749490769071139,25.4285215559887));
#49879=CARTESIAN_POINT('Ctrl Pts',(29.3063266217772,-0.961255466999539,
25.449816563314));
#49880=CARTESIAN_POINT('Ctrl Pts',(29.438949602445,-1.04422897408056,25.4609023529488));
#49881=CARTESIAN_POINT('Ctrl Pts',(29.7169259241077,-1.14948331999011,25.4817038921344));
#49882=CARTESIAN_POINT('Ctrl Pts',(29.8579333178884,-1.17524047358086,25.4912760155257));
#49883=CARTESIAN_POINT('Ctrl Pts',(30.,-1.17524047358085,25.5));
#49884=CARTESIAN_POINT('Origin',(30.,-1.21864324187371E-14,15.78125));
#49885=CARTESIAN_POINT('',(30.,-1.17524047358085,26.0625));
#49886=CARTESIAN_POINT('',(30.,-1.17524047358085,26.));
#49887=CARTESIAN_POINT('',(30.,-1.17524047358085,15.78125));
#49888=CARTESIAN_POINT('Ctrl Pts',(29.9999999999999,-1.17524047358085,26.0625));
#49889=CARTESIAN_POINT('Ctrl Pts',(29.9384679078155,-1.17524047358085,26.0587214573544));
#49890=CARTESIAN_POINT('Ctrl Pts',(29.8769029052424,-1.17040913172972,26.054769604635));
#49891=CARTESIAN_POINT('Ctrl Pts',(29.6659154234359,-1.13693724882076,26.0406266508408));
#49892=CARTESIAN_POINT('Ctrl Pts',(29.5220177711255,-1.084323597792,26.0299248801994));
#49893=CARTESIAN_POINT('Ctrl Pts',(29.2586759114222,-0.925171378535031,
26.0081111282534));
#49894=CARTESIAN_POINT('Ctrl Pts',(29.1425757110306,-0.818746672431791,
25.9972085314777));
#49895=CARTESIAN_POINT('Ctrl Pts',(28.9627703960609,-0.572330389052239,
25.9774307272425));
#49896=CARTESIAN_POINT('Ctrl Pts',(28.8986210699436,-0.436327710221708,
25.9684388957715));
#49897=CARTESIAN_POINT('Ctrl Pts',(28.8234492804003,-0.143169608738148,
25.9476517953103));
#49898=CARTESIAN_POINT('Ctrl Pts',(28.8148292891501,0.0116076754049962,
25.936676929058));
#49899=CARTESIAN_POINT('Ctrl Pts',(28.8579269079672,0.318093458602922,25.9149447963521));
#49900=CARTESIAN_POINT('Ctrl Pts',(28.910158206845,0.466589649123026,25.9045489692953));
#49901=CARTESIAN_POINT('Ctrl Pts',(29.0662354765119,0.729159361472922,25.8856555497038));
#49902=CARTESIAN_POINT('Ctrl Pts',(29.1665620010353,0.841989757161643,25.8754944720367));
#49903=CARTESIAN_POINT('Ctrl Pts',(29.4086828051808,1.02746666351878,25.8540505472151));
#49904=CARTESIAN_POINT('Ctrl Pts',(29.5495956219979,1.09657907822105,25.84294712555));
#49905=CARTESIAN_POINT('Ctrl Pts',(29.8472420936479,1.17519666348882,25.8218820609165));
#49906=CARTESIAN_POINT('Ctrl Pts',(30.000722767755,1.18508027808238,25.8128044743545));
#49907=CARTESIAN_POINT('Ctrl Pts',(30.3019786609575,1.14582802588677,25.7929134117055));
#49908=CARTESIAN_POINT('Ctrl Pts',(30.4468987068161,1.09744171612032,25.7822987333));
#49909=CARTESIAN_POINT('Ctrl Pts',(30.7155809567247,0.94545759821414,25.7604111763944));
#49910=CARTESIAN_POINT('Ctrl Pts',(30.835612326607,0.841258259962285,25.7493460732515));
#49911=CARTESIAN_POINT('Ctrl Pts',(31.0226024258984,0.598138792258194,25.7292439525602));
#49912=CARTESIAN_POINT('Ctrl Pts',(31.0902361983429,0.463547729361891,25.7203689985712));
#49913=CARTESIAN_POINT('Ctrl Pts',(31.1725680326408,0.172449502286477,25.6997279586011));
#49914=CARTESIAN_POINT('Ctrl Pts',(31.1850367066478,0.0183235805600113,
25.6887992788123));
#49915=CARTESIAN_POINT('Ctrl Pts',(31.149849032726,-0.288650006825612,25.6670325571437));
#49916=CARTESIAN_POINT('Ctrl Pts',(31.1014848231134,-0.438439388995189,
25.6564113704209));
#49917=CARTESIAN_POINT('Ctrl Pts',(30.9523589365019,-0.704596833564904,
25.637538818338));
#49918=CARTESIAN_POINT('Ctrl Pts',(30.8552831525205,-0.819746342004528,
25.6276245442916));
#49919=CARTESIAN_POINT('Ctrl Pts',(30.6186741800399,-1.01116668038418,25.6063083713552));
#49920=CARTESIAN_POINT('Ctrl Pts',(30.4800603026513,-1.08386414646939,25.5952190187437));
#49921=CARTESIAN_POINT('Ctrl Pts',(30.2235083443405,-1.15925176820215,25.5767919868584));
#49922=CARTESIAN_POINT('Ctrl Pts',(30.1119520742388,-1.17524047358085,25.5693747164571));
#49923=CARTESIAN_POINT('Ctrl Pts',(29.9999999999995,-1.17524047358085,25.5625));
#49924=CARTESIAN_POINT('Ctrl Pts',(30.,-1.17524047358085,25.5));
#49925=CARTESIAN_POINT('Ctrl Pts',(30.0069574643761,-1.17524047358085,25.5004272417029));
#49926=CARTESIAN_POINT('Ctrl Pts',(30.01391720466,-1.17517869098561,25.5008568135879));
#49927=CARTESIAN_POINT('Ctrl Pts',(30.1767683930213,-1.17228514742378,25.5109597131747));
#49928=CARTESIAN_POINT('Ctrl Pts',(30.3305146751184,-1.13852257214804,25.5215979241794));
#49929=CARTESIAN_POINT('Ctrl Pts',(30.613289571589,-1.01415059475931,25.5433719241602));
#49930=CARTESIAN_POINT('Ctrl Pts',(30.7400483172667,-0.925722033283128,
25.5542910068295));
#49931=CARTESIAN_POINT('Ctrl Pts',(30.9499509146168,-0.707886564918499,
25.5749037184647));
#49932=CARTESIAN_POINT('Ctrl Pts',(31.0321249523172,-0.581569550980178,
25.5837623721801));
#49933=CARTESIAN_POINT('Ctrl Pts',(31.1477905785375,-0.297516308572578,
25.6039038700829));
#49934=CARTESIAN_POINT('Ctrl Pts',(31.1772544504942,-0.141401249469257,
25.6149735945785));
#49935=CARTESIAN_POINT('Ctrl Pts',(31.1730934439483,0.167116297568546,25.636849794526));
#49936=CARTESIAN_POINT('Ctrl Pts',(31.1418645520009,0.316603789635784,25.6474495749843));
#49937=CARTESIAN_POINT('Ctrl Pts',(31.0239238826678,0.596699382032703,25.6673104459219));
#49938=CARTESIAN_POINT('Ctrl Pts',(30.9379157361151,0.724424917792123,25.6764216802641));
#49939=CARTESIAN_POINT('Ctrl Pts',(30.7198518445296,0.941880855114492,25.6975221021999));
#49940=CARTESIAN_POINT('Ctrl Pts',(30.5891826263813,1.02868094414498,25.7086235824532));
#49941=CARTESIAN_POINT('Ctrl Pts',(30.3070725150413,1.14422525077315,25.730043785608));
#49942=CARTESIAN_POINT('Ctrl Pts',(30.1591233913896,1.1739884490527,25.7401842137377));
#49943=CARTESIAN_POINT('Ctrl Pts',(29.8537619113516,1.17646530259176,25.7590235656117));
#49944=CARTESIAN_POINT('Ctrl Pts',(29.6991872299891,1.1467452303545,25.7694824753175));
#49945=CARTESIAN_POINT('Ctrl Pts',(29.4128145699134,1.02954198968741,25.7912232470859));
#49946=CARTESIAN_POINT('Ctrl Pts',(29.2835235645903,0.944145175996724,25.8021903431407));
#49947=CARTESIAN_POINT('Ctrl Pts',(29.0681842616351,0.731537563632497,25.8229515631887));
#49948=CARTESIAN_POINT('Ctrl Pts',(28.9830068906091,0.607571894150497,25.8319186117076));
#49949=CARTESIAN_POINT('Ctrl Pts',(28.8607454143127,0.328058458525624,25.851738203379));
#49950=CARTESIAN_POINT('Ctrl Pts',(28.8273201029076,0.174145192049772,25.8626518043211));
#49951=CARTESIAN_POINT('Ctrl Pts',(28.8225473943512,-0.133454152009573,
25.8844628968148));
#49952=CARTESIAN_POINT('Ctrl Pts',(28.849586199068,-0.284195707441678,25.8951515997385));
#49953=CARTESIAN_POINT('Ctrl Pts',(28.9594336647467,-0.566901683792667,
25.9151975664084));
#49954=CARTESIAN_POINT('Ctrl Pts',(29.0410981500453,-0.696179869303813,
25.9241315793102));
#49955=CARTESIAN_POINT('Ctrl Pts',(29.2520170527073,-0.919779045076863,
25.9450110448572));
#49956=CARTESIAN_POINT('Ctrl Pts',(29.3804160320669,-1.01073211613404,25.95612035376));
#49957=CARTESIAN_POINT('Ctrl Pts',(29.6598179734432,-1.13487834137248,25.9776792246572));
#49958=CARTESIAN_POINT('Ctrl Pts',(29.8072708469184,-1.1689955596726,25.9879435454987));
#49959=CARTESIAN_POINT('Ctrl Pts',(29.9714632607541,-1.17498080122199,25.9982384188692));
#49960=CARTESIAN_POINT('Ctrl Pts',(29.9857363066776,-1.17524047358085,25.9991240997731));
#49961=CARTESIAN_POINT('Ctrl Pts',(29.9999999999999,-1.17524047358085,26.));
#49962=CARTESIAN_POINT('Origin',(30.,-1.21864324187371E-14,15.78125));
#49963=CARTESIAN_POINT('',(30.,-1.17524047358085,26.5625));
#49964=CARTESIAN_POINT('',(29.9999999999997,-1.17524047358085,26.4999999999999));
#49965=CARTESIAN_POINT('',(30.,-1.17524047358085,15.78125));
#49966=CARTESIAN_POINT('Ctrl Pts',(30.,-1.17524047358085,26.5625));
#49967=CARTESIAN_POINT('Ctrl Pts',(29.9189538385986,-1.17524047358085,26.5575231437572));
#49968=CARTESIAN_POINT('Ctrl Pts',(29.8379609361797,-1.16685998242801,26.5522524382954));
#49969=CARTESIAN_POINT('Ctrl Pts',(29.6089811727034,-1.1187361642345,26.5364851544771));
#49970=CARTESIAN_POINT('Ctrl Pts',(29.4672242547403,-1.05858684051961,26.5256476735947));
#49971=CARTESIAN_POINT('Ctrl Pts',(29.2118758464994,-0.885634166979752,
26.5038355032321));
#49972=CARTESIAN_POINT('Ctrl Pts',(29.1014575353795,-0.773390023233997,
26.4930754972477));
#49973=CARTESIAN_POINT('Ctrl Pts',(28.9347073730369,-0.518183463481665,
26.4737877314199));
#49974=CARTESIAN_POINT('Ctrl Pts',(28.8776702380248,-0.379162720284378,
26.4643854707334));
#49975=CARTESIAN_POINT('Ctrl Pts',(28.8174988609875,-0.0818619971934983,
26.4433046274383));
#49976=CARTESIAN_POINT('Ctrl Pts',(28.8169789681977,0.0739680819649894,
26.4322551101507));
#49977=CARTESIAN_POINT('Ctrl Pts',(28.8764093680924,0.378032609649621,26.4106946625572));
#49978=CARTESIAN_POINT('Ctrl Pts',(28.9362017786302,0.523138441896699,26.4009448281074));
#49979=CARTESIAN_POINT('Ctrl Pts',(29.1059813583505,0.777530022962841,26.3814999268455));
#49980=CARTESIAN_POINT('Ctrl Pts',(29.2127271628307,0.885439479708375,26.3711191218038));
#49981=CARTESIAN_POINT('Ctrl Pts',(29.4658882417733,1.05845819806925,26.3494389287095));
#49982=CARTESIAN_POINT('Ctrl Pts',(29.6112162771377,1.12003007041528,26.3383317191495));
#49983=CARTESIAN_POINT('Ctrl Pts',(29.9119535931961,1.18158358217449,26.3176818381253));
#49984=CARTESIAN_POINT('Ctrl Pts',(30.0639561135899,1.18313176493728,26.308852379607));
#49985=CARTESIAN_POINT('Ctrl Pts',(30.3618294498414,1.12846284091072,26.2886224532834));
#49986=CARTESIAN_POINT('Ctrl Pts',(30.5047372110283,1.07218329091309,26.2778514997354));
#49987=CARTESIAN_POINT('Ctrl Pts',(30.7642923496518,0.906285517829887,26.2560311264309));
#49988=CARTESIAN_POINT('Ctrl Pts',(30.8776734787023,0.796998466194141,26.2451940206555));
#49989=CARTESIAN_POINT('Ctrl Pts',(31.0511614964728,0.546283376197254,26.2256517381869));
#49990=CARTESIAN_POINT('Ctrl Pts',(31.1118599586541,0.408839660981002,26.2164897876345));
#49991=CARTESIAN_POINT('Ctrl Pts',(31.179816298086,0.113659355972694,26.1955592978295));
#49992=CARTESIAN_POINT('Ctrl Pts',(31.1845443559052,-0.0416770721755796,
26.1845447840881));
#49993=CARTESIAN_POINT('Ctrl Pts',(31.1333712501869,-0.348241759846019,
26.1628070564654));
#49994=CARTESIAN_POINT('Ctrl Pts',(31.0768319553006,-0.496185033349922,
26.1527007984472));
#49995=CARTESIAN_POINT('Ctrl Pts',(30.9126965034022,-0.755446668894444,
26.1334298283147));
#49996=CARTESIAN_POINT('Ctrl Pts',(30.8088874743598,-0.865675121928193,
26.1231471467367));
#49997=CARTESIAN_POINT('Ctrl Pts',(30.5607504336079,-1.04453090463544,26.1015685223966));
#49998=CARTESIAN_POINT('Ctrl Pts',(30.4174143875892,-1.10962145980108,26.0904588858133));
#49999=CARTESIAN_POINT('Ctrl Pts',(30.1782678600435,-1.16509155074858,26.0738068318412));
#50000=CARTESIAN_POINT('Ctrl Pts',(30.0891908090061,-1.17524047358085,26.0679770001062));
#50001=CARTESIAN_POINT('Ctrl Pts',(29.9999999999999,-1.17524047358085,26.0625));
#50002=CARTESIAN_POINT('Ctrl Pts',(29.9999999999999,-1.17524047358085,26.));
#50003=CARTESIAN_POINT('Ctrl Pts',(30.1425333221801,-1.17524047358085,26.0087526397553));
#50004=CARTESIAN_POINT('Ctrl Pts',(30.2840219111895,-1.14931710997616,26.0183602049923));
#50005=CARTESIAN_POINT('Ctrl Pts',(30.561367295123,-1.04389937746679,26.0391287924253));
#50006=CARTESIAN_POINT('Ctrl Pts',(30.6930583893841,-0.961526015756511,
26.0501360796874));
#50007=CARTESIAN_POINT('Ctrl Pts',(30.9136669465422,-0.754054974126117,
26.0710387617507));
#50008=CARTESIAN_POINT('Ctrl Pts',(31.0017654739708,-0.632326756940585,
26.0801633069178));
#50009=CARTESIAN_POINT('Ctrl Pts',(31.130809796733,-0.356072448301099,26.0997518021271));
#50010=CARTESIAN_POINT('Ctrl Pts',(31.1680189550385,-0.20305033553964,26.1106022136104));
#50011=CARTESIAN_POINT('Ctrl Pts',(31.1804056537492,0.10467710494643,26.1324223890981));
#50012=CARTESIAN_POINT('Ctrl Pts',(31.1569739806732,0.256395498849484,26.1431803571703));
#50013=CARTESIAN_POINT('Ctrl Pts',(31.0540187102742,0.541272174052999,26.1633802426127));
#50014=CARTESIAN_POINT('Ctrl Pts',(30.9759701950171,0.671873752670431,26.1722217092774));
#50015=CARTESIAN_POINT('Ctrl Pts',(30.7711018756191,0.900554058237447,26.1929097676203));
#50016=CARTESIAN_POINT('Ctrl Pts',(30.6447103916025,0.994954099829424,26.2040180088908));
#50017=CARTESIAN_POINT('Ctrl Pts',(30.3677839906361,1.12628386016982,26.2256795457743));
#50018=CARTESIAN_POINT('Ctrl Pts',(30.2208469191431,1.16405670623833,26.2360417980814));
#50019=CARTESIAN_POINT('Ctrl Pts',(29.9153739917407,1.18247957177519,26.2554533393943));
#50020=CARTESIAN_POINT('Ctrl Pts',(29.7596534858204,1.16089584886057,26.265267690896));
#50021=CARTESIAN_POINT('Ctrl Pts',(29.4669798482834,1.05871377618554,26.2868628344935));
#50022=CARTESIAN_POINT('Ctrl Pts',(29.3327683310263,0.97968769950255,26.2979062213058));
#50023=CARTESIAN_POINT('Ctrl Pts',(29.1064857982236,0.777827856716442,26.3189583910466));
#50024=CARTESIAN_POINT('Ctrl Pts',(29.0152252755147,0.658466900754918,26.3283097753497));
#50025=CARTESIAN_POINT('Ctrl Pts',(28.8789732904358,0.385760488964649,26.3476466981555));
#50026=CARTESIAN_POINT('Ctrl Pts',(28.8377485021289,0.233796400613908,26.3584220878003));
#50027=CARTESIAN_POINT('Ctrl Pts',(28.8172159011814,-0.0738574561607104,
26.3802370456529));
#50028=CARTESIAN_POINT('Ctrl Pts',(28.8367587774233,-0.226525134118623,
26.3910623250595));
#50029=CARTESIAN_POINT('Ctrl Pts',(28.9323498389723,-0.513670658612161,
26.411423088874));
#50030=CARTESIAN_POINT('Ctrl Pts',(29.0066122735479,-0.645689070611162,
26.4202237943573));
#50031=CARTESIAN_POINT('Ctrl Pts',(29.2050554476303,-0.879653705731429,
26.4407046487027));
#50032=CARTESIAN_POINT('Ctrl Pts',(29.329232754846,-0.977642983590833,26.4518041743651));
#50033=CARTESIAN_POINT('Ctrl Pts',(29.6033526154654,-1.11649688151574,26.4735601269295));
#50034=CARTESIAN_POINT('Ctrl Pts',(29.7496481694863,-1.15811817689029,26.4840194270505));
#50035=CARTESIAN_POINT('Ctrl Pts',(29.9332052808561,-1.1738184735254,26.4958478764586));
#50036=CARTESIAN_POINT('Ctrl Pts',(29.9666204732331,-1.17524047358085,26.4979502409084));
#50037=CARTESIAN_POINT('Ctrl Pts',(29.9999999999995,-1.17524047358085,26.4999999999999));
#50038=CARTESIAN_POINT('Origin',(30.,-1.21864324187371E-14,15.78125));
#50039=CARTESIAN_POINT('',(30.0000000000002,-1.17524047358085,27.0625));
#50040=CARTESIAN_POINT('',(29.9999999999999,-1.17524047358085,26.9999999999999));
#50041=CARTESIAN_POINT('',(30.,-1.17524047358085,15.78125));
#50042=CARTESIAN_POINT('Ctrl Pts',(30.0000000000003,-1.17524047358085,27.0625));
#50043=CARTESIAN_POINT('Ctrl Pts',(29.898686590649,-1.17524047358088,27.0562785792061));
#50044=CARTESIAN_POINT('Ctrl Pts',(29.7976296484377,-1.16214610940709,27.0496086633191));
#50045=CARTESIAN_POINT('Ctrl Pts',(29.5510548806291,-1.0968832857528,27.032153269422));
#50046=CARTESIAN_POINT('Ctrl Pts',(29.4119274187945,-1.02901377051944,27.0212035476842));
#50047=CARTESIAN_POINT('Ctrl Pts',(29.1656287201027,-0.842194481232163,
26.9994554755857));
#50048=CARTESIAN_POINT('Ctrl Pts',(29.0614102622354,-0.72425366568988,26.9888742198639));
#50049=CARTESIAN_POINT('Ctrl Pts',(28.9083494936521,-0.460199204673261,
26.9701133966982));
#50050=CARTESIAN_POINT('Ctrl Pts',(28.8587194637877,-0.317836463591476,
26.960036980781));
#50051=CARTESIAN_POINT('Ctrl Pts',(28.8146713989512,-0.0163533730831442,
26.9386595763769));
#50052=CARTESIAN_POINT('Ctrl Pts',(28.8228691179041,0.140138676728786,26.9275631204225));
#50053=CARTESIAN_POINT('Ctrl Pts',(28.8990556060477,0.438772825908234,26.9063877272517));
#50054=CARTESIAN_POINT('Ctrl Pts',(28.9654414239268,0.578169376458166,26.8971982372258));
#50055=CARTESIAN_POINT('Ctrl Pts',(29.1468572533747,0.822311817466142,26.8774021512523));
#50056=CARTESIAN_POINT('Ctrl Pts',(29.259591693584,0.925109502257862,26.8668348294397));
#50057=CARTESIAN_POINT('Ctrl Pts',(29.522846414638,1.08544747155122,26.8449843892055));
#50058=CARTESIAN_POINT('Ctrl Pts',(29.672078571298,1.13945389610578,26.8339056600349));
#50059=CARTESIAN_POINT('Ctrl Pts',(29.9754469871149,1.18446101454497,26.813680840772));
#50060=CARTESIAN_POINT('Ctrl Pts',(30.1261553208811,1.17798106873351,26.804850259546));
#50061=CARTESIAN_POINT('Ctrl Pts',(30.4204691708303,1.10805786050355,26.7842980916158));
#50062=CARTESIAN_POINT('Ctrl Pts',(30.5609479127602,1.04399036631935,26.7734001867649));
#50063=CARTESIAN_POINT('Ctrl Pts',(30.8118142126087,0.8639649033663,26.7516124954367));
#50064=CARTESIAN_POINT('Ctrl Pts',(30.9191345732301,0.748795351296203,26.7409390107287));
#50065=CARTESIAN_POINT('Ctrl Pts',(31.0789814493982,0.489082061456906,26.7219153792232));
#50066=CARTESIAN_POINT('Ctrl Pts',(31.13228056467,0.348399841671576,26.7122041527178));
#50067=CARTESIAN_POINT('Ctrl Pts',(31.1843745315803,0.0489678760358684,
26.6909721883974));
#50068=CARTESIAN_POINT('Ctrl Pts',(31.1805251276485,-0.10725425723734,26.6798948715428));
#50069=CARTESIAN_POINT('Ctrl Pts',(31.112642066065,-0.408638429750164,26.658524481164));
#50070=CARTESIAN_POINT('Ctrl Pts',(31.04952452927,-0.550854728541633,26.6490856679416));
#50071=CARTESIAN_POINT('Ctrl Pts',(30.8739065476105,-0.80013916056119,26.6294633115169));
#50072=CARTESIAN_POINT('Ctrl Pts',(30.7641429817239,-0.90553953226469,26.6189861492083));
#50073=CARTESIAN_POINT('Ctrl Pts',(30.5058691930861,-1.0723039712914,26.5972137340794));
#50074=CARTESIAN_POINT('Ctrl Pts',(30.3585462682162,-1.13013161506019,26.5861167698907));
#50075=CARTESIAN_POINT('Ctrl Pts',(30.1366295806596,-1.1692866034305,26.5711011916684));
#50076=CARTESIAN_POINT('Ctrl Pts',(30.0683089619122,-1.17524047358085,26.5666946944513));
#50077=CARTESIAN_POINT('Ctrl Pts',(30.,-1.17524047358085,26.5625));
#50078=CARTESIAN_POINT('Ctrl Pts',(29.9999999999995,-1.17524047358085,26.4999999999999));
#50079=CARTESIAN_POINT('Ctrl Pts',(30.1204914385722,-1.17524047358085,26.5073990989566));
#50080=CARTESIAN_POINT('Ctrl Pts',(30.2404377363977,-1.1567191282047,26.5154213729959));
#50081=CARTESIAN_POINT('Ctrl Pts',(30.503109066672,-1.07331217218126,26.5345084966475));
#50082=CARTESIAN_POINT('Ctrl Pts',(30.6398547835573,-0.997848639879795,
26.5455811972524));
#50083=CARTESIAN_POINT('Ctrl Pts',(30.8720104636609,-0.801888849767787,
26.566784844391));
#50084=CARTESIAN_POINT('Ctrl Pts',(30.9665674240944,-0.684937055709897,
26.5764328435252));
#50085=CARTESIAN_POINT('Ctrl Pts',(31.1101788342394,-0.415941539318355,
26.595506636112));
#50086=CARTESIAN_POINT('Ctrl Pts',(31.1554918067157,-0.265175979373474,
26.606197041135));
#50087=CARTESIAN_POINT('Ctrl Pts',(31.184388668241,0.0421759563922281,26.6279905905315));
#50088=CARTESIAN_POINT('Ctrl Pts',(31.1688709786064,0.195715280062819,26.6388776761339));
#50089=CARTESIAN_POINT('Ctrl Pts',(31.080842595015,0.4851372161482,26.6593998545441));
#50090=CARTESIAN_POINT('Ctrl Pts',(31.0103902901456,0.618617027917578,26.6682199013902));
#50091=CARTESIAN_POINT('Ctrl Pts',(30.8184983590075,0.857859380695496,26.6884855739597));
#50092=CARTESIAN_POINT('Ctrl Pts',(30.6966625458602,0.959431158368461,26.6995683269243));
#50093=CARTESIAN_POINT('Ctrl Pts',(30.4255868085001,1.10584185104675,26.7214052635744));
#50094=CARTESIAN_POINT('Ctrl Pts',(30.280042417997,1.15134883169079,26.7319561985547));
#50095=CARTESIAN_POINT('Ctrl Pts',(29.9776063567648,1.18496921576007,26.7517200618056));
#50096=CARTESIAN_POINT('Ctrl Pts',(29.8235440457018,1.17197554004672,26.7609515037779));
#50097=CARTESIAN_POINT('Ctrl Pts',(29.5271473201095,1.08704252411486,26.7821637300309));
#50098=CARTESIAN_POINT('Ctrl Pts',(29.3879639883513,1.01521369745337,26.7932572549969));
#50099=CARTESIAN_POINT('Ctrl Pts',(29.1499744927664,0.825212607812385,26.8146078849744));
#50100=CARTESIAN_POINT('Ctrl Pts',(29.0521140662545,0.710618013126823,26.8246118717047));
#50101=CARTESIAN_POINT('Ctrl Pts',(28.9012898027458,0.445344450507133,26.8434217499511));
#50102=CARTESIAN_POINT('Ctrl Pts',(28.8519884644377,0.295869143296566,26.8540206664119));
#50103=CARTESIAN_POINT('Ctrl Pts',(28.8148602582687,-0.0109614775297701,
26.8757772506829));
#50104=CARTESIAN_POINT('Ctrl Pts',(28.8263846212866,-0.165256365046284,
26.886717911409));
#50105=CARTESIAN_POINT('Ctrl Pts',(28.90695684434,-0.456865689279699,26.9073951919876));
#50106=CARTESIAN_POINT('Ctrl Pts',(28.9737284626765,-0.591802058760263,
26.9162939800796));
#50107=CARTESIAN_POINT('Ctrl Pts',(29.1592103949543,-0.836102522890621,
26.9363453584795));
#50108=CARTESIAN_POINT('Ctrl Pts',(29.2786778563743,-0.94110103302348,26.9474041669452));
#50109=CARTESIAN_POINT('Ctrl Pts',(29.5466042812102,-1.09478566204523,26.9693055998652));
#50110=CARTESIAN_POINT('Ctrl Pts',(29.6913217184938,-1.14405280529544,26.9799390653881));
#50111=CARTESIAN_POINT('Ctrl Pts',(29.8940937627055,-1.17166523876262,26.9933697888908));
#50112=CARTESIAN_POINT('Ctrl Pts',(29.9470693710243,-1.17524047358085,26.9967496532013));
#50113=CARTESIAN_POINT('Ctrl Pts',(29.9999999999997,-1.17524047358085,26.9999999999999));
#50114=CARTESIAN_POINT('Origin',(30.,-1.21864324187371E-14,15.78125));
#50115=CARTESIAN_POINT('',(30.0000000000002,-1.17524047358085,27.5625));
#50116=CARTESIAN_POINT('',(30.,-1.17524047358085,27.5));
#50117=CARTESIAN_POINT('',(30.,-1.17524047358085,15.78125));
#50118=CARTESIAN_POINT('Ctrl Pts',(30.0000000000004,-1.17524047358085,27.5625));
#50119=CARTESIAN_POINT('Ctrl Pts',(29.8791981655177,-1.17524047358089,27.5550818403526));
#50120=CARTESIAN_POINT('Ctrl Pts',(29.7589726578968,-1.15662316573575,27.547039018461));
#50121=CARTESIAN_POINT('Ctrl Pts',(29.4966785757901,-1.0731279551929,27.5279719317893));
#50122=CARTESIAN_POINT('Ctrl Pts',(29.3604611797136,-0.99796015863462,27.5169421590736));
#50123=CARTESIAN_POINT('Ctrl Pts',(29.1231210583237,-0.797935915977368,
27.495276047424));
#50124=CARTESIAN_POINT('Ctrl Pts',(29.0249429590029,-0.674426740918645,
27.4853218966019));
#50125=CARTESIAN_POINT('Ctrl Pts',(28.8853520572172,-0.401644540260052,
27.4659795997989));
#50126=CARTESIAN_POINT('Ctrl Pts',(28.8432060655213,-0.256055793645229,
27.4556562695324));
#50127=CARTESIAN_POINT('Ctrl Pts',(28.8154546971309,0.0488704066146756,
27.4340347229132));
#50128=CARTESIAN_POINT('Ctrl Pts',(28.8323972811925,0.205546638674019,27.4229252070608));
#50129=CARTESIAN_POINT('Ctrl Pts',(28.9250076761164,0.498408501969224,27.4021591121013));
#50130=CARTESIAN_POINT('Ctrl Pts',(28.997892508521,0.632295921050251,27.3932865033313));
#50131=CARTESIAN_POINT('Ctrl Pts',(29.1909681621961,0.865881565904131,27.3731486925495));
#50132=CARTESIAN_POINT('Ctrl Pts',(29.3095755456334,0.963111668503783,27.3624181185496));
#50133=CARTESIAN_POINT('Ctrl Pts',(29.5806971724252,1.10891198583092,27.3406000040234));
#50134=CARTESIAN_POINT('Ctrl Pts',(29.7313794614454,1.15471361111034,27.3297231163935));
#50135=CARTESIAN_POINT('Ctrl Pts',(30.0349224077729,1.1841311566887,27.3100402882342));
#50136=CARTESIAN_POINT('Ctrl Pts',(30.1845806615862,1.17018311962186,27.3009860288447));
#50137=CARTESIAN_POINT('Ctrl Pts',(30.4753054258698,1.08577187813399,27.2801406033955));
#50138=CARTESIAN_POINT('Ctrl Pts',(30.6130774728742,1.01437069747224,27.2691489037921));
#50139=CARTESIAN_POINT('Ctrl Pts',(30.8550923899249,0.82117912160722,27.2474379673869));
#50140=CARTESIAN_POINT('Ctrl Pts',(30.9563451215602,0.700625408948211,27.2371795779744));
#50141=CARTESIAN_POINT('Ctrl Pts',(31.1030012085855,0.43246305141941,27.218164862578));
#50142=CARTESIAN_POINT('Ctrl Pts',(31.1490749245368,0.288512534258167,27.207957695024));
#50143=CARTESIAN_POINT('Ctrl Pts',(31.1854037082186,-0.0146433585393976,
27.1864616764351));
#50144=CARTESIAN_POINT('Ctrl Pts',(31.173058308365,-0.171282192075426,27.1753548124176));
#50145=CARTESIAN_POINT('Ctrl Pts',(31.089040383827,-0.467218401344852,27.1543707233508));
#50146=CARTESIAN_POINT('Ctrl Pts',(31.0195638166583,-0.603975746358807,
27.1453625116794));
#50147=CARTESIAN_POINT('Ctrl Pts',(30.8326207012815,-0.843150163878356,
27.1254031429327));
#50148=CARTESIAN_POINT('Ctrl Pts',(30.7170833899544,-0.943363872050058,
27.1147553149523));
#50149=CARTESIAN_POINT('Ctrl Pts',(30.4491800434626,-1.09737775442843,27.0928436259578));
#50150=CARTESIAN_POINT('Ctrl Pts',(30.2981995637065,-1.14764798518389,27.0817899983651));
#50151=CARTESIAN_POINT('Ctrl Pts',(30.0946434783266,-1.17238533021172,27.0684130613475));
#50152=CARTESIAN_POINT('Ctrl Pts',(30.0473000417297,-1.17524047358084,27.0654045855337));
#50153=CARTESIAN_POINT('Ctrl Pts',(30.0000000000003,-1.17524047358085,27.0625));
#50154=CARTESIAN_POINT('Ctrl Pts',(29.9999999999997,-1.17524047358085,26.9999999999999));
#50155=CARTESIAN_POINT('Ctrl Pts',(30.0986058905517,-1.17524047358085,27.0060551583626));
#50156=CARTESIAN_POINT('Ctrl Pts',(30.197001235846,-1.16283641910558,27.0125371577158));
#50157=CARTESIAN_POINT('Ctrl Pts',(30.4435331990926,-1.0993899448342,27.029925526711));
#50158=CARTESIAN_POINT('Ctrl Pts',(30.5849622280491,-1.0311122983099,27.0410310521114));
#50159=CARTESIAN_POINT('Ctrl Pts',(30.8283565317534,-0.84700506573289,27.0625046195245));
#50160=CARTESIAN_POINT('Ctrl Pts',(30.9294172599309,-0.734710314399227,
27.0726917923361));
#50161=CARTESIAN_POINT('Ctrl Pts',(31.0870905034712,-0.472970868314495,
27.0916537809288));
#50162=CARTESIAN_POINT('Ctrl Pts',(31.1401926761717,-0.324772377450416,
27.1019712110874));
#50163=CARTESIAN_POINT('Ctrl Pts',(31.1850952185403,-0.0184511332937437,
27.1236916767454));
#50164=CARTESIAN_POINT('Ctrl Pts',(31.1773587357349,0.136461808282747,27.1346761621237));
#50165=CARTESIAN_POINT('Ctrl Pts',(31.1038267733963,0.430084241190232,27.1554961871532));
#50166=CARTESIAN_POINT('Ctrl Pts',(31.0404668538449,0.566412733303589,27.1645221322455));
#50167=CARTESIAN_POINT('Ctrl Pts',(30.8621032542639,0.813817787312719,27.1842464597062));
#50168=CARTESIAN_POINT('Ctrl Pts',(30.746618378735,0.920903307832853,27.195134699154));
#50169=CARTESIAN_POINT('Ctrl Pts',(30.4841269758582,1.08160589165682,27.2169511927423));
#50170=CARTESIAN_POINT('Ctrl Pts',(30.3404475283553,1.13505921838268,27.2276693335753));
#50171=CARTESIAN_POINT('Ctrl Pts',(30.0413373449537,1.18420822105003,27.2477795099651));
#50172=CARTESIAN_POINT('Ctrl Pts',(29.8888261880251,1.17970362185606,27.2566686898965));
#50173=CARTESIAN_POINT('Ctrl Pts',(29.5891419642887,1.11207867848515,27.2774691579106));
#50174=CARTESIAN_POINT('Ctrl Pts',(29.4453407649054,1.04779159085184,27.2885788725534));
#50175=CARTESIAN_POINT('Ctrl Pts',(29.1960372639306,0.870265103883027,27.3101819980009));
#50176=CARTESIAN_POINT('Ctrl Pts',(29.091548794378,0.760562756134129,27.3204877500418));
#50177=CARTESIAN_POINT('Ctrl Pts',(28.9261102653187,0.502419631695097,27.3397990837129));
#50178=CARTESIAN_POINT('Ctrl Pts',(28.8688162363146,0.355135077347701,27.3498182687336));
#50179=CARTESIAN_POINT('Ctrl Pts',(28.8157293168355,0.0491393235848099,
27.3715156546901));
#50180=CARTESIAN_POINT('Ctrl Pts',(28.8194875433144,-0.106321035237959,
27.3825389560425));
#50181=CARTESIAN_POINT('Ctrl Pts',(28.8856486083743,-0.401996025014571,
27.4035045226948));
#50182=CARTESIAN_POINT('Ctrl Pts',(28.9454972717022,-0.539801328338099,
27.4127167480926));
#50183=CARTESIAN_POINT('Ctrl Pts',(29.11742422097,-0.791565441680741,27.4322003607736));
#50184=CARTESIAN_POINT('Ctrl Pts',(29.2301245105903,-0.901546472787143,
27.4430202619491));
#50185=CARTESIAN_POINT('Ctrl Pts',(29.4887201815225,-1.06909180163981,27.4648401285834));
#50186=CARTESIAN_POINT('Ctrl Pts',(29.6313699534066,-1.1262717375032,27.4756271616522));
#50187=CARTESIAN_POINT('Ctrl Pts',(29.853348441796,-1.16837939045814,27.4907512179135));
#50188=CARTESIAN_POINT('Ctrl Pts',(29.9266702080884,-1.17524047358085,27.4954969880578));
#50189=CARTESIAN_POINT('Ctrl Pts',(30.,-1.17524047358085,27.5));
#50190=CARTESIAN_POINT('Origin',(30.,-1.21864324187371E-14,15.78125));
#50191=CARTESIAN_POINT('',(30.,-1.17524047358085,28.0625));
#50192=CARTESIAN_POINT('',(30.0000000000001,-1.17524047358085,28.));
#50193=CARTESIAN_POINT('',(30.,-1.17524047358085,15.78125));
#50194=CARTESIAN_POINT('Ctrl Pts',(30.,-1.17524047358085,28.0625));
#50195=CARTESIAN_POINT('Ctrl Pts',(29.8576309526277,-1.17524047358085,28.0537574479785));
#50196=CARTESIAN_POINT('Ctrl Pts',(29.7163289872701,-1.14937338079985,28.0441633378768));
#50197=CARTESIAN_POINT('Ctrl Pts',(29.4381412694858,-1.0437960185582,28.0233373652109));
#50198=CARTESIAN_POINT('Ctrl Pts',(29.3055725204167,-0.960712774920266,
28.0122510152415));
#50199=CARTESIAN_POINT('Ctrl Pts',(29.0812375157914,-0.748784364739409,
27.9909614703353));
#50200=CARTESIAN_POINT('Ctrl Pts',(28.991345872443,-0.622420436003701,27.9816342608879));
#50201=CARTESIAN_POINT('Ctrl Pts',(28.8663365712296,-0.344659291734443,
27.9619389197703));
#50202=CARTESIAN_POINT('Ctrl Pts',(28.8314934625426,-0.196359386622749,
27.9514233481032));
#50203=CARTESIAN_POINT('Ctrl Pts',(28.8195620391171,0.111178530712451,27.9296166112233));
#50204=CARTESIAN_POINT('Ctrl Pts',(28.8449209434754,0.267584161126331,27.9185262830501));
#50205=CARTESIAN_POINT('Ctrl Pts',(28.9530728770119,0.554595748995939,27.8981750163432));
#50206=CARTESIAN_POINT('Ctrl Pts',(29.0321899221582,0.683358417415679,27.8893700226253));
#50207=CARTESIAN_POINT('Ctrl Pts',(29.2365478324768,0.90645295573766,27.8689113436395));
#50208=CARTESIAN_POINT('Ctrl Pts',(29.3606700385593,0.997879761432882,27.8580478657718));
#50209=CARTESIAN_POINT('Ctrl Pts',(29.6397630167776,1.12947461119937,27.8362438860083));
#50210=CARTESIAN_POINT('Ctrl Pts',(29.7926014521638,1.16725893043214,27.8255188379057));
#50211=CARTESIAN_POINT('Ctrl Pts',(30.0971888483988,1.18064726325309,27.8063401680006));
#50212=CARTESIAN_POINT('Ctrl Pts',(30.2459190189188,1.15884794264961,27.7968175086224));
#50213=CARTESIAN_POINT('Ctrl Pts',(30.5325764826745,1.05897425995597,27.7756736453134));
#50214=CARTESIAN_POINT('Ctrl Pts',(30.6670400332198,0.979858412729581,27.7646115990219));
#50215=CARTESIAN_POINT('Ctrl Pts',(30.8979501916997,0.773870883397489,27.7431289156398));
#50216=CARTESIAN_POINT('Ctrl Pts',(30.9919903689524,0.648942084588862,27.7335148439956));
#50217=CARTESIAN_POINT('Ctrl Pts',(31.1243827012244,0.373674108325156,27.7139962871235));
#50218=CARTESIAN_POINT('Ctrl Pts',(31.1629506296625,0.226703861102418,27.7035749981386));
#50219=CARTESIAN_POINT('Ctrl Pts',(31.182930645767,-0.0796098768690557,
27.6818550647252));
#50220=CARTESIAN_POINT('Ctrl Pts',(31.1618436472684,-0.236207537040712,
27.6707511202069));
#50221=CARTESIAN_POINT('Ctrl Pts',(31.0615541749908,-0.526222674013738,
27.6501868794201));
#50222=CARTESIAN_POINT('Ctrl Pts',(30.9856010212307,-0.657569956578418,
27.641376820382));
#50223=CARTESIAN_POINT('Ctrl Pts',(30.7869826832863,-0.886033452367878,
27.6210802455783));
#50224=CARTESIAN_POINT('Ctrl Pts',(30.6656419827339,-0.980462303947253,
27.6102811397496));
#50225=CARTESIAN_POINT('Ctrl Pts',(30.3905261901255,-1.11936682731598,27.5884622344572));
#50226=CARTESIAN_POINT('Ctrl Pts',(30.2387339000707,-1.16125829953858,27.5776558137839));
#50227=CARTESIAN_POINT('Ctrl Pts',(30.0554488466051,-1.17426038713893,27.5659397324124));
#50228=CARTESIAN_POINT('Ctrl Pts',(30.0277113777332,-1.17524047358084,27.5642016912446));
#50229=CARTESIAN_POINT('Ctrl Pts',(30.0000000000004,-1.17524047358085,27.5625));
#50230=CARTESIAN_POINT('Ctrl Pts',(30.,-1.17524047358085,27.5));
#50231=CARTESIAN_POINT('Ctrl Pts',(30.0764884643488,-1.17524047358085,27.5046969786688));
#50232=CARTESIAN_POINT('Ctrl Pts',(30.1529528341161,-1.16777574296381,27.5096571303415));
#50233=CARTESIAN_POINT('Ctrl Pts',(30.3817494239676,-1.12246086122216,27.5253135785994));
#50234=CARTESIAN_POINT('Ctrl Pts',(30.5275514222186,-1.06175746883915,27.5364191022575));
#50235=CARTESIAN_POINT('Ctrl Pts',(30.7819194324173,-0.890185564641921,
27.5581221152238));
#50236=CARTESIAN_POINT('Ctrl Pts',(30.8893748791333,-0.782854361740771,
27.5685259964847));
#50237=CARTESIAN_POINT('Ctrl Pts',(31.0605234375151,-0.529653947481304,
27.5880127322271));
#50238=CARTESIAN_POINT('Ctrl Pts',(31.1210989339899,-0.385229961573254,
27.5976843165126));
#50239=CARTESIAN_POINT('Ctrl Pts',(31.1825194576632,-0.0817855747122669,
27.6192007914867));
#50240=CARTESIAN_POINT('Ctrl Pts',(31.1830228429167,0.0741472759213479,
27.63025759604));
#50241=CARTESIAN_POINT('Ctrl Pts',(31.1247432077576,0.371953492117145,27.6513742825742));
#50242=CARTESIAN_POINT('Ctrl Pts',(31.0685868115923,0.511361040320207,27.6608435628079));
#50243=CARTESIAN_POINT('Ctrl Pts',(30.9034614818395,0.767636822344003,27.6800694593713));
#50244=CARTESIAN_POINT('Ctrl Pts',(30.7937668420839,0.880579083554765,27.6908097772536));
#50245=CARTESIAN_POINT('Ctrl Pts',(30.5394580202052,1.05521084982092,27.712617639148));
#50246=CARTESIAN_POINT('Ctrl Pts',(30.3979930311562,1.11628678065312,27.7234700450399));
#50247=CARTESIAN_POINT('Ctrl Pts',(30.102283661711,1.18033932531086,27.7438997716137));
#50248=CARTESIAN_POINT('Ctrl Pts',(29.9510987894339,1.18375239925559,27.752701130013));
#50249=CARTESIAN_POINT('Ctrl Pts',(29.6486955420892,1.13241772430468,27.7730910160496));
#50250=CARTESIAN_POINT('Ctrl Pts',(29.5009111395855,1.07549105438516,27.7841843756164));
#50251=CARTESIAN_POINT('Ctrl Pts',(29.2414417758967,0.910237971539166,27.8059766250036));
#50252=CARTESIAN_POINT('Ctrl Pts',(29.1309679987517,0.805447516109976,27.8164757759223));
#50253=CARTESIAN_POINT('Ctrl Pts',(28.9539689931679,0.557381504423619,27.8361397402596));
#50254=CARTESIAN_POINT('Ctrl Pts',(28.8900701663349,0.415841482478183,27.8455137308899));
#50255=CARTESIAN_POINT('Ctrl Pts',(28.8202010476643,0.115104610378523,27.8668382228314));
#50256=CARTESIAN_POINT('Ctrl Pts',(28.8153164753922,-0.0411926086217122,
27.8779208638252));
#50257=CARTESIAN_POINT('Ctrl Pts',(28.8654961586475,-0.341119160610214,
27.8991878980145));
#50258=CARTESIAN_POINT('Ctrl Pts',(28.9179176762722,-0.482198917057609,
27.9089809285524));
#50259=CARTESIAN_POINT('Ctrl Pts',(29.0761417927703,-0.742958176446737,
27.9279419936907));
#50260=CARTESIAN_POINT('Ctrl Pts',(29.1827253034037,-0.858799901268264,
27.938594061191));
#50261=CARTESIAN_POINT('Ctrl Pts',(29.4325136093474,-1.04046451212148,27.9603736693398));
#50262=CARTESIAN_POINT('Ctrl Pts',(29.5726776549044,-1.10544579696665,27.9712846467122));
#50263=CARTESIAN_POINT('Ctrl Pts',(29.8127786384444,-1.16404144712018,27.9881061243607));
#50264=CARTESIAN_POINT('Ctrl Pts',(29.9063068575872,-1.17524047358087,27.9942465220726));
#50265=CARTESIAN_POINT('Ctrl Pts',(30.0000000000002,-1.17524047358085,28.));
#50266=CARTESIAN_POINT('Origin',(30.,-1.21864324187371E-14,15.78125));
#50267=CARTESIAN_POINT('',(30.,-1.17524047358085,28.5625));
#50268=CARTESIAN_POINT('',(30.0000000000002,-1.17524047358085,28.5));
#50269=CARTESIAN_POINT('',(30.,-1.17524047358085,15.78125));
#50270=CARTESIAN_POINT('Ctrl Pts',(29.9999999999999,-1.17524047358085,28.5625));
#50271=CARTESIAN_POINT('Ctrl Pts',(29.9854755687231,-1.17524047358085,28.5616080884619));
#50272=CARTESIAN_POINT('Ctrl Pts',(29.9709414772303,-1.17497122100143,28.5607060377023));
#50273=CARTESIAN_POINT('Ctrl Pts',(29.8064818821414,-1.16886648226933,28.5503905207309));
#50274=CARTESIAN_POINT('Ctrl Pts',(29.6590422242683,-1.13464684706092,28.5401233803667));
#50275=CARTESIAN_POINT('Ctrl Pts',(29.3797071247853,-1.01029888540339,28.5185614617647));
#50276=CARTESIAN_POINT('Ctrl Pts',(29.251363124374,-0.919248746833339,28.507452087585));
#50277=CARTESIAN_POINT('Ctrl Pts',(29.0406130665321,-0.695506305973089,
28.486577911123));
#50278=CARTESIAN_POINT('Ctrl Pts',(28.9590502383724,-0.56619133070644,28.4776471970656));
#50279=CARTESIAN_POINT('Ctrl Pts',(28.8493945968077,-0.283424288620792,
28.4575969003786));
#50280=CARTESIAN_POINT('Ctrl Pts',(28.8224557263032,-0.132654402250458,
28.4469061885797));
#50281=CARTESIAN_POINT('Ctrl Pts',(28.8274401393345,0.174951078681269,28.4250946609358));
#50282=CARTESIAN_POINT('Ctrl Pts',(28.8609710566448,0.328840848056597,28.4141827261138));
#50283=CARTESIAN_POINT('Ctrl Pts',(28.9834218096268,0.608264397886715,28.394369508017));
#50284=CARTESIAN_POINT('Ctrl Pts',(29.0686800279675,0.732167484395331,28.3853987862865));
#50285=CARTESIAN_POINT('Ctrl Pts',(29.2841654510491,0.944633593842617,28.3646336101487));
#50286=CARTESIAN_POINT('Ctrl Pts',(29.4135237499535,1.0299476859008,28.3536653145426));
#50287=CARTESIAN_POINT('Ctrl Pts',(29.6999884026637,1.14695518646917,28.3319258334386));
#50288=CARTESIAN_POINT('Ctrl Pts',(29.8545850153065,1.1765676391467,28.321476648926));
#50289=CARTESIAN_POINT('Ctrl Pts',(30.1599574738008,1.17387642238167,28.3026290229131));
#50290=CARTESIAN_POINT('Ctrl Pts',(30.3078958483554,1.14400535727984,28.2924854305785));
#50291=CARTESIAN_POINT('Ctrl Pts',(30.5899420117525,1.02824734362325,28.2710615776053));
#50292=CARTESIAN_POINT('Ctrl Pts',(30.7205565666579,0.941343746526345,28.2599597843468));
#50293=CARTESIAN_POINT('Ctrl Pts',(30.9384441962492,0.723734320112842,28.2388647444883));
#50294=CARTESIAN_POINT('Ctrl Pts',(31.0243441752868,0.5959705376245,28.2297587654061));
#50295=CARTESIAN_POINT('Ctrl Pts',(31.1420857275796,0.315809924237744,28.2098932839944));
#50296=CARTESIAN_POINT('Ctrl Pts',(31.1732121728651,0.166290213222924,28.1992912189719));
#50297=CARTESIAN_POINT('Ctrl Pts',(31.1771534741222,-0.14225217236566,28.1774132577855));
#50298=CARTESIAN_POINT('Ctrl Pts',(31.1475738082276,-0.298357527790664,
28.1663442213532));
#50299=CARTESIAN_POINT('Ctrl Pts',(31.0316967203975,-0.582326286717529,
28.1462087139606));
#50300=CARTESIAN_POINT('Ctrl Pts',(30.9494361151523,-0.708574806833004,
28.1373477050794));
#50301=CARTESIAN_POINT('Ctrl Pts',(30.7393766183288,-0.926260402286338,
28.1167306721673));
#50302=CARTESIAN_POINT('Ctrl Pts',(30.6125440370362,-1.01460273603848,28.1058101125197));
#50303=CARTESIAN_POINT('Ctrl Pts',(30.3296673321613,-1.13876808424026,28.0840371864985));
#50304=CARTESIAN_POINT('Ctrl Pts',(30.1758968644013,-1.17241612952657,28.0734015508245));
#50305=CARTESIAN_POINT('Ctrl Pts',(30.0133354780172,-1.17518374723503,28.0633209118452));
#50306=CARTESIAN_POINT('Ctrl Pts',(30.0066666906193,-1.17524047358085,28.0629093859629));
#50307=CARTESIAN_POINT('Ctrl Pts',(30.,-1.17524047358085,28.0625));
#50308=CARTESIAN_POINT('Ctrl Pts',(30.0000000000002,-1.17524047358085,28.));
#50309=CARTESIAN_POINT('Ctrl Pts',(30.055120011526,-1.17524047358084,28.0033847916881));
#50310=CARTESIAN_POINT('Ctrl Pts',(30.1102800819057,-1.17136342893539,28.0069094990185));
#50311=CARTESIAN_POINT('Ctrl Pts',(30.320778299587,-1.14149919825233,28.0208945034877));
#50312=CARTESIAN_POINT('Ctrl Pts',(30.4704399584402,-1.08838822567003,28.0319678602702));
#50313=CARTESIAN_POINT('Ctrl Pts',(30.7348284172129,-0.929562358310031,
28.0538343110362));
#50314=CARTESIAN_POINT('Ctrl Pts',(30.8482436418564,-0.827380507129033,
28.0644216046344));
#50315=CARTESIAN_POINT('Ctrl Pts',(31.0309964109232,-0.58443378950115,28.0842573960977));
#50316=CARTESIAN_POINT('Ctrl Pts',(31.0981318171314,-0.445680080400429,
28.0933979512832));
#50317=CARTESIAN_POINT('Ctrl Pts',(31.1762201438822,-0.147691887981632,
28.1145275412917));
#50318=CARTESIAN_POINT('Ctrl Pts',(31.1854211354334,0.00884554012676132,
28.1256272149066));
#50319=CARTESIAN_POINT('Ctrl Pts',(31.1432517249665,0.310649796547867,28.1470273923742));
#50320=CARTESIAN_POINT('Ctrl Pts',(31.0945166442476,0.453415390384783,28.1571505400084));
#50321=CARTESIAN_POINT('Ctrl Pts',(30.9430034157352,0.718468313966014,28.1759447732979));
#50322=CARTESIAN_POINT('Ctrl Pts',(30.8395316819024,0.837077300041102,28.1864571641064));
#50323=CARTESIAN_POINT('Ctrl Pts',(30.594175126874,1.02551549499305,28.2082047776097));
#50324=CARTESIAN_POINT('Ctrl Pts',(30.4553685567187,1.0942445153416,28.2191652668043));
#50325=CARTESIAN_POINT('Ctrl Pts',(30.1633070228503,1.17335763356101,28.2399049418951));
#50326=CARTESIAN_POINT('Ctrl Pts',(30.0132854694265,1.18458952272981,28.2488527114972));
#50327=CARTESIAN_POINT('Ctrl Pts',(29.7101813599922,1.14957783235101,28.2687069250423));
#50328=CARTESIAN_POINT('Ctrl Pts',(29.5603537745588,1.10100720474222,28.2796294987935));
#50329=CARTESIAN_POINT('Ctrl Pts',(29.2921855827035,0.950361389094781,28.3014380407736));
#50330=CARTESIAN_POINT('Ctrl Pts',(29.1755651130251,0.851181456436058,28.3121157317836));
#50331=CARTESIAN_POINT('Ctrl Pts',(28.9864685212412,0.613960284958293,28.3321380906356));
#50332=CARTESIAN_POINT('Ctrl Pts',(28.9157930252681,0.478217809624506,28.341090783094));
#50333=CARTESIAN_POINT('Ctrl Pts',(28.8287462552022,0.18335177826131,28.3619989885486));
#50334=CARTESIAN_POINT('Ctrl Pts',(28.8147855892159,0.0266848358587583,
28.3731078456949));
#50335=CARTESIAN_POINT('Ctrl Pts',(28.8481057813277,-0.277120858900621,
28.3946499400995));
#50336=CARTESIAN_POINT('Ctrl Pts',(28.8928044130046,-0.421659697790202,
28.4048988240612));
#50337=CARTESIAN_POINT('Ctrl Pts',(29.0376019293491,-0.692609521363159,
28.4241111916336));
#50338=CARTESIAN_POINT('Ctrl Pts',(29.1388311172626,-0.815074867447836,
28.4343484054768));
#50339=CARTESIAN_POINT('Ctrl Pts',(29.3808301647318,-1.01067727789171,28.456143840463));
#50340=CARTESIAN_POINT('Ctrl Pts',(29.5182554521743,-1.08294295653866,28.4671448960526));
#50341=CARTESIAN_POINT('Ctrl Pts',(29.7744135979937,-1.15894806924162,28.4855696371912));
#50342=CARTESIAN_POINT('Ctrl Pts',(29.8869899356779,-1.1752404735809,28.493060314833));
#50343=CARTESIAN_POINT('Ctrl Pts',(30.0000000000005,-1.17524047358085,28.5));
#50344=CARTESIAN_POINT('Origin',(30.,-1.21864324187371E-14,15.78125));
#50345=CARTESIAN_POINT('',(29.9999999999997,-1.17524047358085,29.0625));
#50346=CARTESIAN_POINT('',(30.,-1.17524047358085,29.));
#50347=CARTESIAN_POINT('',(30.,-1.17524047358085,15.78125));
#50348=CARTESIAN_POINT('Ctrl Pts',(29.9999999999995,-1.17524047358085,29.0625));
#50349=CARTESIAN_POINT('Ctrl Pts',(29.9663313283337,-1.17524047358085,29.0604324851927));
#50350=CARTESIAN_POINT('Ctrl Pts',(29.9326266255446,-1.17379373293774,29.0583114654359));
#50351=CARTESIAN_POINT('Ctrl Pts',(29.7487805300534,-1.15793171143038,29.046459536434));
#50352=CARTESIAN_POINT('Ctrl Pts',(29.6025054140808,-1.11619705168394,29.0359974721754));
#50353=CARTESIAN_POINT('Ctrl Pts',(29.3284713606868,-0.977122112422326,
29.0142389520917));
#50354=CARTESIAN_POINT('Ctrl Pts',(29.204360853848,-0.879027723836093,29.003139801917));
#50355=CARTESIAN_POINT('Ctrl Pts',(29.0061078341151,-0.644908297203287,
28.9826651365702));
#50356=CARTESIAN_POINT('Ctrl Pts',(28.9319567448549,-0.512847810431858,
28.9738647427883));
#50357=CARTESIAN_POINT('Ctrl Pts',(28.8365844224207,-0.225635628236165,
28.9534992524445));
#50358=CARTESIAN_POINT('Ctrl Pts',(28.8171575566038,-0.0729412609821712,
28.9426720805673));
#50359=CARTESIAN_POINT('Ctrl Pts',(28.8379321785986,0.234707082052963,28.92085751368));
#50360=CARTESIAN_POINT('Ctrl Pts',(28.8792757590782,0.386638085776581,28.9100844699825));
#50361=CARTESIAN_POINT('Ctrl Pts',(29.0157412244589,0.659238101106546,28.8907550914809));
#50362=CARTESIAN_POINT('Ctrl Pts',(29.107096372761,0.778529076561771,28.8813960362208));
#50363=CARTESIAN_POINT('Ctrl Pts',(29.3335481377689,0.980220242371224,28.8603394545531));
#50364=CARTESIAN_POINT('Ctrl Pts',(29.4678337645529,1.05914504636678,28.8492951073424));
#50365=CARTESIAN_POINT('Ctrl Pts',(29.760564366148,1.1610786562004,28.8277052746509));
#50366=CARTESIAN_POINT('Ctrl Pts',(29.9162604257863,1.18253750642917,28.8179009595418));
#50367=CARTESIAN_POINT('Ctrl Pts',(30.2216914945448,1.16389753053477,28.7984842912973));
#50368=CARTESIAN_POINT('Ctrl Pts',(30.3686116386073,1.12601470107769,28.7881191791422));
#50369=CARTESIAN_POINT('Ctrl Pts',(30.645460693513,0.994469364755083,28.7664547489262));
#50370=CARTESIAN_POINT('Ctrl Pts',(30.7717903384927,0.899966183411579,28.7553466483575));
#50371=CARTESIAN_POINT('Ctrl Pts',(30.9764758301347,0.671134004376585,28.7346644325598));
#50372=CARTESIAN_POINT('Ctrl Pts',(31.0544159221586,0.540492245543279,28.7258249398524));
#50373=CARTESIAN_POINT('Ctrl Pts',(31.1571623293156,0.255550540096121,28.7056204432797));
#50374=CARTESIAN_POINT('Ctrl Pts',(31.1804841833933,0.103803871660056,28.6948604703318));
#50375=CARTESIAN_POINT('Ctrl Pts',(31.1678665590545,-0.203924479708025,
28.6730402302557));
#50376=CARTESIAN_POINT('Ctrl Pts',(31.130543099267,-0.356918086122505,28.6621918400855));
#50377=CARTESIAN_POINT('Ctrl Pts',(31.0012937995436,-0.633072694293491,
28.6426104143845));
#50378=CARTESIAN_POINT('Ctrl Pts',(30.9131062008608,-0.754733454165662,
28.6334802730101));
#50379=CARTESIAN_POINT('Ctrl Pts',(30.6923373486102,-0.962047131628042,
28.6125733267459));
#50380=CARTESIAN_POINT('Ctrl Pts',(30.5605741188135,-1.04432722358406,28.6015649165697));
#50381=CARTESIAN_POINT('Ctrl Pts',(30.2834202387706,-1.14942800624881,28.5808193260016));
#50382=CARTESIAN_POINT('Ctrl Pts',(30.1422284632676,-1.17524047358085,28.5712339190787));
#50383=CARTESIAN_POINT('Ctrl Pts',(29.9999999999999,-1.17524047358085,28.5625));
#50384=CARTESIAN_POINT('Ctrl Pts',(30.0000000000005,-1.17524047358085,28.5));
#50385=CARTESIAN_POINT('Ctrl Pts',(30.0354745744302,-1.17524047358084,28.5021784110951));
#50386=CARTESIAN_POINT('Ctrl Pts',(30.070984899228,-1.17363438892678,28.50441595924));
#50387=CARTESIAN_POINT('Ctrl Pts',(30.2617617366305,-1.15628719000694,28.5167461440698));
#50388=CARTESIAN_POINT('Ctrl Pts',(30.4127085422869,-1.11138228847866,28.527607482843));
#50389=CARTESIAN_POINT('Ctrl Pts',(30.6847642885538,-0.967157900388871,
28.5494270868925));
#50390=CARTESIAN_POINT('Ctrl Pts',(30.804005950619,-0.870565283253422,28.5601740092255));
#50391=CARTESIAN_POINT('Ctrl Pts',(30.9983603111577,-0.638155310621775,
28.5803486604476));
#50392=CARTESIAN_POINT('Ctrl Pts',(31.0719538047089,-0.504858427298666,
28.5892017641887));
#50393=CARTESIAN_POINT('Ctrl Pts',(31.1663430846515,-0.212647773407092,
28.6099216835343));
#50394=CARTESIAN_POINT('Ctrl Pts',(31.1842429187448,-0.0559802512603478,
28.6210305817888));
#50395=CARTESIAN_POINT('Ctrl Pts',(31.1582832767207,0.249283949423046,28.6426760951642));
#50396=CARTESIAN_POINT('Ctrl Pts',(31.1169606007789,0.395199803964739,28.6530226198275));
#50397=CARTESIAN_POINT('Ctrl Pts',(30.9790360194058,0.668562290541804,28.6724060632391));
#50398=CARTESIAN_POINT('Ctrl Pts',(30.8818240300007,0.792402281745908,28.6822761930404));
#50399=CARTESIAN_POINT('Ctrl Pts',(30.6459736712074,0.993822232743541,28.7039003049109));
#50400=CARTESIAN_POINT('Ctrl Pts',(30.5101537410361,1.06991069848525,28.7149383113331));
#50401=CARTESIAN_POINT('Ctrl Pts',(30.2218612846042,1.16368326752433,28.7359662684601));
#50402=CARTESIAN_POINT('Ctrl Pts',(30.0727878905027,1.18239624374933,28.7452765661691));
#50403=CARTESIAN_POINT('Ctrl Pts',(29.7685724316717,1.16273575029291,28.764654767797));
#50404=CARTESIAN_POINT('Ctrl Pts',(29.6165255150965,1.12180125661046,28.7754428960271));
#50405=CARTESIAN_POINT('Ctrl Pts',(29.3404632117996,0.984593855919108,28.797259754998));
#50406=CARTESIAN_POINT('Ctrl Pts',(29.2184662863885,0.890859052794272,28.8080745514575));
#50407=CARTESIAN_POINT('Ctrl Pts',(29.0185031029016,0.663646825495766,28.8284093479536));
#50408=CARTESIAN_POINT('Ctrl Pts',(28.9418083423014,0.532910081337728,28.8372126922591));
#50409=CARTESIAN_POINT('Ctrl Pts',(28.8396688119263,0.243593095049782,28.8577274289443));
#50410=CARTESIAN_POINT('Ctrl Pts',(28.8175791014781,0.0870303940346913,
28.8688288945971));
#50411=CARTESIAN_POINT('Ctrl Pts',(28.8356734059559,-0.219589451967425,
28.8905705333577));
#50412=CARTESIAN_POINT('Ctrl Pts',(28.8733703746263,-0.366880393585839,
28.9010145619721));
#50413=CARTESIAN_POINT('Ctrl Pts',(29.0040267448551,-0.642739671975603,
28.9205750465844));
#50414=CARTESIAN_POINT('Ctrl Pts',(29.0970828699605,-0.768007510288218,
28.9301160290222));
#50415=CARTESIAN_POINT('Ctrl Pts',(29.3264450160403,-0.975407631545752,
28.9515537342264));
#50416=CARTESIAN_POINT('Ctrl Pts',(29.4604715589085,-1.05546393671967,28.9626222876417));
#50417=CARTESIAN_POINT('Ctrl Pts',(29.7327334190531,-1.15230702146743,28.9827747043974));
#50418=CARTESIAN_POINT('Ctrl Pts',(29.8659356312532,-1.17524047358086,28.9917674189746));
#50419=CARTESIAN_POINT('Ctrl Pts',(30.0000000000001,-1.17524047358085,29.));
#50420=CARTESIAN_POINT('Origin',(30.,-1.21864324187371E-14,15.78125));
#50421=CARTESIAN_POINT('',(29.9999999999999,-1.17524047358085,29.5625));
#50422=CARTESIAN_POINT('',(30.,-1.17524047358085,29.5));
#50423=CARTESIAN_POINT('',(30.,-1.17524047358085,15.78125));
#50424=CARTESIAN_POINT('Ctrl Pts',(29.9999999999998,-1.17524047358085,29.5625));
#50425=CARTESIAN_POINT('Ctrl Pts',(29.9467973546619,-1.17524047358085,29.5592329493093));
#50426=CARTESIAN_POINT('Ctrl Pts',(29.8935499193759,-1.17162840400865,29.5558350868076));
#50427=CARTESIAN_POINT('Ctrl Pts',(29.6905156464705,-1.14383638937277,29.5423818936273));
#50428=CARTESIAN_POINT('Ctrl Pts',(29.5458229652857,-1.09446322181842,29.531746189361));
#50429=CARTESIAN_POINT('Ctrl Pts',(29.2779882672223,-0.940574047774209,
29.5098431372833));
#50430=CARTESIAN_POINT('Ctrl Pts',(29.1585890601641,-0.835479489994527,
29.4987851149112));
#50431=CARTESIAN_POINT('Ctrl Pts',(28.9732889450876,-0.591037021395749,
29.4787398668936));
#50432=CARTESIAN_POINT('Ctrl Pts',(28.9066211123554,-0.456058910232785,
29.4698379853235));
#50433=CARTESIAN_POINT('Ctrl Pts',(28.8262612459225,-0.164388119091858,
29.4491563462818));
#50434=CARTESIAN_POINT('Ctrl Pts',(28.8148509180816,-0.0100732314283097,
29.4382142673958));
#50435=CARTESIAN_POINT('Ctrl Pts',(28.852213214805,0.296739305134607,29.4164589654342));
#50436=CARTESIAN_POINT('Ctrl Pts',(28.9016274703356,0.446176311860775,29.405862764764));
#50437=CARTESIAN_POINT('Ctrl Pts',(29.0526565417776,0.711342976877612,29.3870604663565));
#50438=CARTESIAN_POINT('Ctrl Pts',(29.1506118786123,0.825870653466757,29.3770454144149));
#50439=CARTESIAN_POINT('Ctrl Pts',(29.3887681357508,1.01569990993121,29.3556906361267));
#50440=CARTESIAN_POINT('Ctrl Pts',(29.5280199399709,1.08742345397384,29.3445966390884));
#50441=CARTESIAN_POINT('Ctrl Pts',(29.8244665773462,1.17210985589585,29.3233900912571));
#50442=CARTESIAN_POINT('Ctrl Pts',(29.9785058773413,1.18498177307898,29.3141652695437));
#50443=CARTESIAN_POINT('Ctrl Pts',(30.2808965556073,1.15114217787766,29.2943964213012));
#50444=CARTESIAN_POINT('Ctrl Pts',(30.4264177470889,1.1055232193301,29.2838429408837));
#50445=CARTESIAN_POINT('Ctrl Pts',(30.697402601783,0.95889535591386,29.2620038856125));
#50446=CARTESIAN_POINT('Ctrl Pts',(30.819169348162,0.85722095894767,29.2509217356401));
#50447=CARTESIAN_POINT('Ctrl Pts',(31.0108714255578,0.617827319896978,29.2306623578836));
#50448=CARTESIAN_POINT('Ctrl Pts',(31.0812140757987,0.48430476852144,29.221840827786));
#50449=CARTESIAN_POINT('Ctrl Pts',(31.1690224491511,0.194817477900372,29.2013140152506));
#50450=CARTESIAN_POINT('Ctrl Pts',(31.1844226308274,0.0412543787619307,
29.1904252437899));
#50451=CARTESIAN_POINT('Ctrl Pts',(31.1552826086302,-0.266085347349785,
29.1686325601491));
#50452=CARTESIAN_POINT('Ctrl Pts',(31.1098513200658,-0.416814367038074,
29.1579447461033));
#50453=CARTESIAN_POINT('Ctrl Pts',(30.9660264712179,-0.685700945491834,
29.1388786780306));
#50454=CARTESIAN_POINT('Ctrl Pts',(30.8713728192914,-0.802582950873403,
29.1292210796557));
#50455=CARTESIAN_POINT('Ctrl Pts',(30.6390456070483,-0.99836896334456,29.1080130601942));
#50456=CARTESIAN_POINT('Ctrl Pts',(30.5022270643229,-1.07372697770931,29.0969396285291));
#50457=CARTESIAN_POINT('Ctrl Pts',(30.2397868247199,-1.15682002769535,29.0778778247601));
#50458=CARTESIAN_POINT('Ctrl Pts',(30.1201628836901,-1.17524047358085,29.0698789231656));
#50459=CARTESIAN_POINT('Ctrl Pts',(29.9999999999995,-1.17524047358085,29.0625));
#50460=CARTESIAN_POINT('Ctrl Pts',(30.0000000000001,-1.17524047358085,29.));
#50461=CARTESIAN_POINT('Ctrl Pts',(30.0146960045521,-1.17524047358085,29.0009024474538));
#50462=CARTESIAN_POINT('Ctrl Pts',(30.0294011894743,-1.17496482224357,29.0018152315228));
#50463=CARTESIAN_POINT('Ctrl Pts',(30.199932441124,-1.16856010735523,29.0125142300756));
#50464=CARTESIAN_POINT('Ctrl Pts',(30.353002562887,-1.13175546267305,29.0232187723758));
#50465=CARTESIAN_POINT('Ctrl Pts',(30.6330116689674,-1.00191414666784,29.0450168400954));
#50466=CARTESIAN_POINT('Ctrl Pts',(30.7577840016447,-0.911212372347243,
29.0558945356534));
#50467=CARTESIAN_POINT('Ctrl Pts',(30.9634990803743,-0.689398439003151,
29.0763911529622));
#50468=CARTESIAN_POINT('Ctrl Pts',(31.0433641152287,-0.561238966842274,
29.0852039625465));
#50469=CARTESIAN_POINT('Ctrl Pts',(31.1533625468904,-0.274946500315461,
29.1055042381753));
#50470=CARTESIAN_POINT('Ctrl Pts',(31.1797284184379,-0.118602529514694,
29.1165901942211));
#50471=CARTESIAN_POINT('Ctrl Pts',(31.1696998210424,0.189193535485508,29.1384152356998));
#50472=CARTESIAN_POINT('Ctrl Pts',(31.1357401287962,0.337792934955289,29.1489520437553));
#50473=CARTESIAN_POINT('Ctrl Pts',(31.0124667812232,0.616132121424454,29.1686883723852));
#50474=CARTESIAN_POINT('Ctrl Pts',(30.9235367823029,0.742831293967475,29.1779572331897));
#50475=CARTESIAN_POINT('Ctrl Pts',(30.7007442503466,0.956131495282673,29.1992006935594));
#50476=CARTESIAN_POINT('Ctrl Pts',(30.5686344749746,1.04013508390185,29.2102914886907));
#50477=CARTESIAN_POINT('Ctrl Pts',(30.2847340927663,1.14996876391647,29.231619165161));
#50478=CARTESIAN_POINT('Ctrl Pts',(30.1365034722987,1.17678287240203,29.241562955497));
#50479=CARTESIAN_POINT('Ctrl Pts',(29.8314130542368,1.17348866622216,29.2604146402912));
#50480=CARTESIAN_POINT('Ctrl Pts',(29.6774432972388,1.14080144691636,29.271028448982));
#50481=CARTESIAN_POINT('Ctrl Pts',(29.3937190869037,1.01837161158084,29.2927918879254));
#50482=CARTESIAN_POINT('Ctrl Pts',(29.2662697773694,0.930754504522398,29.3037246074232));
#50483=CARTESIAN_POINT('Ctrl Pts',(29.0548960664095,0.714326580132712,29.3243777540292));
#50484=CARTESIAN_POINT('Ctrl Pts',(28.9719101496403,0.588650269969742,29.3332602962825));
#50485=CARTESIAN_POINT('Ctrl Pts',(28.8542643011592,0.305390771595589,29.3533455118009));
#50486=CARTESIAN_POINT('Ctrl Pts',(28.8237155837947,0.14936986715794,29.3644085600269));
#50487=CARTESIAN_POINT('Ctrl Pts',(28.8258171170069,-0.159374372506235,
29.386300834176));
#50488=CARTESIAN_POINT('Ctrl Pts',(28.8560851449643,-0.309160959864127,
29.3969218227258));
#50489=CARTESIAN_POINT('Ctrl Pts',(28.9721608102066,-0.589863983624277,
29.416825765087));
#50490=CARTESIAN_POINT('Ctrl Pts',(29.0571584178456,-0.717947603677171,
29.4258895505263));
#50491=CARTESIAN_POINT('Ctrl Pts',(29.2735722711375,-0.936836489269234,
29.4469394508198));
#50492=CARTESIAN_POINT('Ctrl Pts',(29.4037270862843,-1.02460346918986,29.4580436226767));
#50493=CARTESIAN_POINT('Ctrl Pts',(29.6852328519168,-1.14214540943397,29.4794975379443));
#50494=CARTESIAN_POINT('Ctrl Pts',(29.8330783756557,-1.1729174993834,29.4896673732243));
#50495=CARTESIAN_POINT('Ctrl Pts',(29.9885051427478,-1.17519832475183,29.4992926332218));
#50496=CARTESIAN_POINT('Ctrl Pts',(29.9942534046712,-1.17524047358085,29.4996471149485));
#50497=CARTESIAN_POINT('Ctrl Pts',(30.,-1.17524047358085,29.5));
#50498=CARTESIAN_POINT('Origin',(30.,-1.21864324187371E-14,15.78125));
#50499=CARTESIAN_POINT('',(30.,-1.17524047358085,30.0625));
#50500=CARTESIAN_POINT('',(29.9999999999998,-1.17524047358085,29.9999999999999));
#50501=CARTESIAN_POINT('',(30.,-1.17524047358085,15.78125));
#50502=CARTESIAN_POINT('Ctrl Pts',(30.,-1.17524047358085,30.0625));
#50503=CARTESIAN_POINT('Ctrl Pts',(29.9263916760993,-1.17524047358085,30.0579798840563));
#50504=CARTESIAN_POINT('Ctrl Pts',(29.8527927358329,-1.1683271801588,30.0532152422529));
#50505=CARTESIAN_POINT('Ctrl Pts',(29.6305589174408,-1.12600740432272,30.0380679862212));
#50506=CARTESIAN_POINT('Ctrl Pts',(29.4879403212856,-1.06872004039491,30.0272790588551));
#50507=CARTESIAN_POINT('Ctrl Pts',(29.229459906818,-0.900978381114361,30.0054593092048));
#50508=CARTESIAN_POINT('Ctrl Pts',(29.1168411945232,-0.790914788798306,
29.9946414903997));
#50509=CARTESIAN_POINT('Ctrl Pts',(28.9451007627829,-0.539025681180781,
29.975164899812));
#50510=CARTESIAN_POINT('Ctrl Pts',(28.885353566283,-0.401177024850609,29.9659464494622));
#50511=CARTESIAN_POINT('Ctrl Pts',(28.8194073352897,-0.10544306552401,29.944976701428));
#50512=CARTESIAN_POINT('Ctrl Pts',(28.8157651951869,0.0500317181756064,
29.9339523772439));
#50513=CARTESIAN_POINT('Ctrl Pts',(28.8690807484143,0.355959077177534,29.9122598409872));
#50514=CARTESIAN_POINT('Ctrl Pts',(28.9264649062036,0.503164977506288,29.9022508807468));
#50515=CARTESIAN_POINT('Ctrl Pts',(29.0920593097175,0.761174070029624,29.8829347271204));
#50516=CARTESIAN_POINT('Ctrl Pts',(29.1966290016669,0.870813111888444,29.8726262318314));
#50517=CARTESIAN_POINT('Ctrl Pts',(29.4460717811045,1.04817985046692,29.851020217295));
#50518=CARTESIAN_POINT('Ctrl Pts',(29.5899284156368,1.11237046788542,29.8399105187383));
#50519=CARTESIAN_POINT('Ctrl Pts',(29.8896511606184,1.17977836078127,29.8191153804746));
#50520=CARTESIAN_POINT('Ctrl Pts',(30.042143785172,1.18417711729498,29.810228885603));
#50521=CARTESIAN_POINT('Ctrl Pts',(30.3412103985985,1.13483145488925,29.7901144124214));
#50522=CARTESIAN_POINT('Ctrl Pts',(30.484863334991,1.08127741540018,29.7793943289302));
#50523=CARTESIAN_POINT('Ctrl Pts',(30.7472520600478,0.920389087318013,29.7575775552199));
#50524=CARTESIAN_POINT('Ctrl Pts',(30.8626628342488,0.813224513564577,29.7466910634298));
#50525=CARTESIAN_POINT('Ctrl Pts',(31.0408533066038,0.565701034414209,29.7269731686955));
#50526=CARTESIAN_POINT('Ctrl Pts',(31.1041185100332,0.42933329828376,29.7179429396888));
#50527=CARTESIAN_POINT('Ctrl Pts',(31.1774532864279,0.13565521801398,29.6971189688454));
#50528=CARTESIAN_POINT('Ctrl Pts',(31.185083485025,-0.0192736961984122,
29.6861333508878));
#50529=CARTESIAN_POINT('Ctrl Pts',(31.1399640096901,-0.325574493297471,
29.6644143350789));
#50530=CARTESIAN_POINT('Ctrl Pts',(31.0867572532099,-0.473736864086508,
29.654106159393));
#50531=CARTESIAN_POINT('Ctrl Pts',(30.9288924580137,-0.735375844574816,
29.6351359699395));
#50532=CARTESIAN_POINT('Ctrl Pts',(30.827743660758,-0.847605887956935,29.6249456831495));
#50533=CARTESIAN_POINT('Ctrl Pts',(30.5841967794232,-1.03154789843284,29.6034686040399));
#50534=CARTESIAN_POINT('Ctrl Pts',(30.4427060183441,-1.0997249484081,29.5923628543371));
#50535=CARTESIAN_POINT('Ctrl Pts',(30.1964052482032,-1.16291170221409,29.5749978904338));
#50536=CARTESIAN_POINT('Ctrl Pts',(30.0983061450535,-1.17524047358085,29.5685367516888));
#50537=CARTESIAN_POINT('Ctrl Pts',(29.9999999999998,-1.17524047358085,29.5625));
#50538=CARTESIAN_POINT('Ctrl Pts',(30.,-1.17524047358085,29.5));
#50539=CARTESIAN_POINT('Ctrl Pts',(30.1499565209686,-1.17524047358085,29.5092084811251));
#50540=CARTESIAN_POINT('Ctrl Pts',(30.2986551183888,-1.14654165825818,29.5193571963421));
#50541=CARTESIAN_POINT('Ctrl Pts',(30.5805418737435,-1.03331719508937,29.5406814366056));
#50542=CARTESIAN_POINT('Ctrl Pts',(30.7104602238272,-0.948696043146186,
29.5516595563353));
#50543=CARTESIAN_POINT('Ctrl Pts',(30.9271652336418,-0.73741304903825,29.5724576785973));
#50544=CARTESIAN_POINT('Ctrl Pts',(31.0130985609625,-0.614031092469691,
29.5814606062707));
#50545=CARTESIAN_POINT('Ctrl Pts',(31.1371264539894,-0.335358891062759,
29.6012205481486));
#50546=CARTESIAN_POINT('Ctrl Pts',(31.1715373282526,-0.181667965902616,
29.6121183834297));
#50547=CARTESIAN_POINT('Ctrl Pts',(31.1782875351469,0.125982959094587,29.6339331333974));
#50548=CARTESIAN_POINT('Ctrl Pts',(31.1521830035108,0.27698654047903,29.6446404159195));
#50549=CARTESIAN_POINT('Ctrl Pts',(31.0441268483734,0.560261316579686,29.6647267147429));
#50550=CARTESIAN_POINT('Ctrl Pts',(30.9634093757068,0.689883113720223,29.6736315391227));
#50551=CARTESIAN_POINT('Ctrl Pts',(30.7540662315648,0.914815989860588,29.6944615256665));
#50552=CARTESIAN_POINT('Ctrl Pts',(30.6261826944801,1.0066730037076,29.7055712306082));
#50553=CARTESIAN_POINT('Ctrl Pts',(30.3474095969538,1.1326991331979,29.7271581352984));
#50554=CARTESIAN_POINT('Ctrl Pts',(30.2000827038505,1.16777128079541,29.7374485757904));
#50555=CARTESIAN_POINT('Ctrl Pts',(29.8935937537322,1.18085135992657,29.7567330869508));
#50556=CARTESIAN_POINT('Ctrl Pts',(29.7372662628443,1.15617395643532,29.7668098469142));
#50557=CARTESIAN_POINT('Ctrl Pts',(29.4460305983855,1.04785975410839,29.7885340948419));
#50558=CARTESIAN_POINT('Ctrl Pts',(29.3136703421255,0.966357190577468,29.7995516007362));
#50559=CARTESIAN_POINT('Ctrl Pts',(29.091570241583,0.760352988788506,29.8204938700552));
#50560=CARTESIAN_POINT('Ctrl Pts',(29.0026423680915,0.639251124272773,29.8296723175212));
#50561=CARTESIAN_POINT('Ctrl Pts',(28.8716938065568,0.363925746310141,29.8491949446027));
#50562=CARTESIAN_POINT('Ctrl Pts',(28.8334229675251,0.211172023558316,29.8600263252283));
#50563=CARTESIAN_POINT('Ctrl Pts',(28.8188892259004,-0.0965571382164996,
29.8818466227683));
#50564=CARTESIAN_POINT('Ctrl Pts',(28.8412989000486,-0.248535346834791,
29.8926230136456));
#50565=CARTESIAN_POINT('Ctrl Pts',(28.942312504556,-0.5340148591211,29.9128656447428));
#50566=CARTESIAN_POINT('Ctrl Pts',(29.0193556498266,-0.664990211735325,
29.9216906330323));
#50567=CARTESIAN_POINT('Ctrl Pts',(29.2225255933627,-0.895077676800941,
29.9423242871271));
#50568=CARTESIAN_POINT('Ctrl Pts',(29.3483400060408,-0.990433515042349,
29.9534309783521));
#50569=CARTESIAN_POINT('Ctrl Pts',(29.6245422330139,-1.1237624473258,29.9751189235115));
#50570=CARTESIAN_POINT('Ctrl Pts',(29.7713190573348,-1.16255586776877,29.985507518588));
#50571=CARTESIAN_POINT('Ctrl Pts',(29.9476315409713,-1.1743662864253,29.9967531815485));
#50572=CARTESIAN_POINT('Ctrl Pts',(29.9738286104226,-1.17524047358085,29.9983928758457));
#50573=CARTESIAN_POINT('Ctrl Pts',(29.9999999999996,-1.17524047358085,29.9999999999999));
#50574=CARTESIAN_POINT('Origin',(30.,-1.21864324187371E-14,15.78125));
#50575=CARTESIAN_POINT('',(30.,-1.17524047358085,30.5625));
#50576=CARTESIAN_POINT('',(29.9999999999998,-1.17524047358085,30.4999999999999));
#50577=CARTESIAN_POINT('',(30.,-1.17524047358085,15.78125));
#50578=CARTESIAN_POINT('Ctrl Pts',(29.9999999999999,-1.17524047358085,30.5625));
#50579=CARTESIAN_POINT('Ctrl Pts',(29.87859718881,-1.17524047358085,30.555044935771));
#50580=CARTESIAN_POINT('Ctrl Pts',(29.7578462794256,-1.15643017462348,30.5469630079231));
#50581=CARTESIAN_POINT('Ctrl Pts',(29.5223698659242,-1.08113291221706,30.5298333797947));
#50582=CARTESIAN_POINT('Ctrl Pts',(29.4096002088597,-1.02391620699781,30.5208799114591));
#50583=CARTESIAN_POINT('Ctrl Pts',(29.1820826863431,-0.858187725726655,
30.5010328956616));
#50584=CARTESIAN_POINT('Ctrl Pts',(29.0755864711026,-0.74226695058618,30.4903833861391));
#50585=CARTESIAN_POINT('Ctrl Pts',(28.9175541454242,-0.481384400712606,
30.4714297273205));
#50586=CARTESIAN_POINT('Ctrl Pts',(28.8652363337421,-0.340257481842474,
30.4616267985498));
#50587=CARTESIAN_POINT('Ctrl Pts',(28.815283295232,-0.0402726424447981,
30.4403556313474));
#50588=CARTESIAN_POINT('Ctrl Pts',(28.8202904087434,0.116033016014593,30.4292723919329));
#50589=CARTESIAN_POINT('Ctrl Pts',(28.8903942350679,0.41669295482916,30.4079533551363));
#50590=CARTESIAN_POINT('Ctrl Pts',(28.9543854043788,0.558153128819785,30.3985868124474));
#50591=CARTESIAN_POINT('Ctrl Pts',(29.1315478521803,0.806074678810529,30.3789179332106));
#50592=CARTESIAN_POINT('Ctrl Pts',(29.2421055811419,0.910792536064214,30.3684162008828));
#50593=CARTESIAN_POINT('Ctrl Pts',(29.5017160718709,1.07586594659562,30.3466216552675));
#50594=CARTESIAN_POINT('Ctrl Pts',(29.6495548172672,1.13268560353193,30.3355287526402));
#50595=CARTESIAN_POINT('Ctrl Pts',(29.9519945282947,1.1837871612187,30.3151448923318));
#50596=CARTESIAN_POINT('Ctrl Pts',(30.1031613914609,1.18026105601431,30.3063430973327));
#50597=CARTESIAN_POINT('Ctrl Pts',(30.3988201345177,1.11599305235349,30.2859088407808));
#50598=CARTESIAN_POINT('Ctrl Pts',(30.5402500629299,1.05480717912897,30.2750546900124));
#50599=CARTESIAN_POINT('Ctrl Pts',(30.7944347031296,0.879976451319597,30.2532473998958));
#50600=CARTESIAN_POINT('Ctrl Pts',(30.9040431118398,0.766951615348157,30.2425094496776));
#50601=CARTESIAN_POINT('Ctrl Pts',(31.0689753458081,0.510549117592882,30.223290918131));
#50602=CARTESIAN_POINT('Ctrl Pts',(31.1250271192607,0.371095429137332,30.2138134394961));
#50603=CARTESIAN_POINT('Ctrl Pts',(31.1830815580213,0.0732292938782705,
30.1926925042524));
#50604=CARTESIAN_POINT('Ctrl Pts',(31.1824563525586,-0.0827153416037653,
30.1816348640652));
#50605=CARTESIAN_POINT('Ctrl Pts',(31.1207993480439,-0.386085590380016,
30.1601236460354));
#50606=CARTESIAN_POINT('Ctrl Pts',(31.0601308144882,-0.530428613118422,
30.1504611573687));
#50607=CARTESIAN_POINT('Ctrl Pts',(30.8888193562276,-0.783487027384905,
30.1309694527541));
#50608=CARTESIAN_POINT('Ctrl Pts',(30.7812795445953,-0.890749011015136,
30.1205628449218));
#50609=CARTESIAN_POINT('Ctrl Pts',(30.5267682373962,-1.06214794901788,30.0988571647179));
#50610=CARTESIAN_POINT('Ctrl Pts',(30.3809100882996,-1.12274761000244,30.0877518706328));
#50611=CARTESIAN_POINT('Ctrl Pts',(30.1523604876879,-1.16783357423751,30.0721187053907));
#50612=CARTESIAN_POINT('Ctrl Pts',(30.0761915030069,-1.17524047358085,30.0671787429637));
#50613=CARTESIAN_POINT('Ctrl Pts',(30.,-1.17524047358085,30.0625));
#50614=CARTESIAN_POINT('Ctrl Pts',(29.9999999999996,-1.17524047358085,29.9999999999999));
#50615=CARTESIAN_POINT('Ctrl Pts',(30.1287289986958,-1.17524047358085,30.0079049483617));
#50616=CARTESIAN_POINT('Ctrl Pts',(30.2567455299606,-1.1540988796436,30.0165156942669));
#50617=CARTESIAN_POINT('Ctrl Pts',(30.5250941977629,-1.06268366593765,30.0362353726713));
#50618=CARTESIAN_POINT('Ctrl Pts',(30.659989580509,-0.984598569323181,30.0472873928126));
#50619=CARTESIAN_POINT('Ctrl Pts',(30.8878392789542,-0.78430373476697,30.0683803131598));
#50620=CARTESIAN_POINT('Ctrl Pts',(30.9799768519055,-0.665589512740196,
30.0778047289255));
#50621=CARTESIAN_POINT('Ctrl Pts',(31.1182025022512,-0.393869611947964,
30.0970717007283));
#50622=CARTESIAN_POINT('Ctrl Pts',(31.16052513775,-0.242215229337512,30.1078251299214));
#50623=CARTESIAN_POINT('Ctrl Pts',(31.183296750852,0.0653802899747305,30.1296359512119));
#50624=CARTESIAN_POINT('Ctrl Pts',(31.1648281646971,0.218291541355271,30.1404785017947));
#50625=CARTESIAN_POINT('Ctrl Pts',(31.0712608350547,0.506051914399227,30.1608828629668));
#50626=CARTESIAN_POINT('Ctrl Pts',(30.9980258995704,0.638460005209143,30.1696826775517));
#50627=CARTESIAN_POINT('Ctrl Pts',(30.8013405043472,0.873851821952036,30.1901061897083));
#50628=CARTESIAN_POINT('Ctrl Pts',(30.6777833777517,0.972810187954768,30.2012019893176));
#50629=CARTESIAN_POINT('Ctrl Pts',(30.4044625790663,1.11370354858798,30.222981179922));
#50630=CARTESIAN_POINT('Ctrl Pts',(30.2583590845709,1.15637148267232,30.2334657933678));
#50631=CARTESIAN_POINT('Ctrl Pts',(29.9547860481489,1.18442751029054,30.2531021983901));
#50632=CARTESIAN_POINT('Ctrl Pts',(29.8001302980418,1.16832333064129,30.2625187720286));
#50633=CARTESIAN_POINT('Ctrl Pts',(29.5050358022508,1.07710916045235,30.2838737217699));
#50634=CARTESIAN_POINT('Ctrl Pts',(29.3676216445827,1.00262104003874,30.2949528877718));
#50635=CARTESIAN_POINT('Ctrl Pts',(29.133885390368,0.808265735464436,30.3161967092816));
#50636=CARTESIAN_POINT('Ctrl Pts',(29.0384365029953,0.691955856048158,30.3259351581227));
#50637=CARTESIAN_POINT('Ctrl Pts',(28.8928615291795,0.423965303949737,30.3449376912299));
#50638=CARTESIAN_POINT('Ctrl Pts',(28.8464607134353,0.273539680594875,30.3556039922081));
#50639=CARTESIAN_POINT('Ctrl Pts',(28.8153257979048,-0.0336925494769084,
30.3773890535762));
#50640=CARTESIAN_POINT('Ctrl Pts',(28.8297608924994,-0.187447360914171,
30.3882914188718));
#50641=CARTESIAN_POINT('Ctrl Pts',(28.915763813331,-0.477469105343294,30.4088561281766));
#50642=CARTESIAN_POINT('Ctrl Pts',(28.9852090680907,-0.611342914279369,
30.4176917737044));
#50643=CARTESIAN_POINT('Ctrl Pts',(29.1753547758778,-0.851973319195576,
30.4378994263954));
#50644=CARTESIAN_POINT('Ctrl Pts',(29.296552814894,-0.954486386260336,30.4489763873607));
#50645=CARTESIAN_POINT('Ctrl Pts',(29.5667870728762,-1.10289061661543,30.4708323290802));
#50646=CARTESIAN_POINT('Ctrl Pts',(29.7121150852083,-1.14942616389095,30.4814064433112));
#50647=CARTESIAN_POINT('Ctrl Pts',(29.9080894843003,-1.17254804864973,30.4942605325068));
#50648=CARTESIAN_POINT('Ctrl Pts',(29.9540678655128,-1.17524047358085,30.497179414468));
#50649=CARTESIAN_POINT('Ctrl Pts',(29.9999999999996,-1.17524047358085,30.4999999999999));
#50650=CARTESIAN_POINT('Origin',(30.,-1.21864324187371E-14,15.78125));
#50651=CARTESIAN_POINT('',(30.8234078741651,-0.838564036615812,30.5625));
#50652=CARTESIAN_POINT('Ctrl Pts',(29.9999999999996,-1.17524047358085,30.4999999999999));
#50653=CARTESIAN_POINT('Ctrl Pts',(30.1063627165445,-1.17524047358085,30.506531487003));
#50654=CARTESIAN_POINT('Ctrl Pts',(30.2124142608556,-1.16080842479057,30.5135555357051));
#50655=CARTESIAN_POINT('Ctrl Pts',(30.4106617155444,-1.10559796456395,30.5276868678729));
#50656=CARTESIAN_POINT('Ctrl Pts',(30.5022820820407,-1.06709869288998,30.5346780045058));
#50657=CARTESIAN_POINT('Ctrl Pts',(30.673678737238,-0.968061456707972,30.5487143145253));
#50658=CARTESIAN_POINT('Ctrl Pts',(30.7527765496958,-0.90791877422844,30.555703810039));
#50659=CARTESIAN_POINT('Ctrl Pts',(30.823407874166,-0.83856403661491,30.5625000000001));
#50660=CARTESIAN_POINT('Origin',(30.,-1.56558793706907E-14,30.5625000000001));
#50661=CARTESIAN_POINT('Origin',(30.,-1.32966554433622E-14,16.));
#50662=CARTESIAN_POINT('Origin',(30.,-1.32966554433622E-14,16.));
#50663=CARTESIAN_POINT('',(31.2041934952953,-0.894381364904537,16.3247595264192));
#50664=CARTESIAN_POINT('Ctrl Pts',(29.1765921258349,-0.838564036615844,
16.));
#50665=CARTESIAN_POINT('Ctrl Pts',(29.2487520159976,-0.936812680701164,
16.0195455809545));
#50666=CARTESIAN_POINT('Ctrl Pts',(29.3353435467743,-1.0235639347367,16.039234228078));
#50667=CARTESIAN_POINT('Ctrl Pts',(29.5376779891223,-1.17276771461038,16.0788670880384));
#50668=CARTESIAN_POINT('Ctrl Pts',(29.6536089107031,-1.23245734148137,16.0985110228563));
#50669=CARTESIAN_POINT('Ctrl Pts',(29.9561347058367,-1.33132329595442,16.1436679915754));
#50670=CARTESIAN_POINT('Ctrl Pts',(30.1342881765676,-1.34356937043143,16.1651272257976));
#50671=CARTESIAN_POINT('Ctrl Pts',(30.4639364648848,-1.31596498262617,16.2103767681647));
#50672=CARTESIAN_POINT('Ctrl Pts',(30.6256204275016,-1.27296147517128,16.233574208582));
#50673=CARTESIAN_POINT('Ctrl Pts',(30.9367837613818,-1.12785658919505,16.2803666131763));
#50674=CARTESIAN_POINT('Ctrl Pts',(31.0819753809162,-1.0232586553723,16.3034869854933));
#50675=CARTESIAN_POINT('Ctrl Pts',(31.2041934952953,-0.894381364904556,
16.3247595264192));
#50676=CARTESIAN_POINT('',(30.2433378840047,-1.48013062741372,16.3247595264192));
#50677=CARTESIAN_POINT('Origin',(30.,-1.32966554433622E-14,16.3247595264192));
#50678=CARTESIAN_POINT('Ctrl Pts',(30.0000000000046,1.33373412263454,16.1584936490537));
#50679=CARTESIAN_POINT('Ctrl Pts',(29.9229566197526,1.33637706265986,16.161136589079));
#50680=CARTESIAN_POINT('Ctrl Pts',(29.8544450638259,1.33215454753135,16.163603109717));
#50681=CARTESIAN_POINT('Ctrl Pts',(29.6282514683273,1.30599264999734,16.1719556820851));
#50682=CARTESIAN_POINT('Ctrl Pts',(29.4645017898244,1.25493599443995,16.1785525854589));
#50683=CARTESIAN_POINT('Ctrl Pts',(29.1556314965168,1.0904442613039,16.1921322573206));
#50684=CARTESIAN_POINT('Ctrl Pts',(29.0151927695643,0.975180135374777,16.1989814826418));
#50685=CARTESIAN_POINT('Ctrl Pts',(28.7777605589636,0.68493937081347,16.2122079855113));
#50686=CARTESIAN_POINT('Ctrl Pts',(28.6970848553023,0.520026749838233,16.218047438772));
#50687=CARTESIAN_POINT('Ctrl Pts',(28.5955913245901,0.191124499754384,16.2305887595464));
#50688=CARTESIAN_POINT('Ctrl Pts',(28.5759298114947,0.010043627653028,16.2373963058958));
#50689=CARTESIAN_POINT('Ctrl Pts',(28.6063542045486,-0.355647637044131,
16.2509482038391));
#50690=CARTESIAN_POINT('Ctrl Pts',(28.6584675525716,-0.536586390481523,
16.2575508938686));
#50691=CARTESIAN_POINT('Ctrl Pts',(28.804769485922,-0.819110586341092,16.2677424893791));
#50692=CARTESIAN_POINT('Ctrl Pts',(28.9031317119719,-0.969713974958467,
16.273653025791));
#50693=CARTESIAN_POINT('Ctrl Pts',(29.199410976174,-1.23941646392093,16.2879449223019));
#50694=CARTESIAN_POINT('Ctrl Pts',(29.3637987944395,-1.33889148571261,16.2948596529243));
#50695=CARTESIAN_POINT('Ctrl Pts',(29.6508112528307,-1.44362228182862,16.3055460935814));
#50696=CARTESIAN_POINT('Ctrl Pts',(29.7632922636866,-1.47020844863719,16.3094443635539));
#50697=CARTESIAN_POINT('Ctrl Pts',(29.9994132050485,-1.49732183809384,16.3170683877131));
#50698=CARTESIAN_POINT('Ctrl Pts',(30.1229027402064,-1.49587628373705,16.3207589898335));
#50699=CARTESIAN_POINT('Ctrl Pts',(30.2433378840021,-1.48013062741405,16.3247595264191));
#50700=CARTESIAN_POINT('Origin',(30.,-1.32966554433622E-14,16.));
#50701=CARTESIAN_POINT('Ctrl Pts',(30.0000000000002,-1.50000000000001,16.8125));
#50702=CARTESIAN_POINT('Ctrl Pts',(29.8374309170617,-1.50000000000001,16.8046783913503));
#50703=CARTESIAN_POINT('Ctrl Pts',(29.6757197620765,-1.47357729444258,16.7961640957352));
#50704=CARTESIAN_POINT('Ctrl Pts',(29.3345753610171,-1.35867108066285,16.7765589388149));
#50705=CARTESIAN_POINT('Ctrl Pts',(29.1621497524653,-1.25967607222118,16.7655132465099));
#50706=CARTESIAN_POINT('Ctrl Pts',(28.8706191056789,-1.00528518925076,16.7444205583108));
#50707=CARTESIAN_POINT('Ctrl Pts',(28.7525289442937,-0.85433413605806,16.7349630075588));
#50708=CARTESIAN_POINT('Ctrl Pts',(28.5748830688675,-0.508513347476126,
16.7157507415264));
#50709=CARTESIAN_POINT('Ctrl Pts',(28.5201083225798,-0.315342861227666,
16.705019047846));
#50710=CARTESIAN_POINT('Ctrl Pts',(28.4893812381258,0.0768796360488758,
16.6832289091084));
#50711=CARTESIAN_POINT('Ctrl Pts',(28.5120877046559,0.272040866827356,16.6723866185096));
#50712=CARTESIAN_POINT('Ctrl Pts',(28.6297398561329,0.63947572665909,16.6519735707412));
#50713=CARTESIAN_POINT('Ctrl Pts',(28.7222788636186,0.808683440996407,16.6431776245867));
#50714=CARTESIAN_POINT('Ctrl Pts',(28.9715826684579,1.11011928821307,16.6228097717056));
#50715=CARTESIAN_POINT('Ctrl Pts',(29.1285972489479,1.2371944826493,16.6117255376675));
#50716=CARTESIAN_POINT('Ctrl Pts',(29.4764211128784,1.41875808710319,16.5899474207545));
#50717=CARTESIAN_POINT('Ctrl Pts',(29.6625283053455,1.47415762233606,16.5794544583034));
#50718=CARTESIAN_POINT('Ctrl Pts',(30.0492497355351,1.51196727264003,16.5597980467542));
#50719=CARTESIAN_POINT('Ctrl Pts',(30.2463054645629,1.49258742024928,16.5504437178179));
#50720=CARTESIAN_POINT('Ctrl Pts',(30.6231564270347,1.37865583779414,16.529147701253));
#50721=CARTESIAN_POINT('Ctrl Pts',(30.7990856424485,1.28470816478719,16.5180736453463));
#50722=CARTESIAN_POINT('Ctrl Pts',(31.0988336211311,1.03864170876325,16.4968168346638));
#50723=CARTESIAN_POINT('Ctrl Pts',(31.2215556301223,0.891049402060874,16.4870027445589));
#50724=CARTESIAN_POINT('Ctrl Pts',(31.4094506590971,0.550436181771672,16.4680797878762));
#50725=CARTESIAN_POINT('Ctrl Pts',(31.4699049158396,0.359005410515039,16.4574447450286));
#50726=CARTESIAN_POINT('Ctrl Pts',(31.5122933091642,-0.0326520383467692,
16.4356859978696));
#50727=CARTESIAN_POINT('Ctrl Pts',(31.4952196858866,-0.228959953862231,
16.4247800025632));
#50728=CARTESIAN_POINT('Ctrl Pts',(31.3881172406464,-0.599526626811694,
16.4041929651771));
#50729=CARTESIAN_POINT('Ctrl Pts',(31.300844426577,-0.770779121647004,16.3953430421646));
#50730=CARTESIAN_POINT('Ctrl Pts',(31.0690211851343,-1.06871793972269,16.3759133629805));
#50731=CARTESIAN_POINT('Ctrl Pts',(30.9276174608134,-1.1935139431374,16.3656435174717));
#50732=CARTESIAN_POINT('Ctrl Pts',(30.6058972740411,-1.3849221656676,16.3448478526983));
#50733=CARTESIAN_POINT('Ctrl Pts',(30.4282952255496,-1.44972308953241,16.3345029444933));
#50734=CARTESIAN_POINT('Ctrl Pts',(30.2433378840032,-1.48013062741398,16.3247595264191));
#50735=CARTESIAN_POINT('Ctrl Pts',(31.2041934952953,-0.894381364904531,
16.3247595264192));
#50736=CARTESIAN_POINT('Ctrl Pts',(31.2978308567217,-0.768308186313297,
16.33276668881));
#50737=CARTESIAN_POINT('Ctrl Pts',(31.3710758402094,-0.628345765505124,
16.3400919019164));
#50738=CARTESIAN_POINT('Ctrl Pts',(31.4735871865681,-0.324510524004584,
16.3569716375553));
#50739=CARTESIAN_POINT('Ctrl Pts',(31.5001727925959,-0.161986730686535,
16.3660007371841));
#50740=CARTESIAN_POINT('Ctrl Pts',(31.4997859079869,0.202485940247452,16.3862492189027));
#50741=CARTESIAN_POINT('Ctrl Pts',(31.4592164909323,0.401327421311596,16.3972959678507));
#50742=CARTESIAN_POINT('Ctrl Pts',(31.3063109849155,0.761415726638002,16.4173008737022));
#50743=CARTESIAN_POINT('Ctrl Pts',(31.1993149527403,0.920789441682028,16.4262087502572));
#50744=CARTESIAN_POINT('Ctrl Pts',(30.927737201713,1.19478997630558,16.4468861668575));
#50745=CARTESIAN_POINT('Ctrl Pts',(30.7642938567671,1.30539963746525,16.4578223290454));
#50746=CARTESIAN_POINT('Ctrl Pts',(30.4012071029328,1.45894804482998,16.4795565821721));
#50747=CARTESIAN_POINT('Ctrl Pts',(30.2045613271838,1.49922584611532,16.4901365342825));
#50748=CARTESIAN_POINT('Ctrl Pts',(29.8153532439137,1.50071981302521,16.5089038160006));
#50749=CARTESIAN_POINT('Ctrl Pts',(29.6264615866043,1.46518905889,16.5189388458803));
#50750=CARTESIAN_POINT('Ctrl Pts',(29.2652001883276,1.32257698188105,16.5402814895924));
#50751=CARTESIAN_POINT('Ctrl Pts',(29.0973517156097,1.21423683760981,16.5513665514533));
#50752=CARTESIAN_POINT('Ctrl Pts',(28.8152158635768,0.940440031832944,16.5725462857904));
#50753=CARTESIAN_POINT('Ctrl Pts',(28.7029935775965,0.778399491568193,16.5817555838018));
#50754=CARTESIAN_POINT('Ctrl Pts',(28.5479560175053,0.422736814401416,16.6015146214222));
#50755=CARTESIAN_POINT('Ctrl Pts',(28.5057189580682,0.232905312381588,16.6120608159788));
#50756=CARTESIAN_POINT('Ctrl Pts',(28.4951590610144,-0.159927799856357,
16.6338848777698));
#50757=CARTESIAN_POINT('Ctrl Pts',(28.5299387266544,-0.359247208886169,
16.6449581782715));
#50758=CARTESIAN_POINT('Ctrl Pts',(28.6722713443677,-0.723556115441905,
16.665197561969));
#50759=CARTESIAN_POINT('Ctrl Pts',(28.7749427214916,-0.886360478602884,
16.6740138619457));
#50760=CARTESIAN_POINT('Ctrl Pts',(29.0386829229376,-1.16785093047933,16.6945222475229));
#50761=CARTESIAN_POINT('Ctrl Pts',(29.1984334219549,-1.28276611305493,16.7054003353954));
#50762=CARTESIAN_POINT('Ctrl Pts',(29.5564186818177,-1.44663336596446,16.7271757773774));
#50763=CARTESIAN_POINT('Ctrl Pts',(29.7518446854206,-1.49263399091841,16.7378560104973));
#50764=CARTESIAN_POINT('Ctrl Pts',(29.9670564156215,-1.49972884223086,16.7484074688974));
#50765=CARTESIAN_POINT('Ctrl Pts',(29.9835330897433,-1.50000000000001,16.7492077354109));
#50766=CARTESIAN_POINT('Ctrl Pts',(30.,-1.50000000000001,16.75));
#50767=CARTESIAN_POINT('Origin',(27.4975425688509,1.03655180724329,15.7235432561772));
#50768=CARTESIAN_POINT('',(27.507537153458,1.0459948352816,31.5905494329235));
#50769=CARTESIAN_POINT('',(27.4979325782409,1.02280733953167,31.5905494329235));
#50770=CARTESIAN_POINT('Origin',(27.4975191258909,1.03656151763528,31.5962151370756));
#50771=CARTESIAN_POINT('',(27.4979325782409,1.02280733953167,33.8969505670765));
#50772=CARTESIAN_POINT('',(27.4979325782409,1.02280733953167,15.7235432561772));
#50773=CARTESIAN_POINT('',(27.507537153458,1.0459948352816,33.8969505670765));
#50774=CARTESIAN_POINT('Origin',(27.4975191258914,1.03656151763504,33.891284862925));
#50775=CARTESIAN_POINT('',(27.507537153458,1.0459948352816,15.7235432561772));
#50776=CARTESIAN_POINT('Origin',(27.4239298924869,0.837015916807854,15.7235432561772));
#50777=CARTESIAN_POINT('',(27.4331527756843,0.847214001212616,31.5905494329235));
#50778=CARTESIAN_POINT('',(27.4253970781159,0.823344418487269,31.5905494329235));
#50779=CARTESIAN_POINT('Origin',(27.4239057599253,0.837023757952457,31.5962151370753));
#50780=CARTESIAN_POINT('',(27.4253970781159,0.823344418487269,33.8969505670765));
#50781=CARTESIAN_POINT('',(27.4253970781159,0.823344418487269,15.7235432561772));
#50782=CARTESIAN_POINT('',(27.4331527756843,0.847214001212616,33.8969505670765));
#50783=CARTESIAN_POINT('Origin',(27.4239057599256,0.837023757952334,33.8912848629251));
#50784=CARTESIAN_POINT('',(27.4331527756843,0.847214001212616,15.7235432561772));
#50785=CARTESIAN_POINT('Origin',(27.3661995449658,0.632319544909263,15.7235432561772));
#50786=CARTESIAN_POINT('',(27.3745938646118,0.643209811098917,31.5905494329235));
#50787=CARTESIAN_POINT('',(27.3687348611468,0.618805305313091,31.5905494329235));
#50788=CARTESIAN_POINT('Origin',(27.3661748715877,0.632325468463276,31.5962151370755));
#50789=CARTESIAN_POINT('',(27.3687348611468,0.618805305313091,33.8969505670765));
#50790=CARTESIAN_POINT('',(27.3687348611468,0.618805305313091,15.7235432561772));
#50791=CARTESIAN_POINT('',(27.3745938646118,0.643209811098917,33.8969505670765));
#50792=CARTESIAN_POINT('Origin',(27.3661748715881,0.632325468463155,33.891284862925));
#50793=CARTESIAN_POINT('',(27.3745938646118,0.643209811098917,15.7235432561772));
#50794=CARTESIAN_POINT('Origin',(27.3247074530776,0.423724712748722,15.7235432561772));
#50795=CARTESIAN_POINT('',(27.3322214554001,0.435240018610828,31.5905494329235));
#50796=CARTESIAN_POINT('',(27.328295268743,0.410451051658016,31.5905494329235));
#50797=CARTESIAN_POINT('Origin',(27.3246823910025,0.423728682191457,31.5962151370754));
#50798=CARTESIAN_POINT('',(27.328295268743,0.410451051658016,33.8969505670765));
#50799=CARTESIAN_POINT('',(27.328295268743,0.410451051658016,15.7235432561772));
#50800=CARTESIAN_POINT('',(27.3322214554001,0.435240018610828,33.8969505670765));
#50801=CARTESIAN_POINT('Origin',(27.3246823910029,0.423728682191396,33.891284862925));
#50802=CARTESIAN_POINT('',(27.3322214554001,0.435240018610828,15.7235432561772));
#50803=CARTESIAN_POINT('Origin',(27.2997094293662,0.212517476831317,15.7235432561772));
#50804=CARTESIAN_POINT('',(27.3062967880422,0.224586826676008,31.5905494329235));
#50805=CARTESIAN_POINT('',(27.3043276244395,0.199566230780642,31.5905494329235));
#50806=CARTESIAN_POINT('Origin',(27.2996841331102,0.212519467689854,31.5962151370755));
#50807=CARTESIAN_POINT('',(27.3043276244395,0.199566230780642,33.8969505670765));
#50808=CARTESIAN_POINT('',(27.3043276244395,0.199566230780642,15.7235432561772));
#50809=CARTESIAN_POINT('',(27.3062967880422,0.224586826676008,33.8969505670765));
#50810=CARTESIAN_POINT('Origin',(27.2996841331108,0.212519467689809,33.8912848629251));
#50811=CARTESIAN_POINT('',(27.3062967880422,0.224586826676008,15.7235432561772));
#50812=CARTESIAN_POINT('Origin',(27.2913595949605,1.54398896472578E-14,
15.7235432561772));
#50813=CARTESIAN_POINT('',(27.2969796967333,0.0125489822720319,31.5905494329235));
#50814=CARTESIAN_POINT('',(27.2969796967333,-0.0125489822720016,31.5905494329235));
#50815=CARTESIAN_POINT('Origin',(27.2913342204835,1.66533453693773E-14,
31.5962151370755));
#50816=CARTESIAN_POINT('',(27.2969796967333,-0.0125489822720016,33.8969505670765));
#50817=CARTESIAN_POINT('',(27.2969796967333,-0.0125489822720016,15.7235432561772));
#50818=CARTESIAN_POINT('',(27.2969796967333,0.0125489822720319,33.8969505670765));
#50819=CARTESIAN_POINT('Origin',(27.2913342204839,1.44047100636424E-14,
33.891284862925));
#50820=CARTESIAN_POINT('',(27.2969796967333,0.0125489822720319,15.7235432561772));
#50821=CARTESIAN_POINT('Origin',(27.5865837274296,1.22969701109861,15.7235432561772));
#50822=CARTESIAN_POINT('',(27.5972883935087,1.23832676336248,31.5905494329235));
#50823=CARTESIAN_POINT('',(27.5858941560429,1.2159643132099,31.5905494329235));
#50824=CARTESIAN_POINT('Origin',(27.586561118605,1.22970853087013,31.5962151370754));
#50825=CARTESIAN_POINT('',(27.5858941560429,1.2159643132099,33.8969505670765));
#50826=CARTESIAN_POINT('',(27.5858941560429,1.2159643132099,15.7235432561772));
#50827=CARTESIAN_POINT('',(27.5972883935087,1.23832676336248,33.8969505670765));
#50828=CARTESIAN_POINT('Origin',(27.5865611186055,1.22970853086989,33.891284862925));
#50829=CARTESIAN_POINT('',(27.5972883935087,1.23832676336248,15.7235432561772));
#50830=CARTESIAN_POINT('Origin',(27.690504399871,1.41526072396476,15.7235432561772));
#50831=CARTESIAN_POINT('',(27.701853149596,1.42302399516181,31.5905494329235));
#50832=CARTESIAN_POINT('',(27.6887394991445,1.40162446254803,31.5905494329235));
#50833=CARTESIAN_POINT('Origin',(27.6904827645727,1.41527398209261,31.5962151370755));
#50834=CARTESIAN_POINT('',(27.6887394991445,1.40162446254803,33.8969505670765));
#50835=CARTESIAN_POINT('',(27.6887394991445,1.40162446254803,15.7235432561772));
#50836=CARTESIAN_POINT('',(27.701853149596,1.42302399516181,33.8969505670765));
#50837=CARTESIAN_POINT('Origin',(27.6904827645732,1.41527398209234,33.891284862925));
#50838=CARTESIAN_POINT('',(27.701853149596,1.42302399516181,15.7235432561772));
#50839=CARTESIAN_POINT('Origin',(27.8086638806724,1.59209888384573,15.7235432561772));
#50840=CARTESIAN_POINT('',(27.8205867452275,1.59894781082746,31.5905494329235));
#50841=CARTESIAN_POINT('',(27.805834531806,1.57864313098712,31.5905494329235));
#50842=CARTESIAN_POINT('Origin',(27.8086433522893,1.59211379858911,31.5962151370755));
#50843=CARTESIAN_POINT('',(27.805834531806,1.57864313098712,33.8969505670765));
#50844=CARTESIAN_POINT('',(27.805834531806,1.57864313098712,15.7235432561772));
#50845=CARTESIAN_POINT('',(27.8205867452275,1.59894781082746,33.8969505670765));
#50846=CARTESIAN_POINT('Origin',(27.8086433522896,1.59211379858882,33.8912848629251));
#50847=CARTESIAN_POINT('',(27.8205867452275,1.59894781082746,15.7235432561772));
#50848=CARTESIAN_POINT('Origin',(27.9403336773427,1.75912122468118,15.7235432561772));
#50849=CARTESIAN_POINT('',(27.9527571483031,1.76501358153527,31.5905494329235));
#50850=CARTESIAN_POINT('',(27.9364573242129,1.74592893957157,31.5905494329235));
#50851=CARTESIAN_POINT('Origin',(27.9403143824389,1.75913770408581,31.5962151370755));
#50852=CARTESIAN_POINT('',(27.9364573242129,1.74592893957157,33.8969505670765));
#50853=CARTESIAN_POINT('',(27.9364573242129,1.74592893957157,15.7235432561772));
#50854=CARTESIAN_POINT('',(27.9527571483031,1.76501358153527,33.8969505670765));
#50855=CARTESIAN_POINT('Origin',(27.9403143824393,1.75913770408551,33.891284862925));
#50856=CARTESIAN_POINT('',(27.9527571483031,1.76501358153527,15.7235432561772));
#50857=CARTESIAN_POINT('Origin',(28.0847020018007,1.9152979981993,15.7235432561772));
#50858=CARTESIAN_POINT('',(28.0975494843367,1.92019745658633,31.5905494329235));
#50859=CARTESIAN_POINT('',(28.0798025434137,1.90245051566326,31.5905494329235));
#50860=CARTESIAN_POINT('Origin',(28.0846840593359,1.9153159406641,31.5962151370755));
#50861=CARTESIAN_POINT('',(28.0798025434137,1.90245051566326,33.8969505670765));
#50862=CARTESIAN_POINT('',(28.0798025434137,1.90245051566326,15.7235432561772));
#50863=CARTESIAN_POINT('',(28.0975494843367,1.92019745658633,33.8969505670765));
#50864=CARTESIAN_POINT('Origin',(28.0846840593363,1.91531594066375,33.891284862925));
#50865=CARTESIAN_POINT('',(28.0975494843367,1.92019745658633,15.7235432561772));
#50866=CARTESIAN_POINT('Origin',(28.2408787753188,2.05966632265731,15.7235432561772));
#50867=CARTESIAN_POINT('',(28.2540710604285,2.06354267578708,31.5905494329235));
#50868=CARTESIAN_POINT('',(28.2349864184648,2.0472428516969,31.5905494329235));
#50869=CARTESIAN_POINT('Origin',(28.2408622959143,2.05968561756092,31.5962151370754));
#50870=CARTESIAN_POINT('',(28.2349864184648,2.0472428516969,33.8969505670765));
#50871=CARTESIAN_POINT('',(28.2349864184648,2.0472428516969,15.7235432561772));
#50872=CARTESIAN_POINT('',(28.2540710604285,2.06354267578708,33.8969505670765));
#50873=CARTESIAN_POINT('Origin',(28.2408622959145,2.05968561756065,33.891284862925));
#50874=CARTESIAN_POINT('',(28.2540710604285,2.06354267578708,15.7235432561772));
#50875=CARTESIAN_POINT('Origin',(28.4079011161543,2.19133611932758,15.7235432561772));
#50876=CARTESIAN_POINT('',(28.4213568690129,2.19416546819404,31.5905494329235));
#50877=CARTESIAN_POINT('',(28.4010521891726,2.1794132547725,31.5905494329235));
#50878=CARTESIAN_POINT('Origin',(28.407886201411,2.19135664771063,31.5962151370753));
#50879=CARTESIAN_POINT('',(28.4010521891726,2.1794132547725,33.8969505670765));
#50880=CARTESIAN_POINT('',(28.4010521891726,2.1794132547725,15.7235432561772));
#50881=CARTESIAN_POINT('',(28.4213568690129,2.19416546819404,33.8969505670765));
#50882=CARTESIAN_POINT('Origin',(28.4078862014112,2.19135664771024,33.8912848629252));
#50883=CARTESIAN_POINT('',(28.4213568690129,2.19416546819404,15.7235432561772));
#50884=CARTESIAN_POINT('Origin',(28.5847392760353,2.309495600129,15.7235432561772));
#50885=CARTESIAN_POINT('',(28.598375537452,2.31126050085552,31.5905494329235));
#50886=CARTESIAN_POINT('',(28.5769760048382,2.29814685040398,31.5905494329235));
#50887=CARTESIAN_POINT('Origin',(28.5847260179075,2.30951723542729,31.5962151370754));
#50888=CARTESIAN_POINT('',(28.5769760048382,2.29814685040398,33.8969505670765));
#50889=CARTESIAN_POINT('',(28.5769760048382,2.29814685040398,15.7235432561772));
#50890=CARTESIAN_POINT('',(28.598375537452,2.31126050085552,33.8969505670765));
#50891=CARTESIAN_POINT('Origin',(28.5847260179077,2.30951723542689,33.891284862925));
#50892=CARTESIAN_POINT('',(28.598375537452,2.31126050085552,15.7235432561772));
#50893=CARTESIAN_POINT('Origin',(28.7703029889014,2.4134162725704,15.7235432561772));
#50894=CARTESIAN_POINT('',(28.7840356867901,2.41410584395713,31.5905494329235));
#50895=CARTESIAN_POINT('',(28.7616732366375,2.40271160649133,31.5905494329235));
#50896=CARTESIAN_POINT('Origin',(28.7702914691299,2.41343888139489,31.5962151370753));
#50897=CARTESIAN_POINT('',(28.7616732366375,2.40271160649133,33.8969505670765));
#50898=CARTESIAN_POINT('',(28.7616732366375,2.40271160649133,15.7235432561772));
#50899=CARTESIAN_POINT('',(28.7840356867901,2.41410584395713,33.8969505670765));
#50900=CARTESIAN_POINT('Origin',(28.7702914691301,2.41343888139455,33.8912848629251));
#50901=CARTESIAN_POINT('',(28.7840356867901,2.41410584395713,15.7235432561772));
#50902=CARTESIAN_POINT('Origin',(30.,-1.32966554433622E-14,34.));
#50903=CARTESIAN_POINT('',(28.75,0.721687836487017,33.8917468245269));
#50904=CARTESIAN_POINT('',(28.75,-1.44824191072421E-14,33.6983711515529));
#50905=CARTESIAN_POINT('Ctrl Pts',(28.75,0.72168783648698,33.8917468245269));
#50906=CARTESIAN_POINT('Ctrl Pts',(28.75,0.334936490538873,33.6983711515529));
#50907=CARTESIAN_POINT('Ctrl Pts',(28.75,-1.55145598201422E-14,33.6983711515529));
#50908=CARTESIAN_POINT('',(30.,1.44337567297405,33.8917468245269));
#50909=CARTESIAN_POINT('Ctrl Pts',(30.,1.44337567297404,33.8917468245269));
#50910=CARTESIAN_POINT('Ctrl Pts',(29.375,1.08253175473053,33.5309029062834));
#50911=CARTESIAN_POINT('Ctrl Pts',(28.75,0.721687836487025,33.8917468245269));
#50912=CARTESIAN_POINT('',(31.25,0.721687836487017,33.891746824527));
#50913=CARTESIAN_POINT('Ctrl Pts',(31.25,0.721687836487027,33.8917468245269));
#50914=CARTESIAN_POINT('Ctrl Pts',(30.625,1.08253175473053,33.5309029062834));
#50915=CARTESIAN_POINT('Ctrl Pts',(30.,1.44337567297404,33.8917468245269));
#50916=CARTESIAN_POINT('',(31.25,-0.72168783648704,33.8917468245269));
#50917=CARTESIAN_POINT('Ctrl Pts',(31.25,-0.721687836487026,33.8917468245269));
#50918=CARTESIAN_POINT('Ctrl Pts',(31.25,-1.26287869051112E-14,33.5309029062834));
#50919=CARTESIAN_POINT('Ctrl Pts',(31.25,0.721687836487001,33.8917468245269));
#50920=CARTESIAN_POINT('',(30.,-1.44337567297407,33.8917468245269));
#50921=CARTESIAN_POINT('Ctrl Pts',(30.,-1.44337567297406,33.8917468245269));
#50922=CARTESIAN_POINT('Ctrl Pts',(30.625,-1.08253175473056,33.5309029062834));
#50923=CARTESIAN_POINT('Ctrl Pts',(31.25,-0.721687836487049,33.8917468245269));
#50924=CARTESIAN_POINT('',(28.75,-0.721687836487044,33.8917468245269));
#50925=CARTESIAN_POINT('Ctrl Pts',(28.75,-0.721687836487053,33.8917468245269));
#50926=CARTESIAN_POINT('Ctrl Pts',(29.375,-1.08253175473056,33.5309029062834));
#50927=CARTESIAN_POINT('Ctrl Pts',(30.,-1.44337567297406,33.8917468245269));
#50928=CARTESIAN_POINT('Ctrl Pts',(28.75,-1.55145598201422E-14,33.6983711515529));
#50929=CARTESIAN_POINT('Ctrl Pts',(28.75,-0.334936490538901,33.6983711515529));
#50930=CARTESIAN_POINT('Ctrl Pts',(28.75,-0.721687836487005,33.8917468245269));
#50931=CARTESIAN_POINT('',(28.4483711515529,-1.34873480853811E-14,34.));
#50932=CARTESIAN_POINT('',(28.4483711515529,-1.34873480853811E-14,34.));
#50933=CARTESIAN_POINT('Origin',(30.,-1.32966554433622E-14,34.));
#50934=CARTESIAN_POINT('Origin',(30.,-1.32966554433622E-14,33.953125));
#50935=CARTESIAN_POINT('',(30.,-2.6137293696319,33.9862706303681));
#50936=CARTESIAN_POINT('Origin',(30.,-1.32966554433622E-14,33.9862706303681));
#50937=CARTESIAN_POINT('',(30.,-2.58058373926378,34.));
#50938=CARTESIAN_POINT('Origin',(30.,-2.58058373926378,33.953125));
#50939=CARTESIAN_POINT('Origin',(30.,-1.32966554433622E-14,34.));
#50940=CARTESIAN_POINT('Origin',(30.,-1.32966554433622E-14,33.8637293696319));
#50941=CARTESIAN_POINT('',(30.012548982272,-2.70302030326669,33.8969505670765));
#50942=CARTESIAN_POINT('',(30.,-2.69489040503949,33.9051095949605));
#50943=CARTESIAN_POINT('Ctrl Pts',(30.012548982272,-2.70302030326672,33.8969505670765));
#50944=CARTESIAN_POINT('Ctrl Pts',(30.0117595027242,-2.70125749446881,33.8987170220581));
#50945=CARTESIAN_POINT('Ctrl Pts',(30.0105608813139,-2.69960157002983,33.9003782103613));
#50946=CARTESIAN_POINT('Ctrl Pts',(30.0079476416933,-2.69733049287042,33.9026580100842));
#50947=CARTESIAN_POINT('Ctrl Pts',(30.0065751610721,-2.69644647069985,33.9035459832655));
#50948=CARTESIAN_POINT('Ctrl Pts',(30.0034509360646,-2.69522714758869,33.9047710768107));
#50949=CARTESIAN_POINT('Ctrl Pts',(30.0017003028408,-2.69489040503949,33.9051095949605));
#50950=CARTESIAN_POINT('Ctrl Pts',(30.,-2.69489040503949,33.9051095949605));
#50951=CARTESIAN_POINT('',(30.027378900953,-2.73613365141358,33.8637293696319));
#50952=CARTESIAN_POINT('Ctrl Pts',(30.0273789009518,-2.73613365141079,33.8637293696347));
#50953=CARTESIAN_POINT('Ctrl Pts',(30.019918653996,-2.71947585577342,33.8804609779984));
#50954=CARTESIAN_POINT('Ctrl Pts',(30.0125489822686,-2.70302030325915,33.8969505670841));
#50955=CARTESIAN_POINT('',(30.1873800711417,-2.72984718831552,33.8637293696319));
#50956=CARTESIAN_POINT('Origin',(30.,-1.32966554433622E-14,33.8637293696319));
#50957=CARTESIAN_POINT('',(30.1995662307806,-2.69567237556051,33.8969505670765));
#50958=CARTESIAN_POINT('Ctrl Pts',(30.1995662307834,-2.69567237555272,33.8969505670841));
#50959=CARTESIAN_POINT('Ctrl Pts',(30.1935103650644,-2.71265541886991,33.8804609779983));
#50960=CARTESIAN_POINT('Ctrl Pts',(30.1873800711428,-2.72984718831265,33.8637293696347));
#50961=CARTESIAN_POINT('',(30.224586826676,-2.69370321195777,33.8969505670765));
#50962=CARTESIAN_POINT('Origin',(30.2125187883694,-2.70030745889015,33.8912937927563));
#50963=CARTESIAN_POINT('',(30.241969073019,-2.72555094069392,33.8637293696319));
#50964=CARTESIAN_POINT('Ctrl Pts',(30.2419690730176,-2.72555094069121,33.8637293696347));
#50965=CARTESIAN_POINT('Ctrl Pts',(30.233224867931,-2.70952981970859,33.8804609779984));
#50966=CARTESIAN_POINT('Ctrl Pts',(30.2245868266721,-2.69370321195052,33.8969505670841));
#50967=CARTESIAN_POINT('',(30.4009837827878,-2.70673030953518,33.8637293696319));
#50968=CARTESIAN_POINT('Origin',(30.,-1.32966554433622E-14,33.8637293696319));
#50969=CARTESIAN_POINT('',(30.410451051658,-2.67170473125697,33.8969505670765));
#50970=CARTESIAN_POINT('Ctrl Pts',(30.4104510516601,-2.67170473124899,33.8969505670841));
#50971=CARTESIAN_POINT('Ctrl Pts',(30.4057463283755,-2.68911055925959,33.8804609779983));
#50972=CARTESIAN_POINT('Ctrl Pts',(30.4009837827886,-2.70673030953223,33.8637293696347));
#50973=CARTESIAN_POINT('',(30.4352400186108,-2.66777854459992,33.8969505670765));
#50974=CARTESIAN_POINT('Origin',(30.4237273077484,-2.67530902338216,33.8912940899387));
#50975=CARTESIAN_POINT('',(30.455067425287,-2.69816430208722,33.8637293696319));
#50976=CARTESIAN_POINT('Ctrl Pts',(30.4550674252854,-2.69816430208464,33.8637293696347));
#50977=CARTESIAN_POINT('Ctrl Pts',(30.445093173,-2.68287863129519,33.8804609779983));
#50978=CARTESIAN_POINT('Ctrl Pts',(30.4352400186063,-2.667778544593,33.8969505670841));
#50979=CARTESIAN_POINT('',(30.6121152960723,-2.66692553831739,33.8637293696319));
#50980=CARTESIAN_POINT('Origin',(30.,-1.32966554433622E-14,33.8637293696319));
#50981=CARTESIAN_POINT('',(30.618805305313,-2.63126513885325,33.8969505670765));
#50982=CARTESIAN_POINT('Ctrl Pts',(30.6188053053145,-2.63126513884514,33.8969505670841));
#50983=CARTESIAN_POINT('Ctrl Pts',(30.6154807306477,-2.64898643883144,33.8804609779984));
#50984=CARTESIAN_POINT('Ctrl Pts',(30.6121152960728,-2.66692553831439,33.8637293696347));
#50985=CARTESIAN_POINT('',(30.6432098110989,-2.62540613538822,33.8969505670765));
#50986=CARTESIAN_POINT('Origin',(30.6323233823986,-2.63381649164655,33.8912943077151));
#50987=CARTESIAN_POINT('',(30.6653601355529,-2.65414258332748,33.8637293696319));
#50988=CARTESIAN_POINT('Ctrl Pts',(30.665360135551,-2.65414258332505,33.8637293696347));
#50989=CARTESIAN_POINT('Ctrl Pts',(30.6542173306489,-2.63968660397218,33.8804609779983));
#50990=CARTESIAN_POINT('Ctrl Pts',(30.6432098110939,-2.62540613538168,33.8969505670841));
#50991=CARTESIAN_POINT('',(30.8194729150075,-2.61067828431314,33.8637293696319));
#50992=CARTESIAN_POINT('Origin',(30.,-1.32966554433622E-14,33.8637293696319));
#50993=CARTESIAN_POINT('',(30.8233444184872,-2.57460292188405,33.8969505670765));
#50994=CARTESIAN_POINT('Ctrl Pts',(30.8233444184881,-2.57460292187584,33.8969505670841));
#50995=CARTESIAN_POINT('Ctrl Pts',(30.8214204895475,-2.59253043613051,33.8804609779984));
#50996=CARTESIAN_POINT('Ctrl Pts',(30.8194729150079,-2.61067828431011,33.8637293696347));
#50997=CARTESIAN_POINT('',(30.8472140012126,-2.56684722431573,33.8969505670765));
#50998=CARTESIAN_POINT('Origin',(30.837020957759,-2.57608565616367,33.891294472568));
#50999=CARTESIAN_POINT('',(30.8715506793283,-2.59375719294955,33.8637293696319));
#51000=CARTESIAN_POINT('Ctrl Pts',(30.8715506793263,-2.59375719294726,33.8637293696347));
#51001=CARTESIAN_POINT('Ctrl Pts',(30.8593080209051,-2.58022003095079,33.8804609779983));
#51002=CARTESIAN_POINT('Ctrl Pts',(30.8472140012071,-2.5668472243096,33.8969505670841));
#51003=CARTESIAN_POINT('',(31.0217782109194,-2.53833533054748,33.8637293696319));
#51004=CARTESIAN_POINT('Origin',(30.,-1.32966554433622E-14,33.8637293696319));
#51005=CARTESIAN_POINT('',(31.0228073395316,-2.5020674217591,33.8969505670765));
#51006=CARTESIAN_POINT('Ctrl Pts',(31.0228073395319,-2.50206742175084,33.8969505670841));
#51007=CARTESIAN_POINT('Ctrl Pts',(31.0222959179792,-2.52009062118698,33.8804609779983));
#51008=CARTESIAN_POINT('Ctrl Pts',(31.0217782109195,-2.53833533054442,33.8637293696347));
#51009=CARTESIAN_POINT('',(31.0459948352815,-2.49246284654201,33.8969505670765));
#51010=CARTESIAN_POINT('Origin',(31.0365580110689,-2.50247243285094,33.8912946002427));
#51011=CARTESIAN_POINT('',(31.0723678233457,-2.51738042696529,33.8637293696319));
#51012=CARTESIAN_POINT('Ctrl Pts',(31.0723678233435,-2.51738042696321,33.8637293696347));
#51013=CARTESIAN_POINT('Ctrl Pts',(31.0591007914634,-2.5048455434284,33.8804609779984));
#51014=CARTESIAN_POINT('Ctrl Pts',(31.0459948352755,-2.49246284653634,33.8969505670841));
#51015=CARTESIAN_POINT('',(31.2177839043851,-2.45034269538684,33.8637293696319));
#51016=CARTESIAN_POINT('Origin',(30.,-1.32966554433622E-14,33.8637293696319));
#51017=CARTESIAN_POINT('',(31.2159643132098,-2.41410584395714,33.8969505670765));
#51018=CARTESIAN_POINT('Ctrl Pts',(31.2159643132094,-2.4141058439489,33.8969505670841));
#51019=CARTESIAN_POINT('Ctrl Pts',(31.2168685521286,-2.43211360954869,33.8804609779984));
#51020=CARTESIAN_POINT('Ctrl Pts',(31.2177839043849,-2.4503426953838,33.8637293696347));
#51021=CARTESIAN_POINT('',(31.2383267633624,-2.40271160649135,33.8969505670765));
#51022=CARTESIAN_POINT('Origin',(31.2297043338602,-2.41343066267494,33.891294700665));
#51023=CARTESIAN_POINT('',(31.2665734631337,-2.42548317353486,33.8637293696319));
#51024=CARTESIAN_POINT('Ctrl Pts',(31.2665734631313,-2.42548317353296,33.8637293696347));
#51025=CARTESIAN_POINT('Ctrl Pts',(31.2523638534557,-2.41402785018508,33.8804609779983));
#51026=CARTESIAN_POINT('Ctrl Pts',(31.238326763356,-2.40271160648617,33.8969505670841));
#51027=CARTESIAN_POINT('',(31.4062815551261,-2.34724288268751,33.8637293696319));
#51028=CARTESIAN_POINT('Origin',(30.,-1.32966554433622E-14,33.8637293696319));
#51029=CARTESIAN_POINT('',(31.401624462548,-2.31126050085554,33.8969505670765));
#51030=CARTESIAN_POINT('Ctrl Pts',(31.4016244625469,-2.31126050084735,33.8969505670841));
#51031=CARTESIAN_POINT('Ctrl Pts',(31.4039387870044,-2.32914180874765,33.8804609779983));
#51032=CARTESIAN_POINT('Ctrl Pts',(31.4062815551258,-2.34724288268448,33.8637293696347));
#51033=CARTESIAN_POINT('',(31.4230239951618,-2.29814685040399,33.8969505670765));
#51034=CARTESIAN_POINT('Origin',(31.4152691174526,-2.30950931155476,33.8912947803757));
#51035=CARTESIAN_POINT('',(31.452970256343,-2.31863200978458,33.8637293696319));
#51036=CARTESIAN_POINT('Ctrl Pts',(31.4529702563405,-2.31863200978284,33.8637293696347));
#51037=CARTESIAN_POINT('Ctrl Pts',(31.4379056758382,-2.30832687249962,33.8804609779984));
#51038=CARTESIAN_POINT('Ctrl Pts',(31.423023995155,-2.29814685039932,33.8969505670841));
#51039=CARTESIAN_POINT('',(31.5861090124437,-2.22967153707895,33.8637293696319));
#51040=CARTESIAN_POINT('Origin',(30.,-1.32966554433622E-14,33.8637293696319));
#51041=CARTESIAN_POINT('',(31.5786431309871,-2.19416546819406,33.8969505670765));
#51042=CARTESIAN_POINT('Ctrl Pts',(31.5786431309854,-2.19416546818597,33.8969505670841));
#51043=CARTESIAN_POINT('Ctrl Pts',(31.5823532724012,-2.21181007417745,33.8804609779984));
#51044=CARTESIAN_POINT('Ctrl Pts',(31.5861090124431,-2.22967153707596,33.8637293696347));
#51045=CARTESIAN_POINT('',(31.5989478108274,-2.17941325477251,33.8969505670765));
#51046=CARTESIAN_POINT('Origin',(31.5921082951429,-2.19134908471607,33.891294843835));
#51047=CARTESIAN_POINT('',(31.6304090047603,-2.1974857086706,33.8637293696319));
#51048=CARTESIAN_POINT('Ctrl Pts',(31.6304090047577,-2.19748570866908,33.8637293696347));
#51049=CARTESIAN_POINT('Ctrl Pts',(31.6145823315769,-2.18839429204867,33.8804609779984));
#51050=CARTESIAN_POINT('Ctrl Pts',(31.5989478108202,-2.1794132547684,33.8969505670841));
#51051=CARTESIAN_POINT('',(31.7561575802648,-2.09835352500328,33.8637293696319));
#51052=CARTESIAN_POINT('Origin',(30.,-1.32966554433622E-14,33.8637293696319));
#51053=CARTESIAN_POINT('',(31.7459289395715,-2.0635426757871,33.8969505670765));
#51054=CARTESIAN_POINT('Ctrl Pts',(31.7459289395692,-2.06354267577917,33.8969505670841));
#51055=CARTESIAN_POINT('Ctrl Pts',(31.7510120236878,-2.08084179499847,33.8804609779983));
#51056=CARTESIAN_POINT('Ctrl Pts',(31.7561575802639,-2.09835352500035,33.8637293696347));
#51057=CARTESIAN_POINT('',(31.7650135815352,-2.04724285169692,33.8969505670765));
#51058=CARTESIAN_POINT('Origin',(31.7591315960217,-2.05967847590834,33.8912948941586));
#51059=CARTESIAN_POINT('',(31.7977957394973,-2.06279117742452,33.8637293696319));
#51060=CARTESIAN_POINT('Ctrl Pts',(31.7977957394945,-2.06279117742322,33.8637293696347));
#51061=CARTESIAN_POINT('Ctrl Pts',(31.7813045503384,-2.05496953307228,33.8804609779984));
#51062=CARTESIAN_POINT('Ctrl Pts',(31.7650135815277,-2.04724285169338,33.8969505670841));
#51063=CARTESIAN_POINT('',(31.9153788526219,-1.9540984656726,33.8637293696319));
#51064=CARTESIAN_POINT('Origin',(30.,-1.32966554433622E-14,33.8637293696319));
#51065=CARTESIAN_POINT('',(31.9024505156632,-1.92019745658634,33.8969505670765));
#51066=CARTESIAN_POINT('Ctrl Pts',(31.9024505156603,-1.92019745657863,33.8969505670841));
#51067=CARTESIAN_POINT('Ctrl Pts',(31.9088752035777,-1.93704443420321,33.8804609779984));
#51068=CARTESIAN_POINT('Ctrl Pts',(31.9153788526208,-1.95409846566976,33.8637293696347));
#51069=CARTESIAN_POINT('',(31.9201974565863,-1.90245051566327,33.8969505670765));
#51070=CARTESIAN_POINT('Origin',(31.9153092670123,-1.91530927561705,33.891294933562));
#51071=CARTESIAN_POINT('',(31.9540984656725,-1.91537885262194,33.8637293696319));
#51072=CARTESIAN_POINT('Ctrl Pts',(31.9540984656697,-1.91537885262084,33.8637293696347));
#51073=CARTESIAN_POINT('Ctrl Pts',(31.9370444342032,-1.90887520357777,33.8804609779984));
#51074=CARTESIAN_POINT('Ctrl Pts',(31.9201974565786,-1.90245051566033,33.8969505670841));
#51075=CARTESIAN_POINT('',(32.0627911774245,-1.79779573949737,33.8637293696319));
#51076=CARTESIAN_POINT('Origin',(30.,-1.32966554433622E-14,33.8637293696319));
#51077=CARTESIAN_POINT('',(32.0472428516969,-1.76501358153528,33.8969505670765));
#51078=CARTESIAN_POINT('Ctrl Pts',(32.0472428516934,-1.76501358152781,33.8969505670841));
#51079=CARTESIAN_POINT('Ctrl Pts',(32.0549695330723,-1.78130455033843,33.8804609779983));
#51080=CARTESIAN_POINT('Ctrl Pts',(32.0627911774232,-1.7977957394946,33.8637293696347));
#51081=CARTESIAN_POINT('',(32.063542675787,-1.74592893957158,33.8969505670765));
#51082=CARTESIAN_POINT('Origin',(32.0596784217459,-1.75913156587025,33.8912949636253));
#51083=CARTESIAN_POINT('',(32.0983535250032,-1.75615758026484,33.8637293696319));
#51084=CARTESIAN_POINT('Ctrl Pts',(32.0983535250003,-1.75615758026399,33.8637293696347));
#51085=CARTESIAN_POINT('Ctrl Pts',(32.0808417949984,-1.75101202368781,33.8804609779984));
#51086=CARTESIAN_POINT('Ctrl Pts',(32.0635426757791,-1.74592893956926,33.8969505670841));
#51087=CARTESIAN_POINT('',(32.1974857086705,-1.63040900476039,33.8637293696319));
#51088=CARTESIAN_POINT('Origin',(30.,-1.32966554433622E-14,33.8637293696319));
#51089=CARTESIAN_POINT('',(32.1794132547725,-1.59894781082747,33.8969505670765));
#51090=CARTESIAN_POINT('Ctrl Pts',(32.1794132547683,-1.59894781082035,33.8969505670841));
#51091=CARTESIAN_POINT('Ctrl Pts',(32.1883942920486,-1.61458233157699,33.8804609779984));
#51092=CARTESIAN_POINT('Ctrl Pts',(32.197485708669,-1.63040900475776,33.8637293696347));
#51093=CARTESIAN_POINT('',(32.194165468194,-1.57864313098713,33.8969505670765));
#51094=CARTESIAN_POINT('Origin',(32.1913489771416,-1.59210823242541,33.8912949854673));
#51095=CARTESIAN_POINT('',(32.2296715370789,-1.58610901244375,33.8637293696319));
#51096=CARTESIAN_POINT('Ctrl Pts',(32.2296715370759,-1.58610901244313,33.8637293696347));
#51097=CARTESIAN_POINT('Ctrl Pts',(32.2118100741774,-1.58235327240121,33.8804609779984));
#51098=CARTESIAN_POINT('Ctrl Pts',(32.1941654681859,-1.57864313098543,33.8969505670841));
#51099=CARTESIAN_POINT('',(32.3186320097845,-1.45297025634306,33.8637293696319));
#51100=CARTESIAN_POINT('Origin',(30.,-1.32966554433622E-14,33.8637293696319));
#51101=CARTESIAN_POINT('',(32.2981468504039,-1.42302399516182,33.8969505670765));
#51102=CARTESIAN_POINT('Ctrl Pts',(32.2981468503993,-1.42302399515499,33.8969505670841));
#51103=CARTESIAN_POINT('Ctrl Pts',(32.3083268724996,-1.4379056758382,33.8804609779984));
#51104=CARTESIAN_POINT('Ctrl Pts',(32.3186320097828,-1.45297025634053,33.8637293696347));
#51105=CARTESIAN_POINT('',(32.3112605008555,-1.40162446254804,33.8969505670765));
#51106=CARTESIAN_POINT('Origin',(32.3095091411127,-1.41526902814879,33.891294999854));
#51107=CARTESIAN_POINT('',(32.3472428826875,-1.40628155512619,33.8637293696319));
#51108=CARTESIAN_POINT('Ctrl Pts',(32.3472428826845,-1.4062815551258,33.8637293696347));
#51109=CARTESIAN_POINT('Ctrl Pts',(32.3291418087476,-1.4039387870044,33.8804609779983));
#51110=CARTESIAN_POINT('Ctrl Pts',(32.3112605008473,-1.40162446254698,33.8969505670841));
#51111=CARTESIAN_POINT('',(32.4254831735348,-1.26657346313373,33.8637293696319));
#51112=CARTESIAN_POINT('Origin',(30.,-1.32966554433622E-14,33.8637293696319));
#51113=CARTESIAN_POINT('',(32.4027116064913,-1.2383267633625,33.8969505670765));
#51114=CARTESIAN_POINT('Ctrl Pts',(32.4027116064861,-1.23832676335608,33.8969505670841));
#51115=CARTESIAN_POINT('Ctrl Pts',(32.414027850185,-1.25236385345577,33.8804609779983));
#51116=CARTESIAN_POINT('Ctrl Pts',(32.4254831735329,-1.26657346313137,33.8637293696347));
#51117=CARTESIAN_POINT('',(32.4141058439571,-1.21596431320991,33.8969505670765));
#51118=CARTESIAN_POINT('Origin',(32.4134304175703,-1.22970422416536,33.8912950072666));
#51119=CARTESIAN_POINT('',(32.4503426953868,-1.21778390438519,33.8637293696319));
#51120=CARTESIAN_POINT('Ctrl Pts',(32.4503426953838,-1.21778390438504,33.8637293696347));
#51121=CARTESIAN_POINT('Ctrl Pts',(32.4321136095486,-1.21686855212869,33.8804609779984));
#51122=CARTESIAN_POINT('Ctrl Pts',(32.4141058439489,-1.2159643132095,33.8969505670841));
#51123=CARTESIAN_POINT('',(32.5173804269652,-1.07236782334576,33.8637293696319));
#51124=CARTESIAN_POINT('Origin',(30.,-1.32966554433622E-14,33.8637293696319));
#51125=CARTESIAN_POINT('',(32.492462846542,-1.0459948352816,33.8969505670765));
#51126=CARTESIAN_POINT('Ctrl Pts',(32.4924628465363,-1.04599483527564,33.8969505670841));
#51127=CARTESIAN_POINT('Ctrl Pts',(32.5048455434283,-1.05910079146353,33.8804609779984));
#51128=CARTESIAN_POINT('Ctrl Pts',(32.5173804269631,-1.07236782334356,33.8637293696347));
#51129=CARTESIAN_POINT('',(32.5020674217591,-1.02280733953168,33.8969505670765));
#51130=CARTESIAN_POINT('Origin',(32.5024720978725,-1.03655788791108,33.8912950079413));
#51131=CARTESIAN_POINT('',(32.5383353305474,-1.02177821091943,33.8637293696319));
#51132=CARTESIAN_POINT('Ctrl Pts',(32.5383353305444,-1.02177821091952,33.8637293696347));
#51133=CARTESIAN_POINT('Ctrl Pts',(32.5200906211869,-1.02229591797926,33.8804609779983));
#51134=CARTESIAN_POINT('Ctrl Pts',(32.5020674217508,-1.02280733953191,33.8969505670841));
#51135=CARTESIAN_POINT('',(32.5937571929495,-0.871550679328387,33.8637293696319));
#51136=CARTESIAN_POINT('Origin',(30.,-1.32966554433622E-14,33.8637293696319));
#51137=CARTESIAN_POINT('',(32.5668472243157,-0.847214001212625,33.8969505670765));
#51138=CARTESIAN_POINT('Ctrl Pts',(32.5668472243096,-0.847214001207098,
33.8969505670841));
#51139=CARTESIAN_POINT('Ctrl Pts',(32.5802200309508,-0.859308020905142,
33.8804609779983));
#51140=CARTESIAN_POINT('Ctrl Pts',(32.5937571929472,-0.871550679326345,
33.8637293696347));
#51141=CARTESIAN_POINT('',(32.574602921884,-0.823344418487278,33.8969505670765));
#51142=CARTESIAN_POINT('Origin',(32.5760852110325,-0.837020829522246,33.8912950018862));
#51143=CARTESIAN_POINT('',(32.6106782843131,-0.819472915007605,33.8637293696319));
#51144=CARTESIAN_POINT('Ctrl Pts',(32.6106782843101,-0.819472915007929,
33.8637293696347));
#51145=CARTESIAN_POINT('Ctrl Pts',(32.5925304361305,-0.821420489547588,
33.8804609779984));
#51146=CARTESIAN_POINT('Ctrl Pts',(32.5746029218758,-0.823344418488157,
33.8969505670841));
#51147=CARTESIAN_POINT('',(32.6541425833274,-0.665360135552938,33.8637293696319));
#51148=CARTESIAN_POINT('Origin',(30.,-1.32966554433622E-14,33.8637293696319));
#51149=CARTESIAN_POINT('',(32.6254061353882,-0.643209811098926,33.8969505670765));
#51150=CARTESIAN_POINT('Ctrl Pts',(32.6254061353816,-0.643209811093906,
33.8969505670841));
#51151=CARTESIAN_POINT('Ctrl Pts',(32.6396866039721,-0.65421733064898,33.8804609779984));
#51152=CARTESIAN_POINT('Ctrl Pts',(32.654142583325,-0.665360135551083,33.8637293696347));
#51153=CARTESIAN_POINT('',(32.6312651388532,-0.6188053053131,33.8969505670765));
#51154=CARTESIAN_POINT('Origin',(32.633815908334,-0.632323260043048,33.8912949888765));
#51155=CARTESIAN_POINT('',(32.6669255383174,-0.612115296072366,33.8637293696319));
#51156=CARTESIAN_POINT('Ctrl Pts',(32.6669255383144,-0.612115296072921,
33.8637293696347));
#51157=CARTESIAN_POINT('Ctrl Pts',(32.6489864388314,-0.615480730647825,
33.8804609779983));
#51158=CARTESIAN_POINT('Ctrl Pts',(32.6312651388451,-0.618805305314621,
33.8969505670841));
#51159=CARTESIAN_POINT('',(32.6981643020872,-0.455067425287109,33.8637293696319));
#51160=CARTESIAN_POINT('Origin',(30.,-1.32966554433622E-14,33.8637293696319));
#51161=CARTESIAN_POINT('',(32.6677785445999,-0.435240018610835,33.8969505670765));
#51162=CARTESIAN_POINT('Ctrl Pts',(32.667778544593,-0.43524001860635,33.8969505670841));
#51163=CARTESIAN_POINT('Ctrl Pts',(32.6828786312952,-0.445093173000037,
33.8804609779984));
#51164=CARTESIAN_POINT('Ctrl Pts',(32.6981643020846,-0.45506742528547,33.8637293696347));
#51165=CARTESIAN_POINT('',(32.6717047312569,-0.410451051658023,33.8969505670765));
#51166=CARTESIAN_POINT('Origin',(32.6753082614924,-0.423727206709312,33.8912949684251));
#51167=CARTESIAN_POINT('',(32.7067303095351,-0.400983782787849,33.8637293696319));
#51168=CARTESIAN_POINT('Ctrl Pts',(32.7067303095322,-0.400983782788643,
33.8637293696347));
#51169=CARTESIAN_POINT('Ctrl Pts',(32.6891105592595,-0.405746328375509,
33.8804609779984));
#51170=CARTESIAN_POINT('Ctrl Pts',(32.6717047312489,-0.410451051660171,
33.8969505670841));
#51171=CARTESIAN_POINT('',(32.7255509406939,-0.241969073019109,33.8637293696319));
#51172=CARTESIAN_POINT('Origin',(30.,-1.32966554433622E-14,33.8637293696319));
#51173=CARTESIAN_POINT('',(32.6937032119577,-0.224586826676015,33.8969505670765));
#51174=CARTESIAN_POINT('Ctrl Pts',(32.6937032119505,-0.224586826672072,
33.8969505670841));
#51175=CARTESIAN_POINT('Ctrl Pts',(32.7095298197086,-0.233224867931026,
33.8804609779984));
#51176=CARTESIAN_POINT('Ctrl Pts',(32.7255509406912,-0.241969073017673,
33.8637293696347));
#51177=CARTESIAN_POINT('',(32.6956723755605,-0.199566230780649,33.8969505670765));
#51178=CARTESIAN_POINT('Origin',(32.7003064571198,-0.212518732061269,33.8912949397143));
#51179=CARTESIAN_POINT('',(32.7298471883155,-0.187380071141808,33.8637293696319));
#51180=CARTESIAN_POINT('Ctrl Pts',(32.7298471883126,-0.187380071142835,
33.8637293696347));
#51181=CARTESIAN_POINT('Ctrl Pts',(32.7126554188699,-0.19351036506442,33.8804609779983));
#51182=CARTESIAN_POINT('Ctrl Pts',(32.6956723755527,-0.199566230783424,
33.8969505670841));
#51183=CARTESIAN_POINT('',(32.7361336514135,-0.0273789009530657,33.8637293696319));
#51184=CARTESIAN_POINT('Origin',(30.,-1.32966554433622E-14,33.8637293696319));
#51185=CARTESIAN_POINT('',(32.7030203032667,-0.0125489822720396,33.8969505670765));
#51186=CARTESIAN_POINT('Ctrl Pts',(32.7030203032592,-0.0125489822686859,
33.8969505670841));
#51187=CARTESIAN_POINT('Ctrl Pts',(32.7194758557734,-0.0199186539960853,
33.8804609779984));
#51188=CARTESIAN_POINT('Ctrl Pts',(32.7361336514107,-0.0273789009518218,
33.8637293696347));
#51189=CARTESIAN_POINT('',(32.7030203032667,0.0125489822719939,33.8969505670765));
#51190=CARTESIAN_POINT('Origin',(32.7086563646857,-6.24428584025816E-9,
33.8912949140187));
#51191=CARTESIAN_POINT('',(32.7361336514135,0.0273789009530202,33.8637293696319));
#51192=CARTESIAN_POINT('Ctrl Pts',(32.7361336514108,0.027378900951751,33.8637293696347));
#51193=CARTESIAN_POINT('Ctrl Pts',(32.7194758557734,0.0199186539960142,
33.8804609779984));
#51194=CARTESIAN_POINT('Ctrl Pts',(32.7030203032592,0.0125489822686146,
33.8969505670841));
#51195=CARTESIAN_POINT('',(32.7298471883155,0.187380071141762,33.8637293696319));
#51196=CARTESIAN_POINT('Origin',(30.,-1.32966554433622E-14,33.8637293696319));
#51197=CARTESIAN_POINT('',(32.6956723755605,0.199566230780603,33.8969505670765));
#51198=CARTESIAN_POINT('Ctrl Pts',(32.6956723755527,0.199566230783364,33.8969505670841));
#51199=CARTESIAN_POINT('Ctrl Pts',(32.7126554188699,0.193510365064359,33.8804609779983));
#51200=CARTESIAN_POINT('Ctrl Pts',(32.7298471883126,0.187380071142775,33.8637293696347));
#51201=CARTESIAN_POINT('',(32.6937032119577,0.224586826675969,33.8969505670765));
#51202=CARTESIAN_POINT('Origin',(32.7003074588901,0.212518788369426,33.8912937927563));
#51203=CARTESIAN_POINT('',(32.7255509406939,0.241969073019064,33.8637293696319));
#51204=CARTESIAN_POINT('Ctrl Pts',(32.7255509406912,0.241969073017624,33.8637293696347));
#51205=CARTESIAN_POINT('Ctrl Pts',(32.7095298197086,0.233224867930978,33.8804609779984));
#51206=CARTESIAN_POINT('Ctrl Pts',(32.6937032119505,0.224586826672025,33.8969505670841));
#51207=CARTESIAN_POINT('',(32.7067303095351,0.400983782787804,33.8637293696319));
#51208=CARTESIAN_POINT('Origin',(30.,-1.32966554433622E-14,33.8637293696319));
#51209=CARTESIAN_POINT('',(32.6717047312569,0.410451051657977,33.8969505670765));
#51210=CARTESIAN_POINT('Ctrl Pts',(32.6717047312489,0.410451051660138,33.8969505670841));
#51211=CARTESIAN_POINT('Ctrl Pts',(32.6891105592595,0.405746328375475,33.8804609779984));
#51212=CARTESIAN_POINT('Ctrl Pts',(32.7067303095322,0.400983782788608,33.8637293696347));
#51213=CARTESIAN_POINT('',(32.6677785445999,0.435240018610789,33.8969505670765));
#51214=CARTESIAN_POINT('Origin',(32.6753090233822,0.423727307748461,33.8912940899386));
#51215=CARTESIAN_POINT('',(32.6981643020872,0.455067425287063,33.8637293696319));
#51216=CARTESIAN_POINT('Ctrl Pts',(32.6981643020846,0.455067425285395,33.8637293696347));
#51217=CARTESIAN_POINT('Ctrl Pts',(32.6828786312952,0.445093172999962,33.8804609779983));
#51218=CARTESIAN_POINT('Ctrl Pts',(32.667778544593,0.435240018606276,33.8969505670841));
#51219=CARTESIAN_POINT('',(32.6669255383174,0.61211529607232,33.8637293696319));
#51220=CARTESIAN_POINT('Origin',(30.,-1.32966554433622E-14,33.8637293696319));
#51221=CARTESIAN_POINT('',(32.6312651388532,0.618805305313054,33.8969505670765));
#51222=CARTESIAN_POINT('Ctrl Pts',(32.6312651388451,0.618805305314574,33.8969505670841));
#51223=CARTESIAN_POINT('Ctrl Pts',(32.6489864388314,0.615480730647778,33.8804609779983));
#51224=CARTESIAN_POINT('Ctrl Pts',(32.6669255383144,0.612115296072874,33.8637293696347));
#51225=CARTESIAN_POINT('',(32.6254061353882,0.64320981109888,33.8969505670765));
#51226=CARTESIAN_POINT('Origin',(32.6338164916465,0.632323382398585,33.8912943077151));
#51227=CARTESIAN_POINT('',(32.6541425833274,0.665360135552893,33.8637293696319));
#51228=CARTESIAN_POINT('Ctrl Pts',(32.654142583325,0.665360135551018,33.8637293696347));
#51229=CARTESIAN_POINT('Ctrl Pts',(32.6396866039721,0.654217330648915,33.8804609779984));
#51230=CARTESIAN_POINT('Ctrl Pts',(32.6254061353817,0.643209811093841,33.8969505670841));
#51231=CARTESIAN_POINT('',(32.6106782843131,0.81947291500756,33.8637293696319));
#51232=CARTESIAN_POINT('Origin',(30.,-1.32966554433622E-14,33.8637293696319));
#51233=CARTESIAN_POINT('',(32.574602921884,0.823344418487232,33.8969505670765));
#51234=CARTESIAN_POINT('Ctrl Pts',(32.5746029218758,0.823344418488117,33.8969505670841));
#51235=CARTESIAN_POINT('Ctrl Pts',(32.5925304361305,0.821420489547548,33.8804609779984));
#51236=CARTESIAN_POINT('Ctrl Pts',(32.6106782843101,0.819472915007888,33.8637293696347));
#51237=CARTESIAN_POINT('',(32.5668472243157,0.84721400121258,33.8969505670765));
#51238=CARTESIAN_POINT('Origin',(32.5760856561636,0.83702095775897,33.891294472568));
#51239=CARTESIAN_POINT('',(32.5937571929495,0.871550679328342,33.8637293696319));
#51240=CARTESIAN_POINT('Ctrl Pts',(32.5937571929473,0.871550679326287,33.8637293696347));
#51241=CARTESIAN_POINT('Ctrl Pts',(32.5802200309508,0.859308020905083,33.8804609779984));
#51242=CARTESIAN_POINT('Ctrl Pts',(32.5668472243096,0.847214001207037,33.8969505670841));
#51243=CARTESIAN_POINT('',(32.5383353305474,1.02177821091938,33.8637293696319));
#51244=CARTESIAN_POINT('Origin',(30.,-1.32966554433622E-14,33.8637293696319));
#51245=CARTESIAN_POINT('',(32.5020674217591,1.02280733953163,33.8969505670765));
#51246=CARTESIAN_POINT('Ctrl Pts',(32.5020674217508,1.02280733953187,33.8969505670841));
#51247=CARTESIAN_POINT('Ctrl Pts',(32.520090621187,1.02229591797922,33.8804609779984));
#51248=CARTESIAN_POINT('Ctrl Pts',(32.5383353305444,1.02177821091947,33.8637293696347));
#51249=CARTESIAN_POINT('',(32.492462846542,1.04599483528156,33.8969505670765));
#51250=CARTESIAN_POINT('Origin',(32.5024724328509,1.03655801106889,33.8912946002427));
#51251=CARTESIAN_POINT('',(32.5173804269653,1.07236782334572,33.8637293696319));
#51252=CARTESIAN_POINT('Ctrl Pts',(32.5173804269632,1.0723678233435,33.8637293696347));
#51253=CARTESIAN_POINT('Ctrl Pts',(32.5048455434284,1.05910079146346,33.8804609779983));
#51254=CARTESIAN_POINT('Ctrl Pts',(32.4924628465363,1.04599483527555,33.8969505670841));
#51255=CARTESIAN_POINT('',(32.4503426953868,1.21778390438515,33.8637293696319));
#51256=CARTESIAN_POINT('Origin',(30.,-1.32966554433622E-14,33.8637293696319));
#51257=CARTESIAN_POINT('',(32.4141058439571,1.21596431320987,33.8969505670765));
#51258=CARTESIAN_POINT('Ctrl Pts',(32.4141058439489,1.21596431320946,33.8969505670841));
#51259=CARTESIAN_POINT('Ctrl Pts',(32.4321136095487,1.21686855212866,33.8804609779984));
#51260=CARTESIAN_POINT('Ctrl Pts',(32.4503426953838,1.217783904385,33.8637293696347));
#51261=CARTESIAN_POINT('',(32.4027116064913,1.23832676336245,33.8969505670765));
#51262=CARTESIAN_POINT('Origin',(32.4134306626749,1.22970433386022,33.891294700665));
#51263=CARTESIAN_POINT('',(32.4254831735348,1.26657346313369,33.8637293696319));
#51264=CARTESIAN_POINT('Ctrl Pts',(32.4254831735329,1.26657346313132,33.8637293696347));
#51265=CARTESIAN_POINT('Ctrl Pts',(32.414027850185,1.25236385345572,33.8804609779984));
#51266=CARTESIAN_POINT('Ctrl Pts',(32.4027116064861,1.23832676335603,33.8969505670841));
#51267=CARTESIAN_POINT('',(32.3472428826875,1.40628155512614,33.8637293696319));
#51268=CARTESIAN_POINT('Origin',(30.,-1.32966554433622E-14,33.8637293696319));
#51269=CARTESIAN_POINT('',(32.3112605008555,1.401624462548,33.8969505670765));
#51270=CARTESIAN_POINT('Ctrl Pts',(32.3112605008473,1.40162446254694,33.8969505670841));
#51271=CARTESIAN_POINT('Ctrl Pts',(32.3291418087476,1.40393878700437,33.8804609779984));
#51272=CARTESIAN_POINT('Ctrl Pts',(32.3472428826845,1.40628155512576,33.8637293696347));
#51273=CARTESIAN_POINT('',(32.298146850404,1.42302399516178,33.8969505670765));
#51274=CARTESIAN_POINT('Origin',(32.3095093115547,1.41526911745259,33.8912947803757));
#51275=CARTESIAN_POINT('',(32.3186320097845,1.45297025634302,33.8637293696319));
#51276=CARTESIAN_POINT('Ctrl Pts',(32.3186320097828,1.45297025634046,33.8637293696347));
#51277=CARTESIAN_POINT('Ctrl Pts',(32.3083268724996,1.43790567583815,33.8804609779983));
#51278=CARTESIAN_POINT('Ctrl Pts',(32.2981468503993,1.42302399515495,33.8969505670841));
#51279=CARTESIAN_POINT('',(32.2296715370789,1.58610901244371,33.8637293696319));
#51280=CARTESIAN_POINT('Origin',(30.,-1.32966554433622E-14,33.8637293696319));
#51281=CARTESIAN_POINT('',(32.194165468194,1.57864313098709,33.8969505670765));
#51282=CARTESIAN_POINT('Ctrl Pts',(32.1941654681859,1.57864313098539,33.8969505670841));
#51283=CARTESIAN_POINT('Ctrl Pts',(32.2118100741774,1.58235327240116,33.8804609779984));
#51284=CARTESIAN_POINT('Ctrl Pts',(32.2296715370759,1.58610901244308,33.8637293696347));
#51285=CARTESIAN_POINT('',(32.1794132547725,1.59894781082743,33.8969505670765));
#51286=CARTESIAN_POINT('Origin',(32.191349084716,1.59210829514292,33.891294843835));
#51287=CARTESIAN_POINT('',(32.1974857086706,1.63040900476035,33.8637293696319));
#51288=CARTESIAN_POINT('Ctrl Pts',(32.1974857086691,1.6304090047577,33.8637293696347));
#51289=CARTESIAN_POINT('Ctrl Pts',(32.1883942920486,1.61458233157692,33.8804609779983));
#51290=CARTESIAN_POINT('Ctrl Pts',(32.1794132547684,1.59894781082026,33.8969505670841));
#51291=CARTESIAN_POINT('',(32.0983535250032,1.7561575802648,33.8637293696319));
#51292=CARTESIAN_POINT('Origin',(30.,-1.32966554433622E-14,33.8637293696319));
#51293=CARTESIAN_POINT('',(32.0635426757871,1.74592893957153,33.8969505670765));
#51294=CARTESIAN_POINT('Ctrl Pts',(32.0635426757792,1.74592893956921,33.8969505670841));
#51295=CARTESIAN_POINT('Ctrl Pts',(32.0808417949984,1.75101202368776,33.8804609779983));
#51296=CARTESIAN_POINT('Ctrl Pts',(32.0983535250003,1.75615758026393,33.8637293696347));
#51297=CARTESIAN_POINT('',(32.0472428516969,1.76501358153524,33.8969505670765));
#51298=CARTESIAN_POINT('Origin',(32.0596784759083,1.75913159602166,33.8912948941586));
#51299=CARTESIAN_POINT('',(32.0627911774245,1.79779573949733,33.8637293696319));
#51300=CARTESIAN_POINT('Ctrl Pts',(32.0627911774232,1.79779573949457,33.8637293696347));
#51301=CARTESIAN_POINT('Ctrl Pts',(32.0549695330723,1.78130455033839,33.8804609779984));
#51302=CARTESIAN_POINT('Ctrl Pts',(32.0472428516934,1.76501358152777,33.8969505670841));
#51303=CARTESIAN_POINT('',(31.9540984656726,1.9153788526219,33.8637293696319));
#51304=CARTESIAN_POINT('Origin',(30.,-1.32966554433622E-14,33.8637293696319));
#51305=CARTESIAN_POINT('',(31.9201974565863,1.90245051566323,33.8969505670765));
#51306=CARTESIAN_POINT('Ctrl Pts',(31.9201974565786,1.90245051566028,33.8969505670841));
#51307=CARTESIAN_POINT('Ctrl Pts',(31.9370444342032,1.90887520357773,33.8804609779983));
#51308=CARTESIAN_POINT('Ctrl Pts',(31.9540984656697,1.91537885262081,33.8637293696347));
#51309=CARTESIAN_POINT('',(31.9024505156632,1.9201974565863,33.8969505670765));
#51310=CARTESIAN_POINT('Origin',(31.915309275617,1.91530926701235,33.891294933562));
#51311=CARTESIAN_POINT('',(31.9153788526219,1.95409846567256,33.8637293696319));
#51312=CARTESIAN_POINT('Ctrl Pts',(31.9153788526208,1.95409846566973,33.8637293696347));
#51313=CARTESIAN_POINT('Ctrl Pts',(31.9088752035777,1.93704443420319,33.8804609779984));
#51314=CARTESIAN_POINT('Ctrl Pts',(31.9024505156603,1.9201974565786,33.8969505670841));
#51315=CARTESIAN_POINT('',(31.7977957394973,2.06279117742448,33.8637293696319));
#51316=CARTESIAN_POINT('Origin',(30.,-1.32966554433622E-14,33.8637293696319));
#51317=CARTESIAN_POINT('',(31.7650135815352,2.04724285169688,33.8969505670765));
#51318=CARTESIAN_POINT('Ctrl Pts',(31.7650135815278,2.04724285169333,33.8969505670841));
#51319=CARTESIAN_POINT('Ctrl Pts',(31.7813045503384,2.05496953307223,33.8804609779984));
#51320=CARTESIAN_POINT('Ctrl Pts',(31.7977957394946,2.06279117742316,33.8637293696347));
#51321=CARTESIAN_POINT('',(31.7459289395715,2.06354267578706,33.8969505670765));
#51322=CARTESIAN_POINT('Origin',(31.7591315658702,2.05967842174595,33.8912949636253));
#51323=CARTESIAN_POINT('',(31.7561575802648,2.09835352500324,33.8637293696319));
#51324=CARTESIAN_POINT('Ctrl Pts',(31.7561575802639,2.09835352500033,33.8637293696347));
#51325=CARTESIAN_POINT('Ctrl Pts',(31.7510120236877,2.08084179499845,33.8804609779984));
#51326=CARTESIAN_POINT('Ctrl Pts',(31.7459289395692,2.06354267577915,33.8969505670841));
#51327=CARTESIAN_POINT('',(31.6304090047604,2.19748570867057,33.8637293696319));
#51328=CARTESIAN_POINT('Origin',(30.,-1.32966554433622E-14,33.8637293696319));
#51329=CARTESIAN_POINT('',(31.5989478108274,2.17941325477248,33.8969505670765));
#51330=CARTESIAN_POINT('Ctrl Pts',(31.5989478108202,2.17941325476838,33.8969505670841));
#51331=CARTESIAN_POINT('Ctrl Pts',(31.6145823315769,2.18839429204865,33.8804609779983));
#51332=CARTESIAN_POINT('Ctrl Pts',(31.6304090047577,2.19748570866908,33.8637293696347));
#51333=CARTESIAN_POINT('',(31.5786431309871,2.19416546819402,33.8969505670765));
#51334=CARTESIAN_POINT('Origin',(31.5921082324254,2.19134897714166,33.8912949854673));
#51335=CARTESIAN_POINT('',(31.5861090124437,2.22967153707891,33.8637293696319));
#51336=CARTESIAN_POINT('Ctrl Pts',(31.5861090124431,2.22967153707593,33.8637293696347));
#51337=CARTESIAN_POINT('Ctrl Pts',(31.5823532724012,2.21181007417742,33.8804609779984));
#51338=CARTESIAN_POINT('Ctrl Pts',(31.5786431309854,2.19416546818594,33.8969505670841));
#51339=CARTESIAN_POINT('',(31.452970256343,2.31863200978455,33.8637293696319));
#51340=CARTESIAN_POINT('Origin',(30.,-1.32966554433622E-14,33.8637293696319));
#51341=CARTESIAN_POINT('',(31.4230239951618,2.29814685040396,33.8969505670765));
#51342=CARTESIAN_POINT('Ctrl Pts',(31.423023995155,2.29814685039929,33.8969505670841));
#51343=CARTESIAN_POINT('Ctrl Pts',(31.4379056758382,2.30832687249959,33.8804609779983));
#51344=CARTESIAN_POINT('Ctrl Pts',(31.4529702563405,2.31863200978281,33.8637293696347));
#51345=CARTESIAN_POINT('',(31.401624462548,2.3112605008555,33.8969505670765));
#51346=CARTESIAN_POINT('Origin',(31.4152690281487,2.30950914111275,33.891294999854));
#51347=CARTESIAN_POINT('',(31.4062815551261,2.34724288268748,33.8637293696319));
#51348=CARTESIAN_POINT('Ctrl Pts',(31.4062815551258,2.34724288268445,33.8637293696347));
#51349=CARTESIAN_POINT('Ctrl Pts',(31.4039387870044,2.32914180874762,33.8804609779983));
#51350=CARTESIAN_POINT('Ctrl Pts',(31.4016244625469,2.31126050084732,33.8969505670841));
#51351=CARTESIAN_POINT('',(31.2665734631337,2.42548317353483,33.8637293696319));
#51352=CARTESIAN_POINT('Origin',(30.,-1.32966554433622E-14,33.8637293696319));
#51353=CARTESIAN_POINT('',(31.2383267633625,2.40271160649132,33.8969505670765));
#51354=CARTESIAN_POINT('Ctrl Pts',(31.2383267633561,2.40271160648613,33.8969505670841));
#51355=CARTESIAN_POINT('Ctrl Pts',(31.2523638534557,2.41402785018503,33.8804609779983));
#51356=CARTESIAN_POINT('Ctrl Pts',(31.2665734631313,2.4254831735329,33.8637293696347));
#51357=CARTESIAN_POINT('',(31.2159643132099,2.41410584395711,33.8969505670765));
#51358=CARTESIAN_POINT('Origin',(31.2297042241653,2.41343041757031,33.8912950072666));
#51359=CARTESIAN_POINT('',(31.2177839043851,2.45034269538681,33.8637293696319));
#51360=CARTESIAN_POINT('Ctrl Pts',(31.217783904385,2.45034269538375,33.8637293696347));
#51361=CARTESIAN_POINT('Ctrl Pts',(31.2168685521287,2.43211360954864,33.8804609779984));
#51362=CARTESIAN_POINT('Ctrl Pts',(31.2159643132095,2.41410584394886,33.8969505670841));
#51363=CARTESIAN_POINT('',(31.0723678233457,2.51738042696526,33.8637293696319));
#51364=CARTESIAN_POINT('Origin',(30.,-1.32966554433622E-14,33.8637293696319));
#51365=CARTESIAN_POINT('',(31.0459948352816,2.49246284654197,33.8969505670765));
#51366=CARTESIAN_POINT('Ctrl Pts',(31.0459948352756,2.4924628465363,33.8969505670841));
#51367=CARTESIAN_POINT('Ctrl Pts',(31.0591007914635,2.50484554342835,33.8804609779983));
#51368=CARTESIAN_POINT('Ctrl Pts',(31.0723678233435,2.51738042696315,33.8637293696347));
#51369=CARTESIAN_POINT('',(31.0228073395316,2.50206742175906,33.8969505670765));
#51370=CARTESIAN_POINT('Origin',(31.036557887911,2.50247209787251,33.8912950079413));
#51371=CARTESIAN_POINT('',(31.0217782109194,2.53833533054745,33.8637293696319));
#51372=CARTESIAN_POINT('Ctrl Pts',(31.0217782109194,2.5383353305444,33.8637293696347));
#51373=CARTESIAN_POINT('Ctrl Pts',(31.0222959179792,2.52009062118696,33.8804609779984));
#51374=CARTESIAN_POINT('Ctrl Pts',(31.0228073395318,2.50206742175081,33.8969505670841));
#51375=CARTESIAN_POINT('',(30.8715506793283,2.59375719294951,33.8637293696319));
#51376=CARTESIAN_POINT('Origin',(30.,-1.32966554433622E-14,33.8637293696319));
#51377=CARTESIAN_POINT('',(30.8472140012126,2.5668472243157,33.8969505670765));
#51378=CARTESIAN_POINT('Ctrl Pts',(30.847214001207,2.56684722430959,33.8969505670841));
#51379=CARTESIAN_POINT('Ctrl Pts',(30.8593080209051,2.58022003095078,33.8804609779984));
#51380=CARTESIAN_POINT('Ctrl Pts',(30.8715506793263,2.59375719294725,33.8637293696347));
#51381=CARTESIAN_POINT('',(30.8233444184872,2.57460292188402,33.8969505670765));
#51382=CARTESIAN_POINT('Origin',(30.8370208295222,2.57608521103255,33.8912950018862));
#51383=CARTESIAN_POINT('',(30.8194729150076,2.61067828431311,33.8637293696319));
#51384=CARTESIAN_POINT('Ctrl Pts',(30.8194729150079,2.61067828431008,33.8637293696347));
#51385=CARTESIAN_POINT('Ctrl Pts',(30.8214204895475,2.59253043613048,33.8804609779984));
#51386=CARTESIAN_POINT('Ctrl Pts',(30.8233444184881,2.57460292187581,33.8969505670841));
#51387=CARTESIAN_POINT('',(30.6653601355529,2.65414258332745,33.8637293696319));
#51388=CARTESIAN_POINT('Origin',(30.,-1.32966554433622E-14,33.8637293696319));
#51389=CARTESIAN_POINT('',(30.6432098110989,2.62540613538819,33.8969505670765));
#51390=CARTESIAN_POINT('Ctrl Pts',(30.6432098110938,2.62540613538167,33.8969505670841));
#51391=CARTESIAN_POINT('Ctrl Pts',(30.6542173306489,2.63968660397217,33.8804609779983));
#51392=CARTESIAN_POINT('Ctrl Pts',(30.665360135551,2.65414258332504,33.8637293696347));
#51393=CARTESIAN_POINT('',(30.6188053053131,2.63126513885322,33.8969505670765));
#51394=CARTESIAN_POINT('Origin',(30.632323260043,2.633815908334,33.8912949888765));
#51395=CARTESIAN_POINT('',(30.6121152960723,2.66692553831736,33.8637293696319));
#51396=CARTESIAN_POINT('Ctrl Pts',(30.6121152960729,2.66692553831437,33.8637293696347));
#51397=CARTESIAN_POINT('Ctrl Pts',(30.6154807306478,2.6489864388314,33.8804609779983));
#51398=CARTESIAN_POINT('Ctrl Pts',(30.6188053053146,2.63126513884509,33.8969505670841));
#51399=CARTESIAN_POINT('',(30.4550674252871,2.69816430208719,33.8637293696319));
#51400=CARTESIAN_POINT('Origin',(30.,-1.32966554433622E-14,33.8637293696319));
#51401=CARTESIAN_POINT('',(30.4352400186108,2.66777854459989,33.8969505670765));
#51402=CARTESIAN_POINT('Ctrl Pts',(30.4352400186063,2.66777854459299,33.8969505670841));
#51403=CARTESIAN_POINT('Ctrl Pts',(30.4450931729999,2.68287863129519,33.8804609779983));
#51404=CARTESIAN_POINT('Ctrl Pts',(30.4550674252854,2.69816430208465,33.8637293696347));
#51405=CARTESIAN_POINT('',(30.410451051658,2.67170473125694,33.8969505670765));
#51406=CARTESIAN_POINT('Origin',(30.4237272067093,2.67530826149246,33.891294968425));
#51407=CARTESIAN_POINT('',(30.4009837827878,2.70673030953515,33.8637293696319));
#51408=CARTESIAN_POINT('Ctrl Pts',(30.4009837827886,2.7067303095322,33.8637293696347));
#51409=CARTESIAN_POINT('Ctrl Pts',(30.4057463283755,2.68911055925956,33.8804609779984));
#51410=CARTESIAN_POINT('Ctrl Pts',(30.4104510516602,2.67170473124897,33.8969505670841));
#51411=CARTESIAN_POINT('',(30.2419690730191,2.72555094069389,33.8637293696319));
#51412=CARTESIAN_POINT('Origin',(30.,-1.32966554433622E-14,33.8637293696319));
#51413=CARTESIAN_POINT('',(30.224586826676,2.69370321195774,33.8969505670765));
#51414=CARTESIAN_POINT('Ctrl Pts',(30.224586826672,2.6937032119505,33.8969505670841));
#51415=CARTESIAN_POINT('Ctrl Pts',(30.233224867931,2.70952981970859,33.8804609779983));
#51416=CARTESIAN_POINT('Ctrl Pts',(30.2419690730176,2.72555094069122,33.8637293696347));
#51417=CARTESIAN_POINT('',(30.1995662307806,2.69567237556048,33.8969505670765));
#51418=CARTESIAN_POINT('Origin',(30.2125187320612,2.70030645711979,33.8912949397143));
#51419=CARTESIAN_POINT('',(30.1873800711418,2.72984718831549,33.8637293696319));
#51420=CARTESIAN_POINT('Ctrl Pts',(30.1873800711428,2.7298471883126,33.8637293696347));
#51421=CARTESIAN_POINT('Ctrl Pts',(30.1935103650644,2.71265541886987,33.8804609779983));
#51422=CARTESIAN_POINT('Ctrl Pts',(30.1995662307834,2.6956723755527,33.8969505670841));
#51423=CARTESIAN_POINT('',(30.027378900953,2.73613365141356,33.8637293696319));
#51424=CARTESIAN_POINT('Origin',(30.,-1.32966554433622E-14,33.8637293696319));
#51425=CARTESIAN_POINT('',(30.012548982272,2.70302030326666,33.8969505670765));
#51426=CARTESIAN_POINT('Ctrl Pts',(30.0125489822686,2.70302030325912,33.8969505670841));
#51427=CARTESIAN_POINT('Ctrl Pts',(30.019918653996,2.71947585577339,33.8804609779983));
#51428=CARTESIAN_POINT('Ctrl Pts',(30.0273789009518,2.73613365141076,33.8637293696347));
#51429=CARTESIAN_POINT('',(29.987451017728,2.70302030326666,33.8969505670765));
#51430=CARTESIAN_POINT('Origin',(30.,2.70866577951602,33.891284862925));
#51431=CARTESIAN_POINT('',(29.9726210990469,2.73613365141356,33.8637293696319));
#51432=CARTESIAN_POINT('Ctrl Pts',(29.9726210990482,2.73613365141079,33.8637293696347));
#51433=CARTESIAN_POINT('Ctrl Pts',(29.980081346004,2.7194758557734,33.8804609779983));
#51434=CARTESIAN_POINT('Ctrl Pts',(29.9874510177314,2.70302030325912,33.8969505670841));
#51435=CARTESIAN_POINT('',(29.8126199288582,2.72984718831549,33.8637293696319));
#51436=CARTESIAN_POINT('Origin',(30.,-1.32966554433622E-14,33.8637293696319));
#51437=CARTESIAN_POINT('',(29.8004337692194,2.69567237556048,33.8969505670765));
#51438=CARTESIAN_POINT('Ctrl Pts',(29.8004337692166,2.6956723755527,33.8969505670841));
#51439=CARTESIAN_POINT('Ctrl Pts',(29.8064896349356,2.71265541886987,33.8804609779983));
#51440=CARTESIAN_POINT('Ctrl Pts',(29.8126199288572,2.7298471883126,33.8637293696347));
#51441=CARTESIAN_POINT('',(29.775413173324,2.69370321195775,33.8969505670765));
#51442=CARTESIAN_POINT('Origin',(29.7874812116306,2.70030745889017,33.8912937927563));
#51443=CARTESIAN_POINT('',(29.7580309269809,2.72555094069389,33.8637293696319));
#51444=CARTESIAN_POINT('Ctrl Pts',(29.7580309269824,2.72555094069121,33.8637293696347));
#51445=CARTESIAN_POINT('Ctrl Pts',(29.766775132069,2.70952981970858,33.8804609779983));
#51446=CARTESIAN_POINT('Ctrl Pts',(29.775413173328,2.69370321195049,33.8969505670841));
#51447=CARTESIAN_POINT('',(29.5990162172122,2.70673030953515,33.8637293696319));
#51448=CARTESIAN_POINT('Origin',(30.,-1.32966554433622E-14,33.8637293696319));
#51449=CARTESIAN_POINT('',(29.589548948342,2.67170473125694,33.8969505670765));
#51450=CARTESIAN_POINT('Ctrl Pts',(29.5895489483398,2.67170473124897,33.8969505670841));
#51451=CARTESIAN_POINT('Ctrl Pts',(29.5942536716245,2.68911055925956,33.8804609779983));
#51452=CARTESIAN_POINT('Ctrl Pts',(29.5990162172114,2.7067303095322,33.8637293696347));
#51453=CARTESIAN_POINT('',(29.5647599813892,2.6677785445999,33.8969505670765));
#51454=CARTESIAN_POINT('Origin',(29.5762726922515,2.67530902338217,33.8912940899386));
#51455=CARTESIAN_POINT('',(29.5449325747129,2.6981643020872,33.8637293696319));
#51456=CARTESIAN_POINT('Ctrl Pts',(29.5449325747146,2.69816430208465,33.8637293696347));
#51457=CARTESIAN_POINT('Ctrl Pts',(29.554906827,2.68287863129518,33.8804609779983));
#51458=CARTESIAN_POINT('Ctrl Pts',(29.5647599813937,2.66777854459298,33.8969505670841));
#51459=CARTESIAN_POINT('',(29.3878847039277,2.66692553831737,33.8637293696319));
#51460=CARTESIAN_POINT('Origin',(30.,-1.32966554433622E-14,33.8637293696319));
#51461=CARTESIAN_POINT('',(29.3811946946869,2.63126513885323,33.8969505670765));
#51462=CARTESIAN_POINT('Ctrl Pts',(29.3811946946854,2.6312651388451,33.8969505670841));
#51463=CARTESIAN_POINT('Ctrl Pts',(29.3845192693522,2.64898643883141,33.8804609779983));
#51464=CARTESIAN_POINT('Ctrl Pts',(29.3878847039271,2.66692553831437,33.8637293696347));
#51465=CARTESIAN_POINT('',(29.3567901889011,2.6254061353882,33.8969505670765));
#51466=CARTESIAN_POINT('Origin',(29.3676766176014,2.6338164916465,33.8912943077151));
#51467=CARTESIAN_POINT('',(29.3346398644471,2.65414258332745,33.8637293696319));
#51468=CARTESIAN_POINT('Ctrl Pts',(29.334639864449,2.65414258332502,33.8637293696347));
#51469=CARTESIAN_POINT('Ctrl Pts',(29.3457826693511,2.63968660397215,33.8804609779983));
#51470=CARTESIAN_POINT('Ctrl Pts',(29.3567901889061,2.62540613538165,33.8969505670841));
#51471=CARTESIAN_POINT('',(29.1805270849924,2.61067828431312,33.8637293696319));
#51472=CARTESIAN_POINT('Origin',(30.,-1.32966554433622E-14,33.8637293696319));
#51473=CARTESIAN_POINT('',(29.1766555815128,2.57460292188403,33.8969505670765));
#51474=CARTESIAN_POINT('Ctrl Pts',(29.1766555815118,2.57460292187581,33.8969505670841));
#51475=CARTESIAN_POINT('Ctrl Pts',(29.1785795104524,2.59253043613048,33.8804609779983));
#51476=CARTESIAN_POINT('Ctrl Pts',(29.1805270849921,2.61067828431008,33.8637293696347));
#51477=CARTESIAN_POINT('',(29.1527859987874,2.56684722431571,33.8969505670765));
#51478=CARTESIAN_POINT('Origin',(29.162979042241,2.57608565616365,33.891294472568));
#51479=CARTESIAN_POINT('',(29.1284493206716,2.59375719294953,33.8637293696319));
#51480=CARTESIAN_POINT('Ctrl Pts',(29.1284493206737,2.59375719294727,33.8637293696347));
#51481=CARTESIAN_POINT('Ctrl Pts',(29.1406919790949,2.58022003095078,33.8804609779983));
#51482=CARTESIAN_POINT('Ctrl Pts',(29.1527859987929,2.56684722430958,33.8969505670841));
#51483=CARTESIAN_POINT('',(28.9782217890806,2.53833533054746,33.8637293696319));
#51484=CARTESIAN_POINT('Origin',(30.,-1.32966554433622E-14,33.8637293696319));
#51485=CARTESIAN_POINT('',(28.9771926604684,2.50206742175908,33.8969505670765));
#51486=CARTESIAN_POINT('Ctrl Pts',(28.9771926604681,2.50206742175082,33.8969505670841));
#51487=CARTESIAN_POINT('Ctrl Pts',(28.9777040820208,2.52009062118696,33.8804609779983));
#51488=CARTESIAN_POINT('Ctrl Pts',(28.9782217890805,2.5383353305444,33.8637293696347));
#51489=CARTESIAN_POINT('',(28.9540051647184,2.49246284654199,33.8969505670765));
#51490=CARTESIAN_POINT('Origin',(28.9634419889311,2.50247243285091,33.8912946002427));
#51491=CARTESIAN_POINT('',(28.9276321766543,2.51738042696527,33.8637293696319));
#51492=CARTESIAN_POINT('Ctrl Pts',(28.9276321766565,2.51738042696315,33.8637293696347));
#51493=CARTESIAN_POINT('Ctrl Pts',(28.9408992085365,2.50484554342835,33.8804609779983));
#51494=CARTESIAN_POINT('Ctrl Pts',(28.9540051647244,2.49246284653631,33.8969505670841));
#51495=CARTESIAN_POINT('',(28.7822160956148,2.45034269538683,33.8637293696319));
#51496=CARTESIAN_POINT('Origin',(30.,-1.32966554433622E-14,33.8637293696319));
#51497=CARTESIAN_POINT('Ctrl Pts',(28.7840356867905,2.41410584394887,33.8969505670841));
#51498=CARTESIAN_POINT('Ctrl Pts',(28.7831314478713,2.43211360954865,33.8804609779983));
#51499=CARTESIAN_POINT('Ctrl Pts',(28.782216095615,2.45034269538377,33.8637293696347));
#51500=CARTESIAN_POINT('',(28.7334265368663,2.42548317353484,33.8637293696319));
#51501=CARTESIAN_POINT('Ctrl Pts',(28.7334265368687,2.42548317353291,33.8637293696347));
#51502=CARTESIAN_POINT('Ctrl Pts',(28.7476361465443,2.41402785018503,33.8804609779983));
#51503=CARTESIAN_POINT('Ctrl Pts',(28.7616732366439,2.40271160648614,33.8969505670841));
#51504=CARTESIAN_POINT('',(28.5937184448738,2.3472428826875,33.8637293696319));
#51505=CARTESIAN_POINT('Origin',(30.,-1.32966554433622E-14,33.8637293696319));
#51506=CARTESIAN_POINT('Ctrl Pts',(28.5983755374531,2.31126050084732,33.8969505670841));
#51507=CARTESIAN_POINT('Ctrl Pts',(28.5960612129956,2.32914180874763,33.8804609779983));
#51508=CARTESIAN_POINT('Ctrl Pts',(28.5937184448742,2.34724288268447,33.8637293696347));
#51509=CARTESIAN_POINT('',(28.547029743657,2.31863200978457,33.8637293696319));
#51510=CARTESIAN_POINT('Ctrl Pts',(28.5470297436595,2.31863200978283,33.8637293696347));
#51511=CARTESIAN_POINT('Ctrl Pts',(28.5620943241618,2.30832687249961,33.8804609779983));
#51512=CARTESIAN_POINT('Ctrl Pts',(28.576976004845,2.29814685039931,33.8969505670841));
#51513=CARTESIAN_POINT('',(28.4138909875563,2.22967153707894,33.8637293696319));
#51514=CARTESIAN_POINT('Origin',(30.,-1.32966554433622E-14,33.8637293696319));
#51515=CARTESIAN_POINT('Ctrl Pts',(28.4213568690146,2.19416546818595,33.8969505670841));
#51516=CARTESIAN_POINT('Ctrl Pts',(28.4176467275988,2.21181007417744,33.8804609779983));
#51517=CARTESIAN_POINT('Ctrl Pts',(28.4138909875569,2.22967153707594,33.8637293696347));
#51518=CARTESIAN_POINT('',(28.3695909952396,2.19748570867059,33.8637293696319));
#51519=CARTESIAN_POINT('Ctrl Pts',(28.3695909952423,2.19748570866909,33.8637293696347));
#51520=CARTESIAN_POINT('Ctrl Pts',(28.3854176684231,2.18839429204867,33.8804609779983));
#51521=CARTESIAN_POINT('Ctrl Pts',(28.4010521891798,2.17941325476839,33.8969505670841));
#51522=CARTESIAN_POINT('',(28.2438424197352,2.09835352500326,33.8637293696319));
#51523=CARTESIAN_POINT('Origin',(30.,-1.32966554433622E-14,33.8637293696319));
#51524=CARTESIAN_POINT('Ctrl Pts',(28.2540710604308,2.06354267577915,33.8969505670841));
#51525=CARTESIAN_POINT('Ctrl Pts',(28.2489879763122,2.08084179499845,33.8804609779983));
#51526=CARTESIAN_POINT('Ctrl Pts',(28.2438424197361,2.09835352500033,33.8637293696347));
#51527=CARTESIAN_POINT('',(28.2022042605027,2.0627911774245,33.8637293696319));
#51528=CARTESIAN_POINT('Ctrl Pts',(28.2022042605055,2.0627911774232,33.8637293696347));
#51529=CARTESIAN_POINT('Ctrl Pts',(28.2186954496616,2.05496953307227,33.8804609779984));
#51530=CARTESIAN_POINT('Ctrl Pts',(28.2349864184722,2.04724285169337,33.8969505670841));
#51531=CARTESIAN_POINT('',(28.0846211473781,1.95409846567259,33.8637293696319));
#51532=CARTESIAN_POINT('Origin',(30.,-1.32966554433622E-14,33.8637293696319));
#51533=CARTESIAN_POINT('Ctrl Pts',(28.0975494843397,1.92019745657863,33.8969505670841));
#51534=CARTESIAN_POINT('Ctrl Pts',(28.0911247964223,1.9370444342032,33.8804609779983));
#51535=CARTESIAN_POINT('Ctrl Pts',(28.0846211473792,1.95409846566974,33.8637293696347));
#51536=CARTESIAN_POINT('',(28.0459015343274,1.91537885262192,33.8637293696319));
#51537=CARTESIAN_POINT('Ctrl Pts',(28.0459015343303,1.91537885262084,33.8637293696347));
#51538=CARTESIAN_POINT('Ctrl Pts',(28.0629555657968,1.90887520357776,33.8804609779983));
#51539=CARTESIAN_POINT('Ctrl Pts',(28.0798025434214,1.90245051566032,33.8969505670841));
#51540=CARTESIAN_POINT('',(27.9372088225755,1.79779573949736,33.8637293696319));
#51541=CARTESIAN_POINT('Origin',(30.,-1.32966554433622E-14,33.8637293696319));
#51542=CARTESIAN_POINT('Ctrl Pts',(27.9527571483066,1.76501358152779,33.8969505670841));
#51543=CARTESIAN_POINT('Ctrl Pts',(27.9450304669277,1.78130455033841,33.8804609779983));
#51544=CARTESIAN_POINT('Ctrl Pts',(27.9372088225768,1.79779573949458,33.8637293696347));
#51545=CARTESIAN_POINT('',(27.9016464749967,1.75615758026483,33.8637293696319));
#51546=CARTESIAN_POINT('Ctrl Pts',(27.9016464749997,1.75615758026397,33.8637293696347));
#51547=CARTESIAN_POINT('Ctrl Pts',(27.9191582050016,1.75101202368779,33.8804609779983));
#51548=CARTESIAN_POINT('Ctrl Pts',(27.9364573242208,1.74592893956924,33.8969505670841));
#51549=CARTESIAN_POINT('',(27.8025142913294,1.63040900476038,33.8637293696319));
#51550=CARTESIAN_POINT('Origin',(30.,-1.32966554433622E-14,33.8637293696319));
#51551=CARTESIAN_POINT('Ctrl Pts',(27.8205867452316,1.59894781082027,33.8969505670841));
#51552=CARTESIAN_POINT('Ctrl Pts',(27.8116057079513,1.61458233157693,33.8804609779983));
#51553=CARTESIAN_POINT('Ctrl Pts',(27.8025142913309,1.63040900475771,33.8637293696347));
#51554=CARTESIAN_POINT('',(27.7703284629211,1.58610901244374,33.8637293696319));
#51555=CARTESIAN_POINT('Ctrl Pts',(27.7703284629241,1.58610901244311,33.8637293696347));
#51556=CARTESIAN_POINT('Ctrl Pts',(27.7881899258226,1.5823532724012,33.8804609779984));
#51557=CARTESIAN_POINT('Ctrl Pts',(27.8058345318141,1.57864313098542,33.8969505670841));
#51558=CARTESIAN_POINT('',(27.6813679902154,1.45297025634305,33.8637293696319));
#51559=CARTESIAN_POINT('Origin',(30.,-1.32966554433622E-14,33.8637293696319));
#51560=CARTESIAN_POINT('Ctrl Pts',(27.7018531496007,1.423023995155,33.8969505670841));
#51561=CARTESIAN_POINT('Ctrl Pts',(27.6916731275004,1.43790567583821,33.8804609779983));
#51562=CARTESIAN_POINT('Ctrl Pts',(27.6813679902172,1.45297025634054,33.8637293696347));
#51563=CARTESIAN_POINT('',(27.6527571173125,1.40628155512618,33.8637293696319));
#51564=CARTESIAN_POINT('Ctrl Pts',(27.6527571173155,1.40628155512578,33.8637293696347));
#51565=CARTESIAN_POINT('Ctrl Pts',(27.6708581912524,1.40393878700439,33.8804609779983));
#51566=CARTESIAN_POINT('Ctrl Pts',(27.6887394991527,1.40162446254697,33.8969505670841));
#51567=CARTESIAN_POINT('',(27.5745168264652,1.26657346313372,33.8637293696319));
#51568=CARTESIAN_POINT('Origin',(30.,-1.32966554433622E-14,33.8637293696319));
#51569=CARTESIAN_POINT('Ctrl Pts',(27.5972883935138,1.23832676335601,33.8969505670841));
#51570=CARTESIAN_POINT('Ctrl Pts',(27.5859721498149,1.2523638534557,33.8804609779984));
#51571=CARTESIAN_POINT('Ctrl Pts',(27.5745168264671,1.26657346313129,33.8637293696347));
#51572=CARTESIAN_POINT('',(27.5496573046132,1.21778390438518,33.8637293696319));
#51573=CARTESIAN_POINT('Ctrl Pts',(27.5496573046163,1.21778390438503,33.8637293696347));
#51574=CARTESIAN_POINT('Ctrl Pts',(27.5678863904514,1.21686855212868,33.8804609779984));
#51575=CARTESIAN_POINT('Ctrl Pts',(27.5858941560511,1.21596431320949,33.8969505670841));
#51576=CARTESIAN_POINT('',(27.4826195730347,1.07236782334576,33.8637293696319));
#51577=CARTESIAN_POINT('Origin',(30.,-1.32966554433622E-14,33.8637293696319));
#51578=CARTESIAN_POINT('Ctrl Pts',(27.5075371534637,1.04599483527557,33.8969505670841));
#51579=CARTESIAN_POINT('Ctrl Pts',(27.4951544565716,1.05910079146348,33.8804609779983));
#51580=CARTESIAN_POINT('Ctrl Pts',(27.4826195730368,1.07236782334352,33.8637293696347));
#51581=CARTESIAN_POINT('',(27.4616646694525,1.02177821091942,33.8637293696319));
#51582=CARTESIAN_POINT('Ctrl Pts',(27.4616646694556,1.0217782109195,33.8637293696347));
#51583=CARTESIAN_POINT('Ctrl Pts',(27.479909378813,1.02229591797925,33.8804609779983));
#51584=CARTESIAN_POINT('Ctrl Pts',(27.4979325782492,1.0228073395319,33.8969505670841));
#51585=CARTESIAN_POINT('',(27.4062428070505,0.871550679328378,33.8637293696319));
#51586=CARTESIAN_POINT('Origin',(30.,-1.32966554433622E-14,33.8637293696319));
#51587=CARTESIAN_POINT('Ctrl Pts',(27.4331527756904,0.847214001207086,33.8969505670841));
#51588=CARTESIAN_POINT('Ctrl Pts',(27.4197799690492,0.859308020905129,33.8804609779984));
#51589=CARTESIAN_POINT('Ctrl Pts',(27.4062428070528,0.871550679326332,33.8637293696347));
#51590=CARTESIAN_POINT('',(27.3893217156869,0.819472915007596,33.8637293696319));
#51591=CARTESIAN_POINT('Ctrl Pts',(27.3893217156899,0.819472915007932,33.8637293696347));
#51592=CARTESIAN_POINT('Ctrl Pts',(27.4074695638695,0.821420489547589,33.8804609779983));
#51593=CARTESIAN_POINT('Ctrl Pts',(27.4253970781241,0.823344418488154,33.8969505670841));
#51594=CARTESIAN_POINT('',(27.3458574166725,0.665360135552929,33.8637293696319));
#51595=CARTESIAN_POINT('Origin',(30.,-1.32966554433622E-14,33.8637293696319));
#51596=CARTESIAN_POINT('Ctrl Pts',(27.3745938646183,0.643209811093841,33.8969505670841));
#51597=CARTESIAN_POINT('Ctrl Pts',(27.3603133960278,0.654217330648928,33.8804609779983));
#51598=CARTESIAN_POINT('Ctrl Pts',(27.3458574166749,0.665360135551045,33.8637293696347));
#51599=CARTESIAN_POINT('',(27.3330744616826,0.612115296072357,33.8637293696319));
#51600=CARTESIAN_POINT('Ctrl Pts',(27.3330744616856,0.612115296072913,33.8637293696347));
#51601=CARTESIAN_POINT('Ctrl Pts',(27.3510135611686,0.615480730647817,33.8804609779983));
#51602=CARTESIAN_POINT('Ctrl Pts',(27.3687348611549,0.618805305314613,33.8969505670841));
#51603=CARTESIAN_POINT('',(27.3018356979128,0.455067425287102,33.8637293696319));
#51604=CARTESIAN_POINT('Origin',(30.,-1.32966554433622E-14,33.8637293696319));
#51605=CARTESIAN_POINT('Ctrl Pts',(27.332221455407,0.435240018606297,33.8969505670841));
#51606=CARTESIAN_POINT('Ctrl Pts',(27.3171213687048,0.445093172999983,33.8804609779983));
#51607=CARTESIAN_POINT('Ctrl Pts',(27.3018356979154,0.455067425285416,33.8637293696347));
#51608=CARTESIAN_POINT('',(27.2932696904648,0.400983782787843,33.8637293696319));
#51609=CARTESIAN_POINT('Ctrl Pts',(27.2932696904678,0.40098378278865,33.8637293696347));
#51610=CARTESIAN_POINT('Ctrl Pts',(27.3108894407404,0.405746328375518,33.8804609779983));
#51611=CARTESIAN_POINT('Ctrl Pts',(27.328295268751,0.410451051660182,33.8969505670841));
#51612=CARTESIAN_POINT('',(27.2744490593061,0.241969073019103,33.8637293696319));
#51613=CARTESIAN_POINT('Origin',(30.,-1.32966554433622E-14,33.8637293696319));
#51614=CARTESIAN_POINT('Ctrl Pts',(27.3062967880495,0.224586826672042,33.8969505670841));
#51615=CARTESIAN_POINT('Ctrl Pts',(27.2904701802914,0.233224867930985,33.8804609779983));
#51616=CARTESIAN_POINT('Ctrl Pts',(27.2744490593088,0.24196907301762,33.8637293696347));
#51617=CARTESIAN_POINT('',(27.2701528116845,0.1873800711418,33.8637293696319));
#51618=CARTESIAN_POINT('Ctrl Pts',(27.2701528116874,0.187380071142834,33.8637293696347));
#51619=CARTESIAN_POINT('Ctrl Pts',(27.2873445811301,0.193510365064418,33.8804609779983));
#51620=CARTESIAN_POINT('Ctrl Pts',(27.3043276244473,0.199566230783421,33.8969505670841));
#51621=CARTESIAN_POINT('',(27.2638663485864,0.0273789009530583,33.8637293696319));
#51622=CARTESIAN_POINT('Origin',(30.,-1.32966554433622E-14,33.8637293696319));
#51623=CARTESIAN_POINT('Ctrl Pts',(27.2969796967408,0.0125489822686371,
33.8969505670841));
#51624=CARTESIAN_POINT('Ctrl Pts',(27.2805241442266,0.0199186539960461,
33.8804609779983));
#51625=CARTESIAN_POINT('Ctrl Pts',(27.2638663485892,0.0273789009517924,
33.8637293696347));
#51626=CARTESIAN_POINT('',(27.2638663485864,-0.0273789009530277,33.8637293696319));
#51627=CARTESIAN_POINT('Ctrl Pts',(27.2638663485892,-0.0273789009517733,
33.8637293696347));
#51628=CARTESIAN_POINT('Ctrl Pts',(27.2805241442266,-0.0199186539960275,
33.8804609779983));
#51629=CARTESIAN_POINT('Ctrl Pts',(27.2969796967409,-0.012548982268619,
33.8969505670841));
#51630=CARTESIAN_POINT('',(27.2701528116845,-0.18738007114177,33.8637293696319));
#51631=CARTESIAN_POINT('Origin',(30.,-1.32966554433622E-14,33.8637293696319));
#51632=CARTESIAN_POINT('',(27.3043276244395,-0.199566230780611,33.8969505670765));
#51633=CARTESIAN_POINT('Ctrl Pts',(27.3043276244473,-0.199566230783401,
33.8969505670841));
#51634=CARTESIAN_POINT('Ctrl Pts',(27.2873445811301,-0.193510365064398,
33.8804609779983));
#51635=CARTESIAN_POINT('Ctrl Pts',(27.2701528116874,-0.187380071142813,
33.8637293696347));
#51636=CARTESIAN_POINT('',(27.3062967880422,-0.224586826675978,33.8969505670765));
#51637=CARTESIAN_POINT('Origin',(27.2996925411099,-0.212518788369432,33.8912937927564));
#51638=CARTESIAN_POINT('',(27.2744490593061,-0.241969073019072,33.8637293696319));
#51639=CARTESIAN_POINT('Ctrl Pts',(27.2744490593088,-0.241969073017592,
33.8637293696347));
#51640=CARTESIAN_POINT('Ctrl Pts',(27.2904701802914,-0.233224867930958,
33.8804609779983));
#51641=CARTESIAN_POINT('Ctrl Pts',(27.3062967880495,-0.224586826672017,
33.8969505670841));
#51642=CARTESIAN_POINT('',(27.2932696904648,-0.400983782787811,33.8637293696319));
#51643=CARTESIAN_POINT('Origin',(30.,-1.32966554433622E-14,33.8637293696319));
#51644=CARTESIAN_POINT('',(27.328295268743,-0.410451051657984,33.8969505670765));
#51645=CARTESIAN_POINT('Ctrl Pts',(27.328295268751,-0.410451051660133,33.8969505670841));
#51646=CARTESIAN_POINT('Ctrl Pts',(27.3108894407404,-0.40574632837547,33.8804609779983));
#51647=CARTESIAN_POINT('Ctrl Pts',(27.2932696904678,-0.400983782788603,
33.8637293696347));
#51648=CARTESIAN_POINT('',(27.3322214554001,-0.435240018610796,33.8969505670765));
#51649=CARTESIAN_POINT('Origin',(27.3246909766178,-0.423727307748468,33.8912940899386));
#51650=CARTESIAN_POINT('',(27.3018356979128,-0.45506742528707,33.8637293696319));
#51651=CARTESIAN_POINT('Ctrl Pts',(27.3018356979154,-0.455067425285398,
33.8637293696347));
#51652=CARTESIAN_POINT('Ctrl Pts',(27.3171213687048,-0.445093172999969,
33.8804609779984));
#51653=CARTESIAN_POINT('Ctrl Pts',(27.332221455407,-0.435240018606285,33.8969505670841));
#51654=CARTESIAN_POINT('',(27.3330744616826,-0.612115296072328,33.8637293696319));
#51655=CARTESIAN_POINT('Origin',(30.,-1.32966554433622E-14,33.8637293696319));
#51656=CARTESIAN_POINT('',(27.3687348611467,-0.618805305313063,33.8969505670765));
#51657=CARTESIAN_POINT('Ctrl Pts',(27.3687348611549,-0.618805305314591,
33.8969505670841));
#51658=CARTESIAN_POINT('Ctrl Pts',(27.3510135611686,-0.615480730647799,
33.8804609779983));
#51659=CARTESIAN_POINT('Ctrl Pts',(27.3330744616856,-0.6121152960729,33.8637293696347));
#51660=CARTESIAN_POINT('',(27.3745938646118,-0.643209811098888,33.8969505670765));
#51661=CARTESIAN_POINT('Origin',(27.3661835083535,-0.632323382398592,33.8912943077151));
#51662=CARTESIAN_POINT('',(27.3458574166725,-0.665360135552901,33.8637293696319));
#51663=CARTESIAN_POINT('Ctrl Pts',(27.345857416675,-0.665360135551053,33.8637293696347));
#51664=CARTESIAN_POINT('Ctrl Pts',(27.3603133960278,-0.654217330648938,
33.8804609779984));
#51665=CARTESIAN_POINT('Ctrl Pts',(27.3745938646183,-0.643209811093851,
33.8969505670841));
#51666=CARTESIAN_POINT('',(27.3893217156868,-0.819472915007569,33.8637293696319));
#51667=CARTESIAN_POINT('Origin',(30.,-1.32966554433622E-14,33.8637293696319));
#51668=CARTESIAN_POINT('',(27.4253970781159,-0.823344418487241,33.8969505670765));
#51669=CARTESIAN_POINT('Ctrl Pts',(27.4253970781241,-0.823344418488121,
33.8969505670841));
#51670=CARTESIAN_POINT('Ctrl Pts',(27.4074695638695,-0.821420489547552,
33.8804609779983));
#51671=CARTESIAN_POINT('Ctrl Pts',(27.3893217156899,-0.819472915007892,
33.8637293696347));
#51672=CARTESIAN_POINT('',(27.4331527756843,-0.847214001212589,33.8969505670765));
#51673=CARTESIAN_POINT('Origin',(27.4239143438363,-0.837020957758988,33.8912944725679));
#51674=CARTESIAN_POINT('',(27.4062428070504,-0.871550679328351,33.8637293696319));
#51675=CARTESIAN_POINT('Ctrl Pts',(27.4062428070527,-0.871550679326329,
33.8637293696347));
#51676=CARTESIAN_POINT('Ctrl Pts',(27.4197799690492,-0.859308020905111,
33.8804609779983));
#51677=CARTESIAN_POINT('Ctrl Pts',(27.4331527756904,-0.847214001207053,
33.8969505670841));
#51678=CARTESIAN_POINT('',(27.4616646694525,-1.02177821091939,33.8637293696319));
#51679=CARTESIAN_POINT('Origin',(30.,-1.32966554433622E-14,33.8637293696319));
#51680=CARTESIAN_POINT('',(27.4979325782409,-1.02280733953164,33.8969505670765));
#51681=CARTESIAN_POINT('Ctrl Pts',(27.4979325782492,-1.02280733953187,33.8969505670841));
#51682=CARTESIAN_POINT('Ctrl Pts',(27.479909378813,-1.02229591797922,33.8804609779983));
#51683=CARTESIAN_POINT('Ctrl Pts',(27.4616646694556,-1.02177821091947,33.8637293696347));
#51684=CARTESIAN_POINT('',(27.507537153458,-1.04599483528157,33.8969505670765));
#51685=CARTESIAN_POINT('Origin',(27.4975275671491,-1.03655801106889,33.8912946002427));
#51686=CARTESIAN_POINT('',(27.4826195730347,-1.07236782334573,33.8637293696319));
#51687=CARTESIAN_POINT('Ctrl Pts',(27.4826195730368,-1.07236782334351,33.8637293696347));
#51688=CARTESIAN_POINT('Ctrl Pts',(27.4951544565716,-1.05910079146347,33.8804609779983));
#51689=CARTESIAN_POINT('Ctrl Pts',(27.5075371534637,-1.04599483527557,33.8969505670841));
#51690=CARTESIAN_POINT('',(27.5496573046131,-1.21778390438516,33.8637293696319));
#51691=CARTESIAN_POINT('Origin',(30.,-1.32966554433622E-14,33.8637293696319));
#51692=CARTESIAN_POINT('',(27.5858941560428,-1.21596431320988,33.8969505670765));
#51693=CARTESIAN_POINT('Ctrl Pts',(27.5858941560511,-1.21596431320946,33.8969505670841));
#51694=CARTESIAN_POINT('Ctrl Pts',(27.5678863904513,-1.21686855212866,33.8804609779983));
#51695=CARTESIAN_POINT('Ctrl Pts',(27.5496573046162,-1.217783904385,33.8637293696347));
#51696=CARTESIAN_POINT('',(27.5972883935086,-1.23832676336246,33.8969505670765));
#51697=CARTESIAN_POINT('Origin',(27.5865693373251,-1.22970433386023,33.891294700665));
#51698=CARTESIAN_POINT('',(27.5745168264651,-1.2665734631337,33.8637293696319));
#51699=CARTESIAN_POINT('Ctrl Pts',(27.574516826467,-1.26657346313129,33.8637293696347));
#51700=CARTESIAN_POINT('Ctrl Pts',(27.5859721498149,-1.2523638534557,33.8804609779983));
#51701=CARTESIAN_POINT('Ctrl Pts',(27.5972883935138,-1.23832676335601,33.8969505670841));
#51702=CARTESIAN_POINT('',(27.6527571173125,-1.40628155512615,33.8637293696319));
#51703=CARTESIAN_POINT('Origin',(30.,-1.32966554433622E-14,33.8637293696319));
#51704=CARTESIAN_POINT('',(27.6887394991444,-1.40162446254801,33.8969505670765));
#51705=CARTESIAN_POINT('Ctrl Pts',(27.6887394991526,-1.40162446254695,33.8969505670841));
#51706=CARTESIAN_POINT('Ctrl Pts',(27.6708581912523,-1.40393878700437,33.8804609779983));
#51707=CARTESIAN_POINT('Ctrl Pts',(27.6527571173155,-1.40628155512576,33.8637293696347));
#51708=CARTESIAN_POINT('',(27.701853149596,-1.42302399516179,33.8969505670765));
#51709=CARTESIAN_POINT('Origin',(27.6904906884452,-1.4152691174526,33.8912947803756));
#51710=CARTESIAN_POINT('',(27.6813679902154,-1.45297025634303,33.8637293696319));
#51711=CARTESIAN_POINT('Ctrl Pts',(27.6813679902171,-1.4529702563405,33.8637293696347));
#51712=CARTESIAN_POINT('Ctrl Pts',(27.6916731275004,-1.43790567583818,33.8804609779983));
#51713=CARTESIAN_POINT('Ctrl Pts',(27.7018531496007,-1.42302399515497,33.8969505670841));
#51714=CARTESIAN_POINT('',(27.770328462921,-1.58610901244372,33.8637293696319));
#51715=CARTESIAN_POINT('Origin',(30.,-1.32966554433622E-14,33.8637293696319));
#51716=CARTESIAN_POINT('',(27.8058345318059,-1.5786431309871,33.8969505670765));
#51717=CARTESIAN_POINT('Ctrl Pts',(27.805834531814,-1.5786431309854,33.8969505670841));
#51718=CARTESIAN_POINT('Ctrl Pts',(27.7881899258225,-1.58235327240118,33.8804609779983));
#51719=CARTESIAN_POINT('Ctrl Pts',(27.770328462924,-1.5861090124431,33.8637293696347));
#51720=CARTESIAN_POINT('',(27.8205867452275,-1.59894781082744,33.8969505670765));
#51721=CARTESIAN_POINT('Origin',(27.8086509152839,-1.59210829514295,33.8912948438349));
#51722=CARTESIAN_POINT('',(27.8025142913294,-1.63040900476036,33.8637293696319));
#51723=CARTESIAN_POINT('Ctrl Pts',(27.8025142913309,-1.63040900475772,33.8637293696347));
#51724=CARTESIAN_POINT('Ctrl Pts',(27.8116057079513,-1.61458233157693,33.8804609779984));
#51725=CARTESIAN_POINT('Ctrl Pts',(27.8205867452316,-1.59894781082027,33.8969505670841));
#51726=CARTESIAN_POINT('',(27.9016464749967,-1.75615758026481,33.8637293696319));
#51727=CARTESIAN_POINT('Origin',(30.,-1.32966554433622E-14,33.8637293696319));
#51728=CARTESIAN_POINT('',(27.9364573242129,-1.74592893957155,33.8969505670765));
#51729=CARTESIAN_POINT('Ctrl Pts',(27.9364573242208,-1.74592893956922,33.8969505670841));
#51730=CARTESIAN_POINT('Ctrl Pts',(27.9191582050015,-1.75101202368778,33.8804609779983));
#51731=CARTESIAN_POINT('Ctrl Pts',(27.9016464749996,-1.75615758026396,33.8637293696347));
#51732=CARTESIAN_POINT('',(27.9527571483031,-1.76501358153525,33.8969505670765));
#51733=CARTESIAN_POINT('Origin',(27.9403215240917,-1.75913159602167,33.8912948941586));
#51734=CARTESIAN_POINT('',(27.9372088225755,-1.79779573949734,33.8637293696319));
#51735=CARTESIAN_POINT('Ctrl Pts',(27.9372088225768,-1.79779573949458,33.8637293696347));
#51736=CARTESIAN_POINT('Ctrl Pts',(27.9450304669278,-1.78130455033841,33.8804609779984));
#51737=CARTESIAN_POINT('Ctrl Pts',(27.9527571483066,-1.76501358152779,33.8969505670841));
#51738=CARTESIAN_POINT('',(28.0459015343274,-1.91537885262191,33.8637293696319));
#51739=CARTESIAN_POINT('Origin',(30.,-1.32966554433622E-14,33.8637293696319));
#51740=CARTESIAN_POINT('',(28.0798025434136,-1.90245051566325,33.8969505670765));
#51741=CARTESIAN_POINT('Ctrl Pts',(28.0798025434214,-1.90245051566032,33.8969505670841));
#51742=CARTESIAN_POINT('Ctrl Pts',(28.0629555657968,-1.90887520357775,33.8804609779983));
#51743=CARTESIAN_POINT('Ctrl Pts',(28.0459015343303,-1.91537885262082,33.8637293696347));
#51744=CARTESIAN_POINT('',(28.0975494843367,-1.92019745658631,33.8969505670765));
#51745=CARTESIAN_POINT('Origin',(28.0846907243829,-1.91530926701236,33.891294933562));
#51746=CARTESIAN_POINT('',(28.084621147378,-1.95409846567257,33.8637293696319));
#51747=CARTESIAN_POINT('Ctrl Pts',(28.0846211473791,-1.9540984656697,33.8637293696347));
#51748=CARTESIAN_POINT('Ctrl Pts',(28.0911247964222,-1.93704443420316,33.8804609779983));
#51749=CARTESIAN_POINT('Ctrl Pts',(28.0975494843396,-1.92019745657857,33.8969505670841));
#51750=CARTESIAN_POINT('',(28.2022042605026,-2.06279117742449,33.8637293696319));
#51751=CARTESIAN_POINT('Origin',(30.,-1.32966554433622E-14,33.8637293696319));
#51752=CARTESIAN_POINT('',(28.2349864184647,-2.04724285169689,33.8969505670765));
#51753=CARTESIAN_POINT('Ctrl Pts',(28.2349864184722,-2.04724285169334,33.8969505670841));
#51754=CARTESIAN_POINT('Ctrl Pts',(28.2186954496616,-2.05496953307223,33.8804609779983));
#51755=CARTESIAN_POINT('Ctrl Pts',(28.2022042605054,-2.06279117742317,33.8637293696347));
#51756=CARTESIAN_POINT('',(28.2540710604284,-2.06354267578707,33.8969505670765));
#51757=CARTESIAN_POINT('Origin',(28.2408684341297,-2.05967842174595,33.8912949636253));
#51758=CARTESIAN_POINT('',(28.2438424197351,-2.09835352500325,33.8637293696319));
#51759=CARTESIAN_POINT('Ctrl Pts',(28.243842419736,-2.09835352500031,33.8637293696347));
#51760=CARTESIAN_POINT('Ctrl Pts',(28.2489879763122,-2.08084179499844,33.8804609779983));
#51761=CARTESIAN_POINT('Ctrl Pts',(28.2540710604307,-2.06354267577914,33.8969505670841));
#51762=CARTESIAN_POINT('',(28.3695909952396,-2.19748570867058,33.8637293696319));
#51763=CARTESIAN_POINT('Origin',(30.,-1.32966554433622E-14,33.8637293696319));
#51764=CARTESIAN_POINT('',(28.4010521891725,-2.17941325477249,33.8969505670765));
#51765=CARTESIAN_POINT('Ctrl Pts',(28.4010521891797,-2.17941325476838,33.8969505670841));
#51766=CARTESIAN_POINT('Ctrl Pts',(28.385417668423,-2.18839429204864,33.8804609779983));
#51767=CARTESIAN_POINT('Ctrl Pts',(28.3695909952423,-2.19748570866905,33.8637293696347));
#51768=CARTESIAN_POINT('',(28.4213568690129,-2.19416546819403,33.8969505670765));
#51769=CARTESIAN_POINT('Origin',(28.4078917675746,-2.19134897714168,33.8912949854673));
#51770=CARTESIAN_POINT('',(28.4138909875562,-2.22967153707893,33.8637293696319));
#51771=CARTESIAN_POINT('Ctrl Pts',(28.4138909875569,-2.22967153707595,33.8637293696347));
#51772=CARTESIAN_POINT('Ctrl Pts',(28.4176467275988,-2.21181007417744,33.8804609779984));
#51773=CARTESIAN_POINT('Ctrl Pts',(28.4213568690146,-2.19416546818595,33.8969505670841));
#51774=CARTESIAN_POINT('',(28.5470297436569,-2.31863200978456,33.8637293696319));
#51775=CARTESIAN_POINT('Origin',(30.,-1.32966554433622E-14,33.8637293696319));
#51776=CARTESIAN_POINT('',(28.5769760048382,-2.29814685040397,33.8969505670765));
#51777=CARTESIAN_POINT('Ctrl Pts',(28.576976004845,-2.29814685039931,33.8969505670841));
#51778=CARTESIAN_POINT('Ctrl Pts',(28.5620943241618,-2.30832687249962,33.8804609779983));
#51779=CARTESIAN_POINT('Ctrl Pts',(28.5470297436595,-2.31863200978285,33.8637293696347));
#51780=CARTESIAN_POINT('',(28.5983755374519,-2.31126050085552,33.8969505670765));
#51781=CARTESIAN_POINT('Origin',(28.5847309718512,-2.30950914111276,33.891294999854));
#51782=CARTESIAN_POINT('',(28.5937184448738,-2.3472428826875,33.8637293696319));
#51783=CARTESIAN_POINT('Ctrl Pts',(28.5937184448742,-2.34724288268445,33.8637293696347));
#51784=CARTESIAN_POINT('Ctrl Pts',(28.5960612129955,-2.32914180874762,33.8804609779983));
#51785=CARTESIAN_POINT('Ctrl Pts',(28.598375537453,-2.31126050084731,33.8969505670841));
#51786=CARTESIAN_POINT('',(28.7334265368663,-2.42548317353484,33.8637293696319));
#51787=CARTESIAN_POINT('Origin',(30.,-1.32966554433622E-14,33.8637293696319));
#51788=CARTESIAN_POINT('',(28.7616732366375,-2.40271160649133,33.8969505670765));
#51789=CARTESIAN_POINT('Ctrl Pts',(28.761673236644,-2.40271160648615,33.8969505670841));
#51790=CARTESIAN_POINT('Ctrl Pts',(28.7476361465443,-2.41402785018505,33.8804609779983));
#51791=CARTESIAN_POINT('Ctrl Pts',(28.7334265368687,-2.42548317353292,33.8637293696347));
#51792=CARTESIAN_POINT('',(28.7840356867901,-2.41410584395713,33.8969505670765));
#51793=CARTESIAN_POINT('Origin',(28.7702957758346,-2.41343041757033,33.8912950072666));
#51794=CARTESIAN_POINT('',(28.7822160956148,-2.45034269538683,33.8637293696319));
#51795=CARTESIAN_POINT('Ctrl Pts',(28.782216095615,-2.45034269538378,33.8637293696347));
#51796=CARTESIAN_POINT('Ctrl Pts',(28.7831314478713,-2.43211360954867,33.8804609779983));
#51797=CARTESIAN_POINT('Ctrl Pts',(28.7840356867905,-2.41410584394888,33.8969505670841));
#51798=CARTESIAN_POINT('',(28.9276321766542,-2.51738042696528,33.8637293696319));
#51799=CARTESIAN_POINT('Origin',(30.,-1.32966554433622E-14,33.8637293696319));
#51800=CARTESIAN_POINT('',(28.9540051647184,-2.49246284654199,33.8969505670765));
#51801=CARTESIAN_POINT('Ctrl Pts',(28.9540051647244,-2.49246284653629,33.8969505670841));
#51802=CARTESIAN_POINT('Ctrl Pts',(28.9408992085365,-2.50484554342835,33.8804609779984));
#51803=CARTESIAN_POINT('Ctrl Pts',(28.9276321766564,-2.51738042696316,33.8637293696347));
#51804=CARTESIAN_POINT('',(28.9771926604683,-2.50206742175908,33.8969505670765));
#51805=CARTESIAN_POINT('Origin',(28.9634421120889,-2.50247209787259,33.8912950079413));
#51806=CARTESIAN_POINT('',(28.9782217890806,-2.53833533054747,33.8637293696319));
#51807=CARTESIAN_POINT('Ctrl Pts',(28.9782217890805,-2.53833533054441,33.8637293696347));
#51808=CARTESIAN_POINT('Ctrl Pts',(28.9777040820207,-2.52009062118697,33.8804609779983));
#51809=CARTESIAN_POINT('Ctrl Pts',(28.9771926604681,-2.50206742175082,33.8969505670841));
#51810=CARTESIAN_POINT('',(29.1284493206716,-2.59375719294953,33.8637293696319));
#51811=CARTESIAN_POINT('Origin',(30.,-1.32966554433622E-14,33.8637293696319));
#51812=CARTESIAN_POINT('',(29.1527859987874,-2.56684722431572,33.8969505670765));
#51813=CARTESIAN_POINT('Ctrl Pts',(29.1527859987929,-2.56684722430957,33.8969505670841));
#51814=CARTESIAN_POINT('Ctrl Pts',(29.1406919790949,-2.58022003095078,33.8804609779984));
#51815=CARTESIAN_POINT('Ctrl Pts',(29.1284493206736,-2.59375719294726,33.8637293696347));
#51816=CARTESIAN_POINT('',(29.1766555815127,-2.57460292188404,33.8969505670765));
#51817=CARTESIAN_POINT('Origin',(29.1629791704777,-2.57608521103258,33.8912950018861));
#51818=CARTESIAN_POINT('',(29.1805270849924,-2.61067828431313,33.8637293696319));
#51819=CARTESIAN_POINT('Ctrl Pts',(29.1805270849921,-2.61067828431009,33.8637293696347));
#51820=CARTESIAN_POINT('Ctrl Pts',(29.1785795104524,-2.59253043613049,33.8804609779983));
#51821=CARTESIAN_POINT('Ctrl Pts',(29.1766555815118,-2.57460292187582,33.8969505670841));
#51822=CARTESIAN_POINT('',(29.334639864447,-2.65414258332747,33.8637293696319));
#51823=CARTESIAN_POINT('Origin',(30.,-1.32966554433622E-14,33.8637293696319));
#51824=CARTESIAN_POINT('',(29.3567901889011,-2.62540613538822,33.8969505670765));
#51825=CARTESIAN_POINT('Ctrl Pts',(29.3567901889061,-2.62540613538166,33.8969505670841));
#51826=CARTESIAN_POINT('Ctrl Pts',(29.345782669351,-2.63968660397217,33.8804609779983));
#51827=CARTESIAN_POINT('Ctrl Pts',(29.3346398644489,-2.65414258332506,33.8637293696347));
#51828=CARTESIAN_POINT('',(29.3811946946869,-2.63126513885324,33.8969505670765));
#51829=CARTESIAN_POINT('Origin',(29.3676767399569,-2.63381590833404,33.8912949888765));
#51830=CARTESIAN_POINT('',(29.3878847039276,-2.66692553831738,33.8637293696319));
#51831=CARTESIAN_POINT('Ctrl Pts',(29.3878847039271,-2.66692553831437,33.8637293696347));
#51832=CARTESIAN_POINT('Ctrl Pts',(29.3845192693522,-2.64898643883142,33.8804609779983));
#51833=CARTESIAN_POINT('Ctrl Pts',(29.3811946946854,-2.63126513884512,33.8969505670841));
#51834=CARTESIAN_POINT('',(29.5449325747129,-2.69816430208721,33.8637293696319));
#51835=CARTESIAN_POINT('Origin',(30.,-1.32966554433622E-14,33.8637293696319));
#51836=CARTESIAN_POINT('',(29.5647599813891,-2.66777854459992,33.8969505670765));
#51837=CARTESIAN_POINT('Ctrl Pts',(29.5647599813936,-2.667778544593,33.8969505670841));
#51838=CARTESIAN_POINT('Ctrl Pts',(29.554906827,-2.68287863129519,33.8804609779983));
#51839=CARTESIAN_POINT('Ctrl Pts',(29.5449325747145,-2.69816430208464,33.8637293696347));
#51840=CARTESIAN_POINT('',(29.589548948342,-2.67170473125696,33.8969505670765));
#51841=CARTESIAN_POINT('Origin',(29.5762727932907,-2.67530826149246,33.8912949684251));
#51842=CARTESIAN_POINT('',(29.5990162172121,-2.70673030953517,33.8637293696319));
#51843=CARTESIAN_POINT('Ctrl Pts',(29.5990162172114,-2.70673030953221,33.8637293696347));
#51844=CARTESIAN_POINT('Ctrl Pts',(29.5942536716245,-2.68911055925957,33.8804609779984));
#51845=CARTESIAN_POINT('Ctrl Pts',(29.5895489483398,-2.67170473124899,33.8969505670841));
#51846=CARTESIAN_POINT('',(29.7580309269809,-2.72555094069392,33.8637293696319));
#51847=CARTESIAN_POINT('Origin',(30.,-1.32966554433622E-14,33.8637293696319));
#51848=CARTESIAN_POINT('',(29.775413173324,-2.69370321195777,33.8969505670765));
#51849=CARTESIAN_POINT('Ctrl Pts',(29.7754131733279,-2.6937032119505,33.8969505670841));
#51850=CARTESIAN_POINT('Ctrl Pts',(29.766775132069,-2.70952981970859,33.8804609779984));
#51851=CARTESIAN_POINT('Ctrl Pts',(29.7580309269823,-2.72555094069122,33.8637293696347));
#51852=CARTESIAN_POINT('',(29.8004337692193,-2.6956723755605,33.8969505670765));
#51853=CARTESIAN_POINT('Origin',(29.7874812679387,-2.70030645711978,33.8912949397144));
#51854=CARTESIAN_POINT('',(29.8126199288582,-2.72984718831551,33.8637293696319));
#51855=CARTESIAN_POINT('Ctrl Pts',(29.8126199288571,-2.72984718831264,33.8637293696347));
#51856=CARTESIAN_POINT('Ctrl Pts',(29.8064896349355,-2.7126554188699,33.8804609779983));
#51857=CARTESIAN_POINT('Ctrl Pts',(29.8004337692165,-2.69567237555272,33.8969505670841));
#51858=CARTESIAN_POINT('',(29.9726210990469,-2.73613365141358,33.8637293696319));
#51859=CARTESIAN_POINT('Origin',(30.,-1.32966554433622E-14,33.8637293696319));
#51860=CARTESIAN_POINT('',(29.987451017728,-2.70302030326669,33.8969505670765));
#51861=CARTESIAN_POINT('Ctrl Pts',(29.9874510177314,-2.70302030325915,33.8969505670841));
#51862=CARTESIAN_POINT('Ctrl Pts',(29.980081346004,-2.71947585577343,33.8804609779983));
#51863=CARTESIAN_POINT('Ctrl Pts',(29.9726210990482,-2.73613365141081,33.8637293696347));
#51864=CARTESIAN_POINT('Ctrl Pts',(30.,-2.69489040503949,33.9051095949605));
#51865=CARTESIAN_POINT('Ctrl Pts',(29.9982996971592,-2.69489040503949,33.9051095949605));
#51866=CARTESIAN_POINT('Ctrl Pts',(29.9965490639354,-2.69522714758869,33.9047710768107));
#51867=CARTESIAN_POINT('Ctrl Pts',(29.9934248389279,-2.69644647069985,33.9035459832655));
#51868=CARTESIAN_POINT('Ctrl Pts',(29.9920523583067,-2.69733049287042,33.9026580100842));
#51869=CARTESIAN_POINT('Ctrl Pts',(29.9894391186861,-2.69960157002983,33.9003782103613));
#51870=CARTESIAN_POINT('Ctrl Pts',(29.9882404972758,-2.7012574944688,33.8987170220582));
#51871=CARTESIAN_POINT('Ctrl Pts',(29.987451017728,-2.7030203032667,33.8969505670765));
#51872=CARTESIAN_POINT('',(30.,-2.73627063036813,33.8637293696319));
#51873=CARTESIAN_POINT('Origin',(30.,-1.32966554433622E-14,31.5762293696319));
#51874=CARTESIAN_POINT('',(30.012548982272,2.70302030326666,31.5905494329235));
#51875=CARTESIAN_POINT('',(30.,2.69489040503946,31.5823904050395));
#51876=CARTESIAN_POINT('Ctrl Pts',(30.012548982272,2.70302030326668,31.5905494329235));
#51877=CARTESIAN_POINT('Ctrl Pts',(30.0117595027242,2.70125749446877,31.5887829779419));
#51878=CARTESIAN_POINT('Ctrl Pts',(30.0105608813139,2.6996015700298,31.5871217896387));
#51879=CARTESIAN_POINT('Ctrl Pts',(30.0079476416933,2.69733049287039,31.5848419899159));
#51880=CARTESIAN_POINT('Ctrl Pts',(30.0065751610721,2.69644647069982,31.5839540167345));
#51881=CARTESIAN_POINT('Ctrl Pts',(30.0034509360646,2.69522714758867,31.5827289231894));
#51882=CARTESIAN_POINT('Ctrl Pts',(30.0017003028408,2.69489040503946,31.5823904050395));
#51883=CARTESIAN_POINT('Ctrl Pts',(30.,2.69489040503946,31.5823904050395));
#51884=CARTESIAN_POINT('',(30.0273789009535,2.73613365141461,31.6237706303691));
#51885=CARTESIAN_POINT('Ctrl Pts',(30.0273789009505,2.73613365140797,31.6237706303625));
#51886=CARTESIAN_POINT('Ctrl Pts',(30.0199186539932,2.71947585576695,31.6070390219952));
#51887=CARTESIAN_POINT('Ctrl Pts',(30.0125489822642,2.70302030324912,31.5905494329059));
#51888=CARTESIAN_POINT('',(30.1873800711414,2.72984718831658,31.6237706303691));
#51889=CARTESIAN_POINT('Origin',(30.,-1.32966554433622E-14,31.6237706303681));
#51890=CARTESIAN_POINT('',(30.1995662307806,2.69567237556048,31.5905494329235));
#51891=CARTESIAN_POINT('Ctrl Pts',(30.1995662307774,2.69567237556935,31.5905494329321));
#51892=CARTESIAN_POINT('Ctrl Pts',(30.1935103650619,2.71265541887687,31.6070390220085));
#51893=CARTESIAN_POINT('Ctrl Pts',(30.1873800711438,2.72984718830972,31.6237706303625));
#51894=CARTESIAN_POINT('',(30.224586826676,2.69370321195774,31.5905494329235));
#51895=CARTESIAN_POINT('Origin',(30.2125187883694,2.70030745889013,31.5962062072437));
#51896=CARTESIAN_POINT('',(30.2419690730196,2.72555094069491,31.6237706303691));
#51897=CARTESIAN_POINT('Ctrl Pts',(30.2419690730161,2.72555094068852,31.6237706303625));
#51898=CARTESIAN_POINT('Ctrl Pts',(30.2332248679276,2.70952981970239,31.6070390219952));
#51899=CARTESIAN_POINT('Ctrl Pts',(30.2245868266668,2.69370321194088,31.5905494329059));
#51900=CARTESIAN_POINT('',(30.4009837827875,2.70673030953627,31.6237706303691));
#51901=CARTESIAN_POINT('Origin',(30.,-1.32966554433622E-14,31.6237706303681));
#51902=CARTESIAN_POINT('',(30.410451051658,2.67170473125694,31.5905494329235));
#51903=CARTESIAN_POINT('Ctrl Pts',(30.4104510516555,2.67170473126603,31.5905494329321));
#51904=CARTESIAN_POINT('Ctrl Pts',(30.4057463283736,2.68911055926674,31.6070390220085));
#51905=CARTESIAN_POINT('Ctrl Pts',(30.4009837827894,2.70673030952925,31.6237706303625));
#51906=CARTESIAN_POINT('',(30.4352400186108,2.66777854459989,31.5905494329235));
#51907=CARTESIAN_POINT('Origin',(30.4237273077485,2.6753090233822,31.5962059100614));
#51908=CARTESIAN_POINT('',(30.4550674252877,2.69816430208816,31.6237706303691));
#51909=CARTESIAN_POINT('Ctrl Pts',(30.4550674252837,2.69816430208208,31.6237706303625));
#51910=CARTESIAN_POINT('Ctrl Pts',(30.4450931729961,2.68287863128927,31.6070390219952));
#51911=CARTESIAN_POINT('Ctrl Pts',(30.4352400186003,2.66777854458381,31.5905494329059));
#51912=CARTESIAN_POINT('',(30.6121152960721,2.6669255383185,31.6237706303691));
#51913=CARTESIAN_POINT('Origin',(30.,-1.32966554433622E-14,31.6237706303681));
#51914=CARTESIAN_POINT('',(30.6188053053131,2.63126513885322,31.5905494329235));
#51915=CARTESIAN_POINT('Ctrl Pts',(30.6188053053114,2.63126513886247,31.5905494329321));
#51916=CARTESIAN_POINT('Ctrl Pts',(30.6154807306465,2.64898643883871,31.6070390220085));
#51917=CARTESIAN_POINT('Ctrl Pts',(30.6121152960735,2.66692553831135,31.6237706303626));
#51918=CARTESIAN_POINT('',(30.6432098110989,2.62540613538819,31.5905494329235));
#51919=CARTESIAN_POINT('Origin',(30.6323233823986,2.63381649164648,31.5962056922849));
#51920=CARTESIAN_POINT('',(30.6653601355536,2.65414258332836,31.6237706303691));
#51921=CARTESIAN_POINT('Ctrl Pts',(30.6653601355491,2.65414258332261,31.6237706303625));
#51922=CARTESIAN_POINT('Ctrl Pts',(30.6542173306446,2.63968660396658,31.6070390219952));
#51923=CARTESIAN_POINT('Ctrl Pts',(30.6432098110871,2.62540613537299,31.5905494329059));
#51924=CARTESIAN_POINT('',(30.8194729150074,2.61067828431427,31.6237706303691));
#51925=CARTESIAN_POINT('Origin',(30.,-1.32966554433622E-14,31.6237706303681));
#51926=CARTESIAN_POINT('',(30.8233444184872,2.57460292188402,31.5905494329235));
#51927=CARTESIAN_POINT('Ctrl Pts',(30.8233444184862,2.57460292189339,31.5905494329321));
#51928=CARTESIAN_POINT('Ctrl Pts',(30.8214204895467,2.59253043613788,31.6070390220085));
#51929=CARTESIAN_POINT('Ctrl Pts',(30.8194729150082,2.61067828430704,31.6237706303625));
#51930=CARTESIAN_POINT('',(30.8472140012126,2.5668472243157,31.5905494329235));
#51931=CARTESIAN_POINT('Origin',(30.837020957759,2.57608565616362,31.596205527432));
#51932=CARTESIAN_POINT('',(30.8715506793291,2.59375719295037,31.6237706303691));
#51933=CARTESIAN_POINT('Ctrl Pts',(30.8715506793242,2.59375719294498,31.6237706303625));
#51934=CARTESIAN_POINT('Ctrl Pts',(30.8593080209003,2.58022003094555,31.6070390219952));
#51935=CARTESIAN_POINT('Ctrl Pts',(30.8472140011997,2.56684722430147,31.5905494329059));
#51936=CARTESIAN_POINT('',(31.0217782109193,2.53833533054861,31.6237706303691));
#51937=CARTESIAN_POINT('Origin',(30.,-1.32966554433622E-14,31.6237706303681));
#51938=CARTESIAN_POINT('',(31.0228073395316,2.50206742175906,31.5905494329235));
#51939=CARTESIAN_POINT('Ctrl Pts',(31.0228073395313,2.50206742176848,31.5905494329321));
#51940=CARTESIAN_POINT('Ctrl Pts',(31.022295917979,2.52009062119439,31.6070390220085));
#51941=CARTESIAN_POINT('Ctrl Pts',(31.0217782109195,2.53833533054134,31.6237706303625));
#51942=CARTESIAN_POINT('',(31.0459948352816,2.49246284654197,31.5905494329235));
#51943=CARTESIAN_POINT('Origin',(31.0365580110689,2.5024724328509,31.5962053997573));
#51944=CARTESIAN_POINT('',(31.0723678233466,2.51738042696606,31.6237706303691));
#51945=CARTESIAN_POINT('Ctrl Pts',(31.0723678233413,2.51738042696106,31.6237706303625));
#51946=CARTESIAN_POINT('Ctrl Pts',(31.0591007914584,2.50484554342351,31.6070390219952));
#51947=CARTESIAN_POINT('Ctrl Pts',(31.0459948352676,2.49246284652878,31.5905494329059));
#51948=CARTESIAN_POINT('',(31.2177839043852,2.45034269538797,31.6237706303691));
#51949=CARTESIAN_POINT('Origin',(30.,-1.32966554433622E-14,31.6237706303681));
#51950=CARTESIAN_POINT('',(31.2159643132099,2.41410584395711,31.5905494329235));
#51951=CARTESIAN_POINT('Ctrl Pts',(31.2159643132104,2.41410584396651,31.5905494329321));
#51952=CARTESIAN_POINT('Ctrl Pts',(31.216868552129,2.43211360955606,31.6070390220085));
#51953=CARTESIAN_POINT('Ctrl Pts',(31.2177839043849,2.4503426953807,31.6237706303625));
#51954=CARTESIAN_POINT('',(31.2383267633625,2.40271160649132,31.5905494329235));
#51955=CARTESIAN_POINT('Origin',(31.2297043338602,2.41343066267493,31.5962052993351));
#51956=CARTESIAN_POINT('',(31.2665734631346,2.42548317353555,31.6237706303691));
#51957=CARTESIAN_POINT('Ctrl Pts',(31.266573463129,2.42548317353098,31.6237706303625));
#51958=CARTESIAN_POINT('Ctrl Pts',(31.2523638534503,2.4140278501806,31.6070390219952));
#51959=CARTESIAN_POINT('Ctrl Pts',(31.2383267633475,2.40271160647926,31.5905494329059));
#51960=CARTESIAN_POINT('',(31.4062815551263,2.34724288268863,31.6237706303691));
#51961=CARTESIAN_POINT('Origin',(30.,-1.32966554433622E-14,31.6237706303681));
#51962=CARTESIAN_POINT('',(31.401624462548,2.3112605008555,31.5905494329235));
#51963=CARTESIAN_POINT('Ctrl Pts',(31.4016244625492,2.31126050086484,31.5905494329321));
#51964=CARTESIAN_POINT('Ctrl Pts',(31.4039387870053,2.32914180875499,31.6070390220085));
#51965=CARTESIAN_POINT('Ctrl Pts',(31.4062815551254,2.34724288268141,31.6237706303625));
#51966=CARTESIAN_POINT('',(31.4230239951618,2.29814685040396,31.5905494329235));
#51967=CARTESIAN_POINT('Origin',(31.4152691174526,2.30950931155475,31.5962052196244));
#51968=CARTESIAN_POINT('',(31.452970256344,2.3186320097852,31.6237706303691));
#51969=CARTESIAN_POINT('Ctrl Pts',(31.452970256338,2.31863200978109,31.6237706303625));
#51970=CARTESIAN_POINT('Ctrl Pts',(31.4379056758324,2.30832687249561,31.6070390219952));
#51971=CARTESIAN_POINT('Ctrl Pts',(31.4230239951459,2.2981468503931,31.5905494329059));
#51972=CARTESIAN_POINT('',(31.5861090124439,2.22967153708005,31.6237706303691));
#51973=CARTESIAN_POINT('Origin',(30.,-1.32966554433622E-14,31.6237706303681));
#51974=CARTESIAN_POINT('',(31.5786431309871,2.19416546819402,31.5905494329235));
#51975=CARTESIAN_POINT('Ctrl Pts',(31.578643130989,2.19416546820324,31.5905494329321));
#51976=CARTESIAN_POINT('Ctrl Pts',(31.5823532724027,2.21181007418469,31.6070390220085));
#51977=CARTESIAN_POINT('Ctrl Pts',(31.5861090124425,2.22967153707293,31.6237706303625));
#51978=CARTESIAN_POINT('',(31.5989478108274,2.17941325477248,31.5905494329235));
#51979=CARTESIAN_POINT('Origin',(31.5921082951429,2.19134908471604,31.596205156165));
#51980=CARTESIAN_POINT('',(31.6304090047614,2.19748570867114,31.6237706303691));
#51981=CARTESIAN_POINT('Ctrl Pts',(31.6304090047551,2.19748570866755,31.6237706303626));
#51982=CARTESIAN_POINT('Ctrl Pts',(31.6145823315708,2.18839429204514,31.6070390219952));
#51983=CARTESIAN_POINT('Ctrl Pts',(31.5989478108108,2.17941325476293,31.5905494329059));
#51984=CARTESIAN_POINT('',(31.7561575802651,2.09835352500435,31.6237706303691));
#51985=CARTESIAN_POINT('Origin',(30.,-1.32966554433622E-14,31.6237706303681));
#51986=CARTESIAN_POINT('',(31.7459289395715,2.06354267578706,31.5905494329235));
#51987=CARTESIAN_POINT('Ctrl Pts',(31.7459289395742,2.06354267579611,31.5905494329321));
#51988=CARTESIAN_POINT('Ctrl Pts',(31.7510120236898,2.08084179500558,31.6070390220085));
#51989=CARTESIAN_POINT('Ctrl Pts',(31.7561575802631,2.09835352499738,31.6237706303625));
#51990=CARTESIAN_POINT('',(31.7650135815352,2.04724285169688,31.5905494329235));
#51991=CARTESIAN_POINT('Origin',(31.7591315960216,2.05967847590828,31.5962051058414));
#51992=CARTESIAN_POINT('',(31.7977957394984,2.06279117742498,31.6237706303691));
#51993=CARTESIAN_POINT('Ctrl Pts',(31.7977957394918,2.06279117742187,31.6237706303625));
#51994=CARTESIAN_POINT('Ctrl Pts',(31.781304550332,2.05496953306921,31.6070390219952));
#51995=CARTESIAN_POINT('Ctrl Pts',(31.7650135815179,2.04724285168864,31.5905494329059));
#51996=CARTESIAN_POINT('',(31.9153788526223,1.95409846567364,31.6237706303691));
#51997=CARTESIAN_POINT('Origin',(30.,-1.32966554433622E-14,31.6237706303681));
#51998=CARTESIAN_POINT('',(31.9024505156632,1.9201974565863,31.5905494329235));
#51999=CARTESIAN_POINT('Ctrl Pts',(31.9024505156666,1.92019745659511,31.5905494329321));
#52000=CARTESIAN_POINT('Ctrl Pts',(31.9088752035804,1.93704443421013,31.6070390220085));
#52001=CARTESIAN_POINT('Ctrl Pts',(31.9153788526197,1.95409846566686,31.6237706303625));
#52002=CARTESIAN_POINT('',(31.9201974565863,1.90245051566323,31.5905494329235));
#52003=CARTESIAN_POINT('Origin',(31.9153092670123,1.91530927561703,31.596205066438));
#52004=CARTESIAN_POINT('',(31.9540984656736,1.91537885262231,31.6237706303691));
#52005=CARTESIAN_POINT('Ctrl Pts',(31.9540984656668,1.9153788526197,31.6237706303625));
#52006=CARTESIAN_POINT('Ctrl Pts',(31.9370444341966,1.90887520357521,31.6070390219952));
#52007=CARTESIAN_POINT('Ctrl Pts',(31.9201974565683,1.90245051565638,31.5905494329059));
#52008=CARTESIAN_POINT('',(32.062791177425,1.79779573949838,31.6237706303691));
#52009=CARTESIAN_POINT('Origin',(30.,-1.32966554433622E-14,31.6237706303681));
#52010=CARTESIAN_POINT('',(32.0472428516969,1.76501358153524,31.5905494329235));
#52011=CARTESIAN_POINT('Ctrl Pts',(32.0472428517009,1.76501358154374,31.5905494329321));
#52012=CARTESIAN_POINT('Ctrl Pts',(32.0549695330754,1.78130455034511,31.6070390220085));
#52013=CARTESIAN_POINT('Ctrl Pts',(32.0627911774219,1.7977957394918,31.6237706303625));
#52014=CARTESIAN_POINT('',(32.0635426757871,1.74592893957153,31.5905494329235));
#52015=CARTESIAN_POINT('Origin',(32.059678421746,1.75913156587022,31.5962050363748));
#52016=CARTESIAN_POINT('',(32.0983535250043,1.75615758026513,31.6237706303691));
#52017=CARTESIAN_POINT('Ctrl Pts',(32.0983535249974,1.75615758026307,31.6237706303625));
#52018=CARTESIAN_POINT('Ctrl Pts',(32.0808417949917,1.75101202368577,31.6070390219952));
#52019=CARTESIAN_POINT('Ctrl Pts',(32.0635426757687,1.74592893956612,31.5905494329059));
#52020=CARTESIAN_POINT('',(32.1974857086711,1.63040900476136,31.6237706303691));
#52021=CARTESIAN_POINT('Origin',(30.,-1.32966554433622E-14,31.6237706303681));
#52022=CARTESIAN_POINT('',(32.1794132547725,1.59894781082743,31.5905494329235));
#52023=CARTESIAN_POINT('Ctrl Pts',(32.1794132547772,1.59894781083559,31.5905494329321));
#52024=CARTESIAN_POINT('Ctrl Pts',(32.1883942920524,1.61458233158336,31.6070390220085));
#52025=CARTESIAN_POINT('Ctrl Pts',(32.1974857086675,1.63040900475503,31.6237706303625));
#52026=CARTESIAN_POINT('',(32.194165468194,1.57864313098709,31.5905494329235));
#52027=CARTESIAN_POINT('Origin',(32.1913489771416,1.59210823242537,31.5962050145327));
#52028=CARTESIAN_POINT('',(32.22967153708,1.58610901244395,31.6237706303691));
#52029=CARTESIAN_POINT('Ctrl Pts',(32.2296715370729,1.58610901244245,31.6237706303625));
#52030=CARTESIAN_POINT('Ctrl Pts',(32.2118100741705,1.58235327239971,31.6070390219952));
#52031=CARTESIAN_POINT('Ctrl Pts',(32.1941654681752,1.57864313098313,31.5905494329059));
#52032=CARTESIAN_POINT('',(32.3186320097852,1.45297025634397,31.6237706303691));
#52033=CARTESIAN_POINT('Origin',(30.,-1.32966554433622E-14,31.6237706303681));
#52034=CARTESIAN_POINT('',(32.298146850404,1.42302399516178,31.5905494329235));
#52035=CARTESIAN_POINT('Ctrl Pts',(32.2981468504093,1.42302399516954,31.5905494329321));
#52036=CARTESIAN_POINT('Ctrl Pts',(32.3083268725038,1.43790567584429,31.6070390220085));
#52037=CARTESIAN_POINT('Ctrl Pts',(32.3186320097811,1.45297025633794,31.6237706303625));
#52038=CARTESIAN_POINT('',(32.3112605008555,1.401624462548,31.5905494329235));
#52039=CARTESIAN_POINT('Origin',(32.3095091411128,1.41526902814876,31.596205000146));
#52040=CARTESIAN_POINT('',(32.3472428826886,1.40628155512629,31.6237706303691));
#52041=CARTESIAN_POINT('Ctrl Pts',(32.3472428826814,1.40628155512536,31.6237706303625));
#52042=CARTESIAN_POINT('Ctrl Pts',(32.3291418087406,1.40393878700346,31.6070390219952));
#52043=CARTESIAN_POINT('Ctrl Pts',(32.3112605008365,1.40162446254554,31.5905494329059));
#52044=CARTESIAN_POINT('',(32.4254831735355,1.26657346313459,31.6237706303691));
#52045=CARTESIAN_POINT('Origin',(30.,-1.32966554433622E-14,31.6237706303681));
#52046=CARTESIAN_POINT('',(32.4027116064913,1.23832676336245,31.5905494329235));
#52047=CARTESIAN_POINT('Ctrl Pts',(32.4027116064972,1.23832676336979,31.5905494329321));
#52048=CARTESIAN_POINT('Ctrl Pts',(32.4140278501897,1.2523638534615,31.6070390220085));
#52049=CARTESIAN_POINT('Ctrl Pts',(32.425483173531,1.26657346312893,31.6237706303625));
#52050=CARTESIAN_POINT('',(32.4141058439571,1.21596431320987,31.5905494329235));
#52051=CARTESIAN_POINT('Origin',(32.4134304175703,1.22970422416531,31.5962049927334));
#52052=CARTESIAN_POINT('',(32.450342695388,1.21778390438521,31.6237706303691));
#52053=CARTESIAN_POINT('Ctrl Pts',(32.4503426953807,1.21778390438485,31.6237706303625));
#52054=CARTESIAN_POINT('Ctrl Pts',(32.4321136095416,1.2168685521283,31.6070390219952));
#52055=CARTESIAN_POINT('Ctrl Pts',(32.4141058439379,1.21596431320891,31.5905494329059));
#52056=CARTESIAN_POINT('',(32.517380426966,1.07236782334656,31.6237706303691));
#52057=CARTESIAN_POINT('Origin',(30.,-1.32966554433622E-14,31.6237706303681));
#52058=CARTESIAN_POINT('',(32.492462846542,1.04599483528156,31.5905494329235));
#52059=CARTESIAN_POINT('Ctrl Pts',(32.4924628465485,1.04599483528841,31.5905494329321));
#52060=CARTESIAN_POINT('Ctrl Pts',(32.5048455434335,1.05910079146886,31.6070390220085));
#52061=CARTESIAN_POINT('Ctrl Pts',(32.5173804269611,1.07236782334125,31.6237706303625));
#52062=CARTESIAN_POINT('',(32.5020674217591,1.02280733953163,31.5905494329235));
#52063=CARTESIAN_POINT('Origin',(32.5024720978725,1.03655788791103,31.5962049920587));
#52064=CARTESIAN_POINT('',(32.5383353305486,1.02177821091935,31.6237706303691));
#52065=CARTESIAN_POINT('Ctrl Pts',(32.5383353305413,1.02177821091956,31.6237706303625));
#52066=CARTESIAN_POINT('Ctrl Pts',(32.5200906211799,1.02229591797942,31.6070390219952));
#52067=CARTESIAN_POINT('Ctrl Pts',(32.5020674217399,1.02280733953218,31.5905494329059));
#52068=CARTESIAN_POINT('',(32.5937571929504,0.87155067932912,31.6237706303691));
#52069=CARTESIAN_POINT('Origin',(30.,-1.32966554433622E-14,31.6237706303681));
#52070=CARTESIAN_POINT('',(32.5668472243157,0.84721400121258,31.5905494329235));
#52071=CARTESIAN_POINT('Ctrl Pts',(32.5668472243227,0.847214001218895,31.5905494329321));
#52072=CARTESIAN_POINT('Ctrl Pts',(32.5802200309563,0.859308020910075,31.6070390220085));
#52073=CARTESIAN_POINT('Ctrl Pts',(32.593757192945,0.871550679324244,31.6237706303625));
#52074=CARTESIAN_POINT('',(32.574602921884,0.823344418487232,31.5905494329235));
#52075=CARTESIAN_POINT('Origin',(32.5760852110325,0.837020829522203,31.5962049981138));
#52076=CARTESIAN_POINT('',(32.6106782843143,0.819472915007436,31.6237706303691));
#52077=CARTESIAN_POINT('Ctrl Pts',(32.6106782843071,0.819472915008212,31.6237706303625));
#52078=CARTESIAN_POINT('Ctrl Pts',(32.5925304361235,0.8214204895483,31.6070390219952));
#52079=CARTESIAN_POINT('Ctrl Pts',(32.5746029218649,0.823344418489286,31.5905494329059));
#52080=CARTESIAN_POINT('',(32.6541425833284,0.665360135553601,31.6237706303691));
#52081=CARTESIAN_POINT('Origin',(30.,-1.32966554433622E-14,31.6237706303681));
#52082=CARTESIAN_POINT('',(32.6254061353882,0.64320981109888,31.5905494329235));
#52083=CARTESIAN_POINT('Ctrl Pts',(32.6254061353957,0.643209811104633,31.5905494329321));
#52084=CARTESIAN_POINT('Ctrl Pts',(32.639686603978,0.654217330653466,31.6070390220085));
#52085=CARTESIAN_POINT('Ctrl Pts',(32.6541425833226,0.665360135549173,31.6237706303625));
#52086=CARTESIAN_POINT('',(32.6312651388532,0.618805305313054,31.5905494329235));
#52087=CARTESIAN_POINT('Origin',(32.633815908334,0.632323260043002,31.5962050111235));
#52088=CARTESIAN_POINT('',(32.6669255383185,0.612115296072106,31.6237706303691));
#52089=CARTESIAN_POINT('Ctrl Pts',(32.6669255383114,0.61211529607344,31.6237706303625));
#52090=CARTESIAN_POINT('Ctrl Pts',(32.6489864388245,0.61548073064908,31.6070390219952));
#52091=CARTESIAN_POINT('Ctrl Pts',(32.6312651388343,0.618805305316593,31.5905494329059));
#52092=CARTESIAN_POINT('',(32.6981643020882,0.455067425287697,31.6237706303691));
#52093=CARTESIAN_POINT('Origin',(30.,-1.32966554433622E-14,31.6237706303681));
#52094=CARTESIAN_POINT('',(32.6677785445999,0.435240018610789,31.5905494329235));
#52095=CARTESIAN_POINT('Ctrl Pts',(32.6677785446078,0.435240018615936,31.5905494329321));
#52096=CARTESIAN_POINT('Ctrl Pts',(32.6828786313014,0.44509317300403,31.6070390220085));
#52097=CARTESIAN_POINT('Ctrl Pts',(32.6981643020821,0.455067425283731,31.6237706303625));
#52098=CARTESIAN_POINT('',(32.6717047312569,0.410451051657977,31.5905494329235));
#52099=CARTESIAN_POINT('Origin',(32.6753082614925,0.423727206709275,31.596205031575));
#52100=CARTESIAN_POINT('',(32.7067303095363,0.400983782787501,31.6237706303691));
#52101=CARTESIAN_POINT('Ctrl Pts',(32.7067303095293,0.400983782789396,31.6237706303625));
#52102=CARTESIAN_POINT('Ctrl Pts',(32.6891105592528,0.405746328377311,31.6070390219952));
#52103=CARTESIAN_POINT('Ctrl Pts',(32.6717047312384,0.410451051662997,31.5905494329059));
#52104=CARTESIAN_POINT('',(32.7255509406949,0.24196907301962,31.6237706303691));
#52105=CARTESIAN_POINT('Origin',(30.,-1.32966554433622E-14,31.6237706303681));
#52106=CARTESIAN_POINT('',(32.6937032119577,0.224586826675969,31.5905494329235));
#52107=CARTESIAN_POINT('Ctrl Pts',(32.693703211966,0.224586826680493,31.5905494329321));
#52108=CARTESIAN_POINT('Ctrl Pts',(32.7095298197151,0.233224867934539,31.6070390220085));
#52109=CARTESIAN_POINT('Ctrl Pts',(32.7255509406885,0.241969073016156,31.6237706303625));
#52110=CARTESIAN_POINT('',(32.6956723755605,0.199566230780603,31.5905494329235));
#52111=CARTESIAN_POINT('Origin',(32.7003064571198,0.212518732061222,31.5962050602857));
#52112=CARTESIAN_POINT('',(32.7298471883166,0.187380071141372,31.6237706303691));
#52113=CARTESIAN_POINT('Ctrl Pts',(32.7298471883097,0.187380071143799,31.6237706303625));
#52114=CARTESIAN_POINT('Ctrl Pts',(32.7126554188632,0.193510365066728,31.6070390219952));
#52115=CARTESIAN_POINT('Ctrl Pts',(32.6956723755424,0.199566230787043,31.5905494329059));
#52116=CARTESIAN_POINT('',(32.7361336514146,0.0273789009534945,31.6237706303691));
#52117=CARTESIAN_POINT('Origin',(30.,-1.32966554433622E-14,31.6237706303681));
#52118=CARTESIAN_POINT('',(32.7030203032667,0.0125489822719939,31.5905494329235));
#52119=CARTESIAN_POINT('Ctrl Pts',(32.7030203032753,0.0125489822758371,
31.5905494329321));
#52120=CARTESIAN_POINT('Ctrl Pts',(32.7194758557802,0.0199186539990537,
31.6070390220085));
#52121=CARTESIAN_POINT('Ctrl Pts',(32.736133651408,0.0273789009505039,31.6237706303625));
#52122=CARTESIAN_POINT('',(32.7030203032667,-0.0125489822720396,31.5905494329235));
#52123=CARTESIAN_POINT('Origin',(32.7086563646858,6.24424376688964E-9,31.5962050859813));
#52124=CARTESIAN_POINT('',(32.7361336514146,-0.02737890095354,31.6237706303691));
#52125=CARTESIAN_POINT('Ctrl Pts',(32.736133651408,-0.0273789009505768,
31.6237706303625));
#52126=CARTESIAN_POINT('Ctrl Pts',(32.719475855767,-0.0199186539932038,
31.6070390219952));
#52127=CARTESIAN_POINT('Ctrl Pts',(32.7030203032491,-0.0125489822642076,
31.5905494329059));
#52128=CARTESIAN_POINT('',(32.7298471883166,-0.187380071141418,31.6237706303691));
#52129=CARTESIAN_POINT('Origin',(30.,-1.32966554433622E-14,31.6237706303681));
#52130=CARTESIAN_POINT('',(32.6956723755605,-0.199566230780649,31.5905494329235));
#52131=CARTESIAN_POINT('Ctrl Pts',(32.6956723755694,-0.199566230777489,
31.5905494329321));
#52132=CARTESIAN_POINT('Ctrl Pts',(32.7126554188769,-0.193510365061924,
31.6070390220085));
#52133=CARTESIAN_POINT('Ctrl Pts',(32.7298471883097,-0.187380071143864,
31.6237706303625));
#52134=CARTESIAN_POINT('',(32.6937032119577,-0.224586826676015,31.5905494329235));
#52135=CARTESIAN_POINT('Origin',(32.7003074588902,-0.212518788369472,31.5962062072437));
#52136=CARTESIAN_POINT('',(32.7255509406949,-0.241969073019665,31.6237706303691));
#52137=CARTESIAN_POINT('Ctrl Pts',(32.7255509406885,-0.241969073016199,
31.6237706303625));
#52138=CARTESIAN_POINT('Ctrl Pts',(32.7095298197024,-0.23322486792764,31.6070390219952));
#52139=CARTESIAN_POINT('Ctrl Pts',(32.6937032119408,-0.22458682666682,31.5905494329059));
#52140=CARTESIAN_POINT('',(32.7067303095363,-0.400983782787547,31.6237706303691));
#52141=CARTESIAN_POINT('Origin',(30.,-1.32966554433622E-14,31.6237706303681));
#52142=CARTESIAN_POINT('',(32.6717047312569,-0.410451051658023,31.5905494329235));
#52143=CARTESIAN_POINT('Ctrl Pts',(32.671704731266,-0.41045105165556,31.5905494329321));
#52144=CARTESIAN_POINT('Ctrl Pts',(32.6891105592667,-0.405746328373564,
31.6070390220085));
#52145=CARTESIAN_POINT('Ctrl Pts',(32.7067303095293,-0.40098378278943,31.6237706303625));
#52146=CARTESIAN_POINT('',(32.6677785445999,-0.435240018610835,31.5905494329235));
#52147=CARTESIAN_POINT('Origin',(32.6753090233822,-0.42372730774851,31.5962059100614));
#52148=CARTESIAN_POINT('',(32.6981643020882,-0.455067425287743,31.6237706303691));
#52149=CARTESIAN_POINT('Ctrl Pts',(32.6981643020821,-0.455067425283808,
31.6237706303625));
#52150=CARTESIAN_POINT('Ctrl Pts',(32.6828786312893,-0.445093172996188,
31.6070390219952));
#52151=CARTESIAN_POINT('Ctrl Pts',(32.6677785445838,-0.435240018600367,
31.5905494329059));
#52152=CARTESIAN_POINT('',(32.6669255383185,-0.612115296072152,31.6237706303691));
#52153=CARTESIAN_POINT('Origin',(30.,-1.32966554433622E-14,31.6237706303681));
#52154=CARTESIAN_POINT('',(32.6312651388532,-0.6188053053131,31.5905494329235));
#52155=CARTESIAN_POINT('Ctrl Pts',(32.6312651388625,-0.618805305311361,
31.5905494329321));
#52156=CARTESIAN_POINT('Ctrl Pts',(32.6489864388387,-0.615480730646455,
31.6070390220085));
#52157=CARTESIAN_POINT('Ctrl Pts',(32.6669255383114,-0.612115296073488,
31.6237706303625));
#52158=CARTESIAN_POINT('',(32.6254061353882,-0.643209811098926,31.5905494329235));
#52159=CARTESIAN_POINT('Origin',(32.6338164916465,-0.632323382398633,31.5962056922849));
#52160=CARTESIAN_POINT('',(32.6541425833284,-0.665360135553646,31.6237706303691));
#52161=CARTESIAN_POINT('Ctrl Pts',(32.6541425833226,-0.665360135549238,
31.6237706303625));
#52162=CARTESIAN_POINT('Ctrl Pts',(32.6396866039666,-0.654217330644686,
31.6070390219952));
#52163=CARTESIAN_POINT('Ctrl Pts',(32.625406135373,-0.643209811087222,31.5905494329059));
#52164=CARTESIAN_POINT('',(32.6106782843143,-0.819472915007481,31.6237706303691));
#52165=CARTESIAN_POINT('Origin',(30.,-1.32966554433622E-14,31.6237706303681));
#52166=CARTESIAN_POINT('',(32.574602921884,-0.823344418487278,31.5905494329235));
#52167=CARTESIAN_POINT('Ctrl Pts',(32.5746029218934,-0.823344418486272,
31.5905494329321));
#52168=CARTESIAN_POINT('Ctrl Pts',(32.5925304361379,-0.821420489546795,
31.6070390220085));
#52169=CARTESIAN_POINT('Ctrl Pts',(32.610678284307,-0.819472915008254,31.6237706303626));
#52170=CARTESIAN_POINT('',(32.5668472243157,-0.847214001212625,31.5905494329235));
#52171=CARTESIAN_POINT('Origin',(32.5760856561636,-0.837020957759021,31.596205527432));
#52172=CARTESIAN_POINT('',(32.5937571929504,-0.871550679329165,31.6237706303691));
#52173=CARTESIAN_POINT('Ctrl Pts',(32.593757192945,-0.871550679324299,31.6237706303625));
#52174=CARTESIAN_POINT('Ctrl Pts',(32.5802200309455,-0.859308020900409,
31.6070390219952));
#52175=CARTESIAN_POINT('Ctrl Pts',(32.5668472243014,-0.847214001199744,
31.5905494329059));
#52176=CARTESIAN_POINT('',(32.5383353305486,-1.02177821091939,31.6237706303691));
#52177=CARTESIAN_POINT('Origin',(30.,-1.32966554433622E-14,31.6237706303681));
#52178=CARTESIAN_POINT('',(32.5020674217591,-1.02280733953168,31.5905494329235));
#52179=CARTESIAN_POINT('Ctrl Pts',(32.5020674217685,-1.02280733953141,31.5905494329321));
#52180=CARTESIAN_POINT('Ctrl Pts',(32.5200906211944,-1.02229591797905,31.6070390220085));
#52181=CARTESIAN_POINT('Ctrl Pts',(32.5383353305413,-1.0217782109196,31.6237706303625));
#52182=CARTESIAN_POINT('',(32.492462846542,-1.0459948352816,31.5905494329235));
#52183=CARTESIAN_POINT('Origin',(32.5024724328509,-1.03655801106895,31.5962053997573));
#52184=CARTESIAN_POINT('',(32.517380426966,-1.07236782334661,31.6237706303691));
#52185=CARTESIAN_POINT('Ctrl Pts',(32.517380426961,-1.07236782334134,31.6237706303625));
#52186=CARTESIAN_POINT('Ctrl Pts',(32.5048455434235,-1.0591007914584,31.6070390219952));
#52187=CARTESIAN_POINT('Ctrl Pts',(32.4924628465288,-1.04599483526767,31.5905494329059));
#52188=CARTESIAN_POINT('',(32.450342695388,-1.21778390438525,31.6237706303691));
#52189=CARTESIAN_POINT('Origin',(30.,-1.32966554433622E-14,31.6237706303681));
#52190=CARTESIAN_POINT('',(32.4141058439571,-1.21596431320991,31.5905494329235));
#52191=CARTESIAN_POINT('Ctrl Pts',(32.4141058439665,-1.21596431321038,31.5905494329321));
#52192=CARTESIAN_POINT('Ctrl Pts',(32.4321136095561,-1.21686855212907,31.6070390220085));
#52193=CARTESIAN_POINT('Ctrl Pts',(32.4503426953807,-1.21778390438489,31.6237706303625));
#52194=CARTESIAN_POINT('',(32.4027116064913,-1.2383267633625,31.5905494329235));
#52195=CARTESIAN_POINT('Origin',(32.4134306626749,-1.2297043338603,31.5962052993351));
#52196=CARTESIAN_POINT('',(32.4254831735355,-1.26657346313463,31.6237706303691));
#52197=CARTESIAN_POINT('Ctrl Pts',(32.425483173531,-1.26657346312898,31.6237706303625));
#52198=CARTESIAN_POINT('Ctrl Pts',(32.4140278501806,-1.25236385345028,31.6070390219952));
#52199=CARTESIAN_POINT('Ctrl Pts',(32.4027116064792,-1.23832676334755,31.5905494329059));
#52200=CARTESIAN_POINT('',(32.3472428826886,-1.40628155512633,31.6237706303691));
#52201=CARTESIAN_POINT('Origin',(30.,-1.32966554433622E-14,31.6237706303681));
#52202=CARTESIAN_POINT('',(32.3112605008555,-1.40162446254804,31.5905494329235));
#52203=CARTESIAN_POINT('Ctrl Pts',(32.3112605008648,-1.40162446254925,31.5905494329321));
#52204=CARTESIAN_POINT('Ctrl Pts',(32.329141808755,-1.40393878700536,31.6070390220085));
#52205=CARTESIAN_POINT('Ctrl Pts',(32.3472428826814,-1.4062815551254,31.6237706303625));
#52206=CARTESIAN_POINT('',(32.2981468504039,-1.42302399516182,31.5905494329235));
#52207=CARTESIAN_POINT('Origin',(32.3095093115547,-1.41526911745265,31.5962052196244));
#52208=CARTESIAN_POINT('',(32.3186320097852,-1.45297025634402,31.6237706303691));
#52209=CARTESIAN_POINT('Ctrl Pts',(32.3186320097811,-1.45297025633802,31.6237706303625));
#52210=CARTESIAN_POINT('Ctrl Pts',(32.3083268724956,-1.43790567583238,31.6070390219952));
#52211=CARTESIAN_POINT('Ctrl Pts',(32.2981468503931,-1.42302399514595,31.5905494329059));
#52212=CARTESIAN_POINT('',(32.22967153708,-1.58610901244399,31.6237706303691));
#52213=CARTESIAN_POINT('Origin',(30.,-1.32966554433622E-14,31.6237706303681));
#52214=CARTESIAN_POINT('',(32.194165468194,-1.57864313098713,31.5905494329235));
#52215=CARTESIAN_POINT('Ctrl Pts',(32.1941654682032,-1.57864313098907,31.5905494329321));
#52216=CARTESIAN_POINT('Ctrl Pts',(32.2118100741847,-1.58235327240274,31.6070390220085));
#52217=CARTESIAN_POINT('Ctrl Pts',(32.2296715370729,-1.58610901244249,31.6237706303625));
#52218=CARTESIAN_POINT('',(32.1794132547725,-1.59894781082747,31.5905494329235));
#52219=CARTESIAN_POINT('Origin',(32.191349084716,-1.59210829514296,31.596205156165));
#52220=CARTESIAN_POINT('',(32.1974857086711,-1.6304090047614,31.6237706303691));
#52221=CARTESIAN_POINT('Ctrl Pts',(32.1974857086675,-1.63040900475512,31.6237706303625));
#52222=CARTESIAN_POINT('Ctrl Pts',(32.1883942920451,-1.61458233157088,31.6070390219952));
#52223=CARTESIAN_POINT('Ctrl Pts',(32.1794132547629,-1.59894781081085,31.5905494329059));
#52224=CARTESIAN_POINT('',(32.0983535250043,-1.75615758026517,31.6237706303691));
#52225=CARTESIAN_POINT('Origin',(30.,-1.32966554433622E-14,31.6237706303681));
#52226=CARTESIAN_POINT('',(32.063542675787,-1.74592893957158,31.5905494329235));
#52227=CARTESIAN_POINT('Ctrl Pts',(32.0635426757961,-1.74592893957424,31.5905494329321));
#52228=CARTESIAN_POINT('Ctrl Pts',(32.0808417950055,-1.75101202368991,31.6070390220085));
#52229=CARTESIAN_POINT('Ctrl Pts',(32.0983535249973,-1.75615758026313,31.6237706303625));
#52230=CARTESIAN_POINT('',(32.0472428516969,-1.76501358153528,31.5905494329235));
#52231=CARTESIAN_POINT('Origin',(32.0596784759083,-1.75913159602171,31.5962051058414));
#52232=CARTESIAN_POINT('',(32.062791177425,-1.79779573949842,31.6237706303691));
#52233=CARTESIAN_POINT('Ctrl Pts',(32.0627911774219,-1.79779573949184,31.6237706303625));
#52234=CARTESIAN_POINT('Ctrl Pts',(32.0549695330692,-1.78130455033205,31.6070390219952));
#52235=CARTESIAN_POINT('Ctrl Pts',(32.0472428516887,-1.76501358151791,31.5905494329059));
#52236=CARTESIAN_POINT('',(31.9540984656736,-1.91537885262235,31.6237706303691));
#52237=CARTESIAN_POINT('Origin',(30.,-1.32966554433622E-14,31.6237706303681));
#52238=CARTESIAN_POINT('',(31.9201974565863,-1.90245051566327,31.5905494329235));
#52239=CARTESIAN_POINT('Ctrl Pts',(31.9201974565951,-1.90245051566663,31.5905494329321));
#52240=CARTESIAN_POINT('Ctrl Pts',(31.9370444342101,-1.90887520358042,31.6070390220085));
#52241=CARTESIAN_POINT('Ctrl Pts',(31.9540984656668,-1.91537885261975,31.6237706303625));
#52242=CARTESIAN_POINT('',(31.9024505156632,-1.92019745658634,31.5905494329235));
#52243=CARTESIAN_POINT('Origin',(31.915309275617,-1.91530926701241,31.5962050664381));
#52244=CARTESIAN_POINT('',(31.9153788526223,-1.95409846567368,31.6237706303691));
#52245=CARTESIAN_POINT('Ctrl Pts',(31.9153788526197,-1.9540984656669,31.6237706303625));
#52246=CARTESIAN_POINT('Ctrl Pts',(31.9088752035752,-1.93704443419662,31.6070390219952));
#52247=CARTESIAN_POINT('Ctrl Pts',(31.9024505156564,-1.92019745656839,31.5905494329059));
#52248=CARTESIAN_POINT('',(31.7977957394984,-2.06279117742501,31.6237706303691));
#52249=CARTESIAN_POINT('Origin',(30.,-1.32966554433622E-14,31.6237706303681));
#52250=CARTESIAN_POINT('',(31.7650135815352,-2.04724285169692,31.5905494329235));
#52251=CARTESIAN_POINT('Ctrl Pts',(31.7650135815437,-2.04724285170096,31.5905494329321));
#52252=CARTESIAN_POINT('Ctrl Pts',(31.7813045503451,-2.05496953307547,31.6070390220085));
#52253=CARTESIAN_POINT('Ctrl Pts',(31.7977957394918,-2.06279117742192,31.6237706303625));
#52254=CARTESIAN_POINT('',(31.7459289395715,-2.0635426757871,31.5905494329235));
#52255=CARTESIAN_POINT('Origin',(31.7591315658702,-2.05967842174604,31.5962050363748));
#52256=CARTESIAN_POINT('',(31.7561575802651,-2.09835352500439,31.6237706303691));
#52257=CARTESIAN_POINT('Ctrl Pts',(31.7561575802631,-2.09835352499741,31.6237706303625));
#52258=CARTESIAN_POINT('Ctrl Pts',(31.7510120236858,-2.08084179499169,31.6070390219952));
#52259=CARTESIAN_POINT('Ctrl Pts',(31.7459289395661,-2.06354267576866,31.5905494329059));
#52260=CARTESIAN_POINT('',(31.6304090047613,-2.19748570867118,31.6237706303691));
#52261=CARTESIAN_POINT('Origin',(30.,-1.32966554433622E-14,31.6237706303681));
#52262=CARTESIAN_POINT('',(31.5989478108274,-2.17941325477251,31.5905494329235));
#52263=CARTESIAN_POINT('Ctrl Pts',(31.5989478108356,-2.17941325477721,31.5905494329321));
#52264=CARTESIAN_POINT('Ctrl Pts',(31.6145823315833,-2.18839429205237,31.6070390220085));
#52265=CARTESIAN_POINT('Ctrl Pts',(31.630409004755,-2.19748570866756,31.6237706303625));
#52266=CARTESIAN_POINT('',(31.5786431309871,-2.19416546819406,31.5905494329235));
#52267=CARTESIAN_POINT('Origin',(31.5921082324253,-2.19134897714169,31.5962050145327));
#52268=CARTESIAN_POINT('',(31.5861090124439,-2.22967153708009,31.6237706303691));
#52269=CARTESIAN_POINT('Ctrl Pts',(31.5861090124425,-2.22967153707296,31.6237706303625));
#52270=CARTESIAN_POINT('Ctrl Pts',(31.5823532723997,-2.21181007417054,31.6070390219952));
#52271=CARTESIAN_POINT('Ctrl Pts',(31.5786431309832,-2.19416546817524,31.5905494329059));
#52272=CARTESIAN_POINT('',(31.452970256344,-2.31863200978524,31.6237706303691));
#52273=CARTESIAN_POINT('Origin',(30.,-1.32966554433622E-14,31.6237706303681));
#52274=CARTESIAN_POINT('',(31.4230239951618,-2.29814685040399,31.5905494329235));
#52275=CARTESIAN_POINT('Ctrl Pts',(31.4230239951696,-2.2981468504093,31.5905494329321));
#52276=CARTESIAN_POINT('Ctrl Pts',(31.4379056758443,-2.30832687250383,31.6070390220085));
#52277=CARTESIAN_POINT('Ctrl Pts',(31.452970256338,-2.31863200978113,31.6237706303625));
#52278=CARTESIAN_POINT('',(31.401624462548,-2.31126050085554,31.5905494329235));
#52279=CARTESIAN_POINT('Origin',(31.4152690281487,-2.30950914111279,31.596205000146));
#52280=CARTESIAN_POINT('',(31.4062815551263,-2.34724288268866,31.6237706303691));
#52281=CARTESIAN_POINT('Ctrl Pts',(31.4062815551254,-2.34724288268144,31.6237706303625));
#52282=CARTESIAN_POINT('Ctrl Pts',(31.4039387870035,-2.32914180874065,31.6070390219952));
#52283=CARTESIAN_POINT('Ctrl Pts',(31.4016244625455,-2.31126050083648,31.5905494329059));
#52284=CARTESIAN_POINT('',(31.2665734631346,-2.42548317353559,31.6237706303691));
#52285=CARTESIAN_POINT('Origin',(30.,-1.32966554433622E-14,31.6237706303681));
#52286=CARTESIAN_POINT('',(31.2383267633624,-2.40271160649135,31.5905494329235));
#52287=CARTESIAN_POINT('Ctrl Pts',(31.2383267633697,-2.40271160649727,31.5905494329321));
#52288=CARTESIAN_POINT('Ctrl Pts',(31.2523638534615,-2.41402785018975,31.6070390220085));
#52289=CARTESIAN_POINT('Ctrl Pts',(31.2665734631289,-2.42548317353104,31.6237706303625));
#52290=CARTESIAN_POINT('',(31.2159643132098,-2.41410584395714,31.5905494329235));
#52291=CARTESIAN_POINT('Origin',(31.2297042241653,-2.41343041757036,31.5962049927334));
#52292=CARTESIAN_POINT('',(31.2177839043852,-2.450342695388,31.6237706303691));
#52293=CARTESIAN_POINT('Ctrl Pts',(31.2177839043848,-2.45034269538075,31.6237706303625));
#52294=CARTESIAN_POINT('Ctrl Pts',(31.2168685521282,-2.43211360954164,31.6070390219952));
#52295=CARTESIAN_POINT('Ctrl Pts',(31.2159643132088,-2.41410584393796,31.5905494329059));
#52296=CARTESIAN_POINT('',(31.0723678233465,-2.51738042696609,31.6237706303691));
#52297=CARTESIAN_POINT('Origin',(30.,-1.32966554433622E-14,31.6237706303681));
#52298=CARTESIAN_POINT('',(31.0459948352815,-2.49246284654201,31.5905494329235));
#52299=CARTESIAN_POINT('Ctrl Pts',(31.0459948352884,-2.49246284654849,31.5905494329321));
#52300=CARTESIAN_POINT('Ctrl Pts',(31.0591007914688,-2.5048455434335,31.6070390220085));
#52301=CARTESIAN_POINT('Ctrl Pts',(31.0723678233412,-2.51738042696111,31.6237706303625));
#52302=CARTESIAN_POINT('',(31.0228073395316,-2.5020674217591,31.5905494329235));
#52303=CARTESIAN_POINT('Origin',(31.036557887911,-2.50247209787259,31.5962049920587));
#52304=CARTESIAN_POINT('',(31.0217782109193,-2.53833533054864,31.6237706303691));
#52305=CARTESIAN_POINT('Ctrl Pts',(31.0217782109196,-2.53833533054137,31.6237706303625));
#52306=CARTESIAN_POINT('Ctrl Pts',(31.0222959179794,-2.52009062117993,31.6070390219952));
#52307=CARTESIAN_POINT('Ctrl Pts',(31.0228073395322,-2.50206742173989,31.5905494329059));
#52308=CARTESIAN_POINT('',(30.8715506793291,-2.59375719295041,31.6237706303691));
#52309=CARTESIAN_POINT('Origin',(30.,-1.32966554433622E-14,31.6237706303681));
#52310=CARTESIAN_POINT('',(30.8472140012126,-2.56684722431573,31.5905494329235));
#52311=CARTESIAN_POINT('Ctrl Pts',(30.8472140012189,-2.56684722432271,31.5905494329321));
#52312=CARTESIAN_POINT('Ctrl Pts',(30.8593080209101,-2.58022003095631,31.6070390220085));
#52313=CARTESIAN_POINT('Ctrl Pts',(30.8715506793242,-2.593757192945,31.6237706303625));
#52314=CARTESIAN_POINT('',(30.8233444184872,-2.57460292188405,31.5905494329235));
#52315=CARTESIAN_POINT('Origin',(30.8370208295222,-2.5760852110326,31.5962049981139));
#52316=CARTESIAN_POINT('',(30.8194729150074,-2.6106782843143,31.6237706303691));
#52317=CARTESIAN_POINT('Ctrl Pts',(30.8194729150082,-2.61067828430707,31.6237706303625));
#52318=CARTESIAN_POINT('Ctrl Pts',(30.8214204895483,-2.5925304361235,31.6070390219952));
#52319=CARTESIAN_POINT('Ctrl Pts',(30.8233444184892,-2.57460292186495,31.5905494329059));
#52320=CARTESIAN_POINT('',(30.6653601355536,-2.65414258332839,31.6237706303691));
#52321=CARTESIAN_POINT('Origin',(30.,-1.32966554433622E-14,31.6237706303681));
#52322=CARTESIAN_POINT('',(30.6432098110989,-2.62540613538822,31.5905494329235));
#52323=CARTESIAN_POINT('Ctrl Pts',(30.6432098111046,-2.62540613539568,31.5905494329321));
#52324=CARTESIAN_POINT('Ctrl Pts',(30.6542173306535,-2.63968660397806,31.6070390220085));
#52325=CARTESIAN_POINT('Ctrl Pts',(30.6653601355492,-2.65414258332262,31.6237706303625));
#52326=CARTESIAN_POINT('',(30.618805305313,-2.63126513885325,31.5905494329235));
#52327=CARTESIAN_POINT('Origin',(30.632323260043,-2.63381590833404,31.5962050111235));
#52328=CARTESIAN_POINT('',(30.6121152960721,-2.66692553831853,31.6237706303691));
#52329=CARTESIAN_POINT('Ctrl Pts',(30.6121152960734,-2.66692553831138,31.6237706303625));
#52330=CARTESIAN_POINT('Ctrl Pts',(30.615480730649,-2.6489864388245,31.6070390219952));
#52331=CARTESIAN_POINT('Ctrl Pts',(30.6188053053166,-2.63126513883437,31.5905494329059));
#52332=CARTESIAN_POINT('',(30.4550674252877,-2.69816430208819,31.6237706303691));
#52333=CARTESIAN_POINT('Origin',(30.,-1.32966554433622E-14,31.6237706303681));
#52334=CARTESIAN_POINT('',(30.4352400186108,-2.66777854459992,31.5905494329235));
#52335=CARTESIAN_POINT('Ctrl Pts',(30.435240018616,-2.6677785446078,31.5905494329321));
#52336=CARTESIAN_POINT('Ctrl Pts',(30.445093173004,-2.68287863130142,31.6070390220085));
#52337=CARTESIAN_POINT('Ctrl Pts',(30.4550674252837,-2.69816430208209,31.6237706303625));
#52338=CARTESIAN_POINT('',(30.410451051658,-2.67170473125697,31.5905494329235));
#52339=CARTESIAN_POINT('Origin',(30.4237272067093,-2.67530826149246,31.5962050315749));
#52340=CARTESIAN_POINT('',(30.4009837827875,-2.7067303095363,31.6237706303691));
#52341=CARTESIAN_POINT('Ctrl Pts',(30.4009837827894,-2.70673030952928,31.6237706303625));
#52342=CARTESIAN_POINT('Ctrl Pts',(30.4057463283773,-2.68911055925278,31.6070390219952));
#52343=CARTESIAN_POINT('Ctrl Pts',(30.410451051663,-2.67170473123841,31.5905494329059));
#52344=CARTESIAN_POINT('',(30.2419690730196,-2.72555094069494,31.6237706303691));
#52345=CARTESIAN_POINT('Origin',(30.,-1.32966554433622E-14,31.6237706303681));
#52346=CARTESIAN_POINT('',(30.224586826676,-2.69370321195777,31.5905494329235));
#52347=CARTESIAN_POINT('Ctrl Pts',(30.2245868266805,-2.69370321196604,31.5905494329321));
#52348=CARTESIAN_POINT('Ctrl Pts',(30.2332248679346,-2.70952981971513,31.6070390220085));
#52349=CARTESIAN_POINT('Ctrl Pts',(30.2419690730162,-2.72555094068854,31.6237706303625));
#52350=CARTESIAN_POINT('',(30.1995662307806,-2.69567237556051,31.5905494329235));
#52351=CARTESIAN_POINT('Origin',(30.2125187320612,-2.70030645711985,31.5962050602857));
#52352=CARTESIAN_POINT('',(30.1873800711414,-2.72984718831661,31.6237706303691));
#52353=CARTESIAN_POINT('Ctrl Pts',(30.1873800711438,-2.72984718830975,31.6237706303625));
#52354=CARTESIAN_POINT('Ctrl Pts',(30.1935103650667,-2.71265541886325,31.6070390219952));
#52355=CARTESIAN_POINT('Ctrl Pts',(30.199566230787,-2.6956723755424,31.5905494329059));
#52356=CARTESIAN_POINT('',(30.0273789009535,-2.73613365141464,31.6237706303691));
#52357=CARTESIAN_POINT('Origin',(30.,-1.32966554433622E-14,31.6237706303681));
#52358=CARTESIAN_POINT('',(30.012548982272,-2.70302030326669,31.5905494329235));
#52359=CARTESIAN_POINT('Ctrl Pts',(30.0125489822759,-2.70302030327528,31.5905494329321));
#52360=CARTESIAN_POINT('Ctrl Pts',(30.0199186539991,-2.7194758557802,31.6070390220085));
#52361=CARTESIAN_POINT('Ctrl Pts',(30.0273789009505,-2.736133651408,31.6237706303625));
#52362=CARTESIAN_POINT('',(29.987451017728,-2.70302030326669,31.5905494329235));
#52363=CARTESIAN_POINT('Origin',(30.,-2.7086657795165,31.5962151370754));
#52364=CARTESIAN_POINT('',(29.9726210990465,-2.73613365141464,31.6237706303691));
#52365=CARTESIAN_POINT('Ctrl Pts',(29.9726210990495,-2.73613365140799,31.6237706303625));
#52366=CARTESIAN_POINT('Ctrl Pts',(29.9800813460068,-2.71947585576697,31.6070390219952));
#52367=CARTESIAN_POINT('Ctrl Pts',(29.9874510177359,-2.70302030324915,31.5905494329059));
#52368=CARTESIAN_POINT('',(29.8126199288586,-2.72984718831661,31.6237706303691));
#52369=CARTESIAN_POINT('Origin',(30.,-1.32966554433622E-14,31.6237706303681));
#52370=CARTESIAN_POINT('',(29.8004337692193,-2.6956723755605,31.5905494329235));
#52371=CARTESIAN_POINT('Ctrl Pts',(29.8004337692225,-2.69567237556937,31.5905494329321));
#52372=CARTESIAN_POINT('Ctrl Pts',(29.806489634938,-2.71265541887691,31.6070390220085));
#52373=CARTESIAN_POINT('Ctrl Pts',(29.8126199288561,-2.72984718830976,31.6237706303625));
#52374=CARTESIAN_POINT('',(29.775413173324,-2.69370321195777,31.5905494329235));
#52375=CARTESIAN_POINT('Origin',(29.7874812116305,-2.70030745889015,31.5962062072437));
#52376=CARTESIAN_POINT('',(29.7580309269803,-2.72555094069494,31.6237706303691));
#52377=CARTESIAN_POINT('Ctrl Pts',(29.7580309269838,-2.72555094068855,31.6237706303625));
#52378=CARTESIAN_POINT('Ctrl Pts',(29.7667751320723,-2.7095298197024,31.6070390219952));
#52379=CARTESIAN_POINT('Ctrl Pts',(29.7754131733332,-2.69370321194088,31.5905494329059));
#52380=CARTESIAN_POINT('',(29.5990162172124,-2.70673030953629,31.6237706303691));
#52381=CARTESIAN_POINT('Origin',(30.,-1.32966554433622E-14,31.6237706303681));
#52382=CARTESIAN_POINT('',(29.589548948342,-2.67170473125696,31.5905494329235));
#52383=CARTESIAN_POINT('Ctrl Pts',(29.5895489483445,-2.67170473126605,31.5905494329321));
#52384=CARTESIAN_POINT('Ctrl Pts',(29.5942536716264,-2.68911055926676,31.6070390220085));
#52385=CARTESIAN_POINT('Ctrl Pts',(29.5990162172106,-2.70673030952926,31.6237706303625));
#52386=CARTESIAN_POINT('',(29.5647599813891,-2.66777854459992,31.5905494329235));
#52387=CARTESIAN_POINT('Origin',(29.5762726922515,-2.67530902338218,31.5962059100614));
#52388=CARTESIAN_POINT('',(29.5449325747122,-2.69816430208819,31.6237706303691));
#52389=CARTESIAN_POINT('Ctrl Pts',(29.5449325747162,-2.6981643020821,31.6237706303625));
#52390=CARTESIAN_POINT('Ctrl Pts',(29.5549068270038,-2.68287863128929,31.6070390219952));
#52391=CARTESIAN_POINT('Ctrl Pts',(29.5647599813996,-2.66777854458383,31.5905494329059));
#52392=CARTESIAN_POINT('',(29.3878847039278,-2.66692553831852,31.6237706303691));
#52393=CARTESIAN_POINT('Origin',(30.,-1.32966554433622E-14,31.6237706303681));
#52394=CARTESIAN_POINT('',(29.3811946946869,-2.63126513885324,31.5905494329235));
#52395=CARTESIAN_POINT('Ctrl Pts',(29.3811946946886,-2.63126513886249,31.5905494329321));
#52396=CARTESIAN_POINT('Ctrl Pts',(29.3845192693535,-2.64898643883873,31.6070390220085));
#52397=CARTESIAN_POINT('Ctrl Pts',(29.3878847039265,-2.66692553831137,31.6237706303625));
#52398=CARTESIAN_POINT('',(29.3567901889011,-2.62540613538822,31.5905494329235));
#52399=CARTESIAN_POINT('Origin',(29.3676766176013,-2.63381649164654,31.5962056922849));
#52400=CARTESIAN_POINT('',(29.3346398644463,-2.65414258332839,31.6237706303691));
#52401=CARTESIAN_POINT('Ctrl Pts',(29.3346398644508,-2.65414258332263,31.6237706303626));
#52402=CARTESIAN_POINT('Ctrl Pts',(29.3457826693553,-2.63968660396658,31.6070390219952));
#52403=CARTESIAN_POINT('Ctrl Pts',(29.3567901889128,-2.62540613537299,31.5905494329059));
#52404=CARTESIAN_POINT('',(29.1805270849925,-2.61067828431429,31.6237706303691));
#52405=CARTESIAN_POINT('Origin',(30.,-1.32966554433622E-14,31.6237706303681));
#52406=CARTESIAN_POINT('',(29.1766555815127,-2.57460292188404,31.5905494329235));
#52407=CARTESIAN_POINT('Ctrl Pts',(29.1766555815137,-2.5746029218934,31.5905494329321));
#52408=CARTESIAN_POINT('Ctrl Pts',(29.1785795104532,-2.59253043613788,31.6070390220085));
#52409=CARTESIAN_POINT('Ctrl Pts',(29.1805270849917,-2.61067828430705,31.6237706303625));
#52410=CARTESIAN_POINT('',(29.1527859987874,-2.56684722431572,31.5905494329235));
#52411=CARTESIAN_POINT('Origin',(29.162979042241,-2.57608565616368,31.5962055274321));
#52412=CARTESIAN_POINT('',(29.1284493206708,-2.59375719295039,31.6237706303691));
#52413=CARTESIAN_POINT('Ctrl Pts',(29.1284493206757,-2.593757192945,31.6237706303625));
#52414=CARTESIAN_POINT('Ctrl Pts',(29.1406919790996,-2.58022003094555,31.6070390219952));
#52415=CARTESIAN_POINT('Ctrl Pts',(29.1527859988003,-2.56684722430145,31.5905494329059));
#52416=CARTESIAN_POINT('',(28.9782217890806,-2.53833533054863,31.6237706303691));
#52417=CARTESIAN_POINT('Origin',(30.,-1.32966554433622E-14,31.6237706303681));
#52418=CARTESIAN_POINT('',(28.9771926604683,-2.50206742175908,31.5905494329235));
#52419=CARTESIAN_POINT('Ctrl Pts',(28.9771926604686,-2.50206742176849,31.5905494329321));
#52420=CARTESIAN_POINT('Ctrl Pts',(28.9777040820209,-2.5200906211944,31.6070390220085));
#52421=CARTESIAN_POINT('Ctrl Pts',(28.9782217890804,-2.53833533054136,31.6237706303625));
#52422=CARTESIAN_POINT('',(28.9540051647184,-2.49246284654199,31.5905494329235));
#52423=CARTESIAN_POINT('Origin',(28.963441988931,-2.50247243285095,31.5962053997573));
#52424=CARTESIAN_POINT('',(28.9276321766534,-2.51738042696608,31.6237706303691));
#52425=CARTESIAN_POINT('Ctrl Pts',(28.9276321766587,-2.51738042696105,31.6237706303625));
#52426=CARTESIAN_POINT('Ctrl Pts',(28.9408992085416,-2.5048455434235,31.6070390219952));
#52427=CARTESIAN_POINT('Ctrl Pts',(28.9540051647323,-2.49246284652876,31.5905494329059));
#52428=CARTESIAN_POINT('',(28.7822160956147,-2.45034269538798,31.6237706303691));
#52429=CARTESIAN_POINT('Origin',(30.,-1.32966554433622E-14,31.6237706303681));
#52430=CARTESIAN_POINT('',(28.7840356867901,-2.41410584395713,31.5905494329235));
#52431=CARTESIAN_POINT('Ctrl Pts',(28.7840356867896,-2.41410584396654,31.5905494329321));
#52432=CARTESIAN_POINT('Ctrl Pts',(28.783131447871,-2.43211360955609,31.6070390220085));
#52433=CARTESIAN_POINT('Ctrl Pts',(28.7822160956151,-2.45034269538072,31.6237706303625));
#52434=CARTESIAN_POINT('',(28.7616732366375,-2.40271160649133,31.5905494329235));
#52435=CARTESIAN_POINT('Origin',(28.7702956661397,-2.41343066267495,31.5962052993351));
#52436=CARTESIAN_POINT('',(28.7334265368654,-2.42548317353557,31.6237706303691));
#52437=CARTESIAN_POINT('Ctrl Pts',(28.7334265368711,-2.425483173531,31.6237706303625));
#52438=CARTESIAN_POINT('Ctrl Pts',(28.7476361465498,-2.41402785018062,31.6070390219952));
#52439=CARTESIAN_POINT('Ctrl Pts',(28.7616732366525,-2.40271160647928,31.5905494329059));
#52440=CARTESIAN_POINT('',(28.5937184448736,-2.34724288268865,31.6237706303691));
#52441=CARTESIAN_POINT('Origin',(30.,-1.32966554433622E-14,31.6237706303681));
#52442=CARTESIAN_POINT('',(28.5983755374519,-2.31126050085552,31.5905494329235));
#52443=CARTESIAN_POINT('Ctrl Pts',(28.5983755374507,-2.31126050086484,31.5905494329321));
#52444=CARTESIAN_POINT('Ctrl Pts',(28.5960612129946,-2.32914180875499,31.6070390220085));
#52445=CARTESIAN_POINT('Ctrl Pts',(28.5937184448745,-2.34724288268142,31.6237706303625));
#52446=CARTESIAN_POINT('',(28.5769760048382,-2.29814685040397,31.5905494329235));
#52447=CARTESIAN_POINT('Origin',(28.5847308825473,-2.30950931155478,31.5962052196244));
#52448=CARTESIAN_POINT('',(28.547029743656,-2.31863200978522,31.6237706303691));
#52449=CARTESIAN_POINT('Ctrl Pts',(28.547029743662,-2.31863200978111,31.6237706303625));
#52450=CARTESIAN_POINT('Ctrl Pts',(28.5620943241676,-2.30832687249563,31.6070390219952));
#52451=CARTESIAN_POINT('Ctrl Pts',(28.5769760048541,-2.29814685039312,31.5905494329059));
#52452=CARTESIAN_POINT('',(28.413890987556,-2.22967153708007,31.6237706303691));
#52453=CARTESIAN_POINT('Origin',(30.,-1.32966554433622E-14,31.6237706303681));
#52454=CARTESIAN_POINT('',(28.4213568690129,-2.19416546819403,31.5905494329235));
#52455=CARTESIAN_POINT('Ctrl Pts',(28.421356869011,-2.19416546820326,31.5905494329321));
#52456=CARTESIAN_POINT('Ctrl Pts',(28.4176467275973,-2.21181007418472,31.6070390220085));
#52457=CARTESIAN_POINT('Ctrl Pts',(28.4138909875575,-2.22967153707296,31.6237706303625));
#52458=CARTESIAN_POINT('',(28.4010521891725,-2.17941325477249,31.5905494329235));
#52459=CARTESIAN_POINT('Origin',(28.407891704857,-2.19134908471608,31.596205156165));
#52460=CARTESIAN_POINT('',(28.3695909952386,-2.19748570867116,31.6237706303691));
#52461=CARTESIAN_POINT('Ctrl Pts',(28.3695909952449,-2.19748570866753,31.6237706303625));
#52462=CARTESIAN_POINT('Ctrl Pts',(28.3854176684292,-2.18839429204513,31.6070390219952));
#52463=CARTESIAN_POINT('Ctrl Pts',(28.4010521891892,-2.17941325476292,31.5905494329059));
#52464=CARTESIAN_POINT('',(28.2438424197348,-2.09835352500436,31.6237706303691));
#52465=CARTESIAN_POINT('Origin',(30.,-1.32966554433622E-14,31.6237706303681));
#52466=CARTESIAN_POINT('',(28.2540710604284,-2.06354267578707,31.5905494329235));
#52467=CARTESIAN_POINT('Ctrl Pts',(28.2540710604258,-2.0635426757961,31.5905494329321));
#52468=CARTESIAN_POINT('Ctrl Pts',(28.2489879763101,-2.08084179500557,31.6070390220085));
#52469=CARTESIAN_POINT('Ctrl Pts',(28.2438424197369,-2.09835352499738,31.6237706303625));
#52470=CARTESIAN_POINT('',(28.2349864184647,-2.04724285169689,31.5905494329235));
#52471=CARTESIAN_POINT('Origin',(28.2408684039783,-2.05967847590829,31.5962051058414));
#52472=CARTESIAN_POINT('',(28.2022042605016,-2.06279117742499,31.6237706303691));
#52473=CARTESIAN_POINT('Ctrl Pts',(28.2022042605082,-2.06279117742185,31.6237706303625));
#52474=CARTESIAN_POINT('Ctrl Pts',(28.2186954496679,-2.0549695330692,31.6070390219952));
#52475=CARTESIAN_POINT('Ctrl Pts',(28.2349864184821,-2.04724285168864,31.5905494329059));
#52476=CARTESIAN_POINT('',(28.0846211473776,-1.95409846567366,31.6237706303691));
#52477=CARTESIAN_POINT('Origin',(30.,-1.32966554433622E-14,31.6237706303681));
#52478=CARTESIAN_POINT('',(28.0975494843367,-1.92019745658631,31.5905494329235));
#52479=CARTESIAN_POINT('Ctrl Pts',(28.0975494843333,-1.92019745659509,31.5905494329321));
#52480=CARTESIAN_POINT('Ctrl Pts',(28.0911247964195,-1.93704443421011,31.6070390220085));
#52481=CARTESIAN_POINT('Ctrl Pts',(28.0846211473802,-1.95409846566685,31.6237706303626));
#52482=CARTESIAN_POINT('',(28.0798025434136,-1.90245051566325,31.5905494329235));
#52483=CARTESIAN_POINT('Origin',(28.0846907329876,-1.91530927561707,31.5962050664381));
#52484=CARTESIAN_POINT('',(28.0459015343263,-1.91537885262232,31.6237706303691));
#52485=CARTESIAN_POINT('Ctrl Pts',(28.0459015343331,-1.91537885261973,31.6237706303625));
#52486=CARTESIAN_POINT('Ctrl Pts',(28.0629555658034,-1.90887520357524,31.6070390219952));
#52487=CARTESIAN_POINT('Ctrl Pts',(28.0798025434316,-1.90245051565641,31.5905494329059));
#52488=CARTESIAN_POINT('',(27.937208822575,-1.79779573949839,31.6237706303691));
#52489=CARTESIAN_POINT('Origin',(30.,-1.32966554433622E-14,31.6237706303681));
#52490=CARTESIAN_POINT('',(27.9527571483031,-1.76501358153525,31.5905494329235));
#52491=CARTESIAN_POINT('Ctrl Pts',(27.9527571482991,-1.76501358154376,31.5905494329321));
#52492=CARTESIAN_POINT('Ctrl Pts',(27.9450304669246,-1.78130455034514,31.6070390220085));
#52493=CARTESIAN_POINT('Ctrl Pts',(27.9372088225781,-1.79779573949183,31.6237706303625));
#52494=CARTESIAN_POINT('',(27.9364573242129,-1.74592893957155,31.5905494329235));
#52495=CARTESIAN_POINT('Origin',(27.940321578254,-1.75913156587022,31.5962050363747));
#52496=CARTESIAN_POINT('',(27.9016464749956,-1.75615758026514,31.6237706303691));
#52497=CARTESIAN_POINT('Ctrl Pts',(27.9016464750026,-1.75615758026309,31.6237706303625));
#52498=CARTESIAN_POINT('Ctrl Pts',(27.9191582050083,-1.75101202368579,31.6070390219952));
#52499=CARTESIAN_POINT('Ctrl Pts',(27.9364573242313,-1.74592893956614,31.5905494329059));
#52500=CARTESIAN_POINT('',(27.8025142913288,-1.63040900476137,31.6237706303691));
#52501=CARTESIAN_POINT('Origin',(30.,-1.32966554433622E-14,31.6237706303681));
#52502=CARTESIAN_POINT('',(27.8205867452275,-1.59894781082744,31.5905494329235));
#52503=CARTESIAN_POINT('Ctrl Pts',(27.8205867452228,-1.59894781083561,31.5905494329321));
#52504=CARTESIAN_POINT('Ctrl Pts',(27.8116057079476,-1.61458233158338,31.6070390220085));
#52505=CARTESIAN_POINT('Ctrl Pts',(27.8025142913325,-1.63040900475507,31.6237706303625));
#52506=CARTESIAN_POINT('',(27.8058345318059,-1.5786431309871,31.5905494329235));
#52507=CARTESIAN_POINT('Origin',(27.8086510228583,-1.5921082324254,31.5962050145327));
#52508=CARTESIAN_POINT('',(27.7703284629199,-1.58610901244396,31.6237706303691));
#52509=CARTESIAN_POINT('Ctrl Pts',(27.770328462927,-1.58610901244246,31.6237706303625));
#52510=CARTESIAN_POINT('Ctrl Pts',(27.7881899258294,-1.58235327239973,31.6070390219952));
#52511=CARTESIAN_POINT('Ctrl Pts',(27.8058345318247,-1.57864313098315,31.5905494329059));
#52512=CARTESIAN_POINT('',(27.6813679902147,-1.45297025634398,31.6237706303691));
#52513=CARTESIAN_POINT('Origin',(30.,-1.32966554433622E-14,31.6237706303681));
#52514=CARTESIAN_POINT('',(27.701853149596,-1.42302399516179,31.5905494329235));
#52515=CARTESIAN_POINT('Ctrl Pts',(27.7018531495907,-1.42302399516956,31.5905494329321));
#52516=CARTESIAN_POINT('Ctrl Pts',(27.6916731274962,-1.43790567584432,31.6070390220085));
#52517=CARTESIAN_POINT('Ctrl Pts',(27.6813679902189,-1.45297025633799,31.6237706303626));
#52518=CARTESIAN_POINT('',(27.6887394991444,-1.40162446254801,31.5905494329235));
#52519=CARTESIAN_POINT('Origin',(27.6904908588872,-1.41526902814876,31.596205000146));
#52520=CARTESIAN_POINT('',(27.6527571173113,-1.4062815551263,31.6237706303691));
#52521=CARTESIAN_POINT('Ctrl Pts',(27.6527571173185,-1.40628155512537,31.6237706303626));
#52522=CARTESIAN_POINT('Ctrl Pts',(27.6708581912593,-1.40393878700346,31.6070390219953));
#52523=CARTESIAN_POINT('Ctrl Pts',(27.6887394991635,-1.40162446254554,31.5905494329059));
#52524=CARTESIAN_POINT('',(27.5745168264644,-1.2665734631346,31.6237706303691));
#52525=CARTESIAN_POINT('Origin',(30.,-1.32966554433622E-14,31.6237706303681));
#52526=CARTESIAN_POINT('',(27.5972883935086,-1.23832676336246,31.5905494329235));
#52527=CARTESIAN_POINT('Ctrl Pts',(27.5972883935027,-1.23832676336977,31.5905494329321));
#52528=CARTESIAN_POINT('Ctrl Pts',(27.5859721498102,-1.25236385346148,31.6070390220085));
#52529=CARTESIAN_POINT('Ctrl Pts',(27.574516826469,-1.2665734631289,31.6237706303626));
#52530=CARTESIAN_POINT('',(27.5858941560428,-1.21596431320988,31.5905494329235));
#52531=CARTESIAN_POINT('Origin',(27.5865695824296,-1.22970422416533,31.5962049927334));
#52532=CARTESIAN_POINT('',(27.549657304612,-1.21778390438522,31.6237706303691));
#52533=CARTESIAN_POINT('Ctrl Pts',(27.5496573046193,-1.21778390438485,31.6237706303625));
#52534=CARTESIAN_POINT('Ctrl Pts',(27.5678863904584,-1.2168685521283,31.6070390219952));
#52535=CARTESIAN_POINT('Ctrl Pts',(27.585894156062,-1.21596431320891,31.5905494329059));
#52536=CARTESIAN_POINT('',(27.4826195730339,-1.07236782334657,31.6237706303691));
#52537=CARTESIAN_POINT('Origin',(30.,-1.32966554433622E-14,31.6237706303681));
#52538=CARTESIAN_POINT('',(27.507537153458,-1.04599483528157,31.5905494329235));
#52539=CARTESIAN_POINT('Ctrl Pts',(27.5075371534515,-1.04599483528841,31.5905494329321));
#52540=CARTESIAN_POINT('Ctrl Pts',(27.4951544565665,-1.05910079146888,31.6070390220085));
#52541=CARTESIAN_POINT('Ctrl Pts',(27.4826195730389,-1.07236782334129,31.6237706303626));
#52542=CARTESIAN_POINT('',(27.4979325782409,-1.02280733953164,31.5905494329235));
#52543=CARTESIAN_POINT('Origin',(27.4975279021274,-1.03655788791105,31.5962049920587));
#52544=CARTESIAN_POINT('',(27.4616646694513,-1.02177821091936,31.6237706303691));
#52545=CARTESIAN_POINT('Ctrl Pts',(27.4616646694586,-1.02177821091956,31.6237706303626));
#52546=CARTESIAN_POINT('Ctrl Pts',(27.4799093788201,-1.02229591797942,31.6070390219952));
#52547=CARTESIAN_POINT('Ctrl Pts',(27.4979325782601,-1.02280733953218,31.5905494329059));
#52548=CARTESIAN_POINT('',(27.4062428070496,-0.871550679329129,31.6237706303691));
#52549=CARTESIAN_POINT('Origin',(30.,-1.32966554433622E-14,31.6237706303681));
#52550=CARTESIAN_POINT('',(27.4331527756843,-0.847214001212589,31.5905494329235));
#52551=CARTESIAN_POINT('Ctrl Pts',(27.4331527756773,-0.847214001218912,
31.5905494329321));
#52552=CARTESIAN_POINT('Ctrl Pts',(27.4197799690437,-0.859308020910092,
31.6070390220085));
#52553=CARTESIAN_POINT('Ctrl Pts',(27.406242807055,-0.871550679324261,31.6237706303625));
#52554=CARTESIAN_POINT('',(27.4253970781159,-0.823344418487241,31.5905494329235));
#52555=CARTESIAN_POINT('Origin',(27.4239147889674,-0.837020829522197,31.5962049981138));
#52556=CARTESIAN_POINT('',(27.3893217156857,-0.819472915007445,31.6237706303691));
#52557=CARTESIAN_POINT('Ctrl Pts',(27.3893217156929,-0.819472915008222,
31.6237706303625));
#52558=CARTESIAN_POINT('Ctrl Pts',(27.4074695638765,-0.821420489548307,
31.6070390219952));
#52559=CARTESIAN_POINT('Ctrl Pts',(27.425397078135,-0.823344418489291,31.590549432906));
#52560=CARTESIAN_POINT('',(27.3458574166716,-0.665360135553609,31.6237706303691));
#52561=CARTESIAN_POINT('Origin',(30.,-1.32966554433622E-14,31.6237706303681));
#52562=CARTESIAN_POINT('',(27.3745938646118,-0.643209811098888,31.5905494329235));
#52563=CARTESIAN_POINT('Ctrl Pts',(27.3745938646043,-0.643209811104637,
31.5905494329321));
#52564=CARTESIAN_POINT('Ctrl Pts',(27.3603133960219,-0.65421733065347,31.6070390220085));
#52565=CARTESIAN_POINT('Ctrl Pts',(27.3458574166774,-0.665360135549176,
31.6237706303625));
#52566=CARTESIAN_POINT('',(27.3687348611467,-0.618805305313063,31.5905494329235));
#52567=CARTESIAN_POINT('Origin',(27.3661840916659,-0.632323260043008,31.5962050111235));
#52568=CARTESIAN_POINT('',(27.3330744616815,-0.612115296072114,31.6237706303691));
#52569=CARTESIAN_POINT('Ctrl Pts',(27.3330744616886,-0.612115296073467,
31.6237706303625));
#52570=CARTESIAN_POINT('Ctrl Pts',(27.3510135611755,-0.615480730649101,
31.6070390219952));
#52571=CARTESIAN_POINT('Ctrl Pts',(27.3687348611656,-0.61880530531661,31.590549432906));
#52572=CARTESIAN_POINT('',(27.3018356979118,-0.455067425287704,31.6237706303691));
#52573=CARTESIAN_POINT('Origin',(30.,-1.32966554433622E-14,31.6237706303681));
#52574=CARTESIAN_POINT('',(27.3322214554001,-0.435240018610796,31.5905494329235));
#52575=CARTESIAN_POINT('Ctrl Pts',(27.3322214553922,-0.435240018615941,
31.5905494329321));
#52576=CARTESIAN_POINT('Ctrl Pts',(27.3171213686986,-0.445093173004034,
31.6070390220085));
#52577=CARTESIAN_POINT('Ctrl Pts',(27.3018356979179,-0.455067425283735,
31.6237706303625));
#52578=CARTESIAN_POINT('',(27.328295268743,-0.410451051657984,31.5905494329235));
#52579=CARTESIAN_POINT('Origin',(27.3246917385075,-0.423727206709274,31.5962050315749));
#52580=CARTESIAN_POINT('',(27.2932696904637,-0.400983782787508,31.6237706303691));
#52581=CARTESIAN_POINT('Ctrl Pts',(27.2932696904707,-0.400983782789399,
31.6237706303625));
#52582=CARTESIAN_POINT('Ctrl Pts',(27.3108894407472,-0.405746328377308,
31.6070390219952));
#52583=CARTESIAN_POINT('Ctrl Pts',(27.3282952687616,-0.410451051662988,
31.5905494329059));
#52584=CARTESIAN_POINT('',(27.274449059305,-0.241969073019628,31.6237706303691));
#52585=CARTESIAN_POINT('Origin',(30.,-1.32966554433622E-14,31.6237706303681));
#52586=CARTESIAN_POINT('',(27.3062967880422,-0.224586826675978,31.5905494329235));
#52587=CARTESIAN_POINT('Ctrl Pts',(27.306296788034,-0.224586826680481,31.5905494329321));
#52588=CARTESIAN_POINT('Ctrl Pts',(27.2904701802848,-0.233224867934527,
31.6070390220085));
#52589=CARTESIAN_POINT('Ctrl Pts',(27.2744490593114,-0.241969073016143,
31.6237706303626));
#52590=CARTESIAN_POINT('',(27.3043276244395,-0.199566230780611,31.5905494329235));
#52591=CARTESIAN_POINT('Origin',(27.2996935428802,-0.212518732061225,31.5962050602856));
#52592=CARTESIAN_POINT('',(27.2701528116834,-0.18738007114138,31.6237706303691));
#52593=CARTESIAN_POINT('Ctrl Pts',(27.2701528116903,-0.187380071143839,
31.6237706303625));
#52594=CARTESIAN_POINT('Ctrl Pts',(27.2873445811368,-0.193510365066767,
31.6070390219952));
#52595=CARTESIAN_POINT('Ctrl Pts',(27.3043276244576,-0.199566230787083,
31.5905494329059));
#52596=CARTESIAN_POINT('',(27.2638663485853,-0.027378900953502,31.6237706303691));
#52597=CARTESIAN_POINT('Origin',(30.,-1.32966554433622E-14,31.6237706303681));
#52598=CARTESIAN_POINT('Ctrl Pts',(27.2969796967247,-0.0125489822758455,
31.5905494329321));
#52599=CARTESIAN_POINT('Ctrl Pts',(27.2805241442198,-0.0199186539990725,
31.6070390220085));
#52600=CARTESIAN_POINT('Ctrl Pts',(27.263866348592,-0.0273789009505331,
31.6237706303626));
#52601=CARTESIAN_POINT('',(27.2638663485853,0.0273789009535324,31.6237706303691));
#52602=CARTESIAN_POINT('Ctrl Pts',(27.263866348592,0.0273789009505529,31.6237706303626));
#52603=CARTESIAN_POINT('Ctrl Pts',(27.280524144233,0.0199186539931685,31.6070390219952));
#52604=CARTESIAN_POINT('Ctrl Pts',(27.2969796967508,0.012548982264161,31.5905494329059));
#52605=CARTESIAN_POINT('',(27.2701528116834,0.187380071141411,31.6237706303691));
#52606=CARTESIAN_POINT('Origin',(30.,-1.32966554433622E-14,31.6237706303681));
#52607=CARTESIAN_POINT('Ctrl Pts',(27.3043276244306,0.199566230777481,31.5905494329321));
#52608=CARTESIAN_POINT('Ctrl Pts',(27.2873445811231,0.193510365061917,31.6070390220085));
#52609=CARTESIAN_POINT('Ctrl Pts',(27.2701528116902,0.187380071143857,31.6237706303625));
#52610=CARTESIAN_POINT('',(27.2744490593051,0.241969073019658,31.6237706303691));
#52611=CARTESIAN_POINT('Ctrl Pts',(27.2744490593115,0.241969073016152,31.6237706303625));
#52612=CARTESIAN_POINT('Ctrl Pts',(27.2904701802976,0.233224867927605,31.6070390219952));
#52613=CARTESIAN_POINT('Ctrl Pts',(27.3062967880591,0.224586826666795,31.5905494329059));
#52614=CARTESIAN_POINT('',(27.2932696904637,0.40098378278754,31.6237706303691));
#52615=CARTESIAN_POINT('Origin',(30.,-1.32966554433622E-14,31.6237706303681));
#52616=CARTESIAN_POINT('Ctrl Pts',(27.3282952687339,0.410451051655568,31.5905494329321));
#52617=CARTESIAN_POINT('Ctrl Pts',(27.3108894407332,0.405746328373579,31.6070390220085));
#52618=CARTESIAN_POINT('Ctrl Pts',(27.2932696904707,0.400983782789452,31.6237706303626));
#52619=CARTESIAN_POINT('',(27.3018356979118,0.455067425287736,31.6237706303691));
#52620=CARTESIAN_POINT('Ctrl Pts',(27.3018356979179,0.455067425283746,31.6237706303626));
#52621=CARTESIAN_POINT('Ctrl Pts',(27.3171213687107,0.445093172996126,31.6070390219952));
#52622=CARTESIAN_POINT('Ctrl Pts',(27.3322214554162,0.435240018600305,31.5905494329059));
#52623=CARTESIAN_POINT('',(27.3330744616815,0.612115296072143,31.6237706303691));
#52624=CARTESIAN_POINT('Origin',(30.,-1.32966554433622E-14,31.6237706303681));
#52625=CARTESIAN_POINT('Ctrl Pts',(27.3687348611375,0.618805305311351,31.5905494329321));
#52626=CARTESIAN_POINT('Ctrl Pts',(27.3510135611613,0.615480730646445,31.6070390220085));
#52627=CARTESIAN_POINT('Ctrl Pts',(27.3330744616886,0.612115296073478,31.6237706303625));
#52628=CARTESIAN_POINT('',(27.3458574166716,0.665360135553637,31.6237706303691));
#52629=CARTESIAN_POINT('Ctrl Pts',(27.3458574166774,0.665360135549173,31.6237706303626));
#52630=CARTESIAN_POINT('Ctrl Pts',(27.3603133960334,0.65421733064462,31.6070390219952));
#52631=CARTESIAN_POINT('Ctrl Pts',(27.374593864627,0.643209811087154,31.5905494329059));
#52632=CARTESIAN_POINT('',(27.3893217156857,0.819472915007473,31.6237706303691));
#52633=CARTESIAN_POINT('Origin',(30.,-1.32966554433622E-14,31.6237706303681));
#52634=CARTESIAN_POINT('Ctrl Pts',(27.4253970781066,0.823344418486268,31.5905494329322));
#52635=CARTESIAN_POINT('Ctrl Pts',(27.4074695638621,0.821420489546793,31.6070390220085));
#52636=CARTESIAN_POINT('Ctrl Pts',(27.3893217156929,0.819472915008255,31.6237706303625));
#52637=CARTESIAN_POINT('',(27.4062428070496,0.871550679329156,31.6237706303691));
#52638=CARTESIAN_POINT('Ctrl Pts',(27.406242807055,0.87155067932429,31.6237706303625));
#52639=CARTESIAN_POINT('Ctrl Pts',(27.4197799690545,0.8593080209004,31.6070390219952));
#52640=CARTESIAN_POINT('Ctrl Pts',(27.4331527756986,0.847214001199735,31.5905494329059));
#52641=CARTESIAN_POINT('',(27.4616646694514,1.02177821091938,31.6237706303691));
#52642=CARTESIAN_POINT('Origin',(30.,-1.32966554433622E-14,31.6237706303681));
#52643=CARTESIAN_POINT('Ctrl Pts',(27.4979325782315,1.0228073395314,31.5905494329321));
#52644=CARTESIAN_POINT('Ctrl Pts',(27.4799093788056,1.02229591797904,31.6070390220085));
#52645=CARTESIAN_POINT('Ctrl Pts',(27.4616646694587,1.02177821091959,31.6237706303625));
#52646=CARTESIAN_POINT('',(27.4826195730339,1.0723678233466,31.6237706303691));
#52647=CARTESIAN_POINT('Ctrl Pts',(27.4826195730389,1.0723678233413,31.6237706303626));
#52648=CARTESIAN_POINT('Ctrl Pts',(27.4951544565765,1.05910079145835,31.6070390219952));
#52649=CARTESIAN_POINT('Ctrl Pts',(27.5075371534712,1.04599483526761,31.5905494329059));
#52650=CARTESIAN_POINT('',(27.549657304612,1.21778390438524,31.6237706303691));
#52651=CARTESIAN_POINT('Origin',(30.,-1.32966554433622E-14,31.6237706303681));
#52652=CARTESIAN_POINT('Ctrl Pts',(27.5858941560335,1.21596431321037,31.5905494329321));
#52653=CARTESIAN_POINT('Ctrl Pts',(27.5678863904439,1.21686855212906,31.6070390220085));
#52654=CARTESIAN_POINT('Ctrl Pts',(27.5496573046193,1.21778390438488,31.6237706303626));
#52655=CARTESIAN_POINT('',(27.5745168264644,1.26657346313462,31.6237706303691));
#52656=CARTESIAN_POINT('Ctrl Pts',(27.574516826469,1.26657346312892,31.6237706303626));
#52657=CARTESIAN_POINT('Ctrl Pts',(27.5859721498194,1.25236385345021,31.6070390219952));
#52658=CARTESIAN_POINT('Ctrl Pts',(27.5972883935207,1.23832676334747,31.5905494329059));
#52659=CARTESIAN_POINT('',(27.6527571173114,1.40628155512632,31.6237706303691));
#52660=CARTESIAN_POINT('Origin',(30.,-1.32966554433622E-14,31.6237706303681));
#52661=CARTESIAN_POINT('Ctrl Pts',(27.6887394991352,1.40162446254924,31.5905494329321));
#52662=CARTESIAN_POINT('Ctrl Pts',(27.670858191245,1.40393878700535,31.6070390220085));
#52663=CARTESIAN_POINT('Ctrl Pts',(27.6527571173186,1.40628155512539,31.6237706303625));
#52664=CARTESIAN_POINT('',(27.6813679902148,1.45297025634401,31.6237706303691));
#52665=CARTESIAN_POINT('Ctrl Pts',(27.6813679902189,1.452970256338,31.6237706303625));
#52666=CARTESIAN_POINT('Ctrl Pts',(27.6916731275044,1.43790567583238,31.6070390219952));
#52667=CARTESIAN_POINT('Ctrl Pts',(27.7018531496069,1.42302399514596,31.5905494329059));
#52668=CARTESIAN_POINT('',(27.7703284629199,1.58610901244398,31.6237706303691));
#52669=CARTESIAN_POINT('Origin',(30.,-1.32966554433622E-14,31.6237706303681));
#52670=CARTESIAN_POINT('Ctrl Pts',(27.8058345317968,1.57864313098906,31.5905494329321));
#52671=CARTESIAN_POINT('Ctrl Pts',(27.7881899258153,1.58235327240273,31.6070390220085));
#52672=CARTESIAN_POINT('Ctrl Pts',(27.770328462927,1.58610901244249,31.6237706303626));
#52673=CARTESIAN_POINT('',(27.8025142913288,1.63040900476139,31.6237706303691));
#52674=CARTESIAN_POINT('Ctrl Pts',(27.8025142913324,1.63040900475507,31.6237706303626));
#52675=CARTESIAN_POINT('Ctrl Pts',(27.8116057079549,1.61458233157081,31.6070390219952));
#52676=CARTESIAN_POINT('Ctrl Pts',(27.8205867452371,1.59894781081078,31.5905494329059));
#52677=CARTESIAN_POINT('',(27.9016464749956,1.75615758026516,31.6237706303691));
#52678=CARTESIAN_POINT('Origin',(30.,-1.32966554433622E-14,31.6237706303681));
#52679=CARTESIAN_POINT('Ctrl Pts',(27.9364573242039,1.74592893957422,31.5905494329321));
#52680=CARTESIAN_POINT('Ctrl Pts',(27.9191582049944,1.75101202368989,31.6070390220085));
#52681=CARTESIAN_POINT('Ctrl Pts',(27.9016464750026,1.7561575802631,31.6237706303626));
#52682=CARTESIAN_POINT('',(27.937208822575,1.79779573949841,31.6237706303691));
#52683=CARTESIAN_POINT('Ctrl Pts',(27.9372088225781,1.79779573949182,31.6237706303625));
#52684=CARTESIAN_POINT('Ctrl Pts',(27.9450304669308,1.78130455033204,31.6070390219952));
#52685=CARTESIAN_POINT('Ctrl Pts',(27.9527571483113,1.76501358151789,31.5905494329059));
#52686=CARTESIAN_POINT('',(28.0459015343263,1.91537885262234,31.6237706303691));
#52687=CARTESIAN_POINT('Origin',(30.,-1.32966554433622E-14,31.6237706303681));
#52688=CARTESIAN_POINT('Ctrl Pts',(28.0798025434049,1.90245051566662,31.5905494329321));
#52689=CARTESIAN_POINT('Ctrl Pts',(28.0629555657899,1.90887520358041,31.6070390220085));
#52690=CARTESIAN_POINT('Ctrl Pts',(28.0459015343331,1.91537885261975,31.6237706303626));
#52691=CARTESIAN_POINT('',(28.0846211473777,1.95409846567367,31.6237706303691));
#52692=CARTESIAN_POINT('Ctrl Pts',(28.0846211473803,1.95409846566688,31.6237706303625));
#52693=CARTESIAN_POINT('Ctrl Pts',(28.0911247964248,1.93704443419661,31.6070390219952));
#52694=CARTESIAN_POINT('Ctrl Pts',(28.0975494843436,1.9201974565684,31.5905494329059));
#52695=CARTESIAN_POINT('',(28.2022042605016,2.062791177425,31.6237706303691));
#52696=CARTESIAN_POINT('Origin',(30.,-1.32966554433622E-14,31.6237706303681));
#52697=CARTESIAN_POINT('Ctrl Pts',(28.2349864184563,2.04724285170094,31.5905494329321));
#52698=CARTESIAN_POINT('Ctrl Pts',(28.2186954496549,2.05496953307545,31.6070390220085));
#52699=CARTESIAN_POINT('Ctrl Pts',(28.2022042605082,2.0627911774219,31.6237706303626));
#52700=CARTESIAN_POINT('',(28.2438424197349,2.09835352500437,31.6237706303691));
#52701=CARTESIAN_POINT('Ctrl Pts',(28.2438424197369,2.09835352499738,31.6237706303625));
#52702=CARTESIAN_POINT('Ctrl Pts',(28.2489879763142,2.08084179499167,31.6070390219952));
#52703=CARTESIAN_POINT('Ctrl Pts',(28.2540710604339,2.06354267576863,31.5905494329059));
#52704=CARTESIAN_POINT('',(28.3695909952386,2.19748570867117,31.6237706303691));
#52705=CARTESIAN_POINT('Origin',(30.,-1.32966554433622E-14,31.6237706303681));
#52706=CARTESIAN_POINT('Ctrl Pts',(28.4010521891644,2.17941325477719,31.5905494329321));
#52707=CARTESIAN_POINT('Ctrl Pts',(28.3854176684167,2.18839429205237,31.6070390220085));
#52708=CARTESIAN_POINT('Ctrl Pts',(28.369590995245,2.19748570866756,31.6237706303626));
#52709=CARTESIAN_POINT('',(28.413890987556,2.22967153708007,31.6237706303691));
#52710=CARTESIAN_POINT('Ctrl Pts',(28.4138909875575,2.22967153707294,31.6237706303625));
#52711=CARTESIAN_POINT('Ctrl Pts',(28.4176467276003,2.21181007417053,31.6070390219952));
#52712=CARTESIAN_POINT('Ctrl Pts',(28.4213568690169,2.19416546817523,31.5905494329059));
#52713=CARTESIAN_POINT('',(28.547029743656,2.31863200978522,31.6237706303691));
#52714=CARTESIAN_POINT('Origin',(30.,-1.32966554433622E-14,31.6237706303681));
#52715=CARTESIAN_POINT('Ctrl Pts',(28.5769760048304,2.29814685040929,31.5905494329321));
#52716=CARTESIAN_POINT('Ctrl Pts',(28.5620943241557,2.30832687250382,31.6070390220085));
#52717=CARTESIAN_POINT('Ctrl Pts',(28.547029743662,2.31863200978111,31.6237706303625));
#52718=CARTESIAN_POINT('',(28.5937184448737,2.34724288268865,31.6237706303691));
#52719=CARTESIAN_POINT('Ctrl Pts',(28.5937184448746,2.34724288268143,31.6237706303626));
#52720=CARTESIAN_POINT('Ctrl Pts',(28.5960612129965,2.32914180874063,31.6070390219952));
#52721=CARTESIAN_POINT('Ctrl Pts',(28.5983755374545,2.31126050083645,31.5905494329059));
#52722=CARTESIAN_POINT('',(28.7334265368654,2.42548317353557,31.6237706303691));
#52723=CARTESIAN_POINT('Origin',(30.,-1.32966554433622E-14,31.6237706303681));
#52724=CARTESIAN_POINT('Ctrl Pts',(28.7616732366302,2.40271160649724,31.5905494329321));
#52725=CARTESIAN_POINT('Ctrl Pts',(28.7476361465385,2.4140278501897,31.6070390220085));
#52726=CARTESIAN_POINT('Ctrl Pts',(28.7334265368711,2.42548317353099,31.6237706303625));
#52727=CARTESIAN_POINT('',(28.7822160956148,2.45034269538798,31.6237706303691));
#52728=CARTESIAN_POINT('Ctrl Pts',(28.7822160956151,2.45034269538071,31.6237706303626));
#52729=CARTESIAN_POINT('Ctrl Pts',(28.7831314478717,2.4321136095416,31.6070390219952));
#52730=CARTESIAN_POINT('Ctrl Pts',(28.7840356867911,2.41410584393792,31.5905494329059));
#52731=CARTESIAN_POINT('',(28.9276321766534,2.51738042696607,31.6237706303691));
#52732=CARTESIAN_POINT('Origin',(30.,-1.32966554433622E-14,31.6237706303681));
#52733=CARTESIAN_POINT('',(28.9540051647184,2.49246284654199,31.5905494329235));
#52734=CARTESIAN_POINT('Ctrl Pts',(28.9540051647116,2.49246284654845,31.5905494329321));
#52735=CARTESIAN_POINT('Ctrl Pts',(28.9408992085311,2.50484554343346,31.6070390220085));
#52736=CARTESIAN_POINT('Ctrl Pts',(28.9276321766587,2.51738042696107,31.6237706303625));
#52737=CARTESIAN_POINT('',(28.9771926604684,2.50206742175908,31.5905494329235));
#52738=CARTESIAN_POINT('Origin',(28.9634421120889,2.50247209787257,31.5962049920587));
#52739=CARTESIAN_POINT('',(28.9782217890806,2.53833533054862,31.6237706303691));
#52740=CARTESIAN_POINT('Ctrl Pts',(28.9782217890804,2.53833533054134,31.6237706303625));
#52741=CARTESIAN_POINT('Ctrl Pts',(28.9777040820206,2.52009062117991,31.6070390219952));
#52742=CARTESIAN_POINT('Ctrl Pts',(28.9771926604678,2.50206742173986,31.5905494329059));
#52743=CARTESIAN_POINT('',(29.1284493206709,2.59375719295039,31.6237706303691));
#52744=CARTESIAN_POINT('Origin',(30.,-1.32966554433622E-14,31.6237706303681));
#52745=CARTESIAN_POINT('',(29.1527859987874,2.56684722431571,31.5905494329235));
#52746=CARTESIAN_POINT('Ctrl Pts',(29.1527859987811,2.56684722432269,31.5905494329321));
#52747=CARTESIAN_POINT('Ctrl Pts',(29.1406919790899,2.58022003095629,31.6070390220085));
#52748=CARTESIAN_POINT('Ctrl Pts',(29.1284493206758,2.59375719294498,31.6237706303625));
#52749=CARTESIAN_POINT('',(29.1766555815128,2.57460292188403,31.5905494329235));
#52750=CARTESIAN_POINT('Origin',(29.1629791704778,2.57608521103256,31.5962049981139));
#52751=CARTESIAN_POINT('',(29.1805270849926,2.61067828431428,31.6237706303691));
#52752=CARTESIAN_POINT('Ctrl Pts',(29.1805270849917,2.61067828430704,31.6237706303626));
#52753=CARTESIAN_POINT('Ctrl Pts',(29.1785795104516,2.59253043612347,31.6070390219952));
#52754=CARTESIAN_POINT('Ctrl Pts',(29.1766555815107,2.57460292186492,31.5905494329059));
#52755=CARTESIAN_POINT('',(29.3346398644464,2.65414258332837,31.6237706303691));
#52756=CARTESIAN_POINT('Origin',(30.,-1.32966554433622E-14,31.6237706303681));
#52757=CARTESIAN_POINT('',(29.3567901889011,2.6254061353882,31.5905494329235));
#52758=CARTESIAN_POINT('Ctrl Pts',(29.3567901888954,2.62540613539565,31.5905494329321));
#52759=CARTESIAN_POINT('Ctrl Pts',(29.3457826693465,2.63968660397804,31.6070390220085));
#52760=CARTESIAN_POINT('Ctrl Pts',(29.3346398644508,2.6541425833226,31.6237706303625));
#52761=CARTESIAN_POINT('',(29.3811946946869,2.63126513885323,31.5905494329235));
#52762=CARTESIAN_POINT('Origin',(29.367676739957,2.63381590833401,31.5962050111235));
#52763=CARTESIAN_POINT('',(29.3878847039279,2.66692553831851,31.6237706303691));
#52764=CARTESIAN_POINT('Ctrl Pts',(29.3878847039265,2.66692553831136,31.6237706303626));
#52765=CARTESIAN_POINT('Ctrl Pts',(29.3845192693509,2.64898643882447,31.6070390219952));
#52766=CARTESIAN_POINT('Ctrl Pts',(29.3811946946833,2.63126513883434,31.5905494329059));
#52767=CARTESIAN_POINT('',(29.5449325747123,2.69816430208817,31.6237706303691));
#52768=CARTESIAN_POINT('Origin',(30.,-1.32966554433622E-14,31.6237706303681));
#52769=CARTESIAN_POINT('',(29.5647599813892,2.6677785445999,31.5905494329235));
#52770=CARTESIAN_POINT('Ctrl Pts',(29.5647599813841,2.66777854460778,31.5905494329321));
#52771=CARTESIAN_POINT('Ctrl Pts',(29.554906826996,2.6828786313014,31.6070390220085));
#52772=CARTESIAN_POINT('Ctrl Pts',(29.5449325747163,2.69816430208207,31.6237706303625));
#52773=CARTESIAN_POINT('',(29.589548948342,2.67170473125694,31.5905494329235));
#52774=CARTESIAN_POINT('Origin',(29.5762727932907,2.67530826149244,31.5962050315749));
#52775=CARTESIAN_POINT('',(29.5990162172125,2.70673030953627,31.6237706303691));
#52776=CARTESIAN_POINT('Ctrl Pts',(29.5990162172106,2.70673030952925,31.6237706303625));
#52777=CARTESIAN_POINT('Ctrl Pts',(29.5942536716227,2.68911055925274,31.6070390219952));
#52778=CARTESIAN_POINT('Ctrl Pts',(29.589548948337,2.67170473123838,31.5905494329059));
#52779=CARTESIAN_POINT('',(29.7580309269804,2.72555094069491,31.6237706303691));
#52780=CARTESIAN_POINT('Origin',(30.,-1.32966554433622E-14,31.6237706303681));
#52781=CARTESIAN_POINT('',(29.775413173324,2.69370321195775,31.5905494329235));
#52782=CARTESIAN_POINT('Ctrl Pts',(29.7754131733195,2.69370321196601,31.5905494329321));
#52783=CARTESIAN_POINT('Ctrl Pts',(29.7667751320655,2.7095298197151,31.6070390220085));
#52784=CARTESIAN_POINT('Ctrl Pts',(29.7580309269838,2.72555094068851,31.6237706303625));
#52785=CARTESIAN_POINT('',(29.8004337692194,2.69567237556048,31.5905494329235));
#52786=CARTESIAN_POINT('Origin',(29.7874812679388,2.70030645711977,31.5962050602857));
#52787=CARTESIAN_POINT('',(29.8126199288586,2.72984718831658,31.6237706303691));
#52788=CARTESIAN_POINT('Ctrl Pts',(29.8126199288562,2.72984718830972,31.6237706303625));
#52789=CARTESIAN_POINT('Ctrl Pts',(29.8064896349333,2.71265541886322,31.6070390219952));
#52790=CARTESIAN_POINT('Ctrl Pts',(29.800433769213,2.69567237554238,31.5905494329059));
#52791=CARTESIAN_POINT('',(29.9726210990465,2.73613365141461,31.6237706303691));
#52792=CARTESIAN_POINT('Origin',(30.,-1.32966554433622E-14,31.6237706303681));
#52793=CARTESIAN_POINT('',(29.987451017728,2.70302030326666,31.5905494329235));
#52794=CARTESIAN_POINT('Ctrl Pts',(29.9874510177241,2.70302030327525,31.5905494329321));
#52795=CARTESIAN_POINT('Ctrl Pts',(29.9800813460009,2.71947585578017,31.6070390220085));
#52796=CARTESIAN_POINT('Ctrl Pts',(29.9726210990495,2.73613365140797,31.6237706303625));
#52797=CARTESIAN_POINT('Ctrl Pts',(30.,2.69489040503946,31.5823904050395));
#52798=CARTESIAN_POINT('Ctrl Pts',(29.9982996971592,2.69489040503946,31.5823904050395));
#52799=CARTESIAN_POINT('Ctrl Pts',(29.9965490639354,2.69522714758866,31.5827289231894));
#52800=CARTESIAN_POINT('Ctrl Pts',(29.9934248389279,2.69644647069982,31.5839540167345));
#52801=CARTESIAN_POINT('Ctrl Pts',(29.9920523583067,2.69733049287039,31.5848419899159));
#52802=CARTESIAN_POINT('Ctrl Pts',(29.9894391186861,2.6996015700298,31.5871217896387));
#52803=CARTESIAN_POINT('Ctrl Pts',(29.9882404972758,2.70125749446876,31.5887829779419));
#52804=CARTESIAN_POINT('Ctrl Pts',(29.987451017728,2.70302030326666,31.5905494329235));
#52805=CARTESIAN_POINT('',(30.,2.68872936963187,31.5762293696319));
#52806=CARTESIAN_POINT('',(30.,2.68872936963187,31.5762293696319));
#52807=CARTESIAN_POINT('',(30.,-2.68872936963189,31.5762293696319));
#52808=CARTESIAN_POINT('Origin',(30.,-1.32966554433622E-14,31.5762293696319));
#52809=CARTESIAN_POINT('Origin',(30.,-1.32966554433622E-14,31.5762293696319));
#52810=CARTESIAN_POINT('Origin',(30.,-1.32966554433622E-14,31.5430837392638));
#52811=CARTESIAN_POINT('',(30.,-2.67500000000001,31.5430837392638));
#52812=CARTESIAN_POINT('Origin',(30.,-1.32966554433622E-14,31.5430837392638));
#52813=CARTESIAN_POINT('Origin',(30.,-2.72187500000001,31.5430837392638));
#52814=CARTESIAN_POINT('Origin',(30.,-1.32966554433622E-14,16.));
#52815=CARTESIAN_POINT('',(30.,-2.67500000000001,31.06875));
#52816=CARTESIAN_POINT('Origin',(30.,-1.32966554433622E-14,31.06875));
#52817=CARTESIAN_POINT('',(30.,-2.67500000000001,16.));
#52818=CARTESIAN_POINT('Origin',(30.,-1.32966554433622E-14,31.06875));
#52819=CARTESIAN_POINT('',(30.,-2.60625000000001,31.));
#52820=CARTESIAN_POINT('Origin',(30.,-1.32966554433622E-14,31.));
#52821=CARTESIAN_POINT('Origin',(30.,-2.60625000000001,31.06875));
#52822=CARTESIAN_POINT('Origin',(30.,-1.32966554433622E-14,30.85));
#52823=CARTESIAN_POINT('',(30.,-1.65000000000002,31.));
#52824=CARTESIAN_POINT('Origin',(30.,-1.65000000000001,30.85));
#52825=CARTESIAN_POINT('Origin',(30.,-1.32966554433622E-14,31.));
#52826=CARTESIAN_POINT('Origin',(30.,-1.32966554433622E-14,31.6569162607362));
#52827=CARTESIAN_POINT('',(27.4723387620945,1.08324912480478,31.6569162607362));
#52828=CARTESIAN_POINT('Origin',(27.5075595450194,1.04598613791953,31.6570432561871));
#52829=CARTESIAN_POINT('',(27.5347062454699,1.21853465435945,31.6569162607362));
#52830=CARTESIAN_POINT('Origin',(30.,-1.32966554433622E-14,31.6569162607362));
#52831=CARTESIAN_POINT('Origin',(27.5859112932463,1.21595145595199,31.6570220656254));
#52832=CARTESIAN_POINT('Origin',(30.,-1.32966554433622E-14,31.6569162607362));
#52833=CARTESIAN_POINT('',(27.4467007962708,1.0213536000015,31.6569162607362));
#52834=CARTESIAN_POINT('Origin',(27.4979506713832,1.02279586647784,31.6570220656247));
#52835=CARTESIAN_POINT('',(27.3951399513465,0.881591814236737,31.6569162607362));
#52836=CARTESIAN_POINT('Origin',(27.4331757806072,0.847207087483285,31.6570432561871));
#52837=CARTESIAN_POINT('Origin',(30.,-1.32966554433622E-14,31.6569162607362));
#52838=CARTESIAN_POINT('Origin',(30.,-1.32966554433622E-14,31.6569162607362));
#52839=CARTESIAN_POINT('',(27.3744372857209,0.817875561065013,31.6569162607362));
#52840=CARTESIAN_POINT('Origin',(27.4254160156494,0.82333440037271,31.6570220656251));
#52841=CARTESIAN_POINT('',(27.3340009690024,0.674499196974899,31.6569162607362));
#52842=CARTESIAN_POINT('Origin',(27.3746173410621,0.643204723628532,31.6570432561866));
#52843=CARTESIAN_POINT('Origin',(30.,-1.32966554433622E-14,31.6569162607362));
#52844=CARTESIAN_POINT('Origin',(30.,-1.32966554433622E-14,31.6569162607362));
#52845=CARTESIAN_POINT('',(27.3183612423927,0.609355047323335,31.6569162607362));
#52846=CARTESIAN_POINT('Origin',(27.3687545263143,0.61879680390278,31.6570220656251));
#52847=CARTESIAN_POINT('',(27.2892987572189,0.463248067869971,31.6569162607362));
#52848=CARTESIAN_POINT('Origin',(27.3322452586394,0.435236788764015,31.6570432561869));
#52849=CARTESIAN_POINT('Origin',(30.,-1.32966554433622E-14,31.6569162607362));
#52850=CARTESIAN_POINT('Origin',(30.,-1.32966554433622E-14,31.6569162607362));
#52851=CARTESIAN_POINT('',(27.2788183937405,0.397077657083795,31.6569162607362));
#52852=CARTESIAN_POINT('Origin',(27.3283155403022,0.41044411936593,31.6570220656249));
#52853=CARTESIAN_POINT('',(27.2613089199969,0.249140860381007,31.6569162607362));
#52854=CARTESIAN_POINT('Origin',(27.3063207713152,0.224585474366194,31.6570432561871));
#52855=CARTESIAN_POINT('Origin',(30.,-1.32966554433622E-14,31.6569162607362));
#52856=CARTESIAN_POINT('Origin',(30.,-1.32966554433622E-14,31.6569162607362));
#52857=CARTESIAN_POINT('',(27.2560525345756,0.182352151046611,31.6569162607362));
#52858=CARTESIAN_POINT('Origin',(27.3043483774102,0.199560910346922,31.6570220656251));
#52859=CARTESIAN_POINT('',(27.2502040239902,0.0334976166400503,31.6569162607362));
#52860=CARTESIAN_POINT('Origin',(27.2970037121761,0.0125495158363338,31.6570432561875));
#52861=CARTESIAN_POINT('Origin',(30.,-1.32966554433622E-14,31.6569162607362));
#52862=CARTESIAN_POINT('Origin',(30.,-1.32966554433622E-14,31.6569162607362));
#52863=CARTESIAN_POINT('',(27.2502040239902,-0.0334976166400194,31.6569162607362));
#52864=CARTESIAN_POINT('Origin',(27.297000803166,-0.0125526580452972,31.6570220656252));
#52865=CARTESIAN_POINT('',(27.2560525345756,-0.18235215104658,31.6569162607362));
#52866=CARTESIAN_POINT('Origin',(27.3043515239857,-0.199563814630509,31.6570432561868));
#52867=CARTESIAN_POINT('Origin',(30.,-1.32966554433622E-14,31.6569162607362));
#52868=CARTESIAN_POINT('Origin',(30.,-1.32966554433622E-14,31.6569162607362));
#52869=CARTESIAN_POINT('',(27.2613089199969,-0.249140860380976,31.6569162607362));
#52870=CARTESIAN_POINT('Origin',(27.3063181178117,-0.22458883512474,31.6570220656265));
#52871=CARTESIAN_POINT('',(27.2788183937405,-0.397077657083763,31.6569162607362));
#52872=CARTESIAN_POINT('Origin',(27.3283189050458,-0.410446767819208,31.6570432561867));
#52873=CARTESIAN_POINT('Origin',(30.,-1.32966554433622E-14,31.6569162607362));
#52874=CARTESIAN_POINT('Origin',(30.,-1.32966554433622E-14,31.6569162607362));
#52875=CARTESIAN_POINT('',(27.2892987572189,-0.463248067869938,31.6569162607362));
#52876=CARTESIAN_POINT('Origin',(27.3322428769935,-0.4352403473568,31.6570220656245));
#52877=CARTESIAN_POINT('',(27.3183612423927,-0.609355047323306,31.6569162607362));
#52878=CARTESIAN_POINT('Origin',(27.3687580884808,-0.618799180197033,31.6570432561867));
#52879=CARTESIAN_POINT('Origin',(30.,-1.32966554433622E-14,31.6569162607362));
#52880=CARTESIAN_POINT('Origin',(30.,-1.32966554433622E-14,31.6569162607362));
#52881=CARTESIAN_POINT('',(27.3340009690024,-0.674499196974871,31.6569162607362));
#52882=CARTESIAN_POINT('Origin',(27.3746152459701,-0.643208458106799,31.6570220656281));
#52883=CARTESIAN_POINT('',(27.3744372857209,-0.817875561064986,31.6569162607362));
#52884=CARTESIAN_POINT('Origin',(27.4254197532793,-0.823336489857566,31.6570432561877));
#52885=CARTESIAN_POINT('Origin',(30.,-1.32966554433622E-14,31.6569162607362));
#52886=CARTESIAN_POINT('Origin',(30.,-1.32966554433622E-14,31.6569162607362));
#52887=CARTESIAN_POINT('',(27.3951399513465,-0.88159181423671,31.6569162607362));
#52888=CARTESIAN_POINT('Origin',(27.4331739849698,-0.847210974835381,31.6570220656246));
#52889=CARTESIAN_POINT('',(27.4467007962708,-1.02135360000148,31.6569162607362));
#52890=CARTESIAN_POINT('Origin',(27.4979545614299,-1.02279765627042,31.6570432561873));
#52891=CARTESIAN_POINT('Origin',(30.,-1.32966554433622E-14,31.6569162607362));
#52892=CARTESIAN_POINT('Origin',(30.,-1.32966554433622E-14,31.6569162607362));
#52893=CARTESIAN_POINT('',(27.4723387620945,-1.08324912480475,31.6569162607362));
#52894=CARTESIAN_POINT('Origin',(27.5075580599161,-1.04599015417175,31.657022065625));
#52895=CARTESIAN_POINT('',(27.5347062454699,-1.21853465435942,31.6569162607362));
#52896=CARTESIAN_POINT('Origin',(27.5859153117243,-1.21595293501783,31.6570432561869));
#52897=CARTESIAN_POINT('Origin',(30.,-1.32966554433622E-14,31.6569162607362));
#52898=CARTESIAN_POINT('Origin',(30.,-1.32966554433622E-14,31.6569162607362));
#52899=CARTESIAN_POINT('',(27.5651214449068,-1.27822784430149,31.6569162607362));
#52900=CARTESIAN_POINT('Origin',(27.5973088682438,-1.23832045638074,31.6570220656251));
#52901=CARTESIAN_POINT('',(27.637911050459,-1.40820303736935,31.6569162607362));
#52902=CARTESIAN_POINT('Origin',(27.6887596968882,-1.40161145957539,31.6570432561872));
#52903=CARTESIAN_POINT('Origin',(30.,-1.32966554433622E-14,31.6569162607362));
#52904=CARTESIAN_POINT('Origin',(30.,-1.32966554433622E-14,31.6569162607362));
#52905=CARTESIAN_POINT('',(27.6729159636906,-1.46532586408421,31.6569162607362));
#52906=CARTESIAN_POINT('Origin',(27.7018730663766,-1.42301610118967,31.6570220656267));
#52907=CARTESIAN_POINT('',(27.7556789192963,-1.58918938037887,31.6569162607362));
#52908=CARTESIAN_POINT('Origin',(27.8058536470839,-1.57862858340189,31.6570432561867));
#52909=CARTESIAN_POINT('Origin',(30.,-1.32966554433622E-14,31.6569162607362));
#52910=CARTESIAN_POINT('Origin',(30.,-1.32966554433622E-14,31.6569162607362));
#52911=CARTESIAN_POINT('',(27.7950577293922,-1.64338966264456,31.6569162607362));
#52912=CARTESIAN_POINT('Origin',(27.8206059812726,-1.59893837851,31.6570220656387));
#52913=CARTESIAN_POINT('',(27.8872837739086,-1.76037784239926,31.6569162607362));
#52914=CARTESIAN_POINT('Origin',(27.9364752391763,-1.7459129370637,31.6570432561874));
#52915=CARTESIAN_POINT('Origin',(30.,-1.32966554433622E-14,31.6569162607362));
#52916=CARTESIAN_POINT('Origin',(30.,-1.32966554433622E-14,31.6569162607362));
#52917=CARTESIAN_POINT('',(27.9307936974098,-1.81132141745219,31.6569162607362));
#52918=CARTESIAN_POINT('Origin',(27.9527755849842,-1.76500266908356,31.6570220656253));
#52919=CARTESIAN_POINT('',(28.0319142266042,-1.92071298963622,31.6569162607362));
#52920=CARTESIAN_POINT('Origin',(28.0798191476078,-1.90243315689441,31.657043256187));
#52921=CARTESIAN_POINT('Origin',(30.,-1.32966554433622E-14,31.6569162607362));
#52922=CARTESIAN_POINT('Origin',(30.,-1.32966554433622E-14,31.6569162607362));
#52923=CARTESIAN_POINT('',(28.0792870103637,-1.96808577339573,31.6569162607362));
#52924=CARTESIAN_POINT('Origin',(28.097567008002,-1.92018513125043,31.6570220656245));
#52925=CARTESIAN_POINT('',(28.1886785825478,-2.06920630259019,31.6569162607362));
#52926=CARTESIAN_POINT('Origin',(28.2350016095212,-2.0472242436889,31.6570432561873));
#52927=CARTESIAN_POINT('Origin',(30.,-1.32966554433622E-14,31.6569162607362));
#52928=CARTESIAN_POINT('Origin',(30.,-1.32966554433622E-14,31.6569162607362));
#52929=CARTESIAN_POINT('',(28.2396221576007,-2.11271622609136,31.6569162607362));
#52930=CARTESIAN_POINT('Origin',(28.2540875630401,-2.06352901355267,31.6570220656256));
#52931=CARTESIAN_POINT('',(28.3566103373554,-2.20494227060778,31.6569162607362));
#52932=CARTESIAN_POINT('Origin',(28.4010658734316,-2.17939351225073,31.6570432561869));
#52933=CARTESIAN_POINT('Origin',(30.,-1.32966554433622E-14,31.6569162607362));
#52934=CARTESIAN_POINT('Origin',(30.,-1.32966554433622E-14,31.6569162607362));
#52935=CARTESIAN_POINT('',(28.4108106196211,-2.2443210807037,31.6569162607362));
#52936=CARTESIAN_POINT('Origin',(28.4213722488256,-2.19415055329735,31.6570220656249));
#52937=CARTESIAN_POINT('',(28.5346741359157,-2.32708403630936,31.6569162607362));
#52938=CARTESIAN_POINT('Origin',(28.5769880979323,-2.29812609508764,31.6570432561867));
#52939=CARTESIAN_POINT('Origin',(30.,-1.32966554433622E-14,31.6569162607362));
#52940=CARTESIAN_POINT('Origin',(30.,-1.32966554433622E-14,31.6569162607362));
#52941=CARTESIAN_POINT('',(28.5917969626306,-2.362088949541,31.6569162607362));
#52942=CARTESIAN_POINT('Origin',(28.5983896996446,-2.31124442525031,31.6570220656249));
#52943=CARTESIAN_POINT('',(28.7217721556985,-2.43487855509312,31.6569162607362));
#52944=CARTESIAN_POINT('Origin',(28.7616836640096,-2.40268996634326,31.6570432561868));
#52945=CARTESIAN_POINT('Origin',(30.,-1.32966554433622E-14,31.6569162607362));
#52946=CARTESIAN_POINT('Origin',(30.,-1.32966554433622E-14,31.6569162607362));
#52947=CARTESIAN_POINT('',(28.7814653456405,-2.46529375453011,31.6569162607362));
#52948=CARTESIAN_POINT('Origin',(28.784048544048,-2.41408870675338,31.6570220656255));
#52949=CARTESIAN_POINT('',(28.9167508751952,-2.52766123790546,31.6569162607362));
#52950=CARTESIAN_POINT('Origin',(28.9540138620808,-2.49244045498024,31.6570432561872));
#52951=CARTESIAN_POINT('Origin',(30.,-1.32966554433622E-14,31.6569162607362));
#52952=CARTESIAN_POINT('Origin',(30.,-1.32966554433622E-14,31.6569162607362));
#52953=CARTESIAN_POINT('',(28.9786463999985,-2.55329920372917,31.6569162607362));
#52954=CARTESIAN_POINT('Origin',(28.9772041335221,-2.50204932861609,31.657022065625));
#52955=CARTESIAN_POINT('',(29.1184081857632,-2.60486004865345,31.6569162607362));
#52956=CARTESIAN_POINT('Origin',(29.1527929125168,-2.56682421939275,31.6570432561872));
#52957=CARTESIAN_POINT('Origin',(30.,-1.32966554433622E-14,31.6569162607362));
#52958=CARTESIAN_POINT('Origin',(30.,-1.32966554433622E-14,31.6569162607362));
#52959=CARTESIAN_POINT('',(29.182124438935,-2.6255627142791,31.6569162607362));
#52960=CARTESIAN_POINT('Origin',(29.1766655996274,-2.57458398435135,31.6570220656246));
#52961=CARTESIAN_POINT('',(29.3255008030251,-2.66599903099763,31.6569162607362));
#52962=CARTESIAN_POINT('Origin',(29.3567952763715,-2.62538265893786,31.6570432561866));
#52963=CARTESIAN_POINT('Origin',(30.,-1.32966554433622E-14,31.6569162607362));
#52964=CARTESIAN_POINT('Origin',(30.,-1.32966554433622E-14,31.6569162607362));
#52965=CARTESIAN_POINT('',(29.3906449526766,-2.6816387576073,31.6569162607362));
#52966=CARTESIAN_POINT('Origin',(29.3812031960972,-2.63124547368565,31.6570220656251));
#52967=CARTESIAN_POINT('',(29.53675193213,-2.71070124278106,31.6569162607362));
#52968=CARTESIAN_POINT('Origin',(29.5647632112362,-2.66775474136028,31.6570432561871));
#52969=CARTESIAN_POINT('Origin',(30.,-1.32966554433622E-14,31.6569162607362));
#52970=CARTESIAN_POINT('Origin',(30.,-1.32966554433622E-14,31.6569162607362));
#52971=CARTESIAN_POINT('',(29.6029223429162,-2.72118160625948,31.6569162607362));
#52972=CARTESIAN_POINT('Origin',(29.5895558806344,-2.67168445969898,31.6570220656245));
#52973=CARTESIAN_POINT('',(29.750859139619,-2.73869108000313,31.6569162607362));
#52974=CARTESIAN_POINT('Origin',(29.7754145256345,-2.69367922868347,31.6570432561876));
#52975=CARTESIAN_POINT('Origin',(30.,-1.32966554433622E-14,31.6569162607362));
#52976=CARTESIAN_POINT('Origin',(30.,-1.32966554433622E-14,31.6569162607362));
#52977=CARTESIAN_POINT('',(29.8176478489534,-2.74394746542436,31.6569162607362));
#52978=CARTESIAN_POINT('Origin',(29.800439089653,-2.69565162258972,31.6570220656252));
#52979=CARTESIAN_POINT('',(29.9665023833599,-2.74979597600977,31.6569162607362));
#52980=CARTESIAN_POINT('Origin',(29.9874504841626,-2.70299628782621,31.6570432561866));
#52981=CARTESIAN_POINT('Origin',(30.,-1.32966554433622E-14,31.6569162607362));
#52982=CARTESIAN_POINT('Origin',(30.,-1.32966554433622E-14,31.6569162607362));
#52983=CARTESIAN_POINT('',(30.03349761664,-2.74979597600977,31.6569162607362));
#52984=CARTESIAN_POINT('Origin',(30.0125526580435,-2.70299919683014,31.6570220656269));
#52985=CARTESIAN_POINT('',(30.1823521510466,-2.74394746542436,31.6569162607362));
#52986=CARTESIAN_POINT('Origin',(30.1995638146306,-2.69564847601399,31.6570432561868));
#52987=CARTESIAN_POINT('Origin',(30.,-1.32966554433622E-14,31.6569162607362));
#52988=CARTESIAN_POINT('Origin',(30.,-1.32966554433622E-14,31.6569162607362));
#52989=CARTESIAN_POINT('',(30.2491408603809,-2.73869108000313,31.6569162607362));
#52990=CARTESIAN_POINT('Origin',(30.2245888351274,-2.69368188219317,31.6570220656245));
#52991=CARTESIAN_POINT('',(30.3970776570837,-2.72118160625948,31.6569162607362));
#52992=CARTESIAN_POINT('Origin',(30.4104467678196,-2.67168109495285,31.6570432561872));
#52993=CARTESIAN_POINT('Origin',(30.,-1.32966554433622E-14,31.6569162607362));
#52994=CARTESIAN_POINT('Origin',(30.,-1.32966554433622E-14,31.6569162607362));
#52995=CARTESIAN_POINT('',(30.4632480678699,-2.71070124278107,31.6569162607362));
#52996=CARTESIAN_POINT('Origin',(30.4352403473562,-2.66775712300563,31.6570220656249));
#52997=CARTESIAN_POINT('',(30.6093550473233,-2.68163875760731,31.6569162607362));
#52998=CARTESIAN_POINT('Origin',(30.6187991801974,-2.63124191151731,31.6570432561874));
#52999=CARTESIAN_POINT('Origin',(30.,-1.32966554433622E-14,31.6569162607362));
#53000=CARTESIAN_POINT('Origin',(30.,-1.32966554433622E-14,31.6569162607362));
#53001=CARTESIAN_POINT('',(30.6744991969748,-2.66599903099764,31.6569162607362));
#53002=CARTESIAN_POINT('Origin',(30.6432084581108,-2.62538475403506,31.6570220656255));
#53003=CARTESIAN_POINT('',(30.817875561065,-2.62556271427912,31.6569162607362));
#53004=CARTESIAN_POINT('Origin',(30.8233364898573,-2.57458024672293,31.6570432561868));
#53005=CARTESIAN_POINT('Origin',(30.,-1.32966554433622E-14,31.6569162607362));
#53006=CARTESIAN_POINT('Origin',(30.,-1.32966554433622E-14,31.6569162607362));
#53007=CARTESIAN_POINT('',(30.8815918142367,-2.60486004865346,31.6569162607362));
#53008=CARTESIAN_POINT('Origin',(30.8472109748348,-2.56682601502956,31.6570220656249));
#53009=CARTESIAN_POINT('',(31.0213536000014,-2.55329920372919,31.6569162607362));
#53010=CARTESIAN_POINT('Origin',(31.0227976562703,-2.50204543857134,31.6570432561867));
#53011=CARTESIAN_POINT('Origin',(30.,-1.32966554433622E-14,31.6569162607362));
#53012=CARTESIAN_POINT('Origin',(30.,-1.32966554433622E-14,31.6569162607362));
#53013=CARTESIAN_POINT('',(31.0832491248047,-2.52766123790547,31.6569162607362));
#53014=CARTESIAN_POINT('Origin',(31.0459901541642,-2.49244194007693,31.6570220656289));
#53015=CARTESIAN_POINT('',(31.2185346543594,-2.46529375453013,31.6569162607362));
#53016=CARTESIAN_POINT('Origin',(31.2159529350178,-2.41408468827489,31.6570432561872));
#53017=CARTESIAN_POINT('Origin',(30.,-1.32966554433622E-14,31.6569162607362));
#53018=CARTESIAN_POINT('Origin',(30.,-1.32966554433622E-14,31.6569162607362));
#53019=CARTESIAN_POINT('',(31.2782278443015,-2.43487855509314,31.6569162607362));
#53020=CARTESIAN_POINT('Origin',(31.238320456382,-2.40269113175716,31.6570220656245));
#53021=CARTESIAN_POINT('',(31.4082030373693,-2.36208894954102,31.6569162607362));
#53022=CARTESIAN_POINT('Origin',(31.4016114595753,-2.31124030311134,31.6570432561875));
#53023=CARTESIAN_POINT('Origin',(30.,-1.32966554433622E-14,31.6569162607362));
#53024=CARTESIAN_POINT('Origin',(30.,-1.32966554433622E-14,31.6569162607362));
#53025=CARTESIAN_POINT('',(31.4653258640842,-2.32708403630938,31.6569162607362));
#53026=CARTESIAN_POINT('Origin',(31.4230161011935,-2.29812693362589,31.657022065625));
#53027=CARTESIAN_POINT('',(31.5891893803788,-2.24432108070372,31.6569162607362));
#53028=CARTESIAN_POINT('Origin',(31.5786285834021,-2.1941463529175,31.6570432561862));
#53029=CARTESIAN_POINT('Origin',(30.,-1.32966554433622E-14,31.6569162607362));
#53030=CARTESIAN_POINT('Origin',(30.,-1.32966554433622E-14,31.6569162607362));
#53031=CARTESIAN_POINT('',(31.6433896626445,-2.2049422706078,31.6569162607362));
#53032=CARTESIAN_POINT('Origin',(31.5989383785409,-2.17939401874466,31.6570220656252));
#53033=CARTESIAN_POINT('',(31.7603778423992,-2.11271622609138,31.6569162607362));
#53034=CARTESIAN_POINT('Origin',(31.7459129370641,-2.0635247608251,31.6570432561869));
#53035=CARTESIAN_POINT('Origin',(30.,-1.32966554433622E-14,31.6569162607362));
#53036=CARTESIAN_POINT('Origin',(30.,-1.32966554433622E-14,31.6569162607362));
#53037=CARTESIAN_POINT('',(31.8113214174522,-2.06920630259022,31.6569162607362));
#53038=CARTESIAN_POINT('Origin',(31.7650026690826,-2.04722441501533,31.6570220656257));
#53039=CARTESIAN_POINT('',(31.9207129896362,-1.96808577339576,31.6569162607362));
#53040=CARTESIAN_POINT('Origin',(31.9024331568943,-1.92018085239205,31.657043256187));
#53041=CARTESIAN_POINT('Origin',(30.,-1.32966554433622E-14,31.6569162607362));
#53042=CARTESIAN_POINT('Origin',(30.,-1.32966554433622E-14,31.6569162607362));
#53043=CARTESIAN_POINT('',(31.9680857733957,-1.92071298963625,31.6569162607362));
#53044=CARTESIAN_POINT('Origin',(31.9201851312437,-1.90243299199549,31.6570220656273));
#53045=CARTESIAN_POINT('',(32.0692063025902,-1.81132141745222,31.6569162607362));
#53046=CARTESIAN_POINT('Origin',(32.0472242436891,-1.76499839047944,31.6570432561871));
#53047=CARTESIAN_POINT('Origin',(30.,-1.32966554433622E-14,31.6569162607362));
#53048=CARTESIAN_POINT('Origin',(30.,-1.32966554433622E-14,31.6569162607362));
#53049=CARTESIAN_POINT('',(32.1127162260913,-1.76037784239929,31.6569162607362));
#53050=CARTESIAN_POINT('Origin',(32.0635290135546,-1.74591243696045,31.6570220656248));
#53051=CARTESIAN_POINT('',(32.2049422706077,-1.64338966264459,31.6569162607362));
#53052=CARTESIAN_POINT('Origin',(32.1793935122505,-1.59893412656801,31.6570432561871));
#53053=CARTESIAN_POINT('Origin',(30.,-1.32966554433622E-14,31.6569162607362));
#53054=CARTESIAN_POINT('Origin',(30.,-1.32966554433622E-14,31.6569162607362));
#53055=CARTESIAN_POINT('',(32.2443210807037,-1.5891893803789,31.6569162607362));
#53056=CARTESIAN_POINT('Origin',(32.1941505532956,-1.57862775117404,31.6570220656256));
#53057=CARTESIAN_POINT('',(32.3270840363093,-1.46532586408424,31.6569162607362));
#53058=CARTESIAN_POINT('Origin',(32.2981260950875,-1.42301190206755,31.6570432561867));
#53059=CARTESIAN_POINT('Origin',(30.,-1.32966554433622E-14,31.6569162607362));
#53060=CARTESIAN_POINT('Origin',(30.,-1.32966554433622E-14,31.6569162607362));
#53061=CARTESIAN_POINT('',(32.362088949541,-1.40820303736938,31.6569162607362));
#53062=CARTESIAN_POINT('Origin',(32.3112444252322,-1.40161030035328,31.657022065632));
#53063=CARTESIAN_POINT('',(32.4348785550931,-1.27822784430152,31.6569162607362));
#53064=CARTESIAN_POINT('Origin',(32.4026899663432,-1.23831633599041,31.6570432561868));
#53065=CARTESIAN_POINT('Origin',(30.,-1.32966554433622E-14,31.6569162607362));
#53066=CARTESIAN_POINT('Origin',(30.,-1.32966554433622E-14,31.6569162607362));
#53067=CARTESIAN_POINT('',(32.4652937545301,-1.21853465435946,31.6569162607362));
#53068=CARTESIAN_POINT('Origin',(32.414088706754,-1.21595145595202,31.6570220656252));
#53069=CARTESIAN_POINT('',(32.5276612379054,-1.08324912480479,31.6569162607362));
#53070=CARTESIAN_POINT('Origin',(32.4924404549811,-1.04598613792014,31.6570432561868));
#53071=CARTESIAN_POINT('Origin',(30.,-1.32966554433622E-14,31.6569162607362));
#53072=CARTESIAN_POINT('Origin',(30.,-1.32966554433622E-14,31.6569162607362));
#53073=CARTESIAN_POINT('',(32.5532992037291,-1.02135360000151,31.6569162607362));
#53074=CARTESIAN_POINT('Origin',(32.5020493286151,-1.0227958664779,31.6570220656254));
#53075=CARTESIAN_POINT('',(32.6048600486534,-0.881591814236746,31.6569162607362));
#53076=CARTESIAN_POINT('Origin',(32.5668242193914,-0.847207087482045,31.6570432561878));
#53077=CARTESIAN_POINT('Origin',(30.,-1.32966554433622E-14,31.6569162607362));
#53078=CARTESIAN_POINT('Origin',(30.,-1.32966554433622E-14,31.6569162607362));
#53079=CARTESIAN_POINT('',(32.6255627142791,-0.817875561065022,31.6569162607362));
#53080=CARTESIAN_POINT('Origin',(32.5745839843496,-0.82333440037284,31.6570220656255));
#53081=CARTESIAN_POINT('',(32.6659990309976,-0.674499196974908,31.6569162607362));
#53082=CARTESIAN_POINT('Origin',(32.6253826589374,-0.643204723628158,31.6570432561868));
#53083=CARTESIAN_POINT('Origin',(30.,-1.32966554433622E-14,31.6569162607362));
#53084=CARTESIAN_POINT('Origin',(30.,-1.32966554433622E-14,31.6569162607362));
#53085=CARTESIAN_POINT('',(32.6816387576073,-0.609355047323343,31.6569162607362));
#53086=CARTESIAN_POINT('Origin',(32.6312454736857,-0.618796803902764,31.657022065625));
#53087=CARTESIAN_POINT('',(32.710701242781,-0.463248067869977,31.6569162607362));
#53088=CARTESIAN_POINT('Origin',(32.6677547413593,-0.435236788763208,31.6570432561875));
#53089=CARTESIAN_POINT('Origin',(30.,-1.32966554433622E-14,31.6569162607362));
#53090=CARTESIAN_POINT('Origin',(30.,-1.32966554433622E-14,31.6569162607362));
#53091=CARTESIAN_POINT('',(32.7211816062594,-0.397077657083801,31.6569162607362));
#53092=CARTESIAN_POINT('Origin',(32.6716844596186,-0.410444119388296,31.6570220656567));
#53093=CARTESIAN_POINT('',(32.7386910800031,-0.249140860381013,31.6569162607362));
#53094=CARTESIAN_POINT('Origin',(32.6936792286845,-0.224585474366052,31.6570432561872));
#53095=CARTESIAN_POINT('Origin',(30.,-1.32966554433622E-14,31.6569162607362));
#53096=CARTESIAN_POINT('Origin',(30.,-1.32966554433622E-14,31.6569162607362));
#53097=CARTESIAN_POINT('',(32.7439474654243,-0.182352151046618,31.6569162607362));
#53098=CARTESIAN_POINT('Origin',(32.695651622591,-0.19956091034649,31.6570220656247));
#53099=CARTESIAN_POINT('',(32.7497959760097,-0.0334976166400576,31.6569162607362));
#53100=CARTESIAN_POINT('Origin',(32.702996287825,-0.0125495158368562,31.657043256187));
#53101=CARTESIAN_POINT('Origin',(30.,-1.32966554433622E-14,31.6569162607362));
#53102=CARTESIAN_POINT('Origin',(30.,-1.32966554433622E-14,31.6569162607362));
#53103=CARTESIAN_POINT('',(32.7497959760097,0.0334976166400122,31.6569162607362));
#53104=CARTESIAN_POINT('Origin',(32.7029991968315,0.0125526580441019,31.6570220656263));
#53105=CARTESIAN_POINT('',(32.7439474654243,0.182352151046572,31.6569162607362));
#53106=CARTESIAN_POINT('Origin',(32.695648476013,0.199563814630937,31.6570432561873));
#53107=CARTESIAN_POINT('Origin',(30.,-1.32966554433622E-14,31.6569162607362));
#53108=CARTESIAN_POINT('Origin',(30.,-1.32966554433622E-14,31.6569162607362));
#53109=CARTESIAN_POINT('',(32.7386910800031,0.249140860380968,31.6569162607362));
#53110=CARTESIAN_POINT('Origin',(32.6936818821912,0.224588835126342,31.6570220656253));
#53111=CARTESIAN_POINT('',(32.7211816062594,0.397077657083756,31.6569162607362));
#53112=CARTESIAN_POINT('Origin',(32.6716810949533,0.410446767819417,31.657043256187));
#53113=CARTESIAN_POINT('Origin',(30.,-1.32966554433622E-14,31.6569162607362));
#53114=CARTESIAN_POINT('Origin',(30.,-1.32966554433622E-14,31.6569162607362));
#53115=CARTESIAN_POINT('',(32.710701242781,0.463248067869931,31.6569162607362));
#53116=CARTESIAN_POINT('Origin',(32.6677571230054,0.435240347356078,31.6570220656249));
#53117=CARTESIAN_POINT('',(32.6816387576073,0.609355047323298,31.6569162607362));
#53118=CARTESIAN_POINT('Origin',(32.6312419115184,0.618799180197174,31.657043256187));
#53119=CARTESIAN_POINT('Origin',(30.,-1.32966554433622E-14,31.6569162607362));
#53120=CARTESIAN_POINT('Origin',(30.,-1.32966554433622E-14,31.6569162607362));
#53121=CARTESIAN_POINT('',(32.6659990309976,0.674499196974863,31.6569162607362));
#53122=CARTESIAN_POINT('Origin',(32.6253847539863,0.643208458072405,31.6570220656495));
#53123=CARTESIAN_POINT('',(32.6255627142791,0.817875561064977,31.6569162607362));
#53124=CARTESIAN_POINT('Origin',(32.574580246722,0.823336489857403,31.6570432561872));
#53125=CARTESIAN_POINT('Origin',(30.,-1.32966554433622E-14,31.6569162607362));
#53126=CARTESIAN_POINT('Origin',(30.,-1.32966554433622E-14,31.6569162607362));
#53127=CARTESIAN_POINT('',(32.6048600486534,0.881591814236701,31.6569162607362));
#53128=CARTESIAN_POINT('Origin',(32.5668260150295,0.847210974834854,31.6570220656249));
#53129=CARTESIAN_POINT('',(32.5532992037291,1.02135360000147,31.6569162607362));
#53130=CARTESIAN_POINT('Origin',(32.5020454385711,1.02279765627039,31.6570432561869));
#53131=CARTESIAN_POINT('Origin',(30.,-1.32966554433622E-14,31.6569162607362));
#53132=CARTESIAN_POINT('Origin',(30.,-1.32966554433622E-14,31.6569162607362));
#53133=CARTESIAN_POINT('',(32.5276612379054,1.08324912480474,31.6569162607362));
#53134=CARTESIAN_POINT('Origin',(32.4924419400839,1.04599015417185,31.6570220656248));
#53135=CARTESIAN_POINT('',(32.4652937545301,1.21853465435941,31.6569162607362));
#53136=CARTESIAN_POINT('Origin',(32.4140846882753,1.2159529350178,31.657043256187));
#53137=CARTESIAN_POINT('Origin',(30.,-1.32966554433622E-14,31.6569162607362));
#53138=CARTESIAN_POINT('Origin',(30.,-1.32966554433622E-14,31.6569162607362));
#53139=CARTESIAN_POINT('',(32.4348785550931,1.27822784430148,31.6569162607362));
#53140=CARTESIAN_POINT('Origin',(32.4026911317566,1.23832045638126,31.6570220656248));
#53141=CARTESIAN_POINT('',(32.362088949541,1.40820303736934,31.6569162607362));
#53142=CARTESIAN_POINT('Origin',(32.3112403031114,1.40161145957535,31.6570432561874));
#53143=CARTESIAN_POINT('Origin',(30.,-1.32966554433622E-14,31.6569162607362));
#53144=CARTESIAN_POINT('Origin',(30.,-1.32966554433622E-14,31.6569162607362));
#53145=CARTESIAN_POINT('',(32.3270840363093,1.4653258640842,31.6569162607362));
#53146=CARTESIAN_POINT('Origin',(32.2981269336259,1.42301610119356,31.657022065625));
#53147=CARTESIAN_POINT('',(32.2443210807037,1.58918938037886,31.6569162607362));
#53148=CARTESIAN_POINT('Origin',(32.1941463529162,1.57862858340189,31.6570432561866));
#53149=CARTESIAN_POINT('Origin',(30.,-1.32966554433622E-14,31.6569162607362));
#53150=CARTESIAN_POINT('Origin',(30.,-1.32966554433622E-14,31.6569162607362));
#53151=CARTESIAN_POINT('',(32.2049422706078,1.64338966264455,31.6569162607362));
#53152=CARTESIAN_POINT('Origin',(32.1793940187453,1.59893837854221,31.6570220656245));
#53153=CARTESIAN_POINT('',(32.1127162260913,1.76037784239925,31.6569162607362));
#53154=CARTESIAN_POINT('Origin',(32.0635247608241,1.74591293706383,31.6570432561872));
#53155=CARTESIAN_POINT('Origin',(30.,-1.32966554433622E-14,31.6569162607362));
#53156=CARTESIAN_POINT('Origin',(30.,-1.32966554433622E-14,31.6569162607362));
#53157=CARTESIAN_POINT('',(32.0692063025902,1.81132141745218,31.6569162607362));
#53158=CARTESIAN_POINT('Origin',(32.0472244150162,1.76500266908448,31.6570220656248));
#53159=CARTESIAN_POINT('',(31.9680857733957,1.92071298963621,31.6569162607362));
#53160=CARTESIAN_POINT('Origin',(31.9201808523931,1.90243315689474,31.6570432561866));
#53161=CARTESIAN_POINT('Origin',(30.,-1.32966554433622E-14,31.6569162607362));
#53162=CARTESIAN_POINT('Origin',(30.,-1.32966554433622E-14,31.6569162607362));
#53163=CARTESIAN_POINT('',(31.9207129896362,1.96808577339572,31.6569162607362));
#53164=CARTESIAN_POINT('Origin',(31.9024329919958,1.92018513124459,31.657022065627));
#53165=CARTESIAN_POINT('',(31.8113214174522,2.06920630259018,31.6569162607362));
#53166=CARTESIAN_POINT('Origin',(31.7649983904793,2.04722424368911,31.6570432561871));
#53167=CARTESIAN_POINT('Origin',(30.,-1.32966554433622E-14,31.6569162607362));
#53168=CARTESIAN_POINT('Origin',(30.,-1.32966554433622E-14,31.6569162607362));
#53169=CARTESIAN_POINT('',(31.7603778423992,2.11271622609134,31.6569162607362));
#53170=CARTESIAN_POINT('Origin',(31.7459124369604,2.06352901355459,31.6570220656248));
#53171=CARTESIAN_POINT('',(31.6433896626445,2.20494227060776,31.6569162607362));
#53172=CARTESIAN_POINT('Origin',(31.5989341265682,2.17939351225069,31.657043256187));
#53173=CARTESIAN_POINT('Origin',(30.,-1.32966554433622E-14,31.6569162607362));
#53174=CARTESIAN_POINT('Origin',(30.,-1.32966554433622E-14,31.6569162607362));
#53175=CARTESIAN_POINT('',(31.5891893803789,2.24432108070368,31.6569162607362));
#53176=CARTESIAN_POINT('Origin',(31.5786277511742,2.19415055329685,31.6570220656251));
#53177=CARTESIAN_POINT('',(31.4653258640842,2.32708403630934,31.6569162607362));
#53178=CARTESIAN_POINT('Origin',(31.4230119020666,2.29812609508688,31.6570432561872));
#53179=CARTESIAN_POINT('Origin',(30.,-1.32966554433622E-14,31.6569162607362));
#53180=CARTESIAN_POINT('Origin',(30.,-1.32966554433622E-14,31.6569162607362));
#53181=CARTESIAN_POINT('',(31.4082030373693,2.36208894954099,31.6569162607362));
#53182=CARTESIAN_POINT('Origin',(31.4016103003533,2.31124442523252,31.6570220656319));
#53183=CARTESIAN_POINT('',(31.2782278443015,2.4348785550931,31.6569162607362));
#53184=CARTESIAN_POINT('Origin',(31.2383163359906,2.4026899663434,31.6570432561867));
#53185=CARTESIAN_POINT('Origin',(30.,-1.32966554433622E-14,31.6569162607362));
#53186=CARTESIAN_POINT('Origin',(30.,-1.32966554433622E-14,31.6569162607362));
#53187=CARTESIAN_POINT('',(31.2185346543594,2.46529375453009,31.6569162607362));
#53188=CARTESIAN_POINT('Origin',(31.215951455952,2.4140887067551,31.6570220656248));
#53189=CARTESIAN_POINT('',(31.0832491248047,2.52766123790544,31.6569162607362));
#53190=CARTESIAN_POINT('Origin',(31.045986137919,2.49244045498011,31.6570432561873));
#53191=CARTESIAN_POINT('Origin',(30.,-1.32966554433622E-14,31.6569162607362));
#53192=CARTESIAN_POINT('Origin',(30.,-1.32966554433622E-14,31.6569162607362));
#53193=CARTESIAN_POINT('',(31.0213536000015,2.55329920372915,31.6569162607362));
#53194=CARTESIAN_POINT('Origin',(31.0227958664779,2.50204932861496,31.6570220656254));
#53195=CARTESIAN_POINT('',(30.8815918142367,2.60486004865343,31.6569162607362));
#53196=CARTESIAN_POINT('Origin',(30.8472070874836,2.56682421939316,31.6570432561869));
#53197=CARTESIAN_POINT('Origin',(30.,-1.32966554433622E-14,31.6569162607362));
#53198=CARTESIAN_POINT('Origin',(30.,-1.32966554433622E-14,31.6569162607362));
#53199=CARTESIAN_POINT('',(30.817875561065,2.62556271427908,31.6569162607362));
#53200=CARTESIAN_POINT('Origin',(30.8233344003728,2.5745839843498,31.6570220656254));
#53201=CARTESIAN_POINT('',(30.6744991969749,2.6659990309976,31.6569162607362));
#53202=CARTESIAN_POINT('Origin',(30.6432047236281,2.62538265893739,31.6570432561868));
#53203=CARTESIAN_POINT('Origin',(30.,-1.32966554433622E-14,31.6569162607362));
#53204=CARTESIAN_POINT('Origin',(30.,-1.32966554433622E-14,31.6569162607362));
#53205=CARTESIAN_POINT('',(30.6093550473233,2.68163875760728,31.6569162607362));
#53206=CARTESIAN_POINT('Origin',(30.6187968039028,2.63124547368537,31.6570220656252));
#53207=CARTESIAN_POINT('',(30.4632480678699,2.71070124278104,31.6569162607362));
#53208=CARTESIAN_POINT('Origin',(30.4352367887645,2.66775474136143,31.6570432561865));
#53209=CARTESIAN_POINT('Origin',(30.,-1.32966554433622E-14,31.6569162607362));
#53210=CARTESIAN_POINT('Origin',(30.,-1.32966554433622E-14,31.6569162607362));
#53211=CARTESIAN_POINT('',(27.5651214449069,1.27822784430151,31.6569162607362));
#53212=CARTESIAN_POINT('Origin',(27.5973100336575,1.23831633598946,31.6570432561873));
#53213=CARTESIAN_POINT('',(27.637911050459,1.40820303736937,31.6569162607362));
#53214=CARTESIAN_POINT('Origin',(30.,-1.32966554433622E-14,31.6569162607362));
#53215=CARTESIAN_POINT('Origin',(27.6887555747495,1.40161030035545,31.6570220656248));
#53216=CARTESIAN_POINT('Origin',(30.,-1.32966554433622E-14,31.6569162607362));
#53217=CARTESIAN_POINT('',(27.6729159636906,1.46532586408423,31.6569162607362));
#53218=CARTESIAN_POINT('Origin',(27.7018739049127,1.42301190206727,31.6570432561868));
#53219=CARTESIAN_POINT('',(27.7556789192963,1.58918938037889,31.6569162607362));
#53220=CARTESIAN_POINT('Origin',(30.,-1.32966554433622E-14,31.6569162607362));
#53221=CARTESIAN_POINT('Origin',(27.805849446702,1.5786277511745,31.6570220656247));
#53222=CARTESIAN_POINT('Origin',(30.,-1.32966554433622E-14,31.6569162607362));
#53223=CARTESIAN_POINT('',(27.7950577293922,1.64338966264458,31.6569162607362));
#53224=CARTESIAN_POINT('Origin',(27.8206064877494,1.59893412656804,31.6570432561871));
#53225=CARTESIAN_POINT('',(27.8872837739086,1.76037784239928,31.6569162607362));
#53226=CARTESIAN_POINT('Origin',(30.,-1.32966554433622E-14,31.6569162607362));
#53227=CARTESIAN_POINT('Origin',(27.936470986445,1.74591243696058,31.6570220656246));
#53228=CARTESIAN_POINT('Origin',(30.,-1.32966554433622E-14,31.6569162607362));
#53229=CARTESIAN_POINT('',(27.9307936974098,1.81132141745221,31.6569162607362));
#53230=CARTESIAN_POINT('Origin',(27.9527757563104,1.76499839048029,31.6570432561867));
#53231=CARTESIAN_POINT('',(28.0319142266043,1.92071298963623,31.6569162607362));
#53232=CARTESIAN_POINT('Origin',(30.,-1.32966554433622E-14,31.6569162607362));
#53233=CARTESIAN_POINT('Origin',(28.0798148687497,1.90243299199796,31.6570220656246));
#53234=CARTESIAN_POINT('Origin',(30.,-1.32966554433622E-14,31.6569162607362));
#53235=CARTESIAN_POINT('',(28.0792870103638,1.96808577339574,31.6569162607362));
#53236=CARTESIAN_POINT('Origin',(28.0975668431059,1.92018085239124,31.6570432561874));
#53237=CARTESIAN_POINT('',(28.1886785825478,2.0692063025902,31.6569162607362));
#53238=CARTESIAN_POINT('Origin',(30.,-1.32966554433622E-14,31.6569162607362));
#53239=CARTESIAN_POINT('Origin',(28.2349973309159,2.04722441501599,31.657022065625));
#53240=CARTESIAN_POINT('Origin',(30.,-1.32966554433622E-14,31.6569162607362));
#53241=CARTESIAN_POINT('',(28.2396221576007,2.11271622609137,31.6569162607362));
#53242=CARTESIAN_POINT('Origin',(28.2540870629359,2.06352476082518,31.6570432561869));
#53243=CARTESIAN_POINT('',(28.3566103373554,2.20494227060779,31.6569162607362));
#53244=CARTESIAN_POINT('Origin',(30.,-1.32966554433622E-14,31.6569162607362));
#53245=CARTESIAN_POINT('Origin',(28.4010616214895,2.17939401872761,31.6570220656385));
#53246=CARTESIAN_POINT('Origin',(30.,-1.32966554433622E-14,31.6569162607362));
#53247=CARTESIAN_POINT('',(28.4108106196211,2.2443210807037,31.6569162607362));
#53248=CARTESIAN_POINT('Origin',(28.4213714165984,2.19414635291463,31.6570432561873));
#53249=CARTESIAN_POINT('',(28.5346741359158,2.32708403630936,31.6569162607362));
#53250=CARTESIAN_POINT('Origin',(30.,-1.32966554433622E-14,31.6569162607362));
#53251=CARTESIAN_POINT('Origin',(28.5769838988101,2.29812693362349,31.6570220656266));
#53252=CARTESIAN_POINT('Origin',(30.,-1.32966554433622E-14,31.6569162607362));
#53253=CARTESIAN_POINT('',(28.5917969626306,2.36208894954101,31.6569162607362));
#53254=CARTESIAN_POINT('Origin',(28.5983885404246,2.31124030311217,31.6570432561871));
#53255=CARTESIAN_POINT('',(28.7217721556985,2.43487855509312,31.6569162607362));
#53256=CARTESIAN_POINT('Origin',(30.,-1.32966554433622E-14,31.6569162607362));
#53257=CARTESIAN_POINT('Origin',(28.7616795436181,2.40269113175706,31.6570220656245));
#53258=CARTESIAN_POINT('Origin',(30.,-1.32966554433622E-14,31.6569162607362));
#53259=CARTESIAN_POINT('',(28.7814653456406,2.46529375453011,31.6569162607362));
#53260=CARTESIAN_POINT('Origin',(28.7840470649822,2.41408468827519,31.6570432561871));
#53261=CARTESIAN_POINT('',(28.9167508751953,2.52766123790545,31.6569162607362));
#53262=CARTESIAN_POINT('Origin',(30.,-1.32966554433622E-14,31.6569162607362));
#53263=CARTESIAN_POINT('Origin',(28.9540098458282,2.49244194008388,31.6570220656249));
#53264=CARTESIAN_POINT('Origin',(30.,-1.32966554433622E-14,31.6569162607362));
#53265=CARTESIAN_POINT('',(28.9786463999985,2.55329920372917,31.6569162607362));
#53266=CARTESIAN_POINT('Origin',(28.9772023437296,2.50204543857058,31.657043256187));
#53267=CARTESIAN_POINT('',(29.1184081857633,2.60486004865344,31.6569162607362));
#53268=CARTESIAN_POINT('Origin',(30.,-1.32966554433622E-14,31.6569162607362));
#53269=CARTESIAN_POINT('Origin',(29.1527890251647,2.56682601503002,31.6570220656247));
#53270=CARTESIAN_POINT('Origin',(30.,-1.32966554433622E-14,31.6569162607362));
#53271=CARTESIAN_POINT('',(29.182124438935,2.62556271427909,31.6569162607362));
#53272=CARTESIAN_POINT('Origin',(29.1766635101426,2.57458024672254,31.657043256187));
#53273=CARTESIAN_POINT('',(29.3255008030251,2.66599903099761,31.6569162607362));
#53274=CARTESIAN_POINT('Origin',(30.,-1.32966554433622E-14,31.6569162607362));
#53275=CARTESIAN_POINT('Origin',(29.356791541893,2.62538475403008,31.657022065628));
#53276=CARTESIAN_POINT('Origin',(30.,-1.32966554433622E-14,31.6569162607362));
#53277=CARTESIAN_POINT('',(29.3906449526767,2.68163875760729,31.6569162607362));
#53278=CARTESIAN_POINT('Origin',(29.3812008198028,2.6312419115181,31.6570432561872));
#53279=CARTESIAN_POINT('',(29.5367519321301,2.71070124278105,31.6569162607362));
#53280=CARTESIAN_POINT('Origin',(30.,-1.32966554433622E-14,31.6569162607362));
#53281=CARTESIAN_POINT('Origin',(29.5647596526443,2.66775712300484,31.6570220656252));
#53282=CARTESIAN_POINT('Origin',(30.,-1.32966554433622E-14,31.6569162607362));
#53283=CARTESIAN_POINT('',(29.6029223429162,2.72118160625946,31.6569162607362));
#53284=CARTESIAN_POINT('Origin',(29.5895532321803,2.67168109495224,31.6570432561874));
#53285=CARTESIAN_POINT('',(29.750859139619,2.7386910800031,31.6569162607362));
#53286=CARTESIAN_POINT('Origin',(30.,-1.32966554433622E-14,31.6569162607362));
#53287=CARTESIAN_POINT('Origin',(29.7754111648735,2.69368188219135,31.6570220656252));
#53288=CARTESIAN_POINT('Origin',(30.,-1.32966554433622E-14,31.6569162607362));
#53289=CARTESIAN_POINT('',(29.8176478489534,2.74394746542433,31.6569162607362));
#53290=CARTESIAN_POINT('Origin',(29.8004361853695,2.6956484760142,31.6570432561868));
#53291=CARTESIAN_POINT('',(29.9665023833599,2.74979597600974,31.6569162607362));
#53292=CARTESIAN_POINT('Origin',(30.,-1.32966554433622E-14,31.6569162607362));
#53293=CARTESIAN_POINT('Origin',(29.9874473419551,2.70299919683309,31.6570220656256));
#53294=CARTESIAN_POINT('Origin',(30.,-1.32966554433622E-14,31.6569162607362));
#53295=CARTESIAN_POINT('',(30.3970776570838,2.72118160625945,31.6569162607362));
#53296=CARTESIAN_POINT('Origin',(30.4104441193885,2.67168445961759,31.6570220656571));
#53297=CARTESIAN_POINT('',(30.249140860381,2.7386910800031,31.6569162607362));
#53298=CARTESIAN_POINT('Origin',(30.2245854743662,2.69367922868485,31.657043256187));
#53299=CARTESIAN_POINT('Origin',(30.,-1.32966554433622E-14,31.6569162607362));
#53300=CARTESIAN_POINT('Origin',(30.,-1.32966554433622E-14,16.));
#53301=CARTESIAN_POINT('',(27.4723387620945,1.08324912480478,33.8305837392638));
#53302=CARTESIAN_POINT('',(27.4723387620945,1.08324912480478,16.));
#53303=CARTESIAN_POINT('',(27.5347062454699,1.21853465435945,33.8305837392638));
#53304=CARTESIAN_POINT('Origin',(30.,-1.32966554433622E-14,33.8305837392638));
#53305=CARTESIAN_POINT('',(27.5347062454699,1.21853465435945,16.));
#53306=CARTESIAN_POINT('Origin',(30.,-1.32966554433622E-14,16.));
#53307=CARTESIAN_POINT('',(27.4467007962708,1.0213536000015,33.8305837392638));
#53308=CARTESIAN_POINT('',(27.4467007962708,1.0213536000015,16.));
#53309=CARTESIAN_POINT('',(27.3951399513465,0.881591814236741,33.8305837392638));
#53310=CARTESIAN_POINT('',(27.3951399513465,0.881591814236737,16.));
#53311=CARTESIAN_POINT('Origin',(30.,-1.32966554433622E-14,33.8305837392638));
#53312=CARTESIAN_POINT('Origin',(30.,-1.32966554433622E-14,16.));
#53313=CARTESIAN_POINT('',(27.3744372857209,0.817875561065013,33.8305837392638));
#53314=CARTESIAN_POINT('',(27.3744372857209,0.817875561065013,16.));
#53315=CARTESIAN_POINT('',(27.3340009690024,0.674499196974903,33.8305837392638));
#53316=CARTESIAN_POINT('',(27.3340009690024,0.674499196974899,16.));
#53317=CARTESIAN_POINT('Origin',(30.,-1.32966554433622E-14,33.8305837392638));
#53318=CARTESIAN_POINT('Origin',(30.,-1.32966554433622E-14,16.));
#53319=CARTESIAN_POINT('',(27.3183612423927,0.609355047323334,33.8305837392638));
#53320=CARTESIAN_POINT('',(27.3183612423927,0.609355047323335,16.));
#53321=CARTESIAN_POINT('',(27.2892987572189,0.463248067869974,33.8305837392638));
#53322=CARTESIAN_POINT('',(27.2892987572189,0.463248067869971,16.));
#53323=CARTESIAN_POINT('Origin',(30.,-1.32966554433622E-14,33.8305837392638));
#53324=CARTESIAN_POINT('Origin',(30.,-1.32966554433622E-14,16.));
#53325=CARTESIAN_POINT('',(27.2788183937405,0.397077657083793,33.8305837392638));
#53326=CARTESIAN_POINT('',(27.2788183937405,0.397077657083795,16.));
#53327=CARTESIAN_POINT('',(27.2613089199969,0.24914086038101,33.8305837392638));
#53328=CARTESIAN_POINT('',(27.2613089199969,0.249140860381007,16.));
#53329=CARTESIAN_POINT('Origin',(30.,-1.32966554433622E-14,33.8305837392638));
#53330=CARTESIAN_POINT('Origin',(30.,-1.32966554433622E-14,16.));
#53331=CARTESIAN_POINT('',(27.2560525345756,0.182352151046609,33.8305837392638));
#53332=CARTESIAN_POINT('',(27.2560525345756,0.182352151046611,16.));
#53333=CARTESIAN_POINT('',(27.2502040239902,0.0334976166400525,33.8305837392638));
#53334=CARTESIAN_POINT('',(27.2502040239902,0.0334976166400503,16.));
#53335=CARTESIAN_POINT('Origin',(30.,-1.32966554433622E-14,33.8305837392638));
#53336=CARTESIAN_POINT('Origin',(30.,-1.32966554433622E-14,16.));
#53337=CARTESIAN_POINT('',(27.2502040239902,-0.0334976166400219,33.8305837392638));
#53338=CARTESIAN_POINT('',(27.2502040239902,-0.0334976166400194,16.));
#53339=CARTESIAN_POINT('',(27.2560525345756,-0.182352151046578,33.8305837392638));
#53340=CARTESIAN_POINT('',(27.2560525345756,-0.18235215104658,16.));
#53341=CARTESIAN_POINT('Origin',(30.,-1.32966554433622E-14,33.8305837392638));
#53342=CARTESIAN_POINT('Origin',(30.,-1.32966554433622E-14,16.));
#53343=CARTESIAN_POINT('',(27.2613089199969,-0.249140860380979,33.8305837392638));
#53344=CARTESIAN_POINT('',(27.2613089199969,-0.249140860380976,16.));
#53345=CARTESIAN_POINT('',(27.2788183937405,-0.397077657083761,33.8305837392638));
#53346=CARTESIAN_POINT('',(27.2788183937405,-0.397077657083763,16.));
#53347=CARTESIAN_POINT('Origin',(30.,-1.32966554433622E-14,33.8305837392638));
#53348=CARTESIAN_POINT('Origin',(30.,-1.32966554433622E-14,16.));
#53349=CARTESIAN_POINT('',(27.2892987572189,-0.463248067869942,33.8305837392638));
#53350=CARTESIAN_POINT('',(27.2892987572189,-0.463248067869938,16.));
#53351=CARTESIAN_POINT('',(27.3183612423927,-0.609355047323305,33.8305837392638));
#53352=CARTESIAN_POINT('',(27.3183612423927,-0.609355047323306,16.));
#53353=CARTESIAN_POINT('Origin',(30.,-1.32966554433622E-14,33.8305837392638));
#53354=CARTESIAN_POINT('Origin',(30.,-1.32966554433622E-14,16.));
#53355=CARTESIAN_POINT('',(27.3340009690023,-0.674499196974875,33.8305837392638));
#53356=CARTESIAN_POINT('',(27.3340009690024,-0.674499196974871,16.));
#53357=CARTESIAN_POINT('',(27.3744372857209,-0.817875561064985,33.8305837392638));
#53358=CARTESIAN_POINT('',(27.3744372857209,-0.817875561064986,16.));
#53359=CARTESIAN_POINT('Origin',(30.,-1.32966554433622E-14,33.8305837392638));
#53360=CARTESIAN_POINT('Origin',(30.,-1.32966554433622E-14,16.));
#53361=CARTESIAN_POINT('',(27.3951399513465,-0.881591814236714,33.8305837392638));
#53362=CARTESIAN_POINT('',(27.3951399513465,-0.88159181423671,16.));
#53363=CARTESIAN_POINT('',(27.4467007962708,-1.02135360000148,33.8305837392638));
#53364=CARTESIAN_POINT('',(27.4467007962708,-1.02135360000148,16.));
#53365=CARTESIAN_POINT('Origin',(30.,-1.32966554433622E-14,33.8305837392638));
#53366=CARTESIAN_POINT('Origin',(30.,-1.32966554433622E-14,16.));
#53367=CARTESIAN_POINT('',(27.4723387620945,-1.08324912480476,33.8305837392638));
#53368=CARTESIAN_POINT('',(27.4723387620945,-1.08324912480475,16.));
#53369=CARTESIAN_POINT('',(27.5347062454699,-1.21853465435942,33.8305837392638));
#53370=CARTESIAN_POINT('',(27.5347062454699,-1.21853465435942,16.));
#53371=CARTESIAN_POINT('Origin',(30.,-1.32966554433622E-14,33.8305837392638));
#53372=CARTESIAN_POINT('Origin',(30.,-1.32966554433622E-14,16.));
#53373=CARTESIAN_POINT('',(27.5651214449068,-1.27822784430149,33.8305837392638));
#53374=CARTESIAN_POINT('',(27.5651214449068,-1.27822784430149,16.));
#53375=CARTESIAN_POINT('',(27.637911050459,-1.40820303736935,33.8305837392638));
#53376=CARTESIAN_POINT('',(27.637911050459,-1.40820303736935,16.));
#53377=CARTESIAN_POINT('Origin',(30.,-1.32966554433622E-14,33.8305837392638));
#53378=CARTESIAN_POINT('Origin',(30.,-1.32966554433622E-14,16.));
#53379=CARTESIAN_POINT('',(27.6729159636906,-1.46532586408422,33.8305837392638));
#53380=CARTESIAN_POINT('',(27.6729159636906,-1.46532586408421,16.));
#53381=CARTESIAN_POINT('',(27.7556789192963,-1.58918938037887,33.8305837392638));
#53382=CARTESIAN_POINT('',(27.7556789192963,-1.58918938037887,16.));
#53383=CARTESIAN_POINT('Origin',(30.,-1.32966554433622E-14,33.8305837392638));
#53384=CARTESIAN_POINT('Origin',(30.,-1.32966554433622E-14,16.));
#53385=CARTESIAN_POINT('',(27.7950577293922,-1.64338966264456,33.8305837392638));
#53386=CARTESIAN_POINT('',(27.7950577293922,-1.64338966264456,16.));
#53387=CARTESIAN_POINT('',(27.8872837739086,-1.76037784239926,33.8305837392638));
#53388=CARTESIAN_POINT('',(27.8872837739086,-1.76037784239926,16.));
#53389=CARTESIAN_POINT('Origin',(30.,-1.32966554433622E-14,33.8305837392638));
#53390=CARTESIAN_POINT('Origin',(30.,-1.32966554433622E-14,16.));
#53391=CARTESIAN_POINT('',(27.9307936974098,-1.81132141745219,33.8305837392638));
#53392=CARTESIAN_POINT('',(27.9307936974098,-1.81132141745219,16.));
#53393=CARTESIAN_POINT('',(28.0319142266042,-1.92071298963622,33.8305837392638));
#53394=CARTESIAN_POINT('',(28.0319142266042,-1.92071298963622,16.));
#53395=CARTESIAN_POINT('Origin',(30.,-1.32966554433622E-14,33.8305837392638));
#53396=CARTESIAN_POINT('Origin',(30.,-1.32966554433622E-14,16.));
#53397=CARTESIAN_POINT('',(28.0792870103637,-1.96808577339574,33.8305837392638));
#53398=CARTESIAN_POINT('',(28.0792870103637,-1.96808577339573,16.));
#53399=CARTESIAN_POINT('',(28.1886785825478,-2.06920630259019,33.8305837392638));
#53400=CARTESIAN_POINT('',(28.1886785825478,-2.06920630259019,16.));
#53401=CARTESIAN_POINT('Origin',(30.,-1.32966554433622E-14,33.8305837392638));
#53402=CARTESIAN_POINT('Origin',(30.,-1.32966554433622E-14,16.));
#53403=CARTESIAN_POINT('',(28.2396221576007,-2.11271622609136,33.8305837392638));
#53404=CARTESIAN_POINT('',(28.2396221576007,-2.11271622609136,16.));
#53405=CARTESIAN_POINT('',(28.3566103373554,-2.20494227060778,33.8305837392638));
#53406=CARTESIAN_POINT('',(28.3566103373554,-2.20494227060778,16.));
#53407=CARTESIAN_POINT('Origin',(30.,-1.32966554433622E-14,33.8305837392638));
#53408=CARTESIAN_POINT('Origin',(30.,-1.32966554433622E-14,16.));
#53409=CARTESIAN_POINT('',(28.4108106196211,-2.2443210807037,33.8305837392638));
#53410=CARTESIAN_POINT('',(28.4108106196211,-2.2443210807037,16.));
#53411=CARTESIAN_POINT('',(28.5346741359157,-2.32708403630936,33.8305837392638));
#53412=CARTESIAN_POINT('',(28.5346741359157,-2.32708403630936,16.));
#53413=CARTESIAN_POINT('Origin',(30.,-1.32966554433622E-14,33.8305837392638));
#53414=CARTESIAN_POINT('Origin',(30.,-1.32966554433622E-14,16.));
#53415=CARTESIAN_POINT('',(28.5917969626306,-2.36208894954101,33.8305837392638));
#53416=CARTESIAN_POINT('',(28.5917969626306,-2.362088949541,16.));
#53417=CARTESIAN_POINT('',(28.7217721556985,-2.43487855509313,33.8305837392638));
#53418=CARTESIAN_POINT('',(28.7217721556985,-2.43487855509312,16.));
#53419=CARTESIAN_POINT('Origin',(30.,-1.32966554433622E-14,33.8305837392638));
#53420=CARTESIAN_POINT('Origin',(30.,-1.32966554433622E-14,16.));
#53421=CARTESIAN_POINT('',(28.7814653456405,-2.46529375453011,33.8305837392638));
#53422=CARTESIAN_POINT('',(28.7814653456405,-2.46529375453011,16.));
#53423=CARTESIAN_POINT('',(28.9167508751952,-2.52766123790546,33.8305837392638));
#53424=CARTESIAN_POINT('',(28.9167508751952,-2.52766123790546,16.));
#53425=CARTESIAN_POINT('Origin',(30.,-1.32966554433622E-14,33.8305837392638));
#53426=CARTESIAN_POINT('Origin',(30.,-1.32966554433622E-14,16.));
#53427=CARTESIAN_POINT('',(28.9786463999985,-2.55329920372918,33.8305837392638));
#53428=CARTESIAN_POINT('',(28.9786463999985,-2.55329920372917,16.));
#53429=CARTESIAN_POINT('',(29.1184081857632,-2.60486004865345,33.8305837392638));
#53430=CARTESIAN_POINT('',(29.1184081857632,-2.60486004865345,16.));
#53431=CARTESIAN_POINT('Origin',(30.,-1.32966554433622E-14,33.8305837392638));
#53432=CARTESIAN_POINT('Origin',(30.,-1.32966554433622E-14,16.));
#53433=CARTESIAN_POINT('',(29.182124438935,-2.62556271427911,33.8305837392638));
#53434=CARTESIAN_POINT('',(29.182124438935,-2.6255627142791,16.));
#53435=CARTESIAN_POINT('',(29.3255008030251,-2.66599903099763,33.8305837392638));
#53436=CARTESIAN_POINT('',(29.3255008030251,-2.66599903099763,16.));
#53437=CARTESIAN_POINT('Origin',(30.,-1.32966554433622E-14,33.8305837392638));
#53438=CARTESIAN_POINT('Origin',(30.,-1.32966554433622E-14,16.));
#53439=CARTESIAN_POINT('',(29.3906449526766,-2.68163875760731,33.8305837392638));
#53440=CARTESIAN_POINT('',(29.3906449526766,-2.6816387576073,16.));
#53441=CARTESIAN_POINT('',(29.53675193213,-2.71070124278107,33.8305837392638));
#53442=CARTESIAN_POINT('',(29.53675193213,-2.71070124278106,16.));
#53443=CARTESIAN_POINT('Origin',(30.,-1.32966554433622E-14,33.8305837392638));
#53444=CARTESIAN_POINT('Origin',(30.,-1.32966554433622E-14,16.));
#53445=CARTESIAN_POINT('',(29.6029223429162,-2.72118160625948,33.8305837392638));
#53446=CARTESIAN_POINT('',(29.6029223429162,-2.72118160625948,16.));
#53447=CARTESIAN_POINT('',(29.750859139619,-2.73869108000313,33.8305837392638));
#53448=CARTESIAN_POINT('',(29.750859139619,-2.73869108000313,16.));
#53449=CARTESIAN_POINT('Origin',(30.,-1.32966554433622E-14,33.8305837392638));
#53450=CARTESIAN_POINT('Origin',(30.,-1.32966554433622E-14,16.));
#53451=CARTESIAN_POINT('',(29.8176478489534,-2.74394746542436,33.8305837392638));
#53452=CARTESIAN_POINT('',(29.8176478489534,-2.74394746542436,16.));
#53453=CARTESIAN_POINT('',(29.9665023833599,-2.74979597600977,33.8305837392638));
#53454=CARTESIAN_POINT('',(29.9665023833599,-2.74979597600977,16.));
#53455=CARTESIAN_POINT('Origin',(30.,-1.32966554433622E-14,33.8305837392638));
#53456=CARTESIAN_POINT('Origin',(30.,-1.32966554433622E-14,16.));
#53457=CARTESIAN_POINT('',(30.03349761664,-2.74979597600977,33.8305837392638));
#53458=CARTESIAN_POINT('',(30.03349761664,-2.74979597600977,16.));
#53459=CARTESIAN_POINT('',(30.1823521510466,-2.74394746542436,33.8305837392638));
#53460=CARTESIAN_POINT('',(30.1823521510466,-2.74394746542436,16.));
#53461=CARTESIAN_POINT('Origin',(30.,-1.32966554433622E-14,33.8305837392638));
#53462=CARTESIAN_POINT('Origin',(30.,-1.32966554433622E-14,16.));
#53463=CARTESIAN_POINT('',(30.249140860381,-2.73869108000313,33.8305837392638));
#53464=CARTESIAN_POINT('',(30.2491408603809,-2.73869108000313,16.));
#53465=CARTESIAN_POINT('',(30.3970776570837,-2.72118160625949,33.8305837392638));
#53466=CARTESIAN_POINT('',(30.3970776570837,-2.72118160625948,16.));
#53467=CARTESIAN_POINT('Origin',(30.,-1.32966554433622E-14,33.8305837392638));
#53468=CARTESIAN_POINT('Origin',(30.,-1.32966554433622E-14,16.));
#53469=CARTESIAN_POINT('',(30.4632480678699,-2.71070124278108,33.8305837392638));
#53470=CARTESIAN_POINT('',(30.4632480678699,-2.71070124278107,16.));
#53471=CARTESIAN_POINT('',(30.6093550473233,-2.68163875760732,33.8305837392638));
#53472=CARTESIAN_POINT('',(30.6093550473233,-2.68163875760731,16.));
#53473=CARTESIAN_POINT('Origin',(30.,-1.32966554433622E-14,33.8305837392638));
#53474=CARTESIAN_POINT('Origin',(30.,-1.32966554433622E-14,16.));
#53475=CARTESIAN_POINT('',(30.6744991969748,-2.66599903099764,33.8305837392638));
#53476=CARTESIAN_POINT('',(30.6744991969748,-2.66599903099764,16.));
#53477=CARTESIAN_POINT('',(30.817875561065,-2.62556271427912,33.8305837392638));
#53478=CARTESIAN_POINT('',(30.817875561065,-2.62556271427912,16.));
#53479=CARTESIAN_POINT('Origin',(30.,-1.32966554433622E-14,33.8305837392638));
#53480=CARTESIAN_POINT('Origin',(30.,-1.32966554433622E-14,16.));
#53481=CARTESIAN_POINT('',(30.8815918142367,-2.60486004865346,33.8305837392638));
#53482=CARTESIAN_POINT('',(30.8815918142367,-2.60486004865346,16.));
#53483=CARTESIAN_POINT('',(31.0213536000014,-2.55329920372919,33.8305837392638));
#53484=CARTESIAN_POINT('',(31.0213536000014,-2.55329920372919,16.));
#53485=CARTESIAN_POINT('Origin',(30.,-1.32966554433622E-14,33.8305837392638));
#53486=CARTESIAN_POINT('Origin',(30.,-1.32966554433622E-14,16.));
#53487=CARTESIAN_POINT('',(31.0832491248047,-2.52766123790547,33.8305837392638));
#53488=CARTESIAN_POINT('',(31.0832491248047,-2.52766123790547,16.));
#53489=CARTESIAN_POINT('',(31.2185346543594,-2.46529375453013,33.8305837392638));
#53490=CARTESIAN_POINT('',(31.2185346543594,-2.46529375453013,16.));
#53491=CARTESIAN_POINT('Origin',(30.,-1.32966554433622E-14,33.8305837392638));
#53492=CARTESIAN_POINT('Origin',(30.,-1.32966554433622E-14,16.));
#53493=CARTESIAN_POINT('',(31.2782278443015,-2.43487855509314,33.8305837392638));
#53494=CARTESIAN_POINT('',(31.2782278443015,-2.43487855509314,16.));
#53495=CARTESIAN_POINT('',(31.4082030373693,-2.36208894954103,33.8305837392638));
#53496=CARTESIAN_POINT('',(31.4082030373693,-2.36208894954102,16.));
#53497=CARTESIAN_POINT('Origin',(30.,-1.32966554433622E-14,33.8305837392638));
#53498=CARTESIAN_POINT('Origin',(30.,-1.32966554433622E-14,16.));
#53499=CARTESIAN_POINT('',(31.4653258640842,-2.32708403630938,33.8305837392638));
#53500=CARTESIAN_POINT('',(31.4653258640842,-2.32708403630938,16.));
#53501=CARTESIAN_POINT('',(31.5891893803788,-2.24432108070372,33.8305837392638));
#53502=CARTESIAN_POINT('',(31.5891893803788,-2.24432108070372,16.));
#53503=CARTESIAN_POINT('Origin',(30.,-1.32966554433622E-14,33.8305837392638));
#53504=CARTESIAN_POINT('Origin',(30.,-1.32966554433622E-14,16.));
#53505=CARTESIAN_POINT('',(31.6433896626445,-2.2049422706078,33.8305837392638));
#53506=CARTESIAN_POINT('',(31.6433896626445,-2.2049422706078,16.));
#53507=CARTESIAN_POINT('',(31.7603778423992,-2.11271622609139,33.8305837392638));
#53508=CARTESIAN_POINT('',(31.7603778423992,-2.11271622609138,16.));
#53509=CARTESIAN_POINT('Origin',(30.,-1.32966554433622E-14,33.8305837392638));
#53510=CARTESIAN_POINT('Origin',(30.,-1.32966554433622E-14,16.));
#53511=CARTESIAN_POINT('',(31.8113214174522,-2.06920630259022,33.8305837392638));
#53512=CARTESIAN_POINT('',(31.8113214174522,-2.06920630259022,16.));
#53513=CARTESIAN_POINT('',(31.9207129896362,-1.96808577339576,33.8305837392638));
#53514=CARTESIAN_POINT('',(31.9207129896362,-1.96808577339576,16.));
#53515=CARTESIAN_POINT('Origin',(30.,-1.32966554433622E-14,33.8305837392638));
#53516=CARTESIAN_POINT('Origin',(30.,-1.32966554433622E-14,16.));
#53517=CARTESIAN_POINT('',(31.9680857733957,-1.92071298963625,33.8305837392638));
#53518=CARTESIAN_POINT('',(31.9680857733957,-1.92071298963625,16.));
#53519=CARTESIAN_POINT('',(32.0692063025902,-1.81132141745222,33.8305837392638));
#53520=CARTESIAN_POINT('',(32.0692063025902,-1.81132141745222,16.));
#53521=CARTESIAN_POINT('Origin',(30.,-1.32966554433622E-14,33.8305837392638));
#53522=CARTESIAN_POINT('Origin',(30.,-1.32966554433622E-14,16.));
#53523=CARTESIAN_POINT('',(32.1127162260913,-1.76037784239929,33.8305837392638));
#53524=CARTESIAN_POINT('',(32.1127162260913,-1.76037784239929,16.));
#53525=CARTESIAN_POINT('',(32.2049422706078,-1.6433896626446,33.8305837392638));
#53526=CARTESIAN_POINT('',(32.2049422706077,-1.64338966264459,16.));
#53527=CARTESIAN_POINT('Origin',(30.,-1.32966554433622E-14,33.8305837392638));
#53528=CARTESIAN_POINT('Origin',(30.,-1.32966554433622E-14,16.));
#53529=CARTESIAN_POINT('',(32.2443210807037,-1.5891893803789,33.8305837392638));
#53530=CARTESIAN_POINT('',(32.2443210807037,-1.5891893803789,16.));
#53531=CARTESIAN_POINT('',(32.3270840363093,-1.46532586408425,33.8305837392638));
#53532=CARTESIAN_POINT('',(32.3270840363093,-1.46532586408424,16.));
#53533=CARTESIAN_POINT('Origin',(30.,-1.32966554433622E-14,33.8305837392638));
#53534=CARTESIAN_POINT('Origin',(30.,-1.32966554433622E-14,16.));
#53535=CARTESIAN_POINT('',(32.362088949541,-1.40820303736938,33.8305837392638));
#53536=CARTESIAN_POINT('',(32.362088949541,-1.40820303736938,16.));
#53537=CARTESIAN_POINT('',(32.4348785550931,-1.27822784430152,33.8305837392638));
#53538=CARTESIAN_POINT('',(32.4348785550931,-1.27822784430152,16.));
#53539=CARTESIAN_POINT('Origin',(30.,-1.32966554433622E-14,33.8305837392638));
#53540=CARTESIAN_POINT('Origin',(30.,-1.32966554433622E-14,16.));
#53541=CARTESIAN_POINT('',(32.4652937545301,-1.21853465435946,33.8305837392638));
#53542=CARTESIAN_POINT('',(32.4652937545301,-1.21853465435946,16.));
#53543=CARTESIAN_POINT('',(32.5276612379054,-1.08324912480479,33.8305837392638));
#53544=CARTESIAN_POINT('',(32.5276612379054,-1.08324912480479,16.));
#53545=CARTESIAN_POINT('Origin',(30.,-1.32966554433622E-14,33.8305837392638));
#53546=CARTESIAN_POINT('Origin',(30.,-1.32966554433622E-14,16.));
#53547=CARTESIAN_POINT('',(32.5532992037291,-1.02135360000151,33.8305837392638));
#53548=CARTESIAN_POINT('',(32.5532992037291,-1.02135360000151,16.));
#53549=CARTESIAN_POINT('',(32.6048600486534,-0.88159181423675,33.8305837392638));
#53550=CARTESIAN_POINT('',(32.6048600486534,-0.881591814236746,16.));
#53551=CARTESIAN_POINT('Origin',(30.,-1.32966554433622E-14,33.8305837392638));
#53552=CARTESIAN_POINT('Origin',(30.,-1.32966554433622E-14,16.));
#53553=CARTESIAN_POINT('',(32.6255627142791,-0.817875561065022,33.8305837392638));
#53554=CARTESIAN_POINT('',(32.6255627142791,-0.817875561065022,16.));
#53555=CARTESIAN_POINT('',(32.6659990309976,-0.674499196974912,33.8305837392638));
#53556=CARTESIAN_POINT('',(32.6659990309976,-0.674499196974908,16.));
#53557=CARTESIAN_POINT('Origin',(30.,-1.32966554433622E-14,33.8305837392638));
#53558=CARTESIAN_POINT('Origin',(30.,-1.32966554433622E-14,16.));
#53559=CARTESIAN_POINT('',(32.6816387576073,-0.609355047323342,33.8305837392638));
#53560=CARTESIAN_POINT('',(32.6816387576073,-0.609355047323343,16.));
#53561=CARTESIAN_POINT('',(32.710701242781,-0.463248067869981,33.8305837392638));
#53562=CARTESIAN_POINT('',(32.710701242781,-0.463248067869977,16.));
#53563=CARTESIAN_POINT('Origin',(30.,-1.32966554433622E-14,33.8305837392638));
#53564=CARTESIAN_POINT('Origin',(30.,-1.32966554433622E-14,16.));
#53565=CARTESIAN_POINT('',(32.7211816062594,-0.3970776570838,33.8305837392638));
#53566=CARTESIAN_POINT('',(32.7211816062594,-0.397077657083801,16.));
#53567=CARTESIAN_POINT('',(32.7386910800031,-0.249140860381016,33.8305837392638));
#53568=CARTESIAN_POINT('',(32.7386910800031,-0.249140860381013,16.));
#53569=CARTESIAN_POINT('Origin',(30.,-1.32966554433622E-14,33.8305837392638));
#53570=CARTESIAN_POINT('Origin',(30.,-1.32966554433622E-14,16.));
#53571=CARTESIAN_POINT('',(32.7439474654243,-0.182352151046616,33.8305837392638));
#53572=CARTESIAN_POINT('',(32.7439474654243,-0.182352151046618,16.));
#53573=CARTESIAN_POINT('',(32.7497959760097,-0.03349761664006,33.8305837392638));
#53574=CARTESIAN_POINT('',(32.7497959760097,-0.0334976166400576,16.));
#53575=CARTESIAN_POINT('Origin',(30.,-1.32966554433622E-14,33.8305837392638));
#53576=CARTESIAN_POINT('Origin',(30.,-1.32966554433622E-14,16.));
#53577=CARTESIAN_POINT('',(32.7497959760097,0.0334976166400146,33.8305837392638));
#53578=CARTESIAN_POINT('',(32.7497959760097,0.0334976166400122,16.));
#53579=CARTESIAN_POINT('',(32.7439474654243,0.18235215104657,33.8305837392638));
#53580=CARTESIAN_POINT('',(32.7439474654243,0.182352151046572,16.));
#53581=CARTESIAN_POINT('Origin',(30.,-1.32966554433622E-14,33.8305837392638));
#53582=CARTESIAN_POINT('Origin',(30.,-1.32966554433622E-14,16.));
#53583=CARTESIAN_POINT('',(32.7386910800031,0.249140860380971,33.8305837392638));
#53584=CARTESIAN_POINT('',(32.7386910800031,0.249140860380968,16.));
#53585=CARTESIAN_POINT('',(32.7211816062594,0.397077657083754,33.8305837392638));
#53586=CARTESIAN_POINT('',(32.7211816062594,0.397077657083756,16.));
#53587=CARTESIAN_POINT('Origin',(30.,-1.32966554433622E-14,33.8305837392638));
#53588=CARTESIAN_POINT('Origin',(30.,-1.32966554433622E-14,16.));
#53589=CARTESIAN_POINT('',(32.710701242781,0.463248067869934,33.8305837392638));
#53590=CARTESIAN_POINT('',(32.710701242781,0.463248067869931,16.));
#53591=CARTESIAN_POINT('',(32.6816387576073,0.609355047323297,33.8305837392638));
#53592=CARTESIAN_POINT('',(32.6816387576073,0.609355047323298,16.));
#53593=CARTESIAN_POINT('Origin',(30.,-1.32966554433622E-14,33.8305837392638));
#53594=CARTESIAN_POINT('Origin',(30.,-1.32966554433622E-14,16.));
#53595=CARTESIAN_POINT('',(32.6659990309976,0.674499196974867,33.8305837392638));
#53596=CARTESIAN_POINT('',(32.6659990309976,0.674499196974863,16.));
#53597=CARTESIAN_POINT('',(32.6255627142791,0.817875561064977,33.8305837392638));
#53598=CARTESIAN_POINT('',(32.6255627142791,0.817875561064977,16.));
#53599=CARTESIAN_POINT('Origin',(30.,-1.32966554433622E-14,33.8305837392638));
#53600=CARTESIAN_POINT('Origin',(30.,-1.32966554433622E-14,16.));
#53601=CARTESIAN_POINT('',(32.6048600486534,0.881591814236705,33.8305837392638));
#53602=CARTESIAN_POINT('',(32.6048600486534,0.881591814236701,16.));
#53603=CARTESIAN_POINT('',(32.5532992037292,1.02135360000147,33.8305837392638));
#53604=CARTESIAN_POINT('',(32.5532992037291,1.02135360000147,16.));
#53605=CARTESIAN_POINT('Origin',(30.,-1.32966554433622E-14,33.8305837392638));
#53606=CARTESIAN_POINT('Origin',(30.,-1.32966554433622E-14,16.));
#53607=CARTESIAN_POINT('',(32.5276612379054,1.08324912480475,33.8305837392638));
#53608=CARTESIAN_POINT('',(32.5276612379054,1.08324912480474,16.));
#53609=CARTESIAN_POINT('',(32.4652937545301,1.21853465435941,33.8305837392638));
#53610=CARTESIAN_POINT('',(32.4652937545301,1.21853465435941,16.));
#53611=CARTESIAN_POINT('Origin',(30.,-1.32966554433622E-14,33.8305837392638));
#53612=CARTESIAN_POINT('Origin',(30.,-1.32966554433622E-14,16.));
#53613=CARTESIAN_POINT('',(32.4348785550931,1.27822784430148,33.8305837392638));
#53614=CARTESIAN_POINT('',(32.4348785550931,1.27822784430148,16.));
#53615=CARTESIAN_POINT('',(32.362088949541,1.40820303736934,33.8305837392638));
#53616=CARTESIAN_POINT('',(32.362088949541,1.40820303736934,16.));
#53617=CARTESIAN_POINT('Origin',(30.,-1.32966554433622E-14,33.8305837392638));
#53618=CARTESIAN_POINT('Origin',(30.,-1.32966554433622E-14,16.));
#53619=CARTESIAN_POINT('',(32.3270840363093,1.4653258640842,33.8305837392638));
#53620=CARTESIAN_POINT('',(32.3270840363093,1.4653258640842,16.));
#53621=CARTESIAN_POINT('',(32.2443210807037,1.58918938037886,33.8305837392638));
#53622=CARTESIAN_POINT('',(32.2443210807037,1.58918938037886,16.));
#53623=CARTESIAN_POINT('Origin',(30.,-1.32966554433622E-14,33.8305837392638));
#53624=CARTESIAN_POINT('Origin',(30.,-1.32966554433622E-14,16.));
#53625=CARTESIAN_POINT('',(32.2049422706078,1.64338966264455,33.8305837392638));
#53626=CARTESIAN_POINT('',(32.2049422706078,1.64338966264455,16.));
#53627=CARTESIAN_POINT('',(32.1127162260914,1.76037784239925,33.8305837392638));
#53628=CARTESIAN_POINT('',(32.1127162260913,1.76037784239925,16.));
#53629=CARTESIAN_POINT('Origin',(30.,-1.32966554433622E-14,33.8305837392638));
#53630=CARTESIAN_POINT('Origin',(30.,-1.32966554433622E-14,16.));
#53631=CARTESIAN_POINT('',(32.0692063025902,1.81132141745218,33.8305837392638));
#53632=CARTESIAN_POINT('',(32.0692063025902,1.81132141745218,16.));
#53633=CARTESIAN_POINT('',(31.9680857733957,1.92071298963621,33.8305837392638));
#53634=CARTESIAN_POINT('',(31.9680857733957,1.92071298963621,16.));
#53635=CARTESIAN_POINT('Origin',(30.,-1.32966554433622E-14,33.8305837392638));
#53636=CARTESIAN_POINT('Origin',(30.,-1.32966554433622E-14,16.));
#53637=CARTESIAN_POINT('',(31.9207129896362,1.96808577339572,33.8305837392638));
#53638=CARTESIAN_POINT('',(31.9207129896362,1.96808577339572,16.));
#53639=CARTESIAN_POINT('',(31.8113214174522,2.06920630259018,33.8305837392638));
#53640=CARTESIAN_POINT('',(31.8113214174522,2.06920630259018,16.));
#53641=CARTESIAN_POINT('Origin',(30.,-1.32966554433622E-14,33.8305837392638));
#53642=CARTESIAN_POINT('Origin',(30.,-1.32966554433622E-14,16.));
#53643=CARTESIAN_POINT('',(31.7603778423992,2.11271622609135,33.8305837392638));
#53644=CARTESIAN_POINT('',(31.7603778423992,2.11271622609134,16.));
#53645=CARTESIAN_POINT('',(31.6433896626446,2.20494227060777,33.8305837392638));
#53646=CARTESIAN_POINT('',(31.6433896626445,2.20494227060776,16.));
#53647=CARTESIAN_POINT('Origin',(30.,-1.32966554433622E-14,33.8305837392638));
#53648=CARTESIAN_POINT('Origin',(30.,-1.32966554433622E-14,16.));
#53649=CARTESIAN_POINT('',(31.5891893803789,2.24432108070369,33.8305837392638));
#53650=CARTESIAN_POINT('',(31.5891893803789,2.24432108070368,16.));
#53651=CARTESIAN_POINT('',(31.4653258640842,2.32708403630934,33.8305837392638));
#53652=CARTESIAN_POINT('',(31.4653258640842,2.32708403630934,16.));
#53653=CARTESIAN_POINT('Origin',(30.,-1.32966554433622E-14,33.8305837392638));
#53654=CARTESIAN_POINT('Origin',(30.,-1.32966554433622E-14,16.));
#53655=CARTESIAN_POINT('',(31.4082030373693,2.36208894954099,33.8305837392638));
#53656=CARTESIAN_POINT('',(31.4082030373693,2.36208894954099,16.));
#53657=CARTESIAN_POINT('',(31.2782278443015,2.43487855509311,33.8305837392638));
#53658=CARTESIAN_POINT('',(31.2782278443015,2.4348785550931,16.));
#53659=CARTESIAN_POINT('Origin',(30.,-1.32966554433622E-14,33.8305837392638));
#53660=CARTESIAN_POINT('Origin',(30.,-1.32966554433622E-14,16.));
#53661=CARTESIAN_POINT('',(31.2185346543594,2.4652937545301,33.8305837392638));
#53662=CARTESIAN_POINT('',(31.2185346543594,2.46529375453009,16.));
#53663=CARTESIAN_POINT('',(31.0832491248047,2.52766123790544,33.8305837392638));
#53664=CARTESIAN_POINT('',(31.0832491248047,2.52766123790544,16.));
#53665=CARTESIAN_POINT('Origin',(30.,-1.32966554433622E-14,33.8305837392638));
#53666=CARTESIAN_POINT('Origin',(30.,-1.32966554433622E-14,16.));
#53667=CARTESIAN_POINT('',(31.0213536000015,2.55329920372916,33.8305837392638));
#53668=CARTESIAN_POINT('',(31.0213536000015,2.55329920372915,16.));
#53669=CARTESIAN_POINT('',(30.8815918142367,2.60486004865343,33.8305837392638));
#53670=CARTESIAN_POINT('',(30.8815918142367,2.60486004865343,16.));
#53671=CARTESIAN_POINT('Origin',(30.,-1.32966554433622E-14,33.8305837392638));
#53672=CARTESIAN_POINT('Origin',(30.,-1.32966554433622E-14,16.));
#53673=CARTESIAN_POINT('',(30.817875561065,2.62556271427909,33.8305837392638));
#53674=CARTESIAN_POINT('',(30.817875561065,2.62556271427908,16.));
#53675=CARTESIAN_POINT('',(30.6744991969749,2.66599903099761,33.8305837392638));
#53676=CARTESIAN_POINT('',(30.6744991969749,2.6659990309976,16.));
#53677=CARTESIAN_POINT('Origin',(30.,-1.32966554433622E-14,33.8305837392638));
#53678=CARTESIAN_POINT('Origin',(30.,-1.32966554433622E-14,16.));
#53679=CARTESIAN_POINT('',(30.6093550473233,2.68163875760729,33.8305837392638));
#53680=CARTESIAN_POINT('',(30.6093550473233,2.68163875760728,16.));
#53681=CARTESIAN_POINT('',(30.4632480678699,2.71070124278105,33.8305837392638));
#53682=CARTESIAN_POINT('',(30.4632480678699,2.71070124278104,16.));
#53683=CARTESIAN_POINT('Origin',(30.,-1.32966554433622E-14,33.8305837392638));
#53684=CARTESIAN_POINT('Origin',(30.,-1.32966554433622E-14,16.));
#53685=CARTESIAN_POINT('',(27.5651214449069,1.27822784430151,33.8305837392638));
#53686=CARTESIAN_POINT('',(27.5651214449069,1.27822784430151,16.));
#53687=CARTESIAN_POINT('',(27.637911050459,1.40820303736937,33.8305837392638));
#53688=CARTESIAN_POINT('Origin',(30.,-1.32966554433622E-14,33.8305837392638));
#53689=CARTESIAN_POINT('',(27.637911050459,1.40820303736937,16.));
#53690=CARTESIAN_POINT('Origin',(30.,-1.32966554433622E-14,16.));
#53691=CARTESIAN_POINT('',(27.6729159636906,1.46532586408424,33.8305837392638));
#53692=CARTESIAN_POINT('',(27.6729159636906,1.46532586408423,16.));
#53693=CARTESIAN_POINT('',(27.7556789192963,1.58918938037889,33.8305837392638));
#53694=CARTESIAN_POINT('Origin',(30.,-1.32966554433622E-14,33.8305837392638));
#53695=CARTESIAN_POINT('',(27.7556789192963,1.58918938037889,16.));
#53696=CARTESIAN_POINT('Origin',(30.,-1.32966554433622E-14,16.));
#53697=CARTESIAN_POINT('',(27.7950577293922,1.64338966264458,33.8305837392638));
#53698=CARTESIAN_POINT('',(27.7950577293922,1.64338966264458,16.));
#53699=CARTESIAN_POINT('',(27.8872837739086,1.76037784239928,33.8305837392638));
#53700=CARTESIAN_POINT('Origin',(30.,-1.32966554433622E-14,33.8305837392638));
#53701=CARTESIAN_POINT('',(27.8872837739086,1.76037784239928,16.));
#53702=CARTESIAN_POINT('Origin',(30.,-1.32966554433622E-14,16.));
#53703=CARTESIAN_POINT('',(27.9307936974098,1.81132141745221,33.8305837392638));
#53704=CARTESIAN_POINT('',(27.9307936974098,1.81132141745221,16.));
#53705=CARTESIAN_POINT('',(28.0319142266043,1.92071298963624,33.8305837392638));
#53706=CARTESIAN_POINT('Origin',(30.,-1.32966554433622E-14,33.8305837392638));
#53707=CARTESIAN_POINT('',(28.0319142266043,1.92071298963623,16.));
#53708=CARTESIAN_POINT('Origin',(30.,-1.32966554433622E-14,16.));
#53709=CARTESIAN_POINT('',(28.0792870103638,1.96808577339575,33.8305837392638));
#53710=CARTESIAN_POINT('',(28.0792870103638,1.96808577339574,16.));
#53711=CARTESIAN_POINT('',(28.1886785825478,2.06920630259021,33.8305837392638));
#53712=CARTESIAN_POINT('Origin',(30.,-1.32966554433622E-14,33.8305837392638));
#53713=CARTESIAN_POINT('',(28.1886785825478,2.0692063025902,16.));
#53714=CARTESIAN_POINT('Origin',(30.,-1.32966554433622E-14,16.));
#53715=CARTESIAN_POINT('',(28.2396221576007,2.11271622609138,33.8305837392638));
#53716=CARTESIAN_POINT('',(28.2396221576007,2.11271622609137,16.));
#53717=CARTESIAN_POINT('',(28.3566103373554,2.20494227060779,33.8305837392638));
#53718=CARTESIAN_POINT('Origin',(30.,-1.32966554433622E-14,33.8305837392638));
#53719=CARTESIAN_POINT('',(28.3566103373554,2.20494227060779,16.));
#53720=CARTESIAN_POINT('Origin',(30.,-1.32966554433622E-14,16.));
#53721=CARTESIAN_POINT('',(28.4108106196211,2.24432108070371,33.8305837392638));
#53722=CARTESIAN_POINT('',(28.4108106196211,2.2443210807037,16.));
#53723=CARTESIAN_POINT('',(28.5346741359158,2.32708403630936,33.8305837392638));
#53724=CARTESIAN_POINT('Origin',(30.,-1.32966554433622E-14,33.8305837392638));
#53725=CARTESIAN_POINT('',(28.5346741359158,2.32708403630936,16.));
#53726=CARTESIAN_POINT('Origin',(30.,-1.32966554433622E-14,16.));
#53727=CARTESIAN_POINT('',(28.5917969626306,2.36208894954101,33.8305837392638));
#53728=CARTESIAN_POINT('',(28.5917969626306,2.36208894954101,16.));
#53729=CARTESIAN_POINT('',(28.7217721556985,2.43487855509313,33.8305837392638));
#53730=CARTESIAN_POINT('Origin',(30.,-1.32966554433622E-14,33.8305837392638));
#53731=CARTESIAN_POINT('',(28.7217721556985,2.43487855509312,16.));
#53732=CARTESIAN_POINT('Origin',(30.,-1.32966554433622E-14,16.));
#53733=CARTESIAN_POINT('',(28.7814653456406,2.46529375453011,33.8305837392638));
#53734=CARTESIAN_POINT('',(28.7814653456406,2.46529375453011,16.));
#53735=CARTESIAN_POINT('',(28.9167508751952,2.52766123790546,33.8305837392638));
#53736=CARTESIAN_POINT('Origin',(30.,-1.32966554433622E-14,33.8305837392638));
#53737=CARTESIAN_POINT('',(28.9167508751953,2.52766123790545,16.));
#53738=CARTESIAN_POINT('Origin',(30.,-1.32966554433622E-14,16.));
#53739=CARTESIAN_POINT('',(28.9786463999985,2.55329920372917,33.8305837392638));
#53740=CARTESIAN_POINT('',(28.9786463999985,2.55329920372917,16.));
#53741=CARTESIAN_POINT('',(29.1184081857633,2.60486004865344,33.8305837392638));
#53742=CARTESIAN_POINT('Origin',(30.,-1.32966554433622E-14,33.8305837392638));
#53743=CARTESIAN_POINT('',(29.1184081857633,2.60486004865344,16.));
#53744=CARTESIAN_POINT('Origin',(30.,-1.32966554433622E-14,16.));
#53745=CARTESIAN_POINT('',(29.182124438935,2.6255627142791,33.8305837392638));
#53746=CARTESIAN_POINT('',(29.182124438935,2.62556271427909,16.));
#53747=CARTESIAN_POINT('',(29.3255008030251,2.66599903099762,33.8305837392638));
#53748=CARTESIAN_POINT('Origin',(30.,-1.32966554433622E-14,33.8305837392638));
#53749=CARTESIAN_POINT('',(29.3255008030251,2.66599903099761,16.));
#53750=CARTESIAN_POINT('Origin',(30.,-1.32966554433622E-14,16.));
#53751=CARTESIAN_POINT('',(29.3906449526767,2.6816387576073,33.8305837392638));
#53752=CARTESIAN_POINT('',(29.3906449526767,2.68163875760729,16.));
#53753=CARTESIAN_POINT('',(29.5367519321301,2.71070124278105,33.8305837392638));
#53754=CARTESIAN_POINT('Origin',(30.,-1.32966554433622E-14,33.8305837392638));
#53755=CARTESIAN_POINT('',(29.5367519321301,2.71070124278105,16.));
#53756=CARTESIAN_POINT('Origin',(30.,-1.32966554433622E-14,16.));
#53757=CARTESIAN_POINT('',(29.6029223429162,2.72118160625947,33.8305837392638));
#53758=CARTESIAN_POINT('',(29.6029223429162,2.72118160625946,16.));
#53759=CARTESIAN_POINT('',(29.750859139619,2.73869108000311,33.8305837392638));
#53760=CARTESIAN_POINT('Origin',(30.,-1.32966554433622E-14,33.8305837392638));
#53761=CARTESIAN_POINT('',(29.750859139619,2.7386910800031,16.));
#53762=CARTESIAN_POINT('Origin',(30.,-1.32966554433622E-14,16.));
#53763=CARTESIAN_POINT('',(29.8176478489534,2.74394746542434,33.8305837392638));
#53764=CARTESIAN_POINT('',(29.8176478489534,2.74394746542433,16.));
#53765=CARTESIAN_POINT('',(29.9665023833599,2.74979597600975,33.8305837392638));
#53766=CARTESIAN_POINT('Origin',(30.,-1.32966554433622E-14,33.8305837392638));
#53767=CARTESIAN_POINT('',(29.9665023833599,2.74979597600974,16.));
#53768=CARTESIAN_POINT('Origin',(30.,-1.32966554433622E-14,16.));
#53769=CARTESIAN_POINT('',(30.3970776570838,2.72118160625946,33.8305837392638));
#53770=CARTESIAN_POINT('',(30.3970776570838,2.72118160625945,16.));
#53771=CARTESIAN_POINT('',(30.249140860381,2.73869108000311,33.8305837392638));
#53772=CARTESIAN_POINT('',(30.249140860381,2.7386910800031,16.));
#53773=CARTESIAN_POINT('Origin',(30.,-1.32966554433622E-14,33.8305837392638));
#53774=CARTESIAN_POINT('Origin',(30.,-1.32966554433622E-14,33.8305837392638));
#53775=CARTESIAN_POINT('Origin',(27.5075580599235,1.0459901541636,33.8304779343707));
#53776=CARTESIAN_POINT('Origin',(27.5859153117241,1.21595293501799,33.830456743813));
#53777=CARTESIAN_POINT('Origin',(30.,-1.32966554433622E-14,33.8305837392638));
#53778=CARTESIAN_POINT('Origin',(27.4979545614264,1.02279765627048,33.8304567438139));
#53779=CARTESIAN_POINT('Origin',(27.4331739849704,0.847210974834779,33.830477934375));
#53780=CARTESIAN_POINT('Origin',(30.,-1.32966554433622E-14,33.8305837392638));
#53781=CARTESIAN_POINT('Origin',(27.4254197532764,0.823336489857381,33.8304567438132));
#53782=CARTESIAN_POINT('Origin',(27.3746152459633,0.643208458112014,33.8304779343751));
#53783=CARTESIAN_POINT('Origin',(30.,-1.32966554433622E-14,33.8305837392638));
#53784=CARTESIAN_POINT('Origin',(27.368758088479,0.618799180196873,33.8304567438137));
#53785=CARTESIAN_POINT('Origin',(27.3322428769935,0.435240347356666,33.8304779343754));
#53786=CARTESIAN_POINT('Origin',(30.,-1.32966554433622E-14,33.8305837392638));
#53787=CARTESIAN_POINT('Origin',(27.3283189050469,0.410446767819665,33.8304567438127));
#53788=CARTESIAN_POINT('Origin',(27.3063181178076,0.224588835126915,33.8304779343751));
#53789=CARTESIAN_POINT('Origin',(30.,-1.32966554433622E-14,33.8305837392638));
#53790=CARTESIAN_POINT('Origin',(27.3043515239852,0.199563814630461,33.8304567438133));
#53791=CARTESIAN_POINT('Origin',(27.2970008031678,0.0125526580442922,33.8304779343738));
#53792=CARTESIAN_POINT('Origin',(30.,-1.32966554433622E-14,33.8305837392638));
#53793=CARTESIAN_POINT('Origin',(27.2970037121732,-0.012549515837469,33.8304567438135));
#53794=CARTESIAN_POINT('Origin',(27.3043483774083,-0.199560910346332,33.8304779343754));
#53795=CARTESIAN_POINT('Origin',(30.,-1.32966554433622E-14,33.8305837392638));
#53796=CARTESIAN_POINT('Origin',(27.3063207713147,-0.224585474366301,33.8304567438129));
#53797=CARTESIAN_POINT('Origin',(27.3283155403039,-0.410444119366497,33.8304779343742));
#53798=CARTESIAN_POINT('Origin',(30.,-1.32966554433622E-14,33.8305837392638));
#53799=CARTESIAN_POINT('Origin',(27.3322452586388,-0.435236788764194,33.8304567438132));
#53800=CARTESIAN_POINT('Origin',(27.3687545263134,-0.618796803902706,33.8304779343752));
#53801=CARTESIAN_POINT('Origin',(30.,-1.32966554433622E-14,33.8305837392638));
#53802=CARTESIAN_POINT('Origin',(27.3746173410614,-0.643204723628853,33.8304567438136));
#53803=CARTESIAN_POINT('Origin',(27.4254160156486,-0.823334400372707,33.8304779343751));
#53804=CARTESIAN_POINT('Origin',(30.,-1.32966554433622E-14,33.8305837392638));
#53805=CARTESIAN_POINT('Origin',(27.433175780606,-0.847207087484101,33.8304567438133));
#53806=CARTESIAN_POINT('Origin',(27.4979506713824,-1.02279586647791,33.8304779343754));
#53807=CARTESIAN_POINT('Origin',(30.,-1.32966554433622E-14,33.8305837392638));
#53808=CARTESIAN_POINT('Origin',(27.5075595450189,-1.04598613791989,33.830456743813));
#53809=CARTESIAN_POINT('Origin',(27.5859112932449,-1.21595145595217,33.830477934375));
#53810=CARTESIAN_POINT('Origin',(30.,-1.32966554433622E-14,33.8305837392638));
#53811=CARTESIAN_POINT('Origin',(27.5973100336554,-1.23831633599182,33.8304567438138));
#53812=CARTESIAN_POINT('Origin',(27.6887555747498,-1.40161030035549,33.8304779343749));
#53813=CARTESIAN_POINT('Origin',(30.,-1.32966554433622E-14,33.8305837392638));
#53814=CARTESIAN_POINT('Origin',(27.7018739049122,-1.42301190206769,33.8304567438132));
#53815=CARTESIAN_POINT('Origin',(27.8058494467036,-1.57862775117429,33.8304779343746));
#53816=CARTESIAN_POINT('Origin',(30.,-1.32966554433622E-14,33.8305837392638));
#53817=CARTESIAN_POINT('Origin',(27.8206064877493,-1.59893412656796,33.8304567438128));
#53818=CARTESIAN_POINT('Origin',(27.9364709864456,-1.74591243696051,33.830477934375));
#53819=CARTESIAN_POINT('Origin',(30.,-1.32966554433622E-14,33.8305837392638));
#53820=CARTESIAN_POINT('Origin',(27.9527757563098,-1.76499839048126,33.8304567438135));
#53821=CARTESIAN_POINT('Origin',(28.0798148687495,-1.90243299199812,33.8304779343753));
#53822=CARTESIAN_POINT('Origin',(30.,-1.32966554433622E-14,33.8305837392638));
#53823=CARTESIAN_POINT('Origin',(28.0975668431045,-1.92018085239454,33.8304567438138));
#53824=CARTESIAN_POINT('Origin',(28.234997330915,-2.04722441501659,33.8304779343752));
#53825=CARTESIAN_POINT('Origin',(30.,-1.32966554433622E-14,33.8305837392638));
#53826=CARTESIAN_POINT('Origin',(28.2540870629355,-2.06352476082575,33.8304567438132));
#53827=CARTESIAN_POINT('Origin',(28.4010616214883,-2.1793940187284,33.8304779343619));
#53828=CARTESIAN_POINT('Origin',(30.,-1.32966554433622E-14,33.8305837392638));
#53829=CARTESIAN_POINT('Origin',(28.4213714165976,-2.19414635291788,33.8304567438138));
#53830=CARTESIAN_POINT('Origin',(28.5769838988107,-2.29812693362319,33.8304779343729));
#53831=CARTESIAN_POINT('Origin',(30.,-1.32966554433622E-14,33.8305837392638));
#53832=CARTESIAN_POINT('Origin',(28.5983885404242,-2.31124030311337,33.8304567438133));
#53833=CARTESIAN_POINT('Origin',(28.7616795436178,-2.40269113175742,33.8304779343754));
#53834=CARTESIAN_POINT('Origin',(30.,-1.32966554433622E-14,33.8305837392638));
#53835=CARTESIAN_POINT('Origin',(28.7840470649819,-2.41408468827727,33.8304567438135));
#53836=CARTESIAN_POINT('Origin',(28.9540098458287,-2.49244194008352,33.8304779343747));
#53837=CARTESIAN_POINT('Origin',(30.,-1.32966554433622E-14,33.8305837392638));
#53838=CARTESIAN_POINT('Origin',(28.9772023437295,-2.50204543857419,33.8304567438141));
#53839=CARTESIAN_POINT('Origin',(29.1527890251654,-2.5668260150294,33.8304779343748));
#53840=CARTESIAN_POINT('Origin',(30.,-1.32966554433622E-14,33.8305837392638));
#53841=CARTESIAN_POINT('Origin',(29.1766635101425,-2.57458024672298,33.8304567438129));
#53842=CARTESIAN_POINT('Origin',(29.3567915418921,-2.62538475403142,33.8304779343725));
#53843=CARTESIAN_POINT('Origin',(30.,-1.32966554433622E-14,33.8305837392638));
#53844=CARTESIAN_POINT('Origin',(29.3812008198029,-2.63124191151983,33.8304567438133));
#53845=CARTESIAN_POINT('Origin',(29.5647596526443,-2.66775712300496,33.8304779343746));
#53846=CARTESIAN_POINT('Origin',(30.,-1.32966554433622E-14,33.8305837392638));
#53847=CARTESIAN_POINT('Origin',(29.589553232181,-2.67168109495555,33.8304567438136));
#53848=CARTESIAN_POINT('Origin',(29.7754111648755,-2.69368188218804,33.8304779343731));
#53849=CARTESIAN_POINT('Origin',(30.,-1.32966554433622E-14,33.8305837392638));
#53850=CARTESIAN_POINT('Origin',(29.8004361853699,-2.69564847601571,33.8304567438137));
#53851=CARTESIAN_POINT('Origin',(29.9874473419542,-2.70299919683539,33.8304779343752));
#53852=CARTESIAN_POINT('Origin',(30.,-1.32966554433622E-14,33.8305837392638));
#53853=CARTESIAN_POINT('Origin',(30.0125495158367,-2.70299628782517,33.8304567438128));
#53854=CARTESIAN_POINT('Origin',(30.199560910346,-2.6956516225925,33.8304779343757));
#53855=CARTESIAN_POINT('Origin',(30.,-1.32966554433622E-14,33.8305837392638));
#53856=CARTESIAN_POINT('Origin',(30.2245854743665,-2.69367922868563,33.8304567438131));
#53857=CARTESIAN_POINT('Origin',(30.4104441193657,-2.67168445969903,33.8304779343754));
#53858=CARTESIAN_POINT('Origin',(30.,-1.32966554433622E-14,33.8305837392638));
#53859=CARTESIAN_POINT('Origin',(30.4352367887642,-2.66775474136125,33.8304567438132));
#53860=CARTESIAN_POINT('Origin',(30.6187968039027,-2.63124547368644,33.8304779343751));
#53861=CARTESIAN_POINT('Origin',(30.,-1.32966554433622E-14,33.8305837392638));
#53862=CARTESIAN_POINT('Origin',(30.6432047236274,-2.6253826589367,33.8304567438126));
#53863=CARTESIAN_POINT('Origin',(30.8233344003726,-2.57458398435223,33.8304779343755));
#53864=CARTESIAN_POINT('Origin',(30.,-1.32966554433622E-14,33.8305837392638));
#53865=CARTESIAN_POINT('Origin',(30.8472070874839,-2.5668242193938,33.8304567438132));
#53866=CARTESIAN_POINT('Origin',(31.0227958664778,-2.50204932861793,33.8304779343756));
#53867=CARTESIAN_POINT('Origin',(30.,-1.32966554433622E-14,33.8305837392638));
#53868=CARTESIAN_POINT('Origin',(31.0459861379201,-2.49244045498134,33.8304567438131));
#53869=CARTESIAN_POINT('Origin',(31.2159514559521,-2.41408870675381,33.8304779343746));
#53870=CARTESIAN_POINT('Origin',(30.,-1.32966554433622E-14,33.8305837392638));
#53871=CARTESIAN_POINT('Origin',(31.2383163359911,-2.402689966344,33.8304567438135));
#53872=CARTESIAN_POINT('Origin',(31.4016103003557,-2.3112444252517,33.8304779343755));
#53873=CARTESIAN_POINT('Origin',(30.,-1.32966554433622E-14,33.8305837392638));
#53874=CARTESIAN_POINT('Origin',(31.4230119020685,-2.29812609508837,33.8304567438136));
#53875=CARTESIAN_POINT('Origin',(31.5786277511746,-2.19415055329817,33.8304779343753));
#53876=CARTESIAN_POINT('Origin',(30.,-1.32966554433622E-14,33.8305837392638));
#53877=CARTESIAN_POINT('Origin',(31.5989341265715,-2.17939351225268,33.8304567438143));
#53878=CARTESIAN_POINT('Origin',(31.7459124369605,-2.06352901355452,33.8304779343751));
#53879=CARTESIAN_POINT('Origin',(30.,-1.32966554433622E-14,33.8305837392638));
#53880=CARTESIAN_POINT('Origin',(31.764998390482,-2.04722424369058,33.8304567438139));
#53881=CARTESIAN_POINT('Origin',(31.9024329919978,-1.92018513124985,33.8304779343751));
#53882=CARTESIAN_POINT('Origin',(30.,-1.32966554433622E-14,33.8305837392638));
#53883=CARTESIAN_POINT('Origin',(31.9201808523926,-1.90243315689474,33.8304567438131));
#53884=CARTESIAN_POINT('Origin',(32.0472244150163,-1.76500266908446,33.830477934375));
#53885=CARTESIAN_POINT('Origin',(30.,-1.32966554433622E-14,33.8305837392638));
#53886=CARTESIAN_POINT('Origin',(32.0635247608254,-1.74591293706441,33.8304567438131));
#53887=CARTESIAN_POINT('Origin',(32.1793940187282,-1.59893837851134,33.8304779343617));
#53888=CARTESIAN_POINT('Origin',(30.,-1.32966554433622E-14,33.8305837392638));
#53889=CARTESIAN_POINT('Origin',(32.1941463529172,-1.57862858340229,33.8304567438136));
#53890=CARTESIAN_POINT('Origin',(32.2981269336233,-1.42301610118952,33.830477934373));
#53891=CARTESIAN_POINT('Origin',(30.,-1.32966554433622E-14,33.8305837392638));
#53892=CARTESIAN_POINT('Origin',(32.311240303114,-1.40161145957583,33.8304567438134));
#53893=CARTESIAN_POINT('Origin',(32.4026911317571,-1.23832045638176,33.8304779343753));
#53894=CARTESIAN_POINT('Origin',(30.,-1.32966554433622E-14,33.8305837392638));
#53895=CARTESIAN_POINT('Origin',(32.4140846882749,-1.21595293501797,33.8304567438127));
#53896=CARTESIAN_POINT('Origin',(32.4924419400838,-1.04599015417152,33.8304779343749));
#53897=CARTESIAN_POINT('Origin',(30.,-1.32966554433622E-14,33.8305837392638));
#53898=CARTESIAN_POINT('Origin',(32.5020454385714,-1.02279765627054,33.8304567438132));
#53899=CARTESIAN_POINT('Origin',(32.56682601503,-0.847210974835106,33.8304779343751));
#53900=CARTESIAN_POINT('Origin',(30.,-1.32966554433622E-14,33.8305837392638));
#53901=CARTESIAN_POINT('Origin',(32.5745802467237,-0.823336489857386,33.8304567438133));
#53902=CARTESIAN_POINT('Origin',(32.6253847540299,-0.643208458106727,33.8304779343718));
#53903=CARTESIAN_POINT('Origin',(30.,-1.32966554433622E-14,33.8305837392638));
#53904=CARTESIAN_POINT('Origin',(32.6312419115182,-0.618799180197391,33.8304567438127));
#53905=CARTESIAN_POINT('Origin',(32.6677571230055,-0.435240347356057,33.830477934375));
#53906=CARTESIAN_POINT('Origin',(30.,-1.32966554433622E-14,33.8305837392638));
#53907=CARTESIAN_POINT('Origin',(32.6716810949544,-0.410446767819313,33.8304567438133));
#53908=CARTESIAN_POINT('Origin',(32.6936818821919,-0.224588835126652,33.8304779343749));
#53909=CARTESIAN_POINT('Origin',(30.,-1.32966554433622E-14,33.8305837392638));
#53910=CARTESIAN_POINT('Origin',(32.6956484760151,-0.199563814630355,33.8304567438134));
#53911=CARTESIAN_POINT('Origin',(32.7029991968333,-0.0125526580448477,33.8304779343743));
#53912=CARTESIAN_POINT('Origin',(30.,-1.32966554433622E-14,33.8305837392638));
#53913=CARTESIAN_POINT('Origin',(32.7029962878262,0.0125495158371826,33.8304567438133));
#53914=CARTESIAN_POINT('Origin',(32.6956516225903,0.19956091034681,33.8304779343749));
#53915=CARTESIAN_POINT('Origin',(30.,-1.32966554433622E-14,33.8305837392638));
#53916=CARTESIAN_POINT('Origin',(32.6936792286859,0.22458547436666,33.8304567438133));
#53917=CARTESIAN_POINT('Origin',(32.6716844596177,0.410444119388619,33.8304779343428));
#53918=CARTESIAN_POINT('Origin',(30.,-1.32966554433622E-14,33.8305837392638));
#53919=CARTESIAN_POINT('Origin',(32.6677547413622,0.435236788764869,33.8304567438136));
#53920=CARTESIAN_POINT('Origin',(32.6312454736863,0.618796803902747,33.8304779343751));
#53921=CARTESIAN_POINT('Origin',(30.,-1.32966554433622E-14,33.8305837392638));
#53922=CARTESIAN_POINT('Origin',(32.625382658939,0.643204723629168,33.8304567438138));
#53923=CARTESIAN_POINT('Origin',(32.5745839843506,0.823334400372804,33.8304779343749));
#53924=CARTESIAN_POINT('Origin',(30.,-1.32966554433622E-14,33.8305837392638));
#53925=CARTESIAN_POINT('Origin',(32.5668242193939,0.847207087484111,33.8304567438133));
#53926=CARTESIAN_POINT('Origin',(32.5020493286164,1.02279586647793,33.830477934375));
#53927=CARTESIAN_POINT('Origin',(30.,-1.32966554433622E-14,33.8305837392638));
#53928=CARTESIAN_POINT('Origin',(32.4924404549818,1.04598613792066,33.8304567438134));
#53929=CARTESIAN_POINT('Origin',(32.4140887067556,1.21595145595219,33.8304779343752));
#53930=CARTESIAN_POINT('Origin',(30.,-1.32966554433622E-14,33.8305837392638));
#53931=CARTESIAN_POINT('Origin',(32.4026899663445,1.2383163359917,33.8304567438137));
#53932=CARTESIAN_POINT('Origin',(32.3112444252326,1.40161030035344,33.830477934368));
#53933=CARTESIAN_POINT('Origin',(30.,-1.32966554433622E-14,33.8305837392638));
#53934=CARTESIAN_POINT('Origin',(32.2981260950878,1.42301190206775,33.8304567438133));
#53935=CARTESIAN_POINT('Origin',(32.1941505532983,1.57862775117468,33.8304779343753));
#53936=CARTESIAN_POINT('Origin',(30.,-1.32966554433622E-14,33.8305837392638));
#53937=CARTESIAN_POINT('Origin',(32.1793935122518,1.59893412656992,33.8304567438136));
#53938=CARTESIAN_POINT('Origin',(32.0635290135536,1.74591243696026,33.8304779343747));
#53939=CARTESIAN_POINT('Origin',(30.,-1.32966554433622E-14,33.8305837392638));
#53940=CARTESIAN_POINT('Origin',(32.04722424369,1.76499839048088,33.8304567438134));
#53941=CARTESIAN_POINT('Origin',(31.9201851312459,1.90243299199643,33.8304779343734));
#53942=CARTESIAN_POINT('Origin',(30.,-1.32966554433622E-14,33.8305837392638));
#53943=CARTESIAN_POINT('Origin',(31.9024331568948,1.92018085239292,33.8304567438132));
#53944=CARTESIAN_POINT('Origin',(31.7650026690842,2.0472244150162,33.8304779343749));
#53945=CARTESIAN_POINT('Origin',(30.,-1.32966554433622E-14,33.8305837392638));
#53946=CARTESIAN_POINT('Origin',(31.7459129370645,2.06352476082576,33.8304567438132));
#53947=CARTESIAN_POINT('Origin',(31.5989383785419,2.17939401874533,33.8304779343753));
#53948=CARTESIAN_POINT('Origin',(30.,-1.32966554433622E-14,33.8305837392638));
#53949=CARTESIAN_POINT('Origin',(31.5786285834019,2.1941463529156,33.830456743813));
#53950=CARTESIAN_POINT('Origin',(31.4230161011941,2.29812693362645,33.8304779343752));
#53951=CARTESIAN_POINT('Origin',(30.,-1.32966554433622E-14,33.8305837392638));
#53952=CARTESIAN_POINT('Origin',(31.4016114595758,2.31124030311394,33.8304567438134));
#53953=CARTESIAN_POINT('Origin',(31.2383204563814,2.40269113175683,33.8304779343751));
#53954=CARTESIAN_POINT('Origin',(30.,-1.32966554433622E-14,33.8305837392638));
#53955=CARTESIAN_POINT('Origin',(31.215952935018,2.41408468827632,33.8304567438131));
#53956=CARTESIAN_POINT('Origin',(31.0459901541714,2.49244194008366,33.8304779343748));
#53957=CARTESIAN_POINT('Origin',(30.,-1.32966554433622E-14,33.8305837392638));
#53958=CARTESIAN_POINT('Origin',(31.0227976562705,2.50204543857161,33.8304567438132));
#53959=CARTESIAN_POINT('Origin',(30.8472109748356,2.56682601503055,33.8304779343754));
#53960=CARTESIAN_POINT('Origin',(30.,-1.32966554433622E-14,33.8305837392638));
#53961=CARTESIAN_POINT('Origin',(30.8233364898573,2.574580246724,33.8304567438134));
#53962=CARTESIAN_POINT('Origin',(30.6432084580721,2.62538475398616,33.8304779343503));
#53963=CARTESIAN_POINT('Origin',(30.,-1.32966554433622E-14,33.8305837392638));
#53964=CARTESIAN_POINT('Origin',(30.6187991801972,2.63124191151918,33.8304567438131));
#53965=CARTESIAN_POINT('Origin',(30.4352403473569,2.66775712300684,33.8304779343755));
#53966=CARTESIAN_POINT('Origin',(30.,-1.32966554433622E-14,33.8305837392638));
#53967=CARTESIAN_POINT('Origin',(27.5973088682432,1.23832045638137,33.8304779343751));
#53968=CARTESIAN_POINT('Origin',(27.6887596968862,1.40161145957579,33.8304567438134));
#53969=CARTESIAN_POINT('Origin',(30.,-1.32966554433622E-14,33.8305837392638));
#53970=CARTESIAN_POINT('Origin',(27.7018730663741,1.4230161011934,33.8304779343749));
#53971=CARTESIAN_POINT('Origin',(27.8058536470835,1.57862858340213,33.8304567438133));
#53972=CARTESIAN_POINT('Origin',(30.,-1.32966554433622E-14,33.8305837392638));
#53973=CARTESIAN_POINT('Origin',(27.8206059812548,1.59893837854177,33.8304779343751));
#53974=CARTESIAN_POINT('Origin',(27.9364752391745,1.7459129370644,33.8304567438132));
#53975=CARTESIAN_POINT('Origin',(30.,-1.32966554433622E-14,33.8305837392638));
#53976=CARTESIAN_POINT('Origin',(27.952775584984,1.76500266908388,33.8304779343747));
#53977=CARTESIAN_POINT('Origin',(28.0798191476065,1.90243315689505,33.8304567438134));
#53978=CARTESIAN_POINT('Origin',(30.,-1.32966554433622E-14,33.8305837392638));
#53979=CARTESIAN_POINT('Origin',(28.0975670080041,1.92018513124447,33.8304779343728));
#53980=CARTESIAN_POINT('Origin',(28.23500160952,2.04722424368963,33.830456743813));
#53981=CARTESIAN_POINT('Origin',(30.,-1.32966554433622E-14,33.8305837392638));
#53982=CARTESIAN_POINT('Origin',(28.2540875630398,2.06352901355343,33.8304779343746));
#53983=CARTESIAN_POINT('Origin',(28.4010658734306,2.17939351225149,33.8304567438134));
#53984=CARTESIAN_POINT('Origin',(30.,-1.32966554433622E-14,33.8305837392638));
#53985=CARTESIAN_POINT('Origin',(28.4213722488255,2.19415055329726,33.8304779343749));
#53986=CARTESIAN_POINT('Origin',(28.5769880979325,2.29812609508769,33.8304567438131));
#53987=CARTESIAN_POINT('Origin',(30.,-1.32966554433622E-14,33.8305837392638));
#53988=CARTESIAN_POINT('Origin',(28.5983896996467,2.31124442523142,33.8304779343677));
#53989=CARTESIAN_POINT('Origin',(28.7616836640084,2.40268996634441,33.8304567438137));
#53990=CARTESIAN_POINT('Origin',(30.,-1.32966554433622E-14,33.8305837392638));
#53991=CARTESIAN_POINT('Origin',(28.7840485440478,2.41408870675589,33.8304779343753));
#53992=CARTESIAN_POINT('Origin',(28.9540138620795,2.49244045498167,33.8304567438133));
#53993=CARTESIAN_POINT('Origin',(30.,-1.32966554433622E-14,33.8305837392638));
#53994=CARTESIAN_POINT('Origin',(28.9772041335221,2.50204932861683,33.8304779343752));
#53995=CARTESIAN_POINT('Origin',(29.1527929125161,2.56682421939371,33.8304567438132));
#53996=CARTESIAN_POINT('Origin',(30.,-1.32966554433622E-14,33.8305837392638));
#53997=CARTESIAN_POINT('Origin',(29.1766655996273,2.57458398435145,33.8304779343752));
#53998=CARTESIAN_POINT('Origin',(29.3567952763716,2.62538265893797,33.8304567438133));
#53999=CARTESIAN_POINT('Origin',(30.,-1.32966554433622E-14,33.8305837392638));
#54000=CARTESIAN_POINT('Origin',(29.3812031960975,2.63124547368767,33.8304779343756));
#54001=CARTESIAN_POINT('Origin',(29.5647632112354,2.66775474136179,33.8304567438135));
#54002=CARTESIAN_POINT('Origin',(30.,-1.32966554433622E-14,33.8305837392638));
#54003=CARTESIAN_POINT('Origin',(29.5895558806117,2.67168445961877,33.8304779343432));
#54004=CARTESIAN_POINT('Origin',(29.775414525633,2.69367922868643,33.8304567438135));
#54005=CARTESIAN_POINT('Origin',(30.,-1.32966554433622E-14,33.8305837392638));
#54006=CARTESIAN_POINT('Origin',(29.8004390896529,2.69565162258947,33.8304779343745));
#54007=CARTESIAN_POINT('Origin',(29.9874504841622,2.70299628782743,33.8304567438137));
#54008=CARTESIAN_POINT('Origin',(30.,-1.32966554433622E-14,33.8305837392638));
#54009=CARTESIAN_POINT('Origin',(30.4104467678198,2.67168109495229,33.8304567438124));
#54010=CARTESIAN_POINT('Origin',(30.2245888351268,2.69368188219228,33.830477934375));
#54011=CARTESIAN_POINT('Origin',(30.,1.17524047358083,16.));
#54012=CARTESIAN_POINT('Origin',(30.,2.60624999999999,31.));
#54013=CARTESIAN_POINT('Origin',(30.,-1.32966554433622E-14,31.6569162607362));
#54014=CARTESIAN_POINT('',(30.1823521510466,2.74394746542433,31.6569162607362));
#54015=CARTESIAN_POINT('Origin',(30.1995609103462,2.69565162259179,31.6570220656244));
#54016=CARTESIAN_POINT('',(30.03349761664,2.74979597600974,31.6569162607362));
#54017=CARTESIAN_POINT('Origin',(30.0125495158372,2.70299628782596,31.6570432561867));
#54018=CARTESIAN_POINT('Origin',(30.,-1.32966554433622E-14,31.6569162607362));
#54019=CARTESIAN_POINT('Origin',(30.,-1.32966554433622E-14,16.));
#54020=CARTESIAN_POINT('',(30.1823521510466,2.74394746542434,33.8305837392638));
#54021=CARTESIAN_POINT('',(30.1823521510466,2.74394746542433,16.));
#54022=CARTESIAN_POINT('',(30.03349761664,2.74979597600975,33.8305837392638));
#54023=CARTESIAN_POINT('',(30.03349761664,2.74979597600974,16.));
#54024=CARTESIAN_POINT('Origin',(30.,-1.32966554433622E-14,33.8305837392638));
#54025=CARTESIAN_POINT('Origin',(30.,-1.32966554433622E-14,33.8305837392638));
#54026=CARTESIAN_POINT('Origin',(30.1995638146302,2.69564847601544,33.8304567438135));
#54027=CARTESIAN_POINT('Origin',(30.0125526580447,2.70299919683307,33.8304779343742));
#54028=CARTESIAN_POINT('Origin',(30.,-1.32966554433622E-14,34.));
#54029=CARTESIAN_POINT('Origin',(30.,-1.32966554433622E-14,32.5));
#54030=CARTESIAN_POINT('',(30.,-1.44337567297407,32.5));
#54031=CARTESIAN_POINT('',(31.25,-0.72168783648704,32.5));
#54032=CARTESIAN_POINT('',(30.,-1.44337567297407,32.5));
#54033=CARTESIAN_POINT('',(31.25,0.721687836487017,32.5));
#54034=CARTESIAN_POINT('',(31.25,-0.72168783648704,32.5));
#54035=CARTESIAN_POINT('',(30.,1.44337567297405,32.5));
#54036=CARTESIAN_POINT('',(31.25,0.721687836487017,32.5));
#54037=CARTESIAN_POINT('',(28.75,0.721687836487017,32.5));
#54038=CARTESIAN_POINT('',(30.,1.44337567297405,32.5));
#54039=CARTESIAN_POINT('',(28.75,-0.721687836487044,32.5));
#54040=CARTESIAN_POINT('',(28.75,0.721687836487017,32.5));
#54041=CARTESIAN_POINT('',(28.75,-0.721687836487044,32.5));
#54042=CARTESIAN_POINT('Origin',(31.25,-0.72168783648704,32.5));
#54043=CARTESIAN_POINT('',(31.25,-0.72168783648704,32.5));
#54044=CARTESIAN_POINT('',(31.25,0.721687836487017,32.5));
#54045=CARTESIAN_POINT('Origin',(31.25,0.721687836487017,32.5));
#54046=CARTESIAN_POINT('',(30.,1.44337567297405,32.5));
#54047=CARTESIAN_POINT('Origin',(30.,1.44337567297405,32.5));
#54048=CARTESIAN_POINT('',(28.75,0.721687836487017,32.5));
#54049=CARTESIAN_POINT('Origin',(28.75,0.721687836487017,32.5));
#54050=CARTESIAN_POINT('',(28.75,-0.721687836487044,32.5));
#54051=CARTESIAN_POINT('Origin',(28.75,-0.721687836487044,32.5));
#54052=CARTESIAN_POINT('',(30.,-1.44337567297407,32.5));
#54053=CARTESIAN_POINT('Origin',(30.,-1.44337567297407,32.5));
#54054=CARTESIAN_POINT('Ctrl Pts',(30.,1.17523237272422,15.7500046770317));
#54055=CARTESIAN_POINT('Ctrl Pts',(29.3214792732473,1.17523237272422,15.7916713436984));
#54056=CARTESIAN_POINT('Ctrl Pts',(28.9822189098709,0.587616186362105,15.8333380103651));
#54057=CARTESIAN_POINT('Ctrl Pts',(28.6429585464946,-1.32141491426617E-14,
15.8750046770317));
#54058=CARTESIAN_POINT('Ctrl Pts',(28.9822189098709,-0.587616186362132,
15.9166713436984));
#54059=CARTESIAN_POINT('Ctrl Pts',(29.3214792732473,-1.17523237272425,15.9583380103651));
#54060=CARTESIAN_POINT('Ctrl Pts',(30.,-1.17523237272425,16.0000046770317));
#54061=CARTESIAN_POINT('Ctrl Pts',(30.6785207267527,-1.17523237272425,16.0416713436984));
#54062=CARTESIAN_POINT('Ctrl Pts',(31.017781090129,-0.587616186362132,16.0833380103651));
#54063=CARTESIAN_POINT('Ctrl Pts',(31.3570414535054,-1.35453513912972E-14,
16.1250046770317));
#54064=CARTESIAN_POINT('Ctrl Pts',(31.017781090129,0.587616186362104,16.1666713436984));
#54065=CARTESIAN_POINT('Ctrl Pts',(30.6785207267527,1.17523237272422,16.2083380103651));
#54066=CARTESIAN_POINT('Ctrl Pts',(30.,1.17523237272422,16.2500046770317));
#54067=CARTESIAN_POINT('Ctrl Pts',(29.3214792732473,1.17523237272422,16.2916713436984));
#54068=CARTESIAN_POINT('Ctrl Pts',(28.9822189098709,0.587616186362105,16.3333380103651));
#54069=CARTESIAN_POINT('Ctrl Pts',(28.6429585464946,-1.32141491426617E-14,
16.3750046770317));
#54070=CARTESIAN_POINT('Ctrl Pts',(28.9822189098709,-0.587616186362132,
16.4166713436984));
#54071=CARTESIAN_POINT('Ctrl Pts',(29.3214792732473,-1.17523237272425,16.4583380103651));
#54072=CARTESIAN_POINT('Ctrl Pts',(30.,-1.17523237272425,16.5000046770317));
#54073=CARTESIAN_POINT('Ctrl Pts',(30.6785207267527,-1.17523237272425,16.5416713436984));
#54074=CARTESIAN_POINT('Ctrl Pts',(31.017781090129,-0.587616186362132,16.5833380103651));
#54075=CARTESIAN_POINT('Ctrl Pts',(31.3570414535054,-1.35453513912972E-14,
16.6250046770317));
#54076=CARTESIAN_POINT('Ctrl Pts',(31.017781090129,0.587616186362104,16.6666713436984));
#54077=CARTESIAN_POINT('Ctrl Pts',(30.6785207267527,1.17523237272422,16.7083380103651));
#54078=CARTESIAN_POINT('Ctrl Pts',(30.,1.17523237272422,16.7500046770317));
#54079=CARTESIAN_POINT('Ctrl Pts',(29.3214792732473,1.17523237272422,16.7916713436984));
#54080=CARTESIAN_POINT('Ctrl Pts',(28.9822189098709,0.587616186362105,16.8333380103651));
#54081=CARTESIAN_POINT('Ctrl Pts',(28.6429585464946,-1.32141491426617E-14,
16.8750046770317));
#54082=CARTESIAN_POINT('Ctrl Pts',(28.9822189098709,-0.587616186362132,
16.9166713436984));
#54083=CARTESIAN_POINT('Ctrl Pts',(29.3214792732473,-1.17523237272425,16.9583380103651));
#54084=CARTESIAN_POINT('Ctrl Pts',(30.,-1.17523237272425,17.0000046770317));
#54085=CARTESIAN_POINT('Ctrl Pts',(30.6785207267527,-1.17523237272425,17.0416713436984));
#54086=CARTESIAN_POINT('Ctrl Pts',(31.017781090129,-0.587616186362132,17.0833380103651));
#54087=CARTESIAN_POINT('Ctrl Pts',(31.3570414535054,-1.35453513912972E-14,
17.1250046770317));
#54088=CARTESIAN_POINT('Ctrl Pts',(31.017781090129,0.587616186362104,17.1666713436984));
#54089=CARTESIAN_POINT('Ctrl Pts',(30.6785207267527,1.17523237272422,17.2083380103651));
#54090=CARTESIAN_POINT('Ctrl Pts',(30.,1.17523237272422,17.2500046770317));
#54091=CARTESIAN_POINT('Ctrl Pts',(29.3214792732473,1.17523237272422,17.2916713436984));
#54092=CARTESIAN_POINT('Ctrl Pts',(28.9822189098709,0.587616186362105,17.3333380103651));
#54093=CARTESIAN_POINT('Ctrl Pts',(28.6429585464946,-1.32141491426617E-14,
17.3750046770317));
#54094=CARTESIAN_POINT('Ctrl Pts',(28.9822189098709,-0.587616186362132,
17.4166713436984));
#54095=CARTESIAN_POINT('Ctrl Pts',(29.3214792732473,-1.17523237272425,17.4583380103651));
#54096=CARTESIAN_POINT('Ctrl Pts',(30.,-1.17523237272425,17.5000046770317));
#54097=CARTESIAN_POINT('Ctrl Pts',(30.6785207267527,-1.17523237272425,17.5416713436984));
#54098=CARTESIAN_POINT('Ctrl Pts',(31.017781090129,-0.587616186362132,17.5833380103651));
#54099=CARTESIAN_POINT('Ctrl Pts',(31.3570414535054,-1.35453513912972E-14,
17.6250046770317));
#54100=CARTESIAN_POINT('Ctrl Pts',(31.017781090129,0.587616186362104,17.6666713436984));
#54101=CARTESIAN_POINT('Ctrl Pts',(30.6785207267527,1.17523237272422,17.7083380103651));
#54102=CARTESIAN_POINT('Ctrl Pts',(30.,1.17523237272422,17.7500046770317));
#54103=CARTESIAN_POINT('Ctrl Pts',(29.3214792732473,1.17523237272422,17.7916713436984));
#54104=CARTESIAN_POINT('Ctrl Pts',(28.9822189098709,0.587616186362105,17.8333380103651));
#54105=CARTESIAN_POINT('Ctrl Pts',(28.6429585464946,-1.32141491426617E-14,
17.8750046770317));
#54106=CARTESIAN_POINT('Ctrl Pts',(28.9822189098709,-0.587616186362132,
17.9166713436984));
#54107=CARTESIAN_POINT('Ctrl Pts',(29.3214792732473,-1.17523237272425,17.9583380103651));
#54108=CARTESIAN_POINT('Ctrl Pts',(30.,-1.17523237272425,18.0000046770317));
#54109=CARTESIAN_POINT('Ctrl Pts',(30.6785207267527,-1.17523237272425,18.0416713436984));
#54110=CARTESIAN_POINT('Ctrl Pts',(31.017781090129,-0.587616186362132,18.0833380103651));
#54111=CARTESIAN_POINT('Ctrl Pts',(31.3570414535054,-1.35453513912972E-14,
18.1250046770317));
#54112=CARTESIAN_POINT('Ctrl Pts',(31.017781090129,0.587616186362104,18.1666713436984));
#54113=CARTESIAN_POINT('Ctrl Pts',(30.6785207267527,1.17523237272422,18.2083380103651));
#54114=CARTESIAN_POINT('Ctrl Pts',(30.,1.17523237272422,18.2500046770317));
#54115=CARTESIAN_POINT('Ctrl Pts',(29.3214792732473,1.17523237272422,18.2916713436984));
#54116=CARTESIAN_POINT('Ctrl Pts',(28.9822189098709,0.587616186362105,18.3333380103651));
#54117=CARTESIAN_POINT('Ctrl Pts',(28.6429585464946,-1.32141491426617E-14,
18.3750046770317));
#54118=CARTESIAN_POINT('Ctrl Pts',(28.9822189098709,-0.587616186362132,
18.4166713436984));
#54119=CARTESIAN_POINT('Ctrl Pts',(29.3214792732473,-1.17523237272425,18.4583380103651));
#54120=CARTESIAN_POINT('Ctrl Pts',(30.,-1.17523237272425,18.5000046770317));
#54121=CARTESIAN_POINT('Ctrl Pts',(30.6785207267527,-1.17523237272425,18.5416713436984));
#54122=CARTESIAN_POINT('Ctrl Pts',(31.017781090129,-0.587616186362132,18.5833380103651));
#54123=CARTESIAN_POINT('Ctrl Pts',(31.3570414535054,-1.35453513912972E-14,
18.6250046770317));
#54124=CARTESIAN_POINT('Ctrl Pts',(31.017781090129,0.587616186362104,18.6666713436984));
#54125=CARTESIAN_POINT('Ctrl Pts',(30.6785207267527,1.17523237272422,18.7083380103651));
#54126=CARTESIAN_POINT('Ctrl Pts',(30.,1.17523237272422,18.7500046770317));
#54127=CARTESIAN_POINT('Ctrl Pts',(29.3214792732473,1.17523237272422,18.7916713436984));
#54128=CARTESIAN_POINT('Ctrl Pts',(28.9822189098709,0.587616186362105,18.8333380103651));
#54129=CARTESIAN_POINT('Ctrl Pts',(28.6429585464946,-1.32141491426617E-14,
18.8750046770317));
#54130=CARTESIAN_POINT('Ctrl Pts',(28.9822189098709,-0.587616186362132,
18.9166713436984));
#54131=CARTESIAN_POINT('Ctrl Pts',(29.3214792732473,-1.17523237272425,18.9583380103651));
#54132=CARTESIAN_POINT('Ctrl Pts',(30.,-1.17523237272425,19.0000046770317));
#54133=CARTESIAN_POINT('Ctrl Pts',(30.6785207267527,-1.17523237272425,19.0416713436984));
#54134=CARTESIAN_POINT('Ctrl Pts',(31.017781090129,-0.587616186362132,19.0833380103651));
#54135=CARTESIAN_POINT('Ctrl Pts',(31.3570414535054,-1.35453513912972E-14,
19.1250046770317));
#54136=CARTESIAN_POINT('Ctrl Pts',(31.017781090129,0.587616186362104,19.1666713436984));
#54137=CARTESIAN_POINT('Ctrl Pts',(30.6785207267527,1.17523237272422,19.2083380103651));
#54138=CARTESIAN_POINT('Ctrl Pts',(30.,1.17523237272422,19.2500046770317));
#54139=CARTESIAN_POINT('Ctrl Pts',(29.3214792732473,1.17523237272422,19.2916713436984));
#54140=CARTESIAN_POINT('Ctrl Pts',(28.9822189098709,0.587616186362105,19.3333380103651));
#54141=CARTESIAN_POINT('Ctrl Pts',(28.6429585464946,-1.32141491426617E-14,
19.3750046770317));
#54142=CARTESIAN_POINT('Ctrl Pts',(28.9822189098709,-0.587616186362132,
19.4166713436984));
#54143=CARTESIAN_POINT('Ctrl Pts',(29.3214792732473,-1.17523237272425,19.4583380103651));
#54144=CARTESIAN_POINT('Ctrl Pts',(30.,-1.17523237272425,19.5000046770317));
#54145=CARTESIAN_POINT('Ctrl Pts',(30.6785207267527,-1.17523237272425,19.5416713436984));
#54146=CARTESIAN_POINT('Ctrl Pts',(31.017781090129,-0.587616186362132,19.5833380103651));
#54147=CARTESIAN_POINT('Ctrl Pts',(31.3570414535054,-1.35453513912972E-14,
19.6250046770317));
#54148=CARTESIAN_POINT('Ctrl Pts',(31.017781090129,0.587616186362104,19.6666713436984));
#54149=CARTESIAN_POINT('Ctrl Pts',(30.6785207267527,1.17523237272422,19.7083380103651));
#54150=CARTESIAN_POINT('Ctrl Pts',(30.,1.17523237272422,19.7500046770317));
#54151=CARTESIAN_POINT('Ctrl Pts',(29.3214792732473,1.17523237272422,19.7916713436984));
#54152=CARTESIAN_POINT('Ctrl Pts',(28.9822189098709,0.587616186362105,19.8333380103651));
#54153=CARTESIAN_POINT('Ctrl Pts',(28.6429585464946,-1.32141491426617E-14,
19.8750046770317));
#54154=CARTESIAN_POINT('Ctrl Pts',(28.9822189098709,-0.587616186362132,
19.9166713436984));
#54155=CARTESIAN_POINT('Ctrl Pts',(29.3214792732473,-1.17523237272425,19.9583380103651));
#54156=CARTESIAN_POINT('Ctrl Pts',(30.,-1.17523237272425,20.0000046770317));
#54157=CARTESIAN_POINT('Ctrl Pts',(30.6785207267527,-1.17523237272425,20.0416713436984));
#54158=CARTESIAN_POINT('Ctrl Pts',(31.017781090129,-0.587616186362132,20.0833380103651));
#54159=CARTESIAN_POINT('Ctrl Pts',(31.3570414535054,-1.35453513912972E-14,
20.1250046770317));
#54160=CARTESIAN_POINT('Ctrl Pts',(31.017781090129,0.587616186362104,20.1666713436984));
#54161=CARTESIAN_POINT('Ctrl Pts',(30.6785207267527,1.17523237272422,20.2083380103651));
#54162=CARTESIAN_POINT('Ctrl Pts',(30.,1.17523237272422,20.2500046770317));
#54163=CARTESIAN_POINT('Ctrl Pts',(29.3214792732473,1.17523237272422,20.2916713436984));
#54164=CARTESIAN_POINT('Ctrl Pts',(28.9822189098709,0.587616186362105,20.3333380103651));
#54165=CARTESIAN_POINT('Ctrl Pts',(28.6429585464946,-1.32141491426617E-14,
20.3750046770317));
#54166=CARTESIAN_POINT('Ctrl Pts',(28.9822189098709,-0.587616186362132,
20.4166713436984));
#54167=CARTESIAN_POINT('Ctrl Pts',(29.3214792732473,-1.17523237272425,20.4583380103651));
#54168=CARTESIAN_POINT('Ctrl Pts',(30.,-1.17523237272425,20.5000046770317));
#54169=CARTESIAN_POINT('Ctrl Pts',(30.6785207267527,-1.17523237272425,20.5416713436984));
#54170=CARTESIAN_POINT('Ctrl Pts',(31.017781090129,-0.587616186362132,20.5833380103651));
#54171=CARTESIAN_POINT('Ctrl Pts',(31.3570414535054,-1.35453513912972E-14,
20.6250046770317));
#54172=CARTESIAN_POINT('Ctrl Pts',(31.017781090129,0.587616186362104,20.6666713436984));
#54173=CARTESIAN_POINT('Ctrl Pts',(30.6785207267527,1.17523237272422,20.7083380103651));
#54174=CARTESIAN_POINT('Ctrl Pts',(30.,1.17523237272422,20.7500046770317));
#54175=CARTESIAN_POINT('Ctrl Pts',(29.3214792732473,1.17523237272422,20.7916713436984));
#54176=CARTESIAN_POINT('Ctrl Pts',(28.9822189098709,0.587616186362105,20.8333380103651));
#54177=CARTESIAN_POINT('Ctrl Pts',(28.6429585464946,-1.32141491426617E-14,
20.8750046770317));
#54178=CARTESIAN_POINT('Ctrl Pts',(28.9822189098709,-0.587616186362132,
20.9166713436984));
#54179=CARTESIAN_POINT('Ctrl Pts',(29.3214792732473,-1.17523237272425,20.9583380103651));
#54180=CARTESIAN_POINT('Ctrl Pts',(30.,-1.17523237272425,21.0000046770317));
#54181=CARTESIAN_POINT('Ctrl Pts',(30.6785207267527,-1.17523237272425,21.0416713436984));
#54182=CARTESIAN_POINT('Ctrl Pts',(31.017781090129,-0.587616186362132,21.0833380103651));
#54183=CARTESIAN_POINT('Ctrl Pts',(31.3570414535054,-1.35453513912972E-14,
21.1250046770317));
#54184=CARTESIAN_POINT('Ctrl Pts',(31.017781090129,0.587616186362104,21.1666713436984));
#54185=CARTESIAN_POINT('Ctrl Pts',(30.6785207267527,1.17523237272422,21.2083380103651));
#54186=CARTESIAN_POINT('Ctrl Pts',(30.,1.17523237272422,21.2500046770317));
#54187=CARTESIAN_POINT('Ctrl Pts',(29.3214792732473,1.17523237272422,21.2916713436984));
#54188=CARTESIAN_POINT('Ctrl Pts',(28.9822189098709,0.587616186362105,21.3333380103651));
#54189=CARTESIAN_POINT('Ctrl Pts',(28.6429585464946,-1.32141491426617E-14,
21.3750046770317));
#54190=CARTESIAN_POINT('Ctrl Pts',(28.9822189098709,-0.587616186362132,
21.4166713436984));
#54191=CARTESIAN_POINT('Ctrl Pts',(29.3214792732473,-1.17523237272425,21.4583380103651));
#54192=CARTESIAN_POINT('Ctrl Pts',(30.,-1.17523237272425,21.5000046770317));
#54193=CARTESIAN_POINT('Ctrl Pts',(30.6785207267527,-1.17523237272425,21.5416713436984));
#54194=CARTESIAN_POINT('Ctrl Pts',(31.017781090129,-0.587616186362132,21.5833380103651));
#54195=CARTESIAN_POINT('Ctrl Pts',(31.3570414535054,-1.35453513912972E-14,
21.6250046770317));
#54196=CARTESIAN_POINT('Ctrl Pts',(31.017781090129,0.587616186362104,21.6666713436984));
#54197=CARTESIAN_POINT('Ctrl Pts',(30.6785207267527,1.17523237272422,21.7083380103651));
#54198=CARTESIAN_POINT('Ctrl Pts',(30.,1.17523237272422,21.7500046770317));
#54199=CARTESIAN_POINT('Ctrl Pts',(29.3214792732473,1.17523237272422,21.7916713436984));
#54200=CARTESIAN_POINT('Ctrl Pts',(28.9822189098709,0.587616186362105,21.8333380103651));
#54201=CARTESIAN_POINT('Ctrl Pts',(28.6429585464946,-1.32141491426617E-14,
21.8750046770317));
#54202=CARTESIAN_POINT('Ctrl Pts',(28.9822189098709,-0.587616186362132,
21.9166713436984));
#54203=CARTESIAN_POINT('Ctrl Pts',(29.3214792732473,-1.17523237272425,21.9583380103651));
#54204=CARTESIAN_POINT('Ctrl Pts',(30.,-1.17523237272425,22.0000046770317));
#54205=CARTESIAN_POINT('Ctrl Pts',(30.6785207267527,-1.17523237272425,22.0416713436984));
#54206=CARTESIAN_POINT('Ctrl Pts',(31.017781090129,-0.587616186362132,22.0833380103651));
#54207=CARTESIAN_POINT('Ctrl Pts',(31.3570414535054,-1.35453513912972E-14,
22.1250046770317));
#54208=CARTESIAN_POINT('Ctrl Pts',(31.017781090129,0.587616186362104,22.1666713436984));
#54209=CARTESIAN_POINT('Ctrl Pts',(30.6785207267527,1.17523237272422,22.2083380103651));
#54210=CARTESIAN_POINT('Ctrl Pts',(30.,1.17523237272422,22.2500046770317));
#54211=CARTESIAN_POINT('Ctrl Pts',(29.3214792732473,1.17523237272422,22.2916713436984));
#54212=CARTESIAN_POINT('Ctrl Pts',(28.9822189098709,0.587616186362105,22.3333380103651));
#54213=CARTESIAN_POINT('Ctrl Pts',(28.6429585464946,-1.32141491426617E-14,
22.3750046770317));
#54214=CARTESIAN_POINT('Ctrl Pts',(28.9822189098709,-0.587616186362132,
22.4166713436984));
#54215=CARTESIAN_POINT('Ctrl Pts',(29.3214792732473,-1.17523237272425,22.4583380103651));
#54216=CARTESIAN_POINT('Ctrl Pts',(30.,-1.17523237272425,22.5000046770317));
#54217=CARTESIAN_POINT('Ctrl Pts',(30.6785207267527,-1.17523237272425,22.5416713436984));
#54218=CARTESIAN_POINT('Ctrl Pts',(31.017781090129,-0.587616186362132,22.5833380103651));
#54219=CARTESIAN_POINT('Ctrl Pts',(31.3570414535054,-1.35453513912972E-14,
22.6250046770317));
#54220=CARTESIAN_POINT('Ctrl Pts',(31.017781090129,0.587616186362104,22.6666713436984));
#54221=CARTESIAN_POINT('Ctrl Pts',(30.6785207267527,1.17523237272422,22.7083380103651));
#54222=CARTESIAN_POINT('Ctrl Pts',(30.,1.17523237272422,22.7500046770317));
#54223=CARTESIAN_POINT('Ctrl Pts',(29.3214792732473,1.17523237272422,22.7916713436984));
#54224=CARTESIAN_POINT('Ctrl Pts',(28.9822189098709,0.587616186362105,22.8333380103651));
#54225=CARTESIAN_POINT('Ctrl Pts',(28.6429585464946,-1.32141491426617E-14,
22.8750046770317));
#54226=CARTESIAN_POINT('Ctrl Pts',(28.9822189098709,-0.587616186362132,
22.9166713436984));
#54227=CARTESIAN_POINT('Ctrl Pts',(29.3214792732473,-1.17523237272425,22.9583380103651));
#54228=CARTESIAN_POINT('Ctrl Pts',(30.,-1.17523237272425,23.0000046770317));
#54229=CARTESIAN_POINT('Ctrl Pts',(30.6785207267527,-1.17523237272425,23.0416713436984));
#54230=CARTESIAN_POINT('Ctrl Pts',(31.017781090129,-0.587616186362132,23.0833380103651));
#54231=CARTESIAN_POINT('Ctrl Pts',(31.3570414535054,-1.35453513912972E-14,
23.1250046770317));
#54232=CARTESIAN_POINT('Ctrl Pts',(31.017781090129,0.587616186362104,23.1666713436984));
#54233=CARTESIAN_POINT('Ctrl Pts',(30.6785207267527,1.17523237272422,23.2083380103651));
#54234=CARTESIAN_POINT('Ctrl Pts',(30.,1.17523237272422,23.2500046770317));
#54235=CARTESIAN_POINT('Ctrl Pts',(29.3214792732473,1.17523237272422,23.2916713436984));
#54236=CARTESIAN_POINT('Ctrl Pts',(28.9822189098709,0.587616186362105,23.3333380103651));
#54237=CARTESIAN_POINT('Ctrl Pts',(28.6429585464946,-1.32141491426617E-14,
23.3750046770317));
#54238=CARTESIAN_POINT('Ctrl Pts',(28.9822189098709,-0.587616186362132,
23.4166713436984));
#54239=CARTESIAN_POINT('Ctrl Pts',(29.3214792732473,-1.17523237272425,23.4583380103651));
#54240=CARTESIAN_POINT('Ctrl Pts',(30.,-1.17523237272425,23.5000046770317));
#54241=CARTESIAN_POINT('Ctrl Pts',(30.6785207267527,-1.17523237272425,23.5416713436984));
#54242=CARTESIAN_POINT('Ctrl Pts',(31.017781090129,-0.587616186362132,23.5833380103651));
#54243=CARTESIAN_POINT('Ctrl Pts',(31.3570414535054,-1.35453513912972E-14,
23.6250046770317));
#54244=CARTESIAN_POINT('Ctrl Pts',(31.017781090129,0.587616186362104,23.6666713436984));
#54245=CARTESIAN_POINT('Ctrl Pts',(30.6785207267527,1.17523237272422,23.7083380103651));
#54246=CARTESIAN_POINT('Ctrl Pts',(30.,1.17523237272422,23.7500046770317));
#54247=CARTESIAN_POINT('Ctrl Pts',(29.3214792732473,1.17523237272422,23.7916713436984));
#54248=CARTESIAN_POINT('Ctrl Pts',(28.9822189098709,0.587616186362105,23.8333380103651));
#54249=CARTESIAN_POINT('Ctrl Pts',(28.6429585464946,-1.32141491426617E-14,
23.8750046770317));
#54250=CARTESIAN_POINT('Ctrl Pts',(28.9822189098709,-0.587616186362132,
23.9166713436984));
#54251=CARTESIAN_POINT('Ctrl Pts',(29.3214792732473,-1.17523237272425,23.9583380103651));
#54252=CARTESIAN_POINT('Ctrl Pts',(30.,-1.17523237272425,24.0000046770317));
#54253=CARTESIAN_POINT('Ctrl Pts',(30.6785207267527,-1.17523237272425,24.0416713436984));
#54254=CARTESIAN_POINT('Ctrl Pts',(31.017781090129,-0.587616186362132,24.0833380103651));
#54255=CARTESIAN_POINT('Ctrl Pts',(31.3570414535054,-1.35453513912972E-14,
24.1250046770317));
#54256=CARTESIAN_POINT('Ctrl Pts',(31.017781090129,0.587616186362104,24.1666713436984));
#54257=CARTESIAN_POINT('Ctrl Pts',(30.6785207267527,1.17523237272422,24.2083380103651));
#54258=CARTESIAN_POINT('Ctrl Pts',(30.,1.17523237272422,24.2500046770317));
#54259=CARTESIAN_POINT('Ctrl Pts',(29.3214792732473,1.17523237272422,24.2916713436984));
#54260=CARTESIAN_POINT('Ctrl Pts',(28.9822189098709,0.587616186362105,24.3333380103651));
#54261=CARTESIAN_POINT('Ctrl Pts',(28.6429585464946,-1.32141491426617E-14,
24.3750046770317));
#54262=CARTESIAN_POINT('Ctrl Pts',(28.9822189098709,-0.587616186362132,
24.4166713436984));
#54263=CARTESIAN_POINT('Ctrl Pts',(29.3214792732473,-1.17523237272425,24.4583380103651));
#54264=CARTESIAN_POINT('Ctrl Pts',(30.,-1.17523237272425,24.5000046770317));
#54265=CARTESIAN_POINT('Ctrl Pts',(30.6785207267527,-1.17523237272425,24.5416713436984));
#54266=CARTESIAN_POINT('Ctrl Pts',(31.017781090129,-0.587616186362132,24.5833380103651));
#54267=CARTESIAN_POINT('Ctrl Pts',(31.3570414535054,-1.35453513912972E-14,
24.6250046770317));
#54268=CARTESIAN_POINT('Ctrl Pts',(31.017781090129,0.587616186362104,24.6666713436984));
#54269=CARTESIAN_POINT('Ctrl Pts',(30.6785207267527,1.17523237272422,24.7083380103651));
#54270=CARTESIAN_POINT('Ctrl Pts',(30.,1.17523237272422,24.7500046770317));
#54271=CARTESIAN_POINT('Ctrl Pts',(29.3214792732473,1.17523237272422,24.7916713436984));
#54272=CARTESIAN_POINT('Ctrl Pts',(28.9822189098709,0.587616186362105,24.8333380103651));
#54273=CARTESIAN_POINT('Ctrl Pts',(28.6429585464946,-1.32141491426617E-14,
24.8750046770317));
#54274=CARTESIAN_POINT('Ctrl Pts',(28.9822189098709,-0.587616186362132,
24.9166713436984));
#54275=CARTESIAN_POINT('Ctrl Pts',(29.3214792732473,-1.17523237272425,24.9583380103651));
#54276=CARTESIAN_POINT('Ctrl Pts',(30.,-1.17523237272425,25.0000046770317));
#54277=CARTESIAN_POINT('Ctrl Pts',(30.6785207267527,-1.17523237272425,25.0416713436984));
#54278=CARTESIAN_POINT('Ctrl Pts',(31.017781090129,-0.587616186362132,25.0833380103651));
#54279=CARTESIAN_POINT('Ctrl Pts',(31.3570414535054,-1.35453513912972E-14,
25.1250046770317));
#54280=CARTESIAN_POINT('Ctrl Pts',(31.017781090129,0.587616186362104,25.1666713436984));
#54281=CARTESIAN_POINT('Ctrl Pts',(30.6785207267527,1.17523237272422,25.2083380103651));
#54282=CARTESIAN_POINT('Ctrl Pts',(30.,1.17523237272422,25.2500046770317));
#54283=CARTESIAN_POINT('Ctrl Pts',(29.3214792732473,1.17523237272422,25.2916713436984));
#54284=CARTESIAN_POINT('Ctrl Pts',(28.9822189098709,0.587616186362105,25.3333380103651));
#54285=CARTESIAN_POINT('Ctrl Pts',(28.6429585464946,-1.32141491426617E-14,
25.3750046770317));
#54286=CARTESIAN_POINT('Ctrl Pts',(28.9822189098709,-0.587616186362132,
25.4166713436984));
#54287=CARTESIAN_POINT('Ctrl Pts',(29.3214792732473,-1.17523237272425,25.4583380103651));
#54288=CARTESIAN_POINT('Ctrl Pts',(30.,-1.17523237272425,25.5000046770317));
#54289=CARTESIAN_POINT('Ctrl Pts',(30.6785207267527,-1.17523237272425,25.5416713436984));
#54290=CARTESIAN_POINT('Ctrl Pts',(31.017781090129,-0.587616186362132,25.5833380103651));
#54291=CARTESIAN_POINT('Ctrl Pts',(31.3570414535054,-1.35453513912972E-14,
25.6250046770317));
#54292=CARTESIAN_POINT('Ctrl Pts',(31.017781090129,0.587616186362104,25.6666713436984));
#54293=CARTESIAN_POINT('Ctrl Pts',(30.6785207267527,1.17523237272422,25.7083380103651));
#54294=CARTESIAN_POINT('Ctrl Pts',(30.,1.17523237272422,25.7500046770317));
#54295=CARTESIAN_POINT('Ctrl Pts',(29.3214792732473,1.17523237272422,25.7916713436984));
#54296=CARTESIAN_POINT('Ctrl Pts',(28.9822189098709,0.587616186362105,25.8333380103651));
#54297=CARTESIAN_POINT('Ctrl Pts',(28.6429585464946,-1.32141491426617E-14,
25.8750046770317));
#54298=CARTESIAN_POINT('Ctrl Pts',(28.9822189098709,-0.587616186362132,
25.9166713436984));
#54299=CARTESIAN_POINT('Ctrl Pts',(29.3214792732473,-1.17523237272425,25.9583380103651));
#54300=CARTESIAN_POINT('Ctrl Pts',(30.,-1.17523237272425,26.0000046770317));
#54301=CARTESIAN_POINT('Ctrl Pts',(30.6785207267527,-1.17523237272425,26.0416713436984));
#54302=CARTESIAN_POINT('Ctrl Pts',(31.017781090129,-0.587616186362132,26.0833380103651));
#54303=CARTESIAN_POINT('Ctrl Pts',(31.3570414535054,-1.35453513912972E-14,
26.1250046770317));
#54304=CARTESIAN_POINT('Ctrl Pts',(31.017781090129,0.587616186362104,26.1666713436984));
#54305=CARTESIAN_POINT('Ctrl Pts',(30.6785207267527,1.17523237272422,26.2083380103651));
#54306=CARTESIAN_POINT('Ctrl Pts',(30.,1.17523237272422,26.2500046770317));
#54307=CARTESIAN_POINT('Ctrl Pts',(29.3214792732473,1.17523237272422,26.2916713436984));
#54308=CARTESIAN_POINT('Ctrl Pts',(28.9822189098709,0.587616186362105,26.3333380103651));
#54309=CARTESIAN_POINT('Ctrl Pts',(28.6429585464946,-1.32141491426617E-14,
26.3750046770317));
#54310=CARTESIAN_POINT('Ctrl Pts',(28.9822189098709,-0.587616186362132,
26.4166713436984));
#54311=CARTESIAN_POINT('Ctrl Pts',(29.3214792732473,-1.17523237272425,26.4583380103651));
#54312=CARTESIAN_POINT('Ctrl Pts',(30.,-1.17523237272425,26.5000046770317));
#54313=CARTESIAN_POINT('Ctrl Pts',(30.6785207267527,-1.17523237272425,26.5416713436984));
#54314=CARTESIAN_POINT('Ctrl Pts',(31.017781090129,-0.587616186362132,26.5833380103651));
#54315=CARTESIAN_POINT('Ctrl Pts',(31.3570414535054,-1.35453513912972E-14,
26.6250046770317));
#54316=CARTESIAN_POINT('Ctrl Pts',(31.017781090129,0.587616186362104,26.6666713436984));
#54317=CARTESIAN_POINT('Ctrl Pts',(30.6785207267527,1.17523237272422,26.7083380103651));
#54318=CARTESIAN_POINT('Ctrl Pts',(30.,1.17523237272422,26.7500046770317));
#54319=CARTESIAN_POINT('Ctrl Pts',(29.3214792732473,1.17523237272422,26.7916713436984));
#54320=CARTESIAN_POINT('Ctrl Pts',(28.9822189098709,0.587616186362105,26.8333380103651));
#54321=CARTESIAN_POINT('Ctrl Pts',(28.6429585464946,-1.32141491426617E-14,
26.8750046770317));
#54322=CARTESIAN_POINT('Ctrl Pts',(28.9822189098709,-0.587616186362132,
26.9166713436984));
#54323=CARTESIAN_POINT('Ctrl Pts',(29.3214792732473,-1.17523237272425,26.9583380103651));
#54324=CARTESIAN_POINT('Ctrl Pts',(30.,-1.17523237272425,27.0000046770317));
#54325=CARTESIAN_POINT('Ctrl Pts',(30.6785207267527,-1.17523237272425,27.0416713436984));
#54326=CARTESIAN_POINT('Ctrl Pts',(31.017781090129,-0.587616186362132,27.0833380103651));
#54327=CARTESIAN_POINT('Ctrl Pts',(31.3570414535054,-1.35453513912972E-14,
27.1250046770317));
#54328=CARTESIAN_POINT('Ctrl Pts',(31.017781090129,0.587616186362104,27.1666713436984));
#54329=CARTESIAN_POINT('Ctrl Pts',(30.6785207267527,1.17523237272422,27.2083380103651));
#54330=CARTESIAN_POINT('Ctrl Pts',(30.,1.17523237272422,27.2500046770317));
#54331=CARTESIAN_POINT('Ctrl Pts',(29.3214792732473,1.17523237272422,27.2916713436984));
#54332=CARTESIAN_POINT('Ctrl Pts',(28.9822189098709,0.587616186362105,27.3333380103651));
#54333=CARTESIAN_POINT('Ctrl Pts',(28.6429585464946,-1.32141491426617E-14,
27.3750046770317));
#54334=CARTESIAN_POINT('Ctrl Pts',(28.9822189098709,-0.587616186362132,
27.4166713436984));
#54335=CARTESIAN_POINT('Ctrl Pts',(29.3214792732473,-1.17523237272425,27.4583380103651));
#54336=CARTESIAN_POINT('Ctrl Pts',(30.,-1.17523237272425,27.5000046770317));
#54337=CARTESIAN_POINT('Ctrl Pts',(30.6785207267527,-1.17523237272425,27.5416713436984));
#54338=CARTESIAN_POINT('Ctrl Pts',(31.017781090129,-0.587616186362132,27.5833380103651));
#54339=CARTESIAN_POINT('Ctrl Pts',(31.3570414535054,-1.35453513912972E-14,
27.6250046770317));
#54340=CARTESIAN_POINT('Ctrl Pts',(31.017781090129,0.587616186362104,27.6666713436984));
#54341=CARTESIAN_POINT('Ctrl Pts',(30.6785207267527,1.17523237272422,27.7083380103651));
#54342=CARTESIAN_POINT('Ctrl Pts',(30.,1.17523237272422,27.7500046770317));
#54343=CARTESIAN_POINT('Ctrl Pts',(29.3214792732473,1.17523237272422,27.7916713436984));
#54344=CARTESIAN_POINT('Ctrl Pts',(28.9822189098709,0.587616186362105,27.8333380103651));
#54345=CARTESIAN_POINT('Ctrl Pts',(28.6429585464946,-1.32141491426617E-14,
27.8750046770317));
#54346=CARTESIAN_POINT('Ctrl Pts',(28.9822189098709,-0.587616186362132,
27.9166713436984));
#54347=CARTESIAN_POINT('Ctrl Pts',(29.3214792732473,-1.17523237272425,27.9583380103651));
#54348=CARTESIAN_POINT('Ctrl Pts',(30.,-1.17523237272425,28.0000046770317));
#54349=CARTESIAN_POINT('Ctrl Pts',(30.6785207267527,-1.17523237272425,28.0416713436984));
#54350=CARTESIAN_POINT('Ctrl Pts',(31.017781090129,-0.587616186362132,28.0833380103651));
#54351=CARTESIAN_POINT('Ctrl Pts',(31.3570414535054,-1.35453513912972E-14,
28.1250046770317));
#54352=CARTESIAN_POINT('Ctrl Pts',(31.017781090129,0.587616186362104,28.1666713436984));
#54353=CARTESIAN_POINT('Ctrl Pts',(30.6785207267527,1.17523237272422,28.2083380103651));
#54354=CARTESIAN_POINT('Ctrl Pts',(30.,1.17523237272422,28.2500046770317));
#54355=CARTESIAN_POINT('Ctrl Pts',(29.3214792732473,1.17523237272422,28.2916713436984));
#54356=CARTESIAN_POINT('Ctrl Pts',(28.9822189098709,0.587616186362105,28.3333380103651));
#54357=CARTESIAN_POINT('Ctrl Pts',(28.6429585464946,-1.32141491426617E-14,
28.3750046770317));
#54358=CARTESIAN_POINT('Ctrl Pts',(28.9822189098709,-0.587616186362132,
28.4166713436984));
#54359=CARTESIAN_POINT('Ctrl Pts',(29.3214792732473,-1.17523237272425,28.4583380103651));
#54360=CARTESIAN_POINT('Ctrl Pts',(30.,-1.17523237272425,28.5000046770317));
#54361=CARTESIAN_POINT('Ctrl Pts',(30.6785207267527,-1.17523237272425,28.5416713436984));
#54362=CARTESIAN_POINT('Ctrl Pts',(31.017781090129,-0.587616186362132,28.5833380103651));
#54363=CARTESIAN_POINT('Ctrl Pts',(31.3570414535054,-1.35453513912972E-14,
28.6250046770317));
#54364=CARTESIAN_POINT('Ctrl Pts',(31.017781090129,0.587616186362104,28.6666713436984));
#54365=CARTESIAN_POINT('Ctrl Pts',(30.6785207267527,1.17523237272422,28.7083380103651));
#54366=CARTESIAN_POINT('Ctrl Pts',(30.,1.17523237272422,28.7500046770317));
#54367=CARTESIAN_POINT('Ctrl Pts',(29.3214792732473,1.17523237272422,28.7916713436984));
#54368=CARTESIAN_POINT('Ctrl Pts',(28.9822189098709,0.587616186362105,28.8333380103651));
#54369=CARTESIAN_POINT('Ctrl Pts',(28.6429585464946,-1.32141491426617E-14,
28.8750046770317));
#54370=CARTESIAN_POINT('Ctrl Pts',(28.9822189098709,-0.587616186362132,
28.9166713436984));
#54371=CARTESIAN_POINT('Ctrl Pts',(29.3214792732473,-1.17523237272425,28.9583380103651));
#54372=CARTESIAN_POINT('Ctrl Pts',(30.,-1.17523237272425,29.0000046770317));
#54373=CARTESIAN_POINT('Ctrl Pts',(30.6785207267527,-1.17523237272425,29.0416713436984));
#54374=CARTESIAN_POINT('Ctrl Pts',(31.017781090129,-0.587616186362132,29.0833380103651));
#54375=CARTESIAN_POINT('Ctrl Pts',(31.3570414535054,-1.35453513912972E-14,
29.1250046770317));
#54376=CARTESIAN_POINT('Ctrl Pts',(31.017781090129,0.587616186362104,29.1666713436984));
#54377=CARTESIAN_POINT('Ctrl Pts',(30.6785207267527,1.17523237272422,29.2083380103651));
#54378=CARTESIAN_POINT('Ctrl Pts',(30.,1.17523237272422,29.2500046770317));
#54379=CARTESIAN_POINT('Ctrl Pts',(29.3214792732473,1.17523237272422,29.2916713436984));
#54380=CARTESIAN_POINT('Ctrl Pts',(28.9822189098709,0.587616186362105,29.3333380103651));
#54381=CARTESIAN_POINT('Ctrl Pts',(28.6429585464946,-1.32141491426617E-14,
29.3750046770317));
#54382=CARTESIAN_POINT('Ctrl Pts',(28.9822189098709,-0.587616186362132,
29.4166713436984));
#54383=CARTESIAN_POINT('Ctrl Pts',(29.3214792732473,-1.17523237272425,29.4583380103651));
#54384=CARTESIAN_POINT('Ctrl Pts',(30.,-1.17523237272425,29.5000046770317));
#54385=CARTESIAN_POINT('Ctrl Pts',(30.6785207267527,-1.17523237272425,29.5416713436984));
#54386=CARTESIAN_POINT('Ctrl Pts',(31.017781090129,-0.587616186362132,29.5833380103651));
#54387=CARTESIAN_POINT('Ctrl Pts',(31.3570414535054,-1.35453513912972E-14,
29.6250046770317));
#54388=CARTESIAN_POINT('Ctrl Pts',(31.017781090129,0.587616186362104,29.6666713436984));
#54389=CARTESIAN_POINT('Ctrl Pts',(30.6785207267527,1.17523237272422,29.7083380103651));
#54390=CARTESIAN_POINT('Ctrl Pts',(30.,1.17523237272422,29.7500046770317));
#54391=CARTESIAN_POINT('Ctrl Pts',(29.3214792732473,1.17523237272422,29.7916713436984));
#54392=CARTESIAN_POINT('Ctrl Pts',(28.9822189098709,0.587616186362105,29.8333380103651));
#54393=CARTESIAN_POINT('Ctrl Pts',(28.6429585464946,-1.32141491426617E-14,
29.8750046770317));
#54394=CARTESIAN_POINT('Ctrl Pts',(28.9822189098709,-0.587616186362132,
29.9166713436984));
#54395=CARTESIAN_POINT('Ctrl Pts',(29.3214792732473,-1.17523237272425,29.9583380103651));
#54396=CARTESIAN_POINT('Ctrl Pts',(30.,-1.17523237272425,30.0000046770317));
#54397=CARTESIAN_POINT('Ctrl Pts',(30.6785207267527,-1.17523237272425,30.0416713436984));
#54398=CARTESIAN_POINT('Ctrl Pts',(31.017781090129,-0.587616186362132,30.0833380103651));
#54399=CARTESIAN_POINT('Ctrl Pts',(31.3570414535054,-1.35453513912972E-14,
30.1250046770317));
#54400=CARTESIAN_POINT('Ctrl Pts',(31.017781090129,0.587616186362104,30.1666713436984));
#54401=CARTESIAN_POINT('Ctrl Pts',(30.6785207267527,1.17523237272422,30.2083380103651));
#54402=CARTESIAN_POINT('Ctrl Pts',(30.,1.17523237272422,30.2500046770317));
#54403=CARTESIAN_POINT('Ctrl Pts',(29.3214792732473,1.17523237272422,30.2916713436984));
#54404=CARTESIAN_POINT('Ctrl Pts',(28.9822189098709,0.587616186362105,30.3333380103651));
#54405=CARTESIAN_POINT('Ctrl Pts',(28.6429585464946,-1.32141491426617E-14,
30.3750046770317));
#54406=CARTESIAN_POINT('Ctrl Pts',(28.9822189098709,-0.587616186362132,
30.4166713436984));
#54407=CARTESIAN_POINT('Ctrl Pts',(29.3214792732473,-1.17523237272425,30.4583380103651));
#54408=CARTESIAN_POINT('Ctrl Pts',(30.,-1.17523237272425,30.5000046770317));
#54409=CARTESIAN_POINT('Ctrl Pts',(30.6785207267527,-1.17523237272425,30.5416713436984));
#54410=CARTESIAN_POINT('Ctrl Pts',(31.017781090129,-0.587616186362132,30.5833380103651));
#54411=CARTESIAN_POINT('Ctrl Pts',(31.3570414535054,-1.35453513912972E-14,
30.6250046770317));
#54412=CARTESIAN_POINT('Ctrl Pts',(31.017781090129,0.587616186362104,30.6666713436984));
#54413=CARTESIAN_POINT('Ctrl Pts',(30.6785207267527,1.17523237272422,30.7083380103651));
#54414=CARTESIAN_POINT('Ctrl Pts',(30.,1.17523237272422,30.7500046770317));
#54415=CARTESIAN_POINT('Ctrl Pts',(29.3214792732473,1.17523237272422,30.7916713436984));
#54416=CARTESIAN_POINT('Ctrl Pts',(28.9822189098709,0.587616186362105,30.8333380103651));
#54417=CARTESIAN_POINT('Ctrl Pts',(28.6429585464946,-1.32141491426617E-14,
30.8750046770317));
#54418=CARTESIAN_POINT('Ctrl Pts',(28.9822189098709,-0.587616186362132,
30.9166713436984));
#54419=CARTESIAN_POINT('Ctrl Pts',(29.3214792732473,-1.17523237272425,30.9583380103651));
#54420=CARTESIAN_POINT('Ctrl Pts',(30.,-1.17523237272425,31.0000046770317));
#54421=CARTESIAN_POINT('Ctrl Pts',(30.6785207267527,-1.17523237272425,31.0416713436984));
#54422=CARTESIAN_POINT('Ctrl Pts',(31.017781090129,-0.587616186362132,31.0833380103651));
#54423=CARTESIAN_POINT('Ctrl Pts',(31.3570414535054,-1.35453513912972E-14,
31.1250046770317));
#54424=CARTESIAN_POINT('Ctrl Pts',(31.017781090129,0.587616186362104,31.1666713436984));
#54425=CARTESIAN_POINT('Ctrl Pts',(30.6785207267527,1.17523237272422,31.2083380103651));
#54426=CARTESIAN_POINT('Ctrl Pts',(30.,1.17523237272422,31.2500046770317));
#54427=CARTESIAN_POINT('Ctrl Pts',(30.,1.52706329386825,15.546875));
#54428=CARTESIAN_POINT('Ctrl Pts',(29.1183495962155,1.52706329386825,15.5885416666667));
#54429=CARTESIAN_POINT('Ctrl Pts',(28.6775243943233,0.76353164693412,15.6302083333334));
#54430=CARTESIAN_POINT('Ctrl Pts',(28.2366991924311,-1.31894491186926E-14,
15.671875));
#54431=CARTESIAN_POINT('Ctrl Pts',(28.6775243943233,-0.763531646934146,
15.7135416666667));
#54432=CARTESIAN_POINT('Ctrl Pts',(29.1183495962155,-1.52706329386828,15.7552083333334));
#54433=CARTESIAN_POINT('Ctrl Pts',(30.,-1.52706329386828,15.796875));
#54434=CARTESIAN_POINT('Ctrl Pts',(30.8816504037844,-1.52706329386828,15.8385416666667));
#54435=CARTESIAN_POINT('Ctrl Pts',(31.3224756056766,-0.763531646934147,
15.8802083333334));
#54436=CARTESIAN_POINT('Ctrl Pts',(31.7633008075689,-1.36198038370242E-14,
15.921875));
#54437=CARTESIAN_POINT('Ctrl Pts',(31.3224756056766,0.763531646934118,15.9635416666667));
#54438=CARTESIAN_POINT('Ctrl Pts',(30.8816504037844,1.52706329386825,16.0052083333334));
#54439=CARTESIAN_POINT('Ctrl Pts',(30.,1.52706329386825,16.046875));
#54440=CARTESIAN_POINT('Ctrl Pts',(29.1183495962155,1.52706329386825,16.0885416666667));
#54441=CARTESIAN_POINT('Ctrl Pts',(28.6775243943233,0.76353164693412,16.1302083333334));
#54442=CARTESIAN_POINT('Ctrl Pts',(28.2366991924311,-1.31894491186926E-14,
16.171875));
#54443=CARTESIAN_POINT('Ctrl Pts',(28.6775243943233,-0.763531646934146,
16.2135416666667));
#54444=CARTESIAN_POINT('Ctrl Pts',(29.1183495962155,-1.52706329386828,16.2552083333334));
#54445=CARTESIAN_POINT('Ctrl Pts',(30.,-1.52706329386828,16.296875));
#54446=CARTESIAN_POINT('Ctrl Pts',(30.8816504037844,-1.52706329386828,16.3385416666667));
#54447=CARTESIAN_POINT('Ctrl Pts',(31.3224756056766,-0.763531646934147,
16.3802083333334));
#54448=CARTESIAN_POINT('Ctrl Pts',(31.7633008075689,-1.36198038370242E-14,
16.421875));
#54449=CARTESIAN_POINT('Ctrl Pts',(31.3224756056766,0.763531646934118,16.4635416666667));
#54450=CARTESIAN_POINT('Ctrl Pts',(30.8816504037844,1.52706329386825,16.5052083333334));
#54451=CARTESIAN_POINT('Ctrl Pts',(30.,1.52706329386825,16.546875));
#54452=CARTESIAN_POINT('Ctrl Pts',(29.1183495962155,1.52706329386825,16.5885416666667));
#54453=CARTESIAN_POINT('Ctrl Pts',(28.6775243943233,0.76353164693412,16.6302083333334));
#54454=CARTESIAN_POINT('Ctrl Pts',(28.2366991924311,-1.31894491186926E-14,
16.671875));
#54455=CARTESIAN_POINT('Ctrl Pts',(28.6775243943233,-0.763531646934146,
16.7135416666667));
#54456=CARTESIAN_POINT('Ctrl Pts',(29.1183495962155,-1.52706329386828,16.7552083333334));
#54457=CARTESIAN_POINT('Ctrl Pts',(30.,-1.52706329386828,16.796875));
#54458=CARTESIAN_POINT('Ctrl Pts',(30.8816504037844,-1.52706329386828,16.8385416666667));
#54459=CARTESIAN_POINT('Ctrl Pts',(31.3224756056766,-0.763531646934147,
16.8802083333334));
#54460=CARTESIAN_POINT('Ctrl Pts',(31.7633008075689,-1.36198038370242E-14,
16.921875));
#54461=CARTESIAN_POINT('Ctrl Pts',(31.3224756056766,0.763531646934118,16.9635416666667));
#54462=CARTESIAN_POINT('Ctrl Pts',(30.8816504037844,1.52706329386825,17.0052083333334));
#54463=CARTESIAN_POINT('Ctrl Pts',(30.,1.52706329386825,17.046875));
#54464=CARTESIAN_POINT('Ctrl Pts',(29.1183495962155,1.52706329386825,17.0885416666667));
#54465=CARTESIAN_POINT('Ctrl Pts',(28.6775243943233,0.76353164693412,17.1302083333334));
#54466=CARTESIAN_POINT('Ctrl Pts',(28.2366991924311,-1.31894491186926E-14,
17.171875));
#54467=CARTESIAN_POINT('Ctrl Pts',(28.6775243943233,-0.763531646934146,
17.2135416666667));
#54468=CARTESIAN_POINT('Ctrl Pts',(29.1183495962155,-1.52706329386828,17.2552083333334));
#54469=CARTESIAN_POINT('Ctrl Pts',(30.,-1.52706329386828,17.296875));
#54470=CARTESIAN_POINT('Ctrl Pts',(30.8816504037844,-1.52706329386828,17.3385416666667));
#54471=CARTESIAN_POINT('Ctrl Pts',(31.3224756056766,-0.763531646934147,
17.3802083333334));
#54472=CARTESIAN_POINT('Ctrl Pts',(31.7633008075689,-1.36198038370242E-14,
17.421875));
#54473=CARTESIAN_POINT('Ctrl Pts',(31.3224756056766,0.763531646934118,17.4635416666667));
#54474=CARTESIAN_POINT('Ctrl Pts',(30.8816504037844,1.52706329386825,17.5052083333334));
#54475=CARTESIAN_POINT('Ctrl Pts',(30.,1.52706329386825,17.546875));
#54476=CARTESIAN_POINT('Ctrl Pts',(29.1183495962155,1.52706329386825,17.5885416666667));
#54477=CARTESIAN_POINT('Ctrl Pts',(28.6775243943233,0.76353164693412,17.6302083333334));
#54478=CARTESIAN_POINT('Ctrl Pts',(28.2366991924311,-1.31894491186926E-14,
17.671875));
#54479=CARTESIAN_POINT('Ctrl Pts',(28.6775243943233,-0.763531646934146,
17.7135416666667));
#54480=CARTESIAN_POINT('Ctrl Pts',(29.1183495962155,-1.52706329386828,17.7552083333334));
#54481=CARTESIAN_POINT('Ctrl Pts',(30.,-1.52706329386828,17.796875));
#54482=CARTESIAN_POINT('Ctrl Pts',(30.8816504037844,-1.52706329386828,17.8385416666667));
#54483=CARTESIAN_POINT('Ctrl Pts',(31.3224756056766,-0.763531646934147,
17.8802083333334));
#54484=CARTESIAN_POINT('Ctrl Pts',(31.7633008075689,-1.36198038370242E-14,
17.921875));
#54485=CARTESIAN_POINT('Ctrl Pts',(31.3224756056766,0.763531646934118,17.9635416666667));
#54486=CARTESIAN_POINT('Ctrl Pts',(30.8816504037844,1.52706329386825,18.0052083333334));
#54487=CARTESIAN_POINT('Ctrl Pts',(30.,1.52706329386825,18.046875));
#54488=CARTESIAN_POINT('Ctrl Pts',(29.1183495962155,1.52706329386825,18.0885416666667));
#54489=CARTESIAN_POINT('Ctrl Pts',(28.6775243943233,0.76353164693412,18.1302083333334));
#54490=CARTESIAN_POINT('Ctrl Pts',(28.2366991924311,-1.31894491186926E-14,
18.171875));
#54491=CARTESIAN_POINT('Ctrl Pts',(28.6775243943233,-0.763531646934146,
18.2135416666667));
#54492=CARTESIAN_POINT('Ctrl Pts',(29.1183495962155,-1.52706329386828,18.2552083333334));
#54493=CARTESIAN_POINT('Ctrl Pts',(30.,-1.52706329386828,18.296875));
#54494=CARTESIAN_POINT('Ctrl Pts',(30.8816504037844,-1.52706329386828,18.3385416666667));
#54495=CARTESIAN_POINT('Ctrl Pts',(31.3224756056766,-0.763531646934147,
18.3802083333334));
#54496=CARTESIAN_POINT('Ctrl Pts',(31.7633008075689,-1.36198038370242E-14,
18.421875));
#54497=CARTESIAN_POINT('Ctrl Pts',(31.3224756056766,0.763531646934118,18.4635416666667));
#54498=CARTESIAN_POINT('Ctrl Pts',(30.8816504037844,1.52706329386825,18.5052083333334));
#54499=CARTESIAN_POINT('Ctrl Pts',(30.,1.52706329386825,18.546875));
#54500=CARTESIAN_POINT('Ctrl Pts',(29.1183495962155,1.52706329386825,18.5885416666667));
#54501=CARTESIAN_POINT('Ctrl Pts',(28.6775243943233,0.76353164693412,18.6302083333334));
#54502=CARTESIAN_POINT('Ctrl Pts',(28.2366991924311,-1.31894491186926E-14,
18.671875));
#54503=CARTESIAN_POINT('Ctrl Pts',(28.6775243943233,-0.763531646934146,
18.7135416666667));
#54504=CARTESIAN_POINT('Ctrl Pts',(29.1183495962155,-1.52706329386828,18.7552083333334));
#54505=CARTESIAN_POINT('Ctrl Pts',(30.,-1.52706329386828,18.796875));
#54506=CARTESIAN_POINT('Ctrl Pts',(30.8816504037844,-1.52706329386828,18.8385416666667));
#54507=CARTESIAN_POINT('Ctrl Pts',(31.3224756056766,-0.763531646934147,
18.8802083333334));
#54508=CARTESIAN_POINT('Ctrl Pts',(31.7633008075689,-1.36198038370242E-14,
18.921875));
#54509=CARTESIAN_POINT('Ctrl Pts',(31.3224756056766,0.763531646934118,18.9635416666667));
#54510=CARTESIAN_POINT('Ctrl Pts',(30.8816504037844,1.52706329386825,19.0052083333334));
#54511=CARTESIAN_POINT('Ctrl Pts',(30.,1.52706329386825,19.046875));
#54512=CARTESIAN_POINT('Ctrl Pts',(29.1183495962155,1.52706329386825,19.0885416666667));
#54513=CARTESIAN_POINT('Ctrl Pts',(28.6775243943233,0.76353164693412,19.1302083333334));
#54514=CARTESIAN_POINT('Ctrl Pts',(28.2366991924311,-1.31894491186926E-14,
19.171875));
#54515=CARTESIAN_POINT('Ctrl Pts',(28.6775243943233,-0.763531646934146,
19.2135416666667));
#54516=CARTESIAN_POINT('Ctrl Pts',(29.1183495962155,-1.52706329386828,19.2552083333334));
#54517=CARTESIAN_POINT('Ctrl Pts',(30.,-1.52706329386828,19.296875));
#54518=CARTESIAN_POINT('Ctrl Pts',(30.8816504037844,-1.52706329386828,19.3385416666667));
#54519=CARTESIAN_POINT('Ctrl Pts',(31.3224756056766,-0.763531646934147,
19.3802083333334));
#54520=CARTESIAN_POINT('Ctrl Pts',(31.7633008075689,-1.36198038370242E-14,
19.421875));
#54521=CARTESIAN_POINT('Ctrl Pts',(31.3224756056766,0.763531646934118,19.4635416666667));
#54522=CARTESIAN_POINT('Ctrl Pts',(30.8816504037844,1.52706329386825,19.5052083333334));
#54523=CARTESIAN_POINT('Ctrl Pts',(30.,1.52706329386825,19.546875));
#54524=CARTESIAN_POINT('Ctrl Pts',(29.1183495962155,1.52706329386825,19.5885416666667));
#54525=CARTESIAN_POINT('Ctrl Pts',(28.6775243943233,0.76353164693412,19.6302083333334));
#54526=CARTESIAN_POINT('Ctrl Pts',(28.2366991924311,-1.31894491186926E-14,
19.671875));
#54527=CARTESIAN_POINT('Ctrl Pts',(28.6775243943233,-0.763531646934146,
19.7135416666667));
#54528=CARTESIAN_POINT('Ctrl Pts',(29.1183495962155,-1.52706329386828,19.7552083333334));
#54529=CARTESIAN_POINT('Ctrl Pts',(30.,-1.52706329386828,19.796875));
#54530=CARTESIAN_POINT('Ctrl Pts',(30.8816504037844,-1.52706329386828,19.8385416666667));
#54531=CARTESIAN_POINT('Ctrl Pts',(31.3224756056766,-0.763531646934147,
19.8802083333334));
#54532=CARTESIAN_POINT('Ctrl Pts',(31.7633008075689,-1.36198038370242E-14,
19.921875));
#54533=CARTESIAN_POINT('Ctrl Pts',(31.3224756056766,0.763531646934118,19.9635416666667));
#54534=CARTESIAN_POINT('Ctrl Pts',(30.8816504037844,1.52706329386825,20.0052083333334));
#54535=CARTESIAN_POINT('Ctrl Pts',(30.,1.52706329386825,20.046875));
#54536=CARTESIAN_POINT('Ctrl Pts',(29.1183495962155,1.52706329386825,20.0885416666667));
#54537=CARTESIAN_POINT('Ctrl Pts',(28.6775243943233,0.76353164693412,20.1302083333334));
#54538=CARTESIAN_POINT('Ctrl Pts',(28.2366991924311,-1.31894491186926E-14,
20.171875));
#54539=CARTESIAN_POINT('Ctrl Pts',(28.6775243943233,-0.763531646934146,
20.2135416666667));
#54540=CARTESIAN_POINT('Ctrl Pts',(29.1183495962155,-1.52706329386828,20.2552083333334));
#54541=CARTESIAN_POINT('Ctrl Pts',(30.,-1.52706329386828,20.296875));
#54542=CARTESIAN_POINT('Ctrl Pts',(30.8816504037844,-1.52706329386828,20.3385416666667));
#54543=CARTESIAN_POINT('Ctrl Pts',(31.3224756056766,-0.763531646934147,
20.3802083333334));
#54544=CARTESIAN_POINT('Ctrl Pts',(31.7633008075689,-1.36198038370242E-14,
20.421875));
#54545=CARTESIAN_POINT('Ctrl Pts',(31.3224756056766,0.763531646934118,20.4635416666667));
#54546=CARTESIAN_POINT('Ctrl Pts',(30.8816504037844,1.52706329386825,20.5052083333334));
#54547=CARTESIAN_POINT('Ctrl Pts',(30.,1.52706329386825,20.546875));
#54548=CARTESIAN_POINT('Ctrl Pts',(29.1183495962155,1.52706329386825,20.5885416666667));
#54549=CARTESIAN_POINT('Ctrl Pts',(28.6775243943233,0.76353164693412,20.6302083333334));
#54550=CARTESIAN_POINT('Ctrl Pts',(28.2366991924311,-1.31894491186926E-14,
20.671875));
#54551=CARTESIAN_POINT('Ctrl Pts',(28.6775243943233,-0.763531646934146,
20.7135416666667));
#54552=CARTESIAN_POINT('Ctrl Pts',(29.1183495962155,-1.52706329386828,20.7552083333334));
#54553=CARTESIAN_POINT('Ctrl Pts',(30.,-1.52706329386828,20.796875));
#54554=CARTESIAN_POINT('Ctrl Pts',(30.8816504037844,-1.52706329386828,20.8385416666667));
#54555=CARTESIAN_POINT('Ctrl Pts',(31.3224756056766,-0.763531646934147,
20.8802083333334));
#54556=CARTESIAN_POINT('Ctrl Pts',(31.7633008075689,-1.36198038370242E-14,
20.921875));
#54557=CARTESIAN_POINT('Ctrl Pts',(31.3224756056766,0.763531646934118,20.9635416666667));
#54558=CARTESIAN_POINT('Ctrl Pts',(30.8816504037844,1.52706329386825,21.0052083333334));
#54559=CARTESIAN_POINT('Ctrl Pts',(30.,1.52706329386825,21.046875));
#54560=CARTESIAN_POINT('Ctrl Pts',(29.1183495962155,1.52706329386825,21.0885416666667));
#54561=CARTESIAN_POINT('Ctrl Pts',(28.6775243943233,0.76353164693412,21.1302083333334));
#54562=CARTESIAN_POINT('Ctrl Pts',(28.2366991924311,-1.31894491186926E-14,
21.171875));
#54563=CARTESIAN_POINT('Ctrl Pts',(28.6775243943233,-0.763531646934146,
21.2135416666667));
#54564=CARTESIAN_POINT('Ctrl Pts',(29.1183495962155,-1.52706329386828,21.2552083333334));
#54565=CARTESIAN_POINT('Ctrl Pts',(30.,-1.52706329386828,21.296875));
#54566=CARTESIAN_POINT('Ctrl Pts',(30.8816504037844,-1.52706329386828,21.3385416666667));
#54567=CARTESIAN_POINT('Ctrl Pts',(31.3224756056766,-0.763531646934147,
21.3802083333334));
#54568=CARTESIAN_POINT('Ctrl Pts',(31.7633008075689,-1.36198038370242E-14,
21.421875));
#54569=CARTESIAN_POINT('Ctrl Pts',(31.3224756056766,0.763531646934118,21.4635416666667));
#54570=CARTESIAN_POINT('Ctrl Pts',(30.8816504037844,1.52706329386825,21.5052083333334));
#54571=CARTESIAN_POINT('Ctrl Pts',(30.,1.52706329386825,21.546875));
#54572=CARTESIAN_POINT('Ctrl Pts',(29.1183495962155,1.52706329386825,21.5885416666667));
#54573=CARTESIAN_POINT('Ctrl Pts',(28.6775243943233,0.76353164693412,21.6302083333334));
#54574=CARTESIAN_POINT('Ctrl Pts',(28.2366991924311,-1.31894491186926E-14,
21.671875));
#54575=CARTESIAN_POINT('Ctrl Pts',(28.6775243943233,-0.763531646934146,
21.7135416666667));
#54576=CARTESIAN_POINT('Ctrl Pts',(29.1183495962155,-1.52706329386828,21.7552083333334));
#54577=CARTESIAN_POINT('Ctrl Pts',(30.,-1.52706329386828,21.796875));
#54578=CARTESIAN_POINT('Ctrl Pts',(30.8816504037844,-1.52706329386828,21.8385416666667));
#54579=CARTESIAN_POINT('Ctrl Pts',(31.3224756056766,-0.763531646934147,
21.8802083333334));
#54580=CARTESIAN_POINT('Ctrl Pts',(31.7633008075689,-1.36198038370242E-14,
21.921875));
#54581=CARTESIAN_POINT('Ctrl Pts',(31.3224756056766,0.763531646934118,21.9635416666667));
#54582=CARTESIAN_POINT('Ctrl Pts',(30.8816504037844,1.52706329386825,22.0052083333334));
#54583=CARTESIAN_POINT('Ctrl Pts',(30.,1.52706329386825,22.046875));
#54584=CARTESIAN_POINT('Ctrl Pts',(29.1183495962155,1.52706329386825,22.0885416666667));
#54585=CARTESIAN_POINT('Ctrl Pts',(28.6775243943233,0.76353164693412,22.1302083333334));
#54586=CARTESIAN_POINT('Ctrl Pts',(28.2366991924311,-1.31894491186926E-14,
22.171875));
#54587=CARTESIAN_POINT('Ctrl Pts',(28.6775243943233,-0.763531646934146,
22.2135416666667));
#54588=CARTESIAN_POINT('Ctrl Pts',(29.1183495962155,-1.52706329386828,22.2552083333334));
#54589=CARTESIAN_POINT('Ctrl Pts',(30.,-1.52706329386828,22.296875));
#54590=CARTESIAN_POINT('Ctrl Pts',(30.8816504037844,-1.52706329386828,22.3385416666667));
#54591=CARTESIAN_POINT('Ctrl Pts',(31.3224756056766,-0.763531646934147,
22.3802083333334));
#54592=CARTESIAN_POINT('Ctrl Pts',(31.7633008075689,-1.36198038370242E-14,
22.421875));
#54593=CARTESIAN_POINT('Ctrl Pts',(31.3224756056766,0.763531646934118,22.4635416666667));
#54594=CARTESIAN_POINT('Ctrl Pts',(30.8816504037844,1.52706329386825,22.5052083333334));
#54595=CARTESIAN_POINT('Ctrl Pts',(30.,1.52706329386825,22.546875));
#54596=CARTESIAN_POINT('Ctrl Pts',(29.1183495962155,1.52706329386825,22.5885416666667));
#54597=CARTESIAN_POINT('Ctrl Pts',(28.6775243943233,0.76353164693412,22.6302083333334));
#54598=CARTESIAN_POINT('Ctrl Pts',(28.2366991924311,-1.31894491186926E-14,
22.671875));
#54599=CARTESIAN_POINT('Ctrl Pts',(28.6775243943233,-0.763531646934146,
22.7135416666667));
#54600=CARTESIAN_POINT('Ctrl Pts',(29.1183495962155,-1.52706329386828,22.7552083333334));
#54601=CARTESIAN_POINT('Ctrl Pts',(30.,-1.52706329386828,22.796875));
#54602=CARTESIAN_POINT('Ctrl Pts',(30.8816504037844,-1.52706329386828,22.8385416666667));
#54603=CARTESIAN_POINT('Ctrl Pts',(31.3224756056766,-0.763531646934147,
22.8802083333334));
#54604=CARTESIAN_POINT('Ctrl Pts',(31.7633008075689,-1.36198038370242E-14,
22.921875));
#54605=CARTESIAN_POINT('Ctrl Pts',(31.3224756056766,0.763531646934118,22.9635416666667));
#54606=CARTESIAN_POINT('Ctrl Pts',(30.8816504037844,1.52706329386825,23.0052083333334));
#54607=CARTESIAN_POINT('Ctrl Pts',(30.,1.52706329386825,23.046875));
#54608=CARTESIAN_POINT('Ctrl Pts',(29.1183495962155,1.52706329386825,23.0885416666667));
#54609=CARTESIAN_POINT('Ctrl Pts',(28.6775243943233,0.76353164693412,23.1302083333334));
#54610=CARTESIAN_POINT('Ctrl Pts',(28.2366991924311,-1.31894491186926E-14,
23.171875));
#54611=CARTESIAN_POINT('Ctrl Pts',(28.6775243943233,-0.763531646934146,
23.2135416666667));
#54612=CARTESIAN_POINT('Ctrl Pts',(29.1183495962155,-1.52706329386828,23.2552083333334));
#54613=CARTESIAN_POINT('Ctrl Pts',(30.,-1.52706329386828,23.296875));
#54614=CARTESIAN_POINT('Ctrl Pts',(30.8816504037844,-1.52706329386828,23.3385416666667));
#54615=CARTESIAN_POINT('Ctrl Pts',(31.3224756056766,-0.763531646934147,
23.3802083333334));
#54616=CARTESIAN_POINT('Ctrl Pts',(31.7633008075689,-1.36198038370242E-14,
23.421875));
#54617=CARTESIAN_POINT('Ctrl Pts',(31.3224756056766,0.763531646934118,23.4635416666667));
#54618=CARTESIAN_POINT('Ctrl Pts',(30.8816504037844,1.52706329386825,23.5052083333334));
#54619=CARTESIAN_POINT('Ctrl Pts',(30.,1.52706329386825,23.546875));
#54620=CARTESIAN_POINT('Ctrl Pts',(29.1183495962155,1.52706329386825,23.5885416666667));
#54621=CARTESIAN_POINT('Ctrl Pts',(28.6775243943233,0.76353164693412,23.6302083333334));
#54622=CARTESIAN_POINT('Ctrl Pts',(28.2366991924311,-1.31894491186926E-14,
23.671875));
#54623=CARTESIAN_POINT('Ctrl Pts',(28.6775243943233,-0.763531646934146,
23.7135416666667));
#54624=CARTESIAN_POINT('Ctrl Pts',(29.1183495962155,-1.52706329386828,23.7552083333334));
#54625=CARTESIAN_POINT('Ctrl Pts',(30.,-1.52706329386828,23.796875));
#54626=CARTESIAN_POINT('Ctrl Pts',(30.8816504037844,-1.52706329386828,23.8385416666667));
#54627=CARTESIAN_POINT('Ctrl Pts',(31.3224756056766,-0.763531646934147,
23.8802083333334));
#54628=CARTESIAN_POINT('Ctrl Pts',(31.7633008075689,-1.36198038370242E-14,
23.921875));
#54629=CARTESIAN_POINT('Ctrl Pts',(31.3224756056766,0.763531646934118,23.9635416666667));
#54630=CARTESIAN_POINT('Ctrl Pts',(30.8816504037844,1.52706329386825,24.0052083333334));
#54631=CARTESIAN_POINT('Ctrl Pts',(30.,1.52706329386825,24.046875));
#54632=CARTESIAN_POINT('Ctrl Pts',(29.1183495962155,1.52706329386825,24.0885416666667));
#54633=CARTESIAN_POINT('Ctrl Pts',(28.6775243943233,0.76353164693412,24.1302083333334));
#54634=CARTESIAN_POINT('Ctrl Pts',(28.2366991924311,-1.31894491186926E-14,
24.171875));
#54635=CARTESIAN_POINT('Ctrl Pts',(28.6775243943233,-0.763531646934146,
24.2135416666667));
#54636=CARTESIAN_POINT('Ctrl Pts',(29.1183495962155,-1.52706329386828,24.2552083333334));
#54637=CARTESIAN_POINT('Ctrl Pts',(30.,-1.52706329386828,24.296875));
#54638=CARTESIAN_POINT('Ctrl Pts',(30.8816504037844,-1.52706329386828,24.3385416666667));
#54639=CARTESIAN_POINT('Ctrl Pts',(31.3224756056766,-0.763531646934147,
24.3802083333334));
#54640=CARTESIAN_POINT('Ctrl Pts',(31.7633008075689,-1.36198038370242E-14,
24.421875));
#54641=CARTESIAN_POINT('Ctrl Pts',(31.3224756056766,0.763531646934118,24.4635416666667));
#54642=CARTESIAN_POINT('Ctrl Pts',(30.8816504037844,1.52706329386825,24.5052083333334));
#54643=CARTESIAN_POINT('Ctrl Pts',(30.,1.52706329386825,24.546875));
#54644=CARTESIAN_POINT('Ctrl Pts',(29.1183495962155,1.52706329386825,24.5885416666667));
#54645=CARTESIAN_POINT('Ctrl Pts',(28.6775243943233,0.76353164693412,24.6302083333334));
#54646=CARTESIAN_POINT('Ctrl Pts',(28.2366991924311,-1.31894491186926E-14,
24.671875));
#54647=CARTESIAN_POINT('Ctrl Pts',(28.6775243943233,-0.763531646934146,
24.7135416666667));
#54648=CARTESIAN_POINT('Ctrl Pts',(29.1183495962155,-1.52706329386828,24.7552083333334));
#54649=CARTESIAN_POINT('Ctrl Pts',(30.,-1.52706329386828,24.796875));
#54650=CARTESIAN_POINT('Ctrl Pts',(30.8816504037844,-1.52706329386828,24.8385416666667));
#54651=CARTESIAN_POINT('Ctrl Pts',(31.3224756056766,-0.763531646934147,
24.8802083333334));
#54652=CARTESIAN_POINT('Ctrl Pts',(31.7633008075689,-1.36198038370242E-14,
24.921875));
#54653=CARTESIAN_POINT('Ctrl Pts',(31.3224756056766,0.763531646934118,24.9635416666667));
#54654=CARTESIAN_POINT('Ctrl Pts',(30.8816504037844,1.52706329386825,25.0052083333334));
#54655=CARTESIAN_POINT('Ctrl Pts',(30.,1.52706329386825,25.046875));
#54656=CARTESIAN_POINT('Ctrl Pts',(29.1183495962155,1.52706329386825,25.0885416666667));
#54657=CARTESIAN_POINT('Ctrl Pts',(28.6775243943233,0.76353164693412,25.1302083333334));
#54658=CARTESIAN_POINT('Ctrl Pts',(28.2366991924311,-1.31894491186926E-14,
25.171875));
#54659=CARTESIAN_POINT('Ctrl Pts',(28.6775243943233,-0.763531646934146,
25.2135416666667));
#54660=CARTESIAN_POINT('Ctrl Pts',(29.1183495962155,-1.52706329386828,25.2552083333334));
#54661=CARTESIAN_POINT('Ctrl Pts',(30.,-1.52706329386828,25.296875));
#54662=CARTESIAN_POINT('Ctrl Pts',(30.8816504037844,-1.52706329386828,25.3385416666667));
#54663=CARTESIAN_POINT('Ctrl Pts',(31.3224756056766,-0.763531646934147,
25.3802083333334));
#54664=CARTESIAN_POINT('Ctrl Pts',(31.7633008075689,-1.36198038370242E-14,
25.421875));
#54665=CARTESIAN_POINT('Ctrl Pts',(31.3224756056766,0.763531646934118,25.4635416666667));
#54666=CARTESIAN_POINT('Ctrl Pts',(30.8816504037844,1.52706329386825,25.5052083333334));
#54667=CARTESIAN_POINT('Ctrl Pts',(30.,1.52706329386825,25.546875));
#54668=CARTESIAN_POINT('Ctrl Pts',(29.1183495962155,1.52706329386825,25.5885416666667));
#54669=CARTESIAN_POINT('Ctrl Pts',(28.6775243943233,0.76353164693412,25.6302083333334));
#54670=CARTESIAN_POINT('Ctrl Pts',(28.2366991924311,-1.31894491186926E-14,
25.671875));
#54671=CARTESIAN_POINT('Ctrl Pts',(28.6775243943233,-0.763531646934146,
25.7135416666667));
#54672=CARTESIAN_POINT('Ctrl Pts',(29.1183495962155,-1.52706329386828,25.7552083333334));
#54673=CARTESIAN_POINT('Ctrl Pts',(30.,-1.52706329386828,25.796875));
#54674=CARTESIAN_POINT('Ctrl Pts',(30.8816504037844,-1.52706329386828,25.8385416666667));
#54675=CARTESIAN_POINT('Ctrl Pts',(31.3224756056766,-0.763531646934147,
25.8802083333334));
#54676=CARTESIAN_POINT('Ctrl Pts',(31.7633008075689,-1.36198038370242E-14,
25.921875));
#54677=CARTESIAN_POINT('Ctrl Pts',(31.3224756056766,0.763531646934118,25.9635416666667));
#54678=CARTESIAN_POINT('Ctrl Pts',(30.8816504037844,1.52706329386825,26.0052083333334));
#54679=CARTESIAN_POINT('Ctrl Pts',(30.,1.52706329386825,26.046875));
#54680=CARTESIAN_POINT('Ctrl Pts',(29.1183495962155,1.52706329386825,26.0885416666667));
#54681=CARTESIAN_POINT('Ctrl Pts',(28.6775243943233,0.76353164693412,26.1302083333334));
#54682=CARTESIAN_POINT('Ctrl Pts',(28.2366991924311,-1.31894491186926E-14,
26.171875));
#54683=CARTESIAN_POINT('Ctrl Pts',(28.6775243943233,-0.763531646934146,
26.2135416666667));
#54684=CARTESIAN_POINT('Ctrl Pts',(29.1183495962155,-1.52706329386828,26.2552083333334));
#54685=CARTESIAN_POINT('Ctrl Pts',(30.,-1.52706329386828,26.296875));
#54686=CARTESIAN_POINT('Ctrl Pts',(30.8816504037844,-1.52706329386828,26.3385416666667));
#54687=CARTESIAN_POINT('Ctrl Pts',(31.3224756056766,-0.763531646934147,
26.3802083333334));
#54688=CARTESIAN_POINT('Ctrl Pts',(31.7633008075689,-1.36198038370242E-14,
26.421875));
#54689=CARTESIAN_POINT('Ctrl Pts',(31.3224756056766,0.763531646934118,26.4635416666667));
#54690=CARTESIAN_POINT('Ctrl Pts',(30.8816504037844,1.52706329386825,26.5052083333334));
#54691=CARTESIAN_POINT('Ctrl Pts',(30.,1.52706329386825,26.546875));
#54692=CARTESIAN_POINT('Ctrl Pts',(29.1183495962155,1.52706329386825,26.5885416666667));
#54693=CARTESIAN_POINT('Ctrl Pts',(28.6775243943233,0.76353164693412,26.6302083333334));
#54694=CARTESIAN_POINT('Ctrl Pts',(28.2366991924311,-1.31894491186926E-14,
26.671875));
#54695=CARTESIAN_POINT('Ctrl Pts',(28.6775243943233,-0.763531646934146,
26.7135416666667));
#54696=CARTESIAN_POINT('Ctrl Pts',(29.1183495962155,-1.52706329386828,26.7552083333334));
#54697=CARTESIAN_POINT('Ctrl Pts',(30.,-1.52706329386828,26.796875));
#54698=CARTESIAN_POINT('Ctrl Pts',(30.8816504037844,-1.52706329386828,26.8385416666667));
#54699=CARTESIAN_POINT('Ctrl Pts',(31.3224756056766,-0.763531646934147,
26.8802083333334));
#54700=CARTESIAN_POINT('Ctrl Pts',(31.7633008075689,-1.36198038370242E-14,
26.921875));
#54701=CARTESIAN_POINT('Ctrl Pts',(31.3224756056766,0.763531646934118,26.9635416666667));
#54702=CARTESIAN_POINT('Ctrl Pts',(30.8816504037844,1.52706329386825,27.0052083333334));
#54703=CARTESIAN_POINT('Ctrl Pts',(30.,1.52706329386825,27.046875));
#54704=CARTESIAN_POINT('Ctrl Pts',(29.1183495962155,1.52706329386825,27.0885416666667));
#54705=CARTESIAN_POINT('Ctrl Pts',(28.6775243943233,0.76353164693412,27.1302083333334));
#54706=CARTESIAN_POINT('Ctrl Pts',(28.2366991924311,-1.31894491186926E-14,
27.171875));
#54707=CARTESIAN_POINT('Ctrl Pts',(28.6775243943233,-0.763531646934146,
27.2135416666667));
#54708=CARTESIAN_POINT('Ctrl Pts',(29.1183495962155,-1.52706329386828,27.2552083333334));
#54709=CARTESIAN_POINT('Ctrl Pts',(30.,-1.52706329386828,27.296875));
#54710=CARTESIAN_POINT('Ctrl Pts',(30.8816504037844,-1.52706329386828,27.3385416666667));
#54711=CARTESIAN_POINT('Ctrl Pts',(31.3224756056766,-0.763531646934147,
27.3802083333334));
#54712=CARTESIAN_POINT('Ctrl Pts',(31.7633008075689,-1.36198038370242E-14,
27.421875));
#54713=CARTESIAN_POINT('Ctrl Pts',(31.3224756056766,0.763531646934118,27.4635416666667));
#54714=CARTESIAN_POINT('Ctrl Pts',(30.8816504037844,1.52706329386825,27.5052083333334));
#54715=CARTESIAN_POINT('Ctrl Pts',(30.,1.52706329386825,27.546875));
#54716=CARTESIAN_POINT('Ctrl Pts',(29.1183495962155,1.52706329386825,27.5885416666667));
#54717=CARTESIAN_POINT('Ctrl Pts',(28.6775243943233,0.76353164693412,27.6302083333334));
#54718=CARTESIAN_POINT('Ctrl Pts',(28.2366991924311,-1.31894491186926E-14,
27.671875));
#54719=CARTESIAN_POINT('Ctrl Pts',(28.6775243943233,-0.763531646934146,
27.7135416666667));
#54720=CARTESIAN_POINT('Ctrl Pts',(29.1183495962155,-1.52706329386828,27.7552083333334));
#54721=CARTESIAN_POINT('Ctrl Pts',(30.,-1.52706329386828,27.796875));
#54722=CARTESIAN_POINT('Ctrl Pts',(30.8816504037844,-1.52706329386828,27.8385416666667));
#54723=CARTESIAN_POINT('Ctrl Pts',(31.3224756056766,-0.763531646934147,
27.8802083333334));
#54724=CARTESIAN_POINT('Ctrl Pts',(31.7633008075689,-1.36198038370242E-14,
27.921875));
#54725=CARTESIAN_POINT('Ctrl Pts',(31.3224756056766,0.763531646934118,27.9635416666667));
#54726=CARTESIAN_POINT('Ctrl Pts',(30.8816504037844,1.52706329386825,28.0052083333334));
#54727=CARTESIAN_POINT('Ctrl Pts',(30.,1.52706329386825,28.046875));
#54728=CARTESIAN_POINT('Ctrl Pts',(29.1183495962155,1.52706329386825,28.0885416666667));
#54729=CARTESIAN_POINT('Ctrl Pts',(28.6775243943233,0.76353164693412,28.1302083333334));
#54730=CARTESIAN_POINT('Ctrl Pts',(28.2366991924311,-1.31894491186926E-14,
28.171875));
#54731=CARTESIAN_POINT('Ctrl Pts',(28.6775243943233,-0.763531646934146,
28.2135416666667));
#54732=CARTESIAN_POINT('Ctrl Pts',(29.1183495962155,-1.52706329386828,28.2552083333334));
#54733=CARTESIAN_POINT('Ctrl Pts',(30.,-1.52706329386828,28.296875));
#54734=CARTESIAN_POINT('Ctrl Pts',(30.8816504037844,-1.52706329386828,28.3385416666667));
#54735=CARTESIAN_POINT('Ctrl Pts',(31.3224756056766,-0.763531646934147,
28.3802083333334));
#54736=CARTESIAN_POINT('Ctrl Pts',(31.7633008075689,-1.36198038370242E-14,
28.421875));
#54737=CARTESIAN_POINT('Ctrl Pts',(31.3224756056766,0.763531646934118,28.4635416666667));
#54738=CARTESIAN_POINT('Ctrl Pts',(30.8816504037844,1.52706329386825,28.5052083333334));
#54739=CARTESIAN_POINT('Ctrl Pts',(30.,1.52706329386825,28.546875));
#54740=CARTESIAN_POINT('Ctrl Pts',(29.1183495962155,1.52706329386825,28.5885416666667));
#54741=CARTESIAN_POINT('Ctrl Pts',(28.6775243943233,0.76353164693412,28.6302083333334));
#54742=CARTESIAN_POINT('Ctrl Pts',(28.2366991924311,-1.31894491186926E-14,
28.671875));
#54743=CARTESIAN_POINT('Ctrl Pts',(28.6775243943233,-0.763531646934146,
28.7135416666667));
#54744=CARTESIAN_POINT('Ctrl Pts',(29.1183495962155,-1.52706329386828,28.7552083333334));
#54745=CARTESIAN_POINT('Ctrl Pts',(30.,-1.52706329386828,28.796875));
#54746=CARTESIAN_POINT('Ctrl Pts',(30.8816504037844,-1.52706329386828,28.8385416666667));
#54747=CARTESIAN_POINT('Ctrl Pts',(31.3224756056766,-0.763531646934147,
28.8802083333334));
#54748=CARTESIAN_POINT('Ctrl Pts',(31.7633008075689,-1.36198038370242E-14,
28.921875));
#54749=CARTESIAN_POINT('Ctrl Pts',(31.3224756056766,0.763531646934118,28.9635416666667));
#54750=CARTESIAN_POINT('Ctrl Pts',(30.8816504037844,1.52706329386825,29.0052083333334));
#54751=CARTESIAN_POINT('Ctrl Pts',(30.,1.52706329386825,29.046875));
#54752=CARTESIAN_POINT('Ctrl Pts',(29.1183495962155,1.52706329386825,29.0885416666667));
#54753=CARTESIAN_POINT('Ctrl Pts',(28.6775243943233,0.76353164693412,29.1302083333334));
#54754=CARTESIAN_POINT('Ctrl Pts',(28.2366991924311,-1.31894491186926E-14,
29.171875));
#54755=CARTESIAN_POINT('Ctrl Pts',(28.6775243943233,-0.763531646934146,
29.2135416666667));
#54756=CARTESIAN_POINT('Ctrl Pts',(29.1183495962155,-1.52706329386828,29.2552083333334));
#54757=CARTESIAN_POINT('Ctrl Pts',(30.,-1.52706329386828,29.296875));
#54758=CARTESIAN_POINT('Ctrl Pts',(30.8816504037844,-1.52706329386828,29.3385416666667));
#54759=CARTESIAN_POINT('Ctrl Pts',(31.3224756056766,-0.763531646934147,
29.3802083333334));
#54760=CARTESIAN_POINT('Ctrl Pts',(31.7633008075689,-1.36198038370242E-14,
29.421875));
#54761=CARTESIAN_POINT('Ctrl Pts',(31.3224756056766,0.763531646934118,29.4635416666667));
#54762=CARTESIAN_POINT('Ctrl Pts',(30.8816504037844,1.52706329386825,29.5052083333334));
#54763=CARTESIAN_POINT('Ctrl Pts',(30.,1.52706329386825,29.546875));
#54764=CARTESIAN_POINT('Ctrl Pts',(29.1183495962155,1.52706329386825,29.5885416666667));
#54765=CARTESIAN_POINT('Ctrl Pts',(28.6775243943233,0.76353164693412,29.6302083333334));
#54766=CARTESIAN_POINT('Ctrl Pts',(28.2366991924311,-1.31894491186926E-14,
29.671875));
#54767=CARTESIAN_POINT('Ctrl Pts',(28.6775243943233,-0.763531646934146,
29.7135416666667));
#54768=CARTESIAN_POINT('Ctrl Pts',(29.1183495962155,-1.52706329386828,29.7552083333334));
#54769=CARTESIAN_POINT('Ctrl Pts',(30.,-1.52706329386828,29.796875));
#54770=CARTESIAN_POINT('Ctrl Pts',(30.8816504037844,-1.52706329386828,29.8385416666667));
#54771=CARTESIAN_POINT('Ctrl Pts',(31.3224756056766,-0.763531646934147,
29.8802083333334));
#54772=CARTESIAN_POINT('Ctrl Pts',(31.7633008075689,-1.36198038370242E-14,
29.921875));
#54773=CARTESIAN_POINT('Ctrl Pts',(31.3224756056766,0.763531646934118,29.9635416666667));
#54774=CARTESIAN_POINT('Ctrl Pts',(30.8816504037844,1.52706329386825,30.0052083333334));
#54775=CARTESIAN_POINT('Ctrl Pts',(30.,1.52706329386825,30.046875));
#54776=CARTESIAN_POINT('Ctrl Pts',(29.1183495962155,1.52706329386825,30.0885416666667));
#54777=CARTESIAN_POINT('Ctrl Pts',(28.6775243943233,0.76353164693412,30.1302083333334));
#54778=CARTESIAN_POINT('Ctrl Pts',(28.2366991924311,-1.31894491186926E-14,
30.171875));
#54779=CARTESIAN_POINT('Ctrl Pts',(28.6775243943233,-0.763531646934146,
30.2135416666667));
#54780=CARTESIAN_POINT('Ctrl Pts',(29.1183495962155,-1.52706329386828,30.2552083333334));
#54781=CARTESIAN_POINT('Ctrl Pts',(30.,-1.52706329386828,30.296875));
#54782=CARTESIAN_POINT('Ctrl Pts',(30.8816504037844,-1.52706329386828,30.3385416666667));
#54783=CARTESIAN_POINT('Ctrl Pts',(31.3224756056766,-0.763531646934147,
30.3802083333334));
#54784=CARTESIAN_POINT('Ctrl Pts',(31.7633008075689,-1.36198038370242E-14,
30.421875));
#54785=CARTESIAN_POINT('Ctrl Pts',(31.3224756056766,0.763531646934118,30.4635416666667));
#54786=CARTESIAN_POINT('Ctrl Pts',(30.8816504037844,1.52706329386825,30.5052083333334));
#54787=CARTESIAN_POINT('Ctrl Pts',(30.,1.52706329386825,30.546875));
#54788=CARTESIAN_POINT('Ctrl Pts',(29.1183495962155,1.52706329386825,30.5885416666667));
#54789=CARTESIAN_POINT('Ctrl Pts',(28.6775243943233,0.76353164693412,30.6302083333334));
#54790=CARTESIAN_POINT('Ctrl Pts',(28.2366991924311,-1.31894491186926E-14,
30.671875));
#54791=CARTESIAN_POINT('Ctrl Pts',(28.6775243943233,-0.763531646934146,
30.7135416666667));
#54792=CARTESIAN_POINT('Ctrl Pts',(29.1183495962155,-1.52706329386828,30.7552083333334));
#54793=CARTESIAN_POINT('Ctrl Pts',(30.,-1.52706329386828,30.796875));
#54794=CARTESIAN_POINT('Ctrl Pts',(30.8816504037844,-1.52706329386828,30.8385416666667));
#54795=CARTESIAN_POINT('Ctrl Pts',(31.3224756056766,-0.763531646934147,
30.8802083333334));
#54796=CARTESIAN_POINT('Ctrl Pts',(31.7633008075689,-1.36198038370242E-14,
30.921875));
#54797=CARTESIAN_POINT('Ctrl Pts',(31.3224756056766,0.763531646934118,30.9635416666667));
#54798=CARTESIAN_POINT('Ctrl Pts',(30.8816504037844,1.52706329386825,31.0052083333334));
#54799=CARTESIAN_POINT('Ctrl Pts',(30.,1.52706329386825,31.046875));
#54800=CARTESIAN_POINT('Ctrl Pts',(30.8234003400376,-0.838570603170131,
30.5624996575278));
#54801=CARTESIAN_POINT('Ctrl Pts',(30.9252409219315,-0.749808119816165,
30.5671289662449));
#54802=CARTESIAN_POINT('Ctrl Pts',(31.0094069192668,-0.645130506686946,
30.571193014068));
#54803=CARTESIAN_POINT('Ctrl Pts',(31.1396529784097,-0.412074319923831,
30.5795221820465));
#54804=CARTESIAN_POINT('Ctrl Pts',(31.1849584507844,-0.287685440765051,
30.5838904393726));
#54805=CARTESIAN_POINT('Ctrl Pts',(31.2386945750578,-0.00655181811616603,
30.5935664195233));
#54806=CARTESIAN_POINT('Ctrl Pts',(31.2387490550162,0.149503133824081,30.5988162542928));
#54807=CARTESIAN_POINT('Ctrl Pts',(31.1719223736106,0.500568259068406,30.610386374166));
#54808=CARTESIAN_POINT('Ctrl Pts',(31.0923154827319,0.652496494934345,30.6150433766711));
#54809=CARTESIAN_POINT('Ctrl Pts',(30.9283336729762,0.900293879400657,30.6239504439807));
#54810=CARTESIAN_POINT('Ctrl Pts',(30.8055598520391,1.02369588322745,30.6294622341334));
#54811=CARTESIAN_POINT('Ctrl Pts',(30.5288337282237,1.20882504193349,30.6401101417162));
#54812=CARTESIAN_POINT('Ctrl Pts',(30.3799906896905,1.27260041719159,30.6451552807199));
#54813=CARTESIAN_POINT('Ctrl Pts',(30.0014927028803,1.35728019461807,30.6565651904367));
#54814=CARTESIAN_POINT('Ctrl Pts',(29.8132785668206,1.33887636851719,30.6613880776071));
#54815=CARTESIAN_POINT('Ctrl Pts',(29.5198061598154,1.28660005614596,30.6701589170659));
#54816=CARTESIAN_POINT('Ctrl Pts',(29.3521505621284,1.22147978200258,30.6756096035631));
#54817=CARTESIAN_POINT('Ctrl Pts',(29.0485837866741,1.02916361274227,30.6863949411503));
#54818=CARTESIAN_POINT('Ctrl Pts',(28.9162494293832,0.902843317652004,30.6916208752244));
#54819=CARTESIAN_POINT('Ctrl Pts',(28.7272437086822,0.633185410868888,30.7002552651022));
#54820=CARTESIAN_POINT('Ctrl Pts',(28.6461891944724,0.476094037694283,30.7048351996635));
#54821=CARTESIAN_POINT('Ctrl Pts',(28.551105022901,0.105569064666544,30.715730913862));
#54822=CARTESIAN_POINT('Ctrl Pts',(28.5402826505383,-0.0831493783931786,
30.7211721595761));
#54823=CARTESIAN_POINT('Ctrl Pts',(28.5859138822382,-0.415083694084825,
30.7305650693331));
#54824=CARTESIAN_POINT('Ctrl Pts',(28.6283908398168,-0.557537406078615,
30.7345346397522));
#54825=CARTESIAN_POINT('Ctrl Pts',(28.7447696187018,-0.802908073480822,
30.7412906353098));
#54826=CARTESIAN_POINT('Ctrl Pts',(28.8264704242263,-0.938163811130005,
30.7451577422722));
#54827=CARTESIAN_POINT('Ctrl Pts',(28.9490560961683,-1.07028823734174,30.7500000000014));
#54828=CARTESIAN_POINT('Ctrl Pts',(30.,1.52706329386825,16.015625));
#54829=CARTESIAN_POINT('Ctrl Pts',(29.1183495962155,1.52706329386825,16.0572916666666));
#54830=CARTESIAN_POINT('Ctrl Pts',(28.6775243943233,0.76353164693412,16.0989583333333));
#54831=CARTESIAN_POINT('Ctrl Pts',(28.2366991924311,-1.31894491186926E-14,
16.140625));
#54832=CARTESIAN_POINT('Ctrl Pts',(28.6775243943233,-0.763531646934146,
16.1822916666666));
#54833=CARTESIAN_POINT('Ctrl Pts',(29.1183495962155,-1.52706329386828,16.2239583333333));
#54834=CARTESIAN_POINT('Ctrl Pts',(30.,-1.52706329386828,16.265625));
#54835=CARTESIAN_POINT('Ctrl Pts',(30.8816504037844,-1.52706329386828,16.3072916666666));
#54836=CARTESIAN_POINT('Ctrl Pts',(31.3224756056766,-0.763531646934147,
16.3489583333333));
#54837=CARTESIAN_POINT('Ctrl Pts',(31.7633008075689,-1.36198038370242E-14,
16.390625));
#54838=CARTESIAN_POINT('Ctrl Pts',(31.3224756056766,0.763531646934118,16.4322916666666));
#54839=CARTESIAN_POINT('Ctrl Pts',(30.8816504037844,1.52706329386825,16.4739583333333));
#54840=CARTESIAN_POINT('Ctrl Pts',(30.,1.52706329386825,16.515625));
#54841=CARTESIAN_POINT('Ctrl Pts',(29.1183495962155,1.52706329386825,16.5572916666666));
#54842=CARTESIAN_POINT('Ctrl Pts',(28.6775243943233,0.76353164693412,16.5989583333333));
#54843=CARTESIAN_POINT('Ctrl Pts',(28.2366991924311,-1.31894491186926E-14,
16.640625));
#54844=CARTESIAN_POINT('Ctrl Pts',(28.6775243943233,-0.763531646934146,
16.6822916666666));
#54845=CARTESIAN_POINT('Ctrl Pts',(29.1183495962155,-1.52706329386828,16.7239583333333));
#54846=CARTESIAN_POINT('Ctrl Pts',(30.,-1.52706329386828,16.765625));
#54847=CARTESIAN_POINT('Ctrl Pts',(30.8816504037844,-1.52706329386828,16.8072916666666));
#54848=CARTESIAN_POINT('Ctrl Pts',(31.3224756056766,-0.763531646934147,
16.8489583333333));
#54849=CARTESIAN_POINT('Ctrl Pts',(31.7633008075689,-1.36198038370242E-14,
16.890625));
#54850=CARTESIAN_POINT('Ctrl Pts',(31.3224756056766,0.763531646934118,16.9322916666666));
#54851=CARTESIAN_POINT('Ctrl Pts',(30.8816504037844,1.52706329386825,16.9739583333333));
#54852=CARTESIAN_POINT('Ctrl Pts',(30.,1.52706329386825,17.015625));
#54853=CARTESIAN_POINT('Ctrl Pts',(29.1183495962155,1.52706329386825,17.0572916666666));
#54854=CARTESIAN_POINT('Ctrl Pts',(28.6775243943233,0.76353164693412,17.0989583333333));
#54855=CARTESIAN_POINT('Ctrl Pts',(28.2366991924311,-1.31894491186926E-14,
17.140625));
#54856=CARTESIAN_POINT('Ctrl Pts',(28.6775243943233,-0.763531646934146,
17.1822916666666));
#54857=CARTESIAN_POINT('Ctrl Pts',(29.1183495962155,-1.52706329386828,17.2239583333333));
#54858=CARTESIAN_POINT('Ctrl Pts',(30.,-1.52706329386828,17.265625));
#54859=CARTESIAN_POINT('Ctrl Pts',(30.8816504037844,-1.52706329386828,17.3072916666666));
#54860=CARTESIAN_POINT('Ctrl Pts',(31.3224756056766,-0.763531646934147,
17.3489583333333));
#54861=CARTESIAN_POINT('Ctrl Pts',(31.7633008075689,-1.36198038370242E-14,
17.390625));
#54862=CARTESIAN_POINT('Ctrl Pts',(31.3224756056766,0.763531646934118,17.4322916666666));
#54863=CARTESIAN_POINT('Ctrl Pts',(30.8816504037844,1.52706329386825,17.4739583333333));
#54864=CARTESIAN_POINT('Ctrl Pts',(30.,1.52706329386825,17.515625));
#54865=CARTESIAN_POINT('Ctrl Pts',(29.1183495962155,1.52706329386825,17.5572916666666));
#54866=CARTESIAN_POINT('Ctrl Pts',(28.6775243943233,0.76353164693412,17.5989583333333));
#54867=CARTESIAN_POINT('Ctrl Pts',(28.2366991924311,-1.31894491186926E-14,
17.640625));
#54868=CARTESIAN_POINT('Ctrl Pts',(28.6775243943233,-0.763531646934146,
17.6822916666666));
#54869=CARTESIAN_POINT('Ctrl Pts',(29.1183495962155,-1.52706329386828,17.7239583333333));
#54870=CARTESIAN_POINT('Ctrl Pts',(30.,-1.52706329386828,17.765625));
#54871=CARTESIAN_POINT('Ctrl Pts',(30.8816504037844,-1.52706329386828,17.8072916666666));
#54872=CARTESIAN_POINT('Ctrl Pts',(31.3224756056766,-0.763531646934147,
17.8489583333333));
#54873=CARTESIAN_POINT('Ctrl Pts',(31.7633008075689,-1.36198038370242E-14,
17.890625));
#54874=CARTESIAN_POINT('Ctrl Pts',(31.3224756056766,0.763531646934118,17.9322916666666));
#54875=CARTESIAN_POINT('Ctrl Pts',(30.8816504037844,1.52706329386825,17.9739583333333));
#54876=CARTESIAN_POINT('Ctrl Pts',(30.,1.52706329386825,18.015625));
#54877=CARTESIAN_POINT('Ctrl Pts',(29.1183495962155,1.52706329386825,18.0572916666666));
#54878=CARTESIAN_POINT('Ctrl Pts',(28.6775243943233,0.76353164693412,18.0989583333333));
#54879=CARTESIAN_POINT('Ctrl Pts',(28.2366991924311,-1.31894491186926E-14,
18.140625));
#54880=CARTESIAN_POINT('Ctrl Pts',(28.6775243943233,-0.763531646934146,
18.1822916666666));
#54881=CARTESIAN_POINT('Ctrl Pts',(29.1183495962155,-1.52706329386828,18.2239583333333));
#54882=CARTESIAN_POINT('Ctrl Pts',(30.,-1.52706329386828,18.265625));
#54883=CARTESIAN_POINT('Ctrl Pts',(30.8816504037844,-1.52706329386828,18.3072916666666));
#54884=CARTESIAN_POINT('Ctrl Pts',(31.3224756056766,-0.763531646934147,
18.3489583333333));
#54885=CARTESIAN_POINT('Ctrl Pts',(31.7633008075689,-1.36198038370242E-14,
18.390625));
#54886=CARTESIAN_POINT('Ctrl Pts',(31.3224756056766,0.763531646934118,18.4322916666666));
#54887=CARTESIAN_POINT('Ctrl Pts',(30.8816504037844,1.52706329386825,18.4739583333333));
#54888=CARTESIAN_POINT('Ctrl Pts',(30.,1.52706329386825,18.515625));
#54889=CARTESIAN_POINT('Ctrl Pts',(29.1183495962155,1.52706329386825,18.5572916666666));
#54890=CARTESIAN_POINT('Ctrl Pts',(28.6775243943233,0.76353164693412,18.5989583333333));
#54891=CARTESIAN_POINT('Ctrl Pts',(28.2366991924311,-1.31894491186926E-14,
18.640625));
#54892=CARTESIAN_POINT('Ctrl Pts',(28.6775243943233,-0.763531646934146,
18.6822916666666));
#54893=CARTESIAN_POINT('Ctrl Pts',(29.1183495962155,-1.52706329386828,18.7239583333333));
#54894=CARTESIAN_POINT('Ctrl Pts',(30.,-1.52706329386828,18.765625));
#54895=CARTESIAN_POINT('Ctrl Pts',(30.8816504037844,-1.52706329386828,18.8072916666666));
#54896=CARTESIAN_POINT('Ctrl Pts',(31.3224756056766,-0.763531646934147,
18.8489583333333));
#54897=CARTESIAN_POINT('Ctrl Pts',(31.7633008075689,-1.36198038370242E-14,
18.890625));
#54898=CARTESIAN_POINT('Ctrl Pts',(31.3224756056766,0.763531646934118,18.9322916666666));
#54899=CARTESIAN_POINT('Ctrl Pts',(30.8816504037844,1.52706329386825,18.9739583333333));
#54900=CARTESIAN_POINT('Ctrl Pts',(30.,1.52706329386825,19.015625));
#54901=CARTESIAN_POINT('Ctrl Pts',(29.1183495962155,1.52706329386825,19.0572916666666));
#54902=CARTESIAN_POINT('Ctrl Pts',(28.6775243943233,0.76353164693412,19.0989583333333));
#54903=CARTESIAN_POINT('Ctrl Pts',(28.2366991924311,-1.31894491186926E-14,
19.140625));
#54904=CARTESIAN_POINT('Ctrl Pts',(28.6775243943233,-0.763531646934146,
19.1822916666666));
#54905=CARTESIAN_POINT('Ctrl Pts',(29.1183495962155,-1.52706329386828,19.2239583333333));
#54906=CARTESIAN_POINT('Ctrl Pts',(30.,-1.52706329386828,19.265625));
#54907=CARTESIAN_POINT('Ctrl Pts',(30.8816504037844,-1.52706329386828,19.3072916666666));
#54908=CARTESIAN_POINT('Ctrl Pts',(31.3224756056766,-0.763531646934147,
19.3489583333333));
#54909=CARTESIAN_POINT('Ctrl Pts',(31.7633008075689,-1.36198038370242E-14,
19.390625));
#54910=CARTESIAN_POINT('Ctrl Pts',(31.3224756056766,0.763531646934118,19.4322916666666));
#54911=CARTESIAN_POINT('Ctrl Pts',(30.8816504037844,1.52706329386825,19.4739583333333));
#54912=CARTESIAN_POINT('Ctrl Pts',(30.,1.52706329386825,19.515625));
#54913=CARTESIAN_POINT('Ctrl Pts',(29.1183495962155,1.52706329386825,19.5572916666666));
#54914=CARTESIAN_POINT('Ctrl Pts',(28.6775243943233,0.76353164693412,19.5989583333333));
#54915=CARTESIAN_POINT('Ctrl Pts',(28.2366991924311,-1.31894491186926E-14,
19.640625));
#54916=CARTESIAN_POINT('Ctrl Pts',(28.6775243943233,-0.763531646934146,
19.6822916666666));
#54917=CARTESIAN_POINT('Ctrl Pts',(29.1183495962155,-1.52706329386828,19.7239583333333));
#54918=CARTESIAN_POINT('Ctrl Pts',(30.,-1.52706329386828,19.765625));
#54919=CARTESIAN_POINT('Ctrl Pts',(30.8816504037844,-1.52706329386828,19.8072916666666));
#54920=CARTESIAN_POINT('Ctrl Pts',(31.3224756056766,-0.763531646934147,
19.8489583333333));
#54921=CARTESIAN_POINT('Ctrl Pts',(31.7633008075689,-1.36198038370242E-14,
19.890625));
#54922=CARTESIAN_POINT('Ctrl Pts',(31.3224756056766,0.763531646934118,19.9322916666666));
#54923=CARTESIAN_POINT('Ctrl Pts',(30.8816504037844,1.52706329386825,19.9739583333333));
#54924=CARTESIAN_POINT('Ctrl Pts',(30.,1.52706329386825,20.015625));
#54925=CARTESIAN_POINT('Ctrl Pts',(29.1183495962155,1.52706329386825,20.0572916666666));
#54926=CARTESIAN_POINT('Ctrl Pts',(28.6775243943233,0.76353164693412,20.0989583333333));
#54927=CARTESIAN_POINT('Ctrl Pts',(28.2366991924311,-1.31894491186926E-14,
20.140625));
#54928=CARTESIAN_POINT('Ctrl Pts',(28.6775243943233,-0.763531646934146,
20.1822916666666));
#54929=CARTESIAN_POINT('Ctrl Pts',(29.1183495962155,-1.52706329386828,20.2239583333333));
#54930=CARTESIAN_POINT('Ctrl Pts',(30.,-1.52706329386828,20.265625));
#54931=CARTESIAN_POINT('Ctrl Pts',(30.8816504037844,-1.52706329386828,20.3072916666666));
#54932=CARTESIAN_POINT('Ctrl Pts',(31.3224756056766,-0.763531646934147,
20.3489583333333));
#54933=CARTESIAN_POINT('Ctrl Pts',(31.7633008075689,-1.36198038370242E-14,
20.390625));
#54934=CARTESIAN_POINT('Ctrl Pts',(31.3224756056766,0.763531646934118,20.4322916666666));
#54935=CARTESIAN_POINT('Ctrl Pts',(30.8816504037844,1.52706329386825,20.4739583333333));
#54936=CARTESIAN_POINT('Ctrl Pts',(30.,1.52706329386825,20.515625));
#54937=CARTESIAN_POINT('Ctrl Pts',(29.1183495962155,1.52706329386825,20.5572916666666));
#54938=CARTESIAN_POINT('Ctrl Pts',(28.6775243943233,0.76353164693412,20.5989583333333));
#54939=CARTESIAN_POINT('Ctrl Pts',(28.2366991924311,-1.31894491186926E-14,
20.640625));
#54940=CARTESIAN_POINT('Ctrl Pts',(28.6775243943233,-0.763531646934146,
20.6822916666666));
#54941=CARTESIAN_POINT('Ctrl Pts',(29.1183495962155,-1.52706329386828,20.7239583333333));
#54942=CARTESIAN_POINT('Ctrl Pts',(30.,-1.52706329386828,20.765625));
#54943=CARTESIAN_POINT('Ctrl Pts',(30.8816504037844,-1.52706329386828,20.8072916666666));
#54944=CARTESIAN_POINT('Ctrl Pts',(31.3224756056766,-0.763531646934147,
20.8489583333333));
#54945=CARTESIAN_POINT('Ctrl Pts',(31.7633008075689,-1.36198038370242E-14,
20.890625));
#54946=CARTESIAN_POINT('Ctrl Pts',(31.3224756056766,0.763531646934118,20.9322916666666));
#54947=CARTESIAN_POINT('Ctrl Pts',(30.8816504037844,1.52706329386825,20.9739583333333));
#54948=CARTESIAN_POINT('Ctrl Pts',(30.,1.52706329386825,21.015625));
#54949=CARTESIAN_POINT('Ctrl Pts',(29.1183495962155,1.52706329386825,21.0572916666666));
#54950=CARTESIAN_POINT('Ctrl Pts',(28.6775243943233,0.76353164693412,21.0989583333333));
#54951=CARTESIAN_POINT('Ctrl Pts',(28.2366991924311,-1.31894491186926E-14,
21.140625));
#54952=CARTESIAN_POINT('Ctrl Pts',(28.6775243943233,-0.763531646934146,
21.1822916666666));
#54953=CARTESIAN_POINT('Ctrl Pts',(29.1183495962155,-1.52706329386828,21.2239583333333));
#54954=CARTESIAN_POINT('Ctrl Pts',(30.,-1.52706329386828,21.265625));
#54955=CARTESIAN_POINT('Ctrl Pts',(30.8816504037844,-1.52706329386828,21.3072916666666));
#54956=CARTESIAN_POINT('Ctrl Pts',(31.3224756056766,-0.763531646934147,
21.3489583333333));
#54957=CARTESIAN_POINT('Ctrl Pts',(31.7633008075689,-1.36198038370242E-14,
21.390625));
#54958=CARTESIAN_POINT('Ctrl Pts',(31.3224756056766,0.763531646934118,21.4322916666666));
#54959=CARTESIAN_POINT('Ctrl Pts',(30.8816504037844,1.52706329386825,21.4739583333333));
#54960=CARTESIAN_POINT('Ctrl Pts',(30.,1.52706329386825,21.515625));
#54961=CARTESIAN_POINT('Ctrl Pts',(29.1183495962155,1.52706329386825,21.5572916666666));
#54962=CARTESIAN_POINT('Ctrl Pts',(28.6775243943233,0.76353164693412,21.5989583333333));
#54963=CARTESIAN_POINT('Ctrl Pts',(28.2366991924311,-1.31894491186926E-14,
21.640625));
#54964=CARTESIAN_POINT('Ctrl Pts',(28.6775243943233,-0.763531646934146,
21.6822916666666));
#54965=CARTESIAN_POINT('Ctrl Pts',(29.1183495962155,-1.52706329386828,21.7239583333333));
#54966=CARTESIAN_POINT('Ctrl Pts',(30.,-1.52706329386828,21.765625));
#54967=CARTESIAN_POINT('Ctrl Pts',(30.8816504037844,-1.52706329386828,21.8072916666666));
#54968=CARTESIAN_POINT('Ctrl Pts',(31.3224756056766,-0.763531646934147,
21.8489583333333));
#54969=CARTESIAN_POINT('Ctrl Pts',(31.7633008075689,-1.36198038370242E-14,
21.890625));
#54970=CARTESIAN_POINT('Ctrl Pts',(31.3224756056766,0.763531646934118,21.9322916666666));
#54971=CARTESIAN_POINT('Ctrl Pts',(30.8816504037844,1.52706329386825,21.9739583333333));
#54972=CARTESIAN_POINT('Ctrl Pts',(30.,1.52706329386825,22.015625));
#54973=CARTESIAN_POINT('Ctrl Pts',(29.1183495962155,1.52706329386825,22.0572916666666));
#54974=CARTESIAN_POINT('Ctrl Pts',(28.6775243943233,0.76353164693412,22.0989583333333));
#54975=CARTESIAN_POINT('Ctrl Pts',(28.2366991924311,-1.31894491186926E-14,
22.140625));
#54976=CARTESIAN_POINT('Ctrl Pts',(28.6775243943233,-0.763531646934146,
22.1822916666666));
#54977=CARTESIAN_POINT('Ctrl Pts',(29.1183495962155,-1.52706329386828,22.2239583333333));
#54978=CARTESIAN_POINT('Ctrl Pts',(30.,-1.52706329386828,22.265625));
#54979=CARTESIAN_POINT('Ctrl Pts',(30.8816504037844,-1.52706329386828,22.3072916666666));
#54980=CARTESIAN_POINT('Ctrl Pts',(31.3224756056766,-0.763531646934147,
22.3489583333333));
#54981=CARTESIAN_POINT('Ctrl Pts',(31.7633008075689,-1.36198038370242E-14,
22.390625));
#54982=CARTESIAN_POINT('Ctrl Pts',(31.3224756056766,0.763531646934118,22.4322916666666));
#54983=CARTESIAN_POINT('Ctrl Pts',(30.8816504037844,1.52706329386825,22.4739583333333));
#54984=CARTESIAN_POINT('Ctrl Pts',(30.,1.52706329386825,22.515625));
#54985=CARTESIAN_POINT('Ctrl Pts',(29.1183495962155,1.52706329386825,22.5572916666666));
#54986=CARTESIAN_POINT('Ctrl Pts',(28.6775243943233,0.76353164693412,22.5989583333333));
#54987=CARTESIAN_POINT('Ctrl Pts',(28.2366991924311,-1.31894491186926E-14,
22.640625));
#54988=CARTESIAN_POINT('Ctrl Pts',(28.6775243943233,-0.763531646934146,
22.6822916666666));
#54989=CARTESIAN_POINT('Ctrl Pts',(29.1183495962155,-1.52706329386828,22.7239583333333));
#54990=CARTESIAN_POINT('Ctrl Pts',(30.,-1.52706329386828,22.765625));
#54991=CARTESIAN_POINT('Ctrl Pts',(30.8816504037844,-1.52706329386828,22.8072916666666));
#54992=CARTESIAN_POINT('Ctrl Pts',(31.3224756056766,-0.763531646934147,
22.8489583333333));
#54993=CARTESIAN_POINT('Ctrl Pts',(31.7633008075689,-1.36198038370242E-14,
22.890625));
#54994=CARTESIAN_POINT('Ctrl Pts',(31.3224756056766,0.763531646934118,22.9322916666666));
#54995=CARTESIAN_POINT('Ctrl Pts',(30.8816504037844,1.52706329386825,22.9739583333333));
#54996=CARTESIAN_POINT('Ctrl Pts',(30.,1.52706329386825,23.015625));
#54997=CARTESIAN_POINT('Ctrl Pts',(29.1183495962155,1.52706329386825,23.0572916666666));
#54998=CARTESIAN_POINT('Ctrl Pts',(28.6775243943233,0.76353164693412,23.0989583333333));
#54999=CARTESIAN_POINT('Ctrl Pts',(28.2366991924311,-1.31894491186926E-14,
23.140625));
#55000=CARTESIAN_POINT('Ctrl Pts',(28.6775243943233,-0.763531646934146,
23.1822916666666));
#55001=CARTESIAN_POINT('Ctrl Pts',(29.1183495962155,-1.52706329386828,23.2239583333333));
#55002=CARTESIAN_POINT('Ctrl Pts',(30.,-1.52706329386828,23.265625));
#55003=CARTESIAN_POINT('Ctrl Pts',(30.8816504037844,-1.52706329386828,23.3072916666666));
#55004=CARTESIAN_POINT('Ctrl Pts',(31.3224756056766,-0.763531646934147,
23.3489583333333));
#55005=CARTESIAN_POINT('Ctrl Pts',(31.7633008075689,-1.36198038370242E-14,
23.390625));
#55006=CARTESIAN_POINT('Ctrl Pts',(31.3224756056766,0.763531646934118,23.4322916666666));
#55007=CARTESIAN_POINT('Ctrl Pts',(30.8816504037844,1.52706329386825,23.4739583333333));
#55008=CARTESIAN_POINT('Ctrl Pts',(30.,1.52706329386825,23.515625));
#55009=CARTESIAN_POINT('Ctrl Pts',(29.1183495962155,1.52706329386825,23.5572916666666));
#55010=CARTESIAN_POINT('Ctrl Pts',(28.6775243943233,0.76353164693412,23.5989583333333));
#55011=CARTESIAN_POINT('Ctrl Pts',(28.2366991924311,-1.31894491186926E-14,
23.640625));
#55012=CARTESIAN_POINT('Ctrl Pts',(28.6775243943233,-0.763531646934146,
23.6822916666666));
#55013=CARTESIAN_POINT('Ctrl Pts',(29.1183495962155,-1.52706329386828,23.7239583333333));
#55014=CARTESIAN_POINT('Ctrl Pts',(30.,-1.52706329386828,23.765625));
#55015=CARTESIAN_POINT('Ctrl Pts',(30.8816504037844,-1.52706329386828,23.8072916666666));
#55016=CARTESIAN_POINT('Ctrl Pts',(31.3224756056766,-0.763531646934147,
23.8489583333333));
#55017=CARTESIAN_POINT('Ctrl Pts',(31.7633008075689,-1.36198038370242E-14,
23.890625));
#55018=CARTESIAN_POINT('Ctrl Pts',(31.3224756056766,0.763531646934118,23.9322916666666));
#55019=CARTESIAN_POINT('Ctrl Pts',(30.8816504037844,1.52706329386825,23.9739583333333));
#55020=CARTESIAN_POINT('Ctrl Pts',(30.,1.52706329386825,24.015625));
#55021=CARTESIAN_POINT('Ctrl Pts',(29.1183495962155,1.52706329386825,24.0572916666666));
#55022=CARTESIAN_POINT('Ctrl Pts',(28.6775243943233,0.76353164693412,24.0989583333333));
#55023=CARTESIAN_POINT('Ctrl Pts',(28.2366991924311,-1.31894491186926E-14,
24.140625));
#55024=CARTESIAN_POINT('Ctrl Pts',(28.6775243943233,-0.763531646934146,
24.1822916666666));
#55025=CARTESIAN_POINT('Ctrl Pts',(29.1183495962155,-1.52706329386828,24.2239583333333));
#55026=CARTESIAN_POINT('Ctrl Pts',(30.,-1.52706329386828,24.265625));
#55027=CARTESIAN_POINT('Ctrl Pts',(30.8816504037844,-1.52706329386828,24.3072916666666));
#55028=CARTESIAN_POINT('Ctrl Pts',(31.3224756056766,-0.763531646934147,
24.3489583333333));
#55029=CARTESIAN_POINT('Ctrl Pts',(31.7633008075689,-1.36198038370242E-14,
24.390625));
#55030=CARTESIAN_POINT('Ctrl Pts',(31.3224756056766,0.763531646934118,24.4322916666666));
#55031=CARTESIAN_POINT('Ctrl Pts',(30.8816504037844,1.52706329386825,24.4739583333333));
#55032=CARTESIAN_POINT('Ctrl Pts',(30.,1.52706329386825,24.515625));
#55033=CARTESIAN_POINT('Ctrl Pts',(29.1183495962155,1.52706329386825,24.5572916666666));
#55034=CARTESIAN_POINT('Ctrl Pts',(28.6775243943233,0.76353164693412,24.5989583333333));
#55035=CARTESIAN_POINT('Ctrl Pts',(28.2366991924311,-1.31894491186926E-14,
24.640625));
#55036=CARTESIAN_POINT('Ctrl Pts',(28.6775243943233,-0.763531646934146,
24.6822916666666));
#55037=CARTESIAN_POINT('Ctrl Pts',(29.1183495962155,-1.52706329386828,24.7239583333333));
#55038=CARTESIAN_POINT('Ctrl Pts',(30.,-1.52706329386828,24.765625));
#55039=CARTESIAN_POINT('Ctrl Pts',(30.8816504037844,-1.52706329386828,24.8072916666666));
#55040=CARTESIAN_POINT('Ctrl Pts',(31.3224756056766,-0.763531646934147,
24.8489583333333));
#55041=CARTESIAN_POINT('Ctrl Pts',(31.7633008075689,-1.36198038370242E-14,
24.890625));
#55042=CARTESIAN_POINT('Ctrl Pts',(31.3224756056766,0.763531646934118,24.9322916666666));
#55043=CARTESIAN_POINT('Ctrl Pts',(30.8816504037844,1.52706329386825,24.9739583333333));
#55044=CARTESIAN_POINT('Ctrl Pts',(30.,1.52706329386825,25.015625));
#55045=CARTESIAN_POINT('Ctrl Pts',(29.1183495962155,1.52706329386825,25.0572916666666));
#55046=CARTESIAN_POINT('Ctrl Pts',(28.6775243943233,0.76353164693412,25.0989583333333));
#55047=CARTESIAN_POINT('Ctrl Pts',(28.2366991924311,-1.31894491186926E-14,
25.140625));
#55048=CARTESIAN_POINT('Ctrl Pts',(28.6775243943233,-0.763531646934146,
25.1822916666666));
#55049=CARTESIAN_POINT('Ctrl Pts',(29.1183495962155,-1.52706329386828,25.2239583333333));
#55050=CARTESIAN_POINT('Ctrl Pts',(30.,-1.52706329386828,25.265625));
#55051=CARTESIAN_POINT('Ctrl Pts',(30.8816504037844,-1.52706329386828,25.3072916666666));
#55052=CARTESIAN_POINT('Ctrl Pts',(31.3224756056766,-0.763531646934147,
25.3489583333333));
#55053=CARTESIAN_POINT('Ctrl Pts',(31.7633008075689,-1.36198038370242E-14,
25.390625));
#55054=CARTESIAN_POINT('Ctrl Pts',(31.3224756056766,0.763531646934118,25.4322916666666));
#55055=CARTESIAN_POINT('Ctrl Pts',(30.8816504037844,1.52706329386825,25.4739583333333));
#55056=CARTESIAN_POINT('Ctrl Pts',(30.,1.52706329386825,25.515625));
#55057=CARTESIAN_POINT('Ctrl Pts',(29.1183495962155,1.52706329386825,25.5572916666666));
#55058=CARTESIAN_POINT('Ctrl Pts',(28.6775243943233,0.76353164693412,25.5989583333333));
#55059=CARTESIAN_POINT('Ctrl Pts',(28.2366991924311,-1.31894491186926E-14,
25.640625));
#55060=CARTESIAN_POINT('Ctrl Pts',(28.6775243943233,-0.763531646934146,
25.6822916666666));
#55061=CARTESIAN_POINT('Ctrl Pts',(29.1183495962155,-1.52706329386828,25.7239583333333));
#55062=CARTESIAN_POINT('Ctrl Pts',(30.,-1.52706329386828,25.765625));
#55063=CARTESIAN_POINT('Ctrl Pts',(30.8816504037844,-1.52706329386828,25.8072916666666));
#55064=CARTESIAN_POINT('Ctrl Pts',(31.3224756056766,-0.763531646934147,
25.8489583333333));
#55065=CARTESIAN_POINT('Ctrl Pts',(31.7633008075689,-1.36198038370242E-14,
25.890625));
#55066=CARTESIAN_POINT('Ctrl Pts',(31.3224756056766,0.763531646934118,25.9322916666666));
#55067=CARTESIAN_POINT('Ctrl Pts',(30.8816504037844,1.52706329386825,25.9739583333333));
#55068=CARTESIAN_POINT('Ctrl Pts',(30.,1.52706329386825,26.015625));
#55069=CARTESIAN_POINT('Ctrl Pts',(29.1183495962155,1.52706329386825,26.0572916666666));
#55070=CARTESIAN_POINT('Ctrl Pts',(28.6775243943233,0.76353164693412,26.0989583333333));
#55071=CARTESIAN_POINT('Ctrl Pts',(28.2366991924311,-1.31894491186926E-14,
26.140625));
#55072=CARTESIAN_POINT('Ctrl Pts',(28.6775243943233,-0.763531646934146,
26.1822916666666));
#55073=CARTESIAN_POINT('Ctrl Pts',(29.1183495962155,-1.52706329386828,26.2239583333333));
#55074=CARTESIAN_POINT('Ctrl Pts',(30.,-1.52706329386828,26.265625));
#55075=CARTESIAN_POINT('Ctrl Pts',(30.8816504037844,-1.52706329386828,26.3072916666666));
#55076=CARTESIAN_POINT('Ctrl Pts',(31.3224756056766,-0.763531646934147,
26.3489583333333));
#55077=CARTESIAN_POINT('Ctrl Pts',(31.7633008075689,-1.36198038370242E-14,
26.390625));
#55078=CARTESIAN_POINT('Ctrl Pts',(31.3224756056766,0.763531646934118,26.4322916666666));
#55079=CARTESIAN_POINT('Ctrl Pts',(30.8816504037844,1.52706329386825,26.4739583333333));
#55080=CARTESIAN_POINT('Ctrl Pts',(30.,1.52706329386825,26.515625));
#55081=CARTESIAN_POINT('Ctrl Pts',(29.1183495962155,1.52706329386825,26.5572916666666));
#55082=CARTESIAN_POINT('Ctrl Pts',(28.6775243943233,0.76353164693412,26.5989583333333));
#55083=CARTESIAN_POINT('Ctrl Pts',(28.2366991924311,-1.31894491186926E-14,
26.640625));
#55084=CARTESIAN_POINT('Ctrl Pts',(28.6775243943233,-0.763531646934146,
26.6822916666666));
#55085=CARTESIAN_POINT('Ctrl Pts',(29.1183495962155,-1.52706329386828,26.7239583333333));
#55086=CARTESIAN_POINT('Ctrl Pts',(30.,-1.52706329386828,26.765625));
#55087=CARTESIAN_POINT('Ctrl Pts',(30.8816504037844,-1.52706329386828,26.8072916666666));
#55088=CARTESIAN_POINT('Ctrl Pts',(31.3224756056766,-0.763531646934147,
26.8489583333333));
#55089=CARTESIAN_POINT('Ctrl Pts',(31.7633008075689,-1.36198038370242E-14,
26.890625));
#55090=CARTESIAN_POINT('Ctrl Pts',(31.3224756056766,0.763531646934118,26.9322916666666));
#55091=CARTESIAN_POINT('Ctrl Pts',(30.8816504037844,1.52706329386825,26.9739583333333));
#55092=CARTESIAN_POINT('Ctrl Pts',(30.,1.52706329386825,27.015625));
#55093=CARTESIAN_POINT('Ctrl Pts',(29.1183495962155,1.52706329386825,27.0572916666666));
#55094=CARTESIAN_POINT('Ctrl Pts',(28.6775243943233,0.76353164693412,27.0989583333333));
#55095=CARTESIAN_POINT('Ctrl Pts',(28.2366991924311,-1.31894491186926E-14,
27.140625));
#55096=CARTESIAN_POINT('Ctrl Pts',(28.6775243943233,-0.763531646934146,
27.1822916666666));
#55097=CARTESIAN_POINT('Ctrl Pts',(29.1183495962155,-1.52706329386828,27.2239583333333));
#55098=CARTESIAN_POINT('Ctrl Pts',(30.,-1.52706329386828,27.265625));
#55099=CARTESIAN_POINT('Ctrl Pts',(30.8816504037844,-1.52706329386828,27.3072916666666));
#55100=CARTESIAN_POINT('Ctrl Pts',(31.3224756056766,-0.763531646934147,
27.3489583333333));
#55101=CARTESIAN_POINT('Ctrl Pts',(31.7633008075689,-1.36198038370242E-14,
27.390625));
#55102=CARTESIAN_POINT('Ctrl Pts',(31.3224756056766,0.763531646934118,27.4322916666666));
#55103=CARTESIAN_POINT('Ctrl Pts',(30.8816504037844,1.52706329386825,27.4739583333333));
#55104=CARTESIAN_POINT('Ctrl Pts',(30.,1.52706329386825,27.515625));
#55105=CARTESIAN_POINT('Ctrl Pts',(29.1183495962155,1.52706329386825,27.5572916666666));
#55106=CARTESIAN_POINT('Ctrl Pts',(28.6775243943233,0.76353164693412,27.5989583333333));
#55107=CARTESIAN_POINT('Ctrl Pts',(28.2366991924311,-1.31894491186926E-14,
27.640625));
#55108=CARTESIAN_POINT('Ctrl Pts',(28.6775243943233,-0.763531646934146,
27.6822916666666));
#55109=CARTESIAN_POINT('Ctrl Pts',(29.1183495962155,-1.52706329386828,27.7239583333333));
#55110=CARTESIAN_POINT('Ctrl Pts',(30.,-1.52706329386828,27.765625));
#55111=CARTESIAN_POINT('Ctrl Pts',(30.8816504037844,-1.52706329386828,27.8072916666666));
#55112=CARTESIAN_POINT('Ctrl Pts',(31.3224756056766,-0.763531646934147,
27.8489583333333));
#55113=CARTESIAN_POINT('Ctrl Pts',(31.7633008075689,-1.36198038370242E-14,
27.890625));
#55114=CARTESIAN_POINT('Ctrl Pts',(31.3224756056766,0.763531646934118,27.9322916666666));
#55115=CARTESIAN_POINT('Ctrl Pts',(30.8816504037844,1.52706329386825,27.9739583333333));
#55116=CARTESIAN_POINT('Ctrl Pts',(30.,1.52706329386825,28.015625));
#55117=CARTESIAN_POINT('Ctrl Pts',(29.1183495962155,1.52706329386825,28.0572916666666));
#55118=CARTESIAN_POINT('Ctrl Pts',(28.6775243943233,0.76353164693412,28.0989583333333));
#55119=CARTESIAN_POINT('Ctrl Pts',(28.2366991924311,-1.31894491186926E-14,
28.140625));
#55120=CARTESIAN_POINT('Ctrl Pts',(28.6775243943233,-0.763531646934146,
28.1822916666666));
#55121=CARTESIAN_POINT('Ctrl Pts',(29.1183495962155,-1.52706329386828,28.2239583333333));
#55122=CARTESIAN_POINT('Ctrl Pts',(30.,-1.52706329386828,28.265625));
#55123=CARTESIAN_POINT('Ctrl Pts',(30.8816504037844,-1.52706329386828,28.3072916666666));
#55124=CARTESIAN_POINT('Ctrl Pts',(31.3224756056766,-0.763531646934147,
28.3489583333333));
#55125=CARTESIAN_POINT('Ctrl Pts',(31.7633008075689,-1.36198038370242E-14,
28.390625));
#55126=CARTESIAN_POINT('Ctrl Pts',(31.3224756056766,0.763531646934118,28.4322916666666));
#55127=CARTESIAN_POINT('Ctrl Pts',(30.8816504037844,1.52706329386825,28.4739583333333));
#55128=CARTESIAN_POINT('Ctrl Pts',(30.,1.52706329386825,28.515625));
#55129=CARTESIAN_POINT('Ctrl Pts',(29.1183495962155,1.52706329386825,28.5572916666666));
#55130=CARTESIAN_POINT('Ctrl Pts',(28.6775243943233,0.76353164693412,28.5989583333333));
#55131=CARTESIAN_POINT('Ctrl Pts',(28.2366991924311,-1.31894491186926E-14,
28.640625));
#55132=CARTESIAN_POINT('Ctrl Pts',(28.6775243943233,-0.763531646934146,
28.6822916666666));
#55133=CARTESIAN_POINT('Ctrl Pts',(29.1183495962155,-1.52706329386828,28.7239583333333));
#55134=CARTESIAN_POINT('Ctrl Pts',(30.,-1.52706329386828,28.765625));
#55135=CARTESIAN_POINT('Ctrl Pts',(30.8816504037844,-1.52706329386828,28.8072916666666));
#55136=CARTESIAN_POINT('Ctrl Pts',(31.3224756056766,-0.763531646934147,
28.8489583333333));
#55137=CARTESIAN_POINT('Ctrl Pts',(31.7633008075689,-1.36198038370242E-14,
28.890625));
#55138=CARTESIAN_POINT('Ctrl Pts',(31.3224756056766,0.763531646934118,28.9322916666666));
#55139=CARTESIAN_POINT('Ctrl Pts',(30.8816504037844,1.52706329386825,28.9739583333333));
#55140=CARTESIAN_POINT('Ctrl Pts',(30.,1.52706329386825,29.015625));
#55141=CARTESIAN_POINT('Ctrl Pts',(29.1183495962155,1.52706329386825,29.0572916666666));
#55142=CARTESIAN_POINT('Ctrl Pts',(28.6775243943233,0.76353164693412,29.0989583333333));
#55143=CARTESIAN_POINT('Ctrl Pts',(28.2366991924311,-1.31894491186926E-14,
29.140625));
#55144=CARTESIAN_POINT('Ctrl Pts',(28.6775243943233,-0.763531646934146,
29.1822916666666));
#55145=CARTESIAN_POINT('Ctrl Pts',(29.1183495962155,-1.52706329386828,29.2239583333333));
#55146=CARTESIAN_POINT('Ctrl Pts',(30.,-1.52706329386828,29.265625));
#55147=CARTESIAN_POINT('Ctrl Pts',(30.8816504037844,-1.52706329386828,29.3072916666666));
#55148=CARTESIAN_POINT('Ctrl Pts',(31.3224756056766,-0.763531646934147,
29.3489583333333));
#55149=CARTESIAN_POINT('Ctrl Pts',(31.7633008075689,-1.36198038370242E-14,
29.390625));
#55150=CARTESIAN_POINT('Ctrl Pts',(31.3224756056766,0.763531646934118,29.4322916666666));
#55151=CARTESIAN_POINT('Ctrl Pts',(30.8816504037844,1.52706329386825,29.4739583333333));
#55152=CARTESIAN_POINT('Ctrl Pts',(30.,1.52706329386825,29.515625));
#55153=CARTESIAN_POINT('Ctrl Pts',(29.1183495962155,1.52706329386825,29.5572916666666));
#55154=CARTESIAN_POINT('Ctrl Pts',(28.6775243943233,0.76353164693412,29.5989583333333));
#55155=CARTESIAN_POINT('Ctrl Pts',(28.2366991924311,-1.31894491186926E-14,
29.640625));
#55156=CARTESIAN_POINT('Ctrl Pts',(28.6775243943233,-0.763531646934146,
29.6822916666666));
#55157=CARTESIAN_POINT('Ctrl Pts',(29.1183495962155,-1.52706329386828,29.7239583333333));
#55158=CARTESIAN_POINT('Ctrl Pts',(30.,-1.52706329386828,29.765625));
#55159=CARTESIAN_POINT('Ctrl Pts',(30.8816504037844,-1.52706329386828,29.8072916666666));
#55160=CARTESIAN_POINT('Ctrl Pts',(31.3224756056766,-0.763531646934147,
29.8489583333333));
#55161=CARTESIAN_POINT('Ctrl Pts',(31.7633008075689,-1.36198038370242E-14,
29.890625));
#55162=CARTESIAN_POINT('Ctrl Pts',(31.3224756056766,0.763531646934118,29.9322916666666));
#55163=CARTESIAN_POINT('Ctrl Pts',(30.8816504037844,1.52706329386825,29.9739583333333));
#55164=CARTESIAN_POINT('Ctrl Pts',(30.,1.52706329386825,30.015625));
#55165=CARTESIAN_POINT('Ctrl Pts',(29.1183495962155,1.52706329386825,30.0572916666666));
#55166=CARTESIAN_POINT('Ctrl Pts',(28.6775243943233,0.76353164693412,30.0989583333333));
#55167=CARTESIAN_POINT('Ctrl Pts',(28.2366991924311,-1.31894491186926E-14,
30.140625));
#55168=CARTESIAN_POINT('Ctrl Pts',(28.6775243943233,-0.763531646934146,
30.1822916666666));
#55169=CARTESIAN_POINT('Ctrl Pts',(29.1183495962155,-1.52706329386828,30.2239583333333));
#55170=CARTESIAN_POINT('Ctrl Pts',(30.,-1.52706329386828,30.265625));
#55171=CARTESIAN_POINT('Ctrl Pts',(30.8816504037844,-1.52706329386828,30.3072916666666));
#55172=CARTESIAN_POINT('Ctrl Pts',(31.3224756056766,-0.763531646934147,
30.3489583333333));
#55173=CARTESIAN_POINT('Ctrl Pts',(31.7633008075689,-1.36198038370242E-14,
30.390625));
#55174=CARTESIAN_POINT('Ctrl Pts',(31.3224756056766,0.763531646934118,30.4322916666666));
#55175=CARTESIAN_POINT('Ctrl Pts',(30.8816504037844,1.52706329386825,30.4739583333333));
#55176=CARTESIAN_POINT('Ctrl Pts',(30.,1.52706329386825,30.515625));
#55177=CARTESIAN_POINT('Ctrl Pts',(29.1183495962155,1.52706329386825,30.5572916666666));
#55178=CARTESIAN_POINT('Ctrl Pts',(28.6775243943233,0.76353164693412,30.5989583333333));
#55179=CARTESIAN_POINT('Ctrl Pts',(28.2366991924311,-1.31894491186926E-14,
30.640625));
#55180=CARTESIAN_POINT('Ctrl Pts',(28.6775243943233,-0.763531646934146,
30.6822916666666));
#55181=CARTESIAN_POINT('Ctrl Pts',(29.1183495962155,-1.52706329386828,30.7239583333333));
#55182=CARTESIAN_POINT('Ctrl Pts',(30.,-1.52706329386828,30.765625));
#55183=CARTESIAN_POINT('Ctrl Pts',(30.8816504037844,-1.52706329386828,30.8072916666666));
#55184=CARTESIAN_POINT('Ctrl Pts',(31.3224756056766,-0.763531646934147,
30.8489583333333));
#55185=CARTESIAN_POINT('Ctrl Pts',(31.7633008075689,-1.36198038370242E-14,
30.890625));
#55186=CARTESIAN_POINT('Ctrl Pts',(31.3224756056766,0.763531646934118,30.9322916666666));
#55187=CARTESIAN_POINT('Ctrl Pts',(30.8816504037844,1.52706329386825,30.9739583333333));
#55188=CARTESIAN_POINT('Ctrl Pts',(30.,1.52706329386825,31.015625));
#55189=CARTESIAN_POINT('Ctrl Pts',(29.1183495962155,1.52706329386825,31.0572916666666));
#55190=CARTESIAN_POINT('Ctrl Pts',(28.6775243943233,0.76353164693412,31.0989583333333));
#55191=CARTESIAN_POINT('Ctrl Pts',(28.2366991924311,-1.31894491186926E-14,
31.140625));
#55192=CARTESIAN_POINT('Ctrl Pts',(28.6775243943233,-0.763531646934146,
31.1822916666666));
#55193=CARTESIAN_POINT('Ctrl Pts',(29.1183495962155,-1.52706329386828,31.2239583333333));
#55194=CARTESIAN_POINT('Ctrl Pts',(30.,-1.52706329386828,31.265625));
#55195=CARTESIAN_POINT('Ctrl Pts',(30.8816504037844,-1.52706329386828,31.3072916666666));
#55196=CARTESIAN_POINT('Ctrl Pts',(31.3224756056766,-0.763531646934147,
31.3489583333333));
#55197=CARTESIAN_POINT('Ctrl Pts',(31.7633008075689,-1.36198038370242E-14,
31.390625));
#55198=CARTESIAN_POINT('Ctrl Pts',(31.3224756056766,0.763531646934118,31.4322916666666));
#55199=CARTESIAN_POINT('Ctrl Pts',(30.8816504037844,1.52706329386825,31.4739583333333));
#55200=CARTESIAN_POINT('Ctrl Pts',(30.,1.52706329386825,31.515625));
#55201=CARTESIAN_POINT('Ctrl Pts',(30.,1.17523507120987,15.8124968809397));
#55202=CARTESIAN_POINT('Ctrl Pts',(29.3214777152758,1.17523507120987,15.8541635476064));
#55203=CARTESIAN_POINT('Ctrl Pts',(28.9822165729138,0.587617535604928,15.895830214273));
#55204=CARTESIAN_POINT('Ctrl Pts',(28.6429554305518,-1.32141489532166E-14,
15.9374968809397));
#55205=CARTESIAN_POINT('Ctrl Pts',(28.9822165729138,-0.587617535604954,
15.9791635476064));
#55206=CARTESIAN_POINT('Ctrl Pts',(29.3214777152758,-1.17523507120989,16.020830214273));
#55207=CARTESIAN_POINT('Ctrl Pts',(30.,-1.17523507120989,16.0624968809397));
#55208=CARTESIAN_POINT('Ctrl Pts',(30.6785222847241,-1.17523507120989,16.1041635476064));
#55209=CARTESIAN_POINT('Ctrl Pts',(31.0177834270861,-0.587617535604955,
16.145830214273));
#55210=CARTESIAN_POINT('Ctrl Pts',(31.3570445694482,-1.35453519623354E-14,
16.1874968809397));
#55211=CARTESIAN_POINT('Ctrl Pts',(31.0177834270861,0.587617535604927,16.2291635476064));
#55212=CARTESIAN_POINT('Ctrl Pts',(30.6785222847241,1.17523507120987,16.270830214273));
#55213=CARTESIAN_POINT('Ctrl Pts',(30.,1.17523507120987,16.3124968809397));
#55214=CARTESIAN_POINT('Ctrl Pts',(29.3214777152758,1.17523507120987,16.3541635476064));
#55215=CARTESIAN_POINT('Ctrl Pts',(28.9822165729138,0.587617535604928,16.395830214273));
#55216=CARTESIAN_POINT('Ctrl Pts',(28.6429554305518,-1.32141489532166E-14,
16.4374968809397));
#55217=CARTESIAN_POINT('Ctrl Pts',(28.9822165729138,-0.587617535604954,
16.4791635476064));
#55218=CARTESIAN_POINT('Ctrl Pts',(29.3214777152758,-1.17523507120989,16.520830214273));
#55219=CARTESIAN_POINT('Ctrl Pts',(30.,-1.17523507120989,16.5624968809397));
#55220=CARTESIAN_POINT('Ctrl Pts',(30.6785222847241,-1.17523507120989,16.6041635476064));
#55221=CARTESIAN_POINT('Ctrl Pts',(31.0177834270861,-0.587617535604955,
16.645830214273));
#55222=CARTESIAN_POINT('Ctrl Pts',(31.3570445694482,-1.35453519623354E-14,
16.6874968809397));
#55223=CARTESIAN_POINT('Ctrl Pts',(31.0177834270861,0.587617535604927,16.7291635476064));
#55224=CARTESIAN_POINT('Ctrl Pts',(30.6785222847241,1.17523507120987,16.770830214273));
#55225=CARTESIAN_POINT('Ctrl Pts',(30.,1.17523507120987,16.8124968809397));
#55226=CARTESIAN_POINT('Ctrl Pts',(29.3214777152758,1.17523507120987,16.8541635476064));
#55227=CARTESIAN_POINT('Ctrl Pts',(28.9822165729138,0.587617535604928,16.895830214273));
#55228=CARTESIAN_POINT('Ctrl Pts',(28.6429554305518,-1.32141489532166E-14,
16.9374968809397));
#55229=CARTESIAN_POINT('Ctrl Pts',(28.9822165729138,-0.587617535604954,
16.9791635476064));
#55230=CARTESIAN_POINT('Ctrl Pts',(29.3214777152758,-1.17523507120989,17.020830214273));
#55231=CARTESIAN_POINT('Ctrl Pts',(30.,-1.17523507120989,17.0624968809397));
#55232=CARTESIAN_POINT('Ctrl Pts',(30.6785222847241,-1.17523507120989,17.1041635476064));
#55233=CARTESIAN_POINT('Ctrl Pts',(31.0177834270861,-0.587617535604955,
17.145830214273));
#55234=CARTESIAN_POINT('Ctrl Pts',(31.3570445694482,-1.35453519623354E-14,
17.1874968809397));
#55235=CARTESIAN_POINT('Ctrl Pts',(31.0177834270861,0.587617535604927,17.2291635476064));
#55236=CARTESIAN_POINT('Ctrl Pts',(30.6785222847241,1.17523507120987,17.270830214273));
#55237=CARTESIAN_POINT('Ctrl Pts',(30.,1.17523507120987,17.3124968809397));
#55238=CARTESIAN_POINT('Ctrl Pts',(29.3214777152758,1.17523507120987,17.3541635476064));
#55239=CARTESIAN_POINT('Ctrl Pts',(28.9822165729138,0.587617535604928,17.395830214273));
#55240=CARTESIAN_POINT('Ctrl Pts',(28.6429554305518,-1.32141489532166E-14,
17.4374968809397));
#55241=CARTESIAN_POINT('Ctrl Pts',(28.9822165729138,-0.587617535604954,
17.4791635476064));
#55242=CARTESIAN_POINT('Ctrl Pts',(29.3214777152758,-1.17523507120989,17.520830214273));
#55243=CARTESIAN_POINT('Ctrl Pts',(30.,-1.17523507120989,17.5624968809397));
#55244=CARTESIAN_POINT('Ctrl Pts',(30.6785222847241,-1.17523507120989,17.6041635476064));
#55245=CARTESIAN_POINT('Ctrl Pts',(31.0177834270861,-0.587617535604955,
17.645830214273));
#55246=CARTESIAN_POINT('Ctrl Pts',(31.3570445694482,-1.35453519623354E-14,
17.6874968809397));
#55247=CARTESIAN_POINT('Ctrl Pts',(31.0177834270861,0.587617535604927,17.7291635476064));
#55248=CARTESIAN_POINT('Ctrl Pts',(30.6785222847241,1.17523507120987,17.770830214273));
#55249=CARTESIAN_POINT('Ctrl Pts',(30.,1.17523507120987,17.8124968809397));
#55250=CARTESIAN_POINT('Ctrl Pts',(29.3214777152758,1.17523507120987,17.8541635476064));
#55251=CARTESIAN_POINT('Ctrl Pts',(28.9822165729138,0.587617535604928,17.895830214273));
#55252=CARTESIAN_POINT('Ctrl Pts',(28.6429554305518,-1.32141489532166E-14,
17.9374968809397));
#55253=CARTESIAN_POINT('Ctrl Pts',(28.9822165729138,-0.587617535604954,
17.9791635476064));
#55254=CARTESIAN_POINT('Ctrl Pts',(29.3214777152758,-1.17523507120989,18.020830214273));
#55255=CARTESIAN_POINT('Ctrl Pts',(30.,-1.17523507120989,18.0624968809397));
#55256=CARTESIAN_POINT('Ctrl Pts',(30.6785222847241,-1.17523507120989,18.1041635476064));
#55257=CARTESIAN_POINT('Ctrl Pts',(31.0177834270861,-0.587617535604955,
18.145830214273));
#55258=CARTESIAN_POINT('Ctrl Pts',(31.3570445694482,-1.35453519623354E-14,
18.1874968809397));
#55259=CARTESIAN_POINT('Ctrl Pts',(31.0177834270861,0.587617535604927,18.2291635476064));
#55260=CARTESIAN_POINT('Ctrl Pts',(30.6785222847241,1.17523507120987,18.270830214273));
#55261=CARTESIAN_POINT('Ctrl Pts',(30.,1.17523507120987,18.3124968809397));
#55262=CARTESIAN_POINT('Ctrl Pts',(29.3214777152758,1.17523507120987,18.3541635476064));
#55263=CARTESIAN_POINT('Ctrl Pts',(28.9822165729138,0.587617535604928,18.395830214273));
#55264=CARTESIAN_POINT('Ctrl Pts',(28.6429554305518,-1.32141489532166E-14,
18.4374968809397));
#55265=CARTESIAN_POINT('Ctrl Pts',(28.9822165729138,-0.587617535604954,
18.4791635476064));
#55266=CARTESIAN_POINT('Ctrl Pts',(29.3214777152758,-1.17523507120989,18.520830214273));
#55267=CARTESIAN_POINT('Ctrl Pts',(30.,-1.17523507120989,18.5624968809397));
#55268=CARTESIAN_POINT('Ctrl Pts',(30.6785222847241,-1.17523507120989,18.6041635476064));
#55269=CARTESIAN_POINT('Ctrl Pts',(31.0177834270861,-0.587617535604955,
18.645830214273));
#55270=CARTESIAN_POINT('Ctrl Pts',(31.3570445694482,-1.35453519623354E-14,
18.6874968809397));
#55271=CARTESIAN_POINT('Ctrl Pts',(31.0177834270861,0.587617535604927,18.7291635476064));
#55272=CARTESIAN_POINT('Ctrl Pts',(30.6785222847241,1.17523507120987,18.770830214273));
#55273=CARTESIAN_POINT('Ctrl Pts',(30.,1.17523507120987,18.8124968809397));
#55274=CARTESIAN_POINT('Ctrl Pts',(29.3214777152758,1.17523507120987,18.8541635476064));
#55275=CARTESIAN_POINT('Ctrl Pts',(28.9822165729138,0.587617535604928,18.895830214273));
#55276=CARTESIAN_POINT('Ctrl Pts',(28.6429554305518,-1.32141489532166E-14,
18.9374968809397));
#55277=CARTESIAN_POINT('Ctrl Pts',(28.9822165729138,-0.587617535604954,
18.9791635476064));
#55278=CARTESIAN_POINT('Ctrl Pts',(29.3214777152758,-1.17523507120989,19.020830214273));
#55279=CARTESIAN_POINT('Ctrl Pts',(30.,-1.17523507120989,19.0624968809397));
#55280=CARTESIAN_POINT('Ctrl Pts',(30.6785222847241,-1.17523507120989,19.1041635476064));
#55281=CARTESIAN_POINT('Ctrl Pts',(31.0177834270861,-0.587617535604955,
19.145830214273));
#55282=CARTESIAN_POINT('Ctrl Pts',(31.3570445694482,-1.35453519623354E-14,
19.1874968809397));
#55283=CARTESIAN_POINT('Ctrl Pts',(31.0177834270861,0.587617535604927,19.2291635476064));
#55284=CARTESIAN_POINT('Ctrl Pts',(30.6785222847241,1.17523507120987,19.270830214273));
#55285=CARTESIAN_POINT('Ctrl Pts',(30.,1.17523507120987,19.3124968809397));
#55286=CARTESIAN_POINT('Ctrl Pts',(29.3214777152758,1.17523507120987,19.3541635476064));
#55287=CARTESIAN_POINT('Ctrl Pts',(28.9822165729138,0.587617535604928,19.395830214273));
#55288=CARTESIAN_POINT('Ctrl Pts',(28.6429554305518,-1.32141489532166E-14,
19.4374968809397));
#55289=CARTESIAN_POINT('Ctrl Pts',(28.9822165729138,-0.587617535604954,
19.4791635476064));
#55290=CARTESIAN_POINT('Ctrl Pts',(29.3214777152758,-1.17523507120989,19.520830214273));
#55291=CARTESIAN_POINT('Ctrl Pts',(30.,-1.17523507120989,19.5624968809397));
#55292=CARTESIAN_POINT('Ctrl Pts',(30.6785222847241,-1.17523507120989,19.6041635476064));
#55293=CARTESIAN_POINT('Ctrl Pts',(31.0177834270861,-0.587617535604955,
19.645830214273));
#55294=CARTESIAN_POINT('Ctrl Pts',(31.3570445694482,-1.35453519623354E-14,
19.6874968809397));
#55295=CARTESIAN_POINT('Ctrl Pts',(31.0177834270861,0.587617535604927,19.7291635476064));
#55296=CARTESIAN_POINT('Ctrl Pts',(30.6785222847241,1.17523507120987,19.770830214273));
#55297=CARTESIAN_POINT('Ctrl Pts',(30.,1.17523507120987,19.8124968809397));
#55298=CARTESIAN_POINT('Ctrl Pts',(29.3214777152758,1.17523507120987,19.8541635476064));
#55299=CARTESIAN_POINT('Ctrl Pts',(28.9822165729138,0.587617535604928,19.895830214273));
#55300=CARTESIAN_POINT('Ctrl Pts',(28.6429554305518,-1.32141489532166E-14,
19.9374968809397));
#55301=CARTESIAN_POINT('Ctrl Pts',(28.9822165729138,-0.587617535604954,
19.9791635476064));
#55302=CARTESIAN_POINT('Ctrl Pts',(29.3214777152758,-1.17523507120989,20.020830214273));
#55303=CARTESIAN_POINT('Ctrl Pts',(30.,-1.17523507120989,20.0624968809397));
#55304=CARTESIAN_POINT('Ctrl Pts',(30.6785222847241,-1.17523507120989,20.1041635476064));
#55305=CARTESIAN_POINT('Ctrl Pts',(31.0177834270861,-0.587617535604955,
20.145830214273));
#55306=CARTESIAN_POINT('Ctrl Pts',(31.3570445694482,-1.35453519623354E-14,
20.1874968809397));
#55307=CARTESIAN_POINT('Ctrl Pts',(31.0177834270861,0.587617535604927,20.2291635476064));
#55308=CARTESIAN_POINT('Ctrl Pts',(30.6785222847241,1.17523507120987,20.270830214273));
#55309=CARTESIAN_POINT('Ctrl Pts',(30.,1.17523507120987,20.3124968809397));
#55310=CARTESIAN_POINT('Ctrl Pts',(29.3214777152758,1.17523507120987,20.3541635476064));
#55311=CARTESIAN_POINT('Ctrl Pts',(28.9822165729138,0.587617535604928,20.395830214273));
#55312=CARTESIAN_POINT('Ctrl Pts',(28.6429554305518,-1.32141489532166E-14,
20.4374968809397));
#55313=CARTESIAN_POINT('Ctrl Pts',(28.9822165729138,-0.587617535604954,
20.4791635476064));
#55314=CARTESIAN_POINT('Ctrl Pts',(29.3214777152758,-1.17523507120989,20.520830214273));
#55315=CARTESIAN_POINT('Ctrl Pts',(30.,-1.17523507120989,20.5624968809397));
#55316=CARTESIAN_POINT('Ctrl Pts',(30.6785222847241,-1.17523507120989,20.6041635476064));
#55317=CARTESIAN_POINT('Ctrl Pts',(31.0177834270861,-0.587617535604955,
20.645830214273));
#55318=CARTESIAN_POINT('Ctrl Pts',(31.3570445694482,-1.35453519623354E-14,
20.6874968809397));
#55319=CARTESIAN_POINT('Ctrl Pts',(31.0177834270861,0.587617535604927,20.7291635476064));
#55320=CARTESIAN_POINT('Ctrl Pts',(30.6785222847241,1.17523507120987,20.770830214273));
#55321=CARTESIAN_POINT('Ctrl Pts',(30.,1.17523507120987,20.8124968809397));
#55322=CARTESIAN_POINT('Ctrl Pts',(29.3214777152758,1.17523507120987,20.8541635476064));
#55323=CARTESIAN_POINT('Ctrl Pts',(28.9822165729138,0.587617535604928,20.895830214273));
#55324=CARTESIAN_POINT('Ctrl Pts',(28.6429554305518,-1.32141489532166E-14,
20.9374968809397));
#55325=CARTESIAN_POINT('Ctrl Pts',(28.9822165729138,-0.587617535604954,
20.9791635476064));
#55326=CARTESIAN_POINT('Ctrl Pts',(29.3214777152758,-1.17523507120989,21.020830214273));
#55327=CARTESIAN_POINT('Ctrl Pts',(30.,-1.17523507120989,21.0624968809397));
#55328=CARTESIAN_POINT('Ctrl Pts',(30.6785222847241,-1.17523507120989,21.1041635476064));
#55329=CARTESIAN_POINT('Ctrl Pts',(31.0177834270861,-0.587617535604955,
21.145830214273));
#55330=CARTESIAN_POINT('Ctrl Pts',(31.3570445694482,-1.35453519623354E-14,
21.1874968809397));
#55331=CARTESIAN_POINT('Ctrl Pts',(31.0177834270861,0.587617535604927,21.2291635476064));
#55332=CARTESIAN_POINT('Ctrl Pts',(30.6785222847241,1.17523507120987,21.270830214273));
#55333=CARTESIAN_POINT('Ctrl Pts',(30.,1.17523507120987,21.3124968809397));
#55334=CARTESIAN_POINT('Ctrl Pts',(29.3214777152758,1.17523507120987,21.3541635476064));
#55335=CARTESIAN_POINT('Ctrl Pts',(28.9822165729138,0.587617535604928,21.395830214273));
#55336=CARTESIAN_POINT('Ctrl Pts',(28.6429554305518,-1.32141489532166E-14,
21.4374968809397));
#55337=CARTESIAN_POINT('Ctrl Pts',(28.9822165729138,-0.587617535604954,
21.4791635476064));
#55338=CARTESIAN_POINT('Ctrl Pts',(29.3214777152758,-1.17523507120989,21.520830214273));
#55339=CARTESIAN_POINT('Ctrl Pts',(30.,-1.17523507120989,21.5624968809397));
#55340=CARTESIAN_POINT('Ctrl Pts',(30.6785222847241,-1.17523507120989,21.6041635476064));
#55341=CARTESIAN_POINT('Ctrl Pts',(31.0177834270861,-0.587617535604955,
21.645830214273));
#55342=CARTESIAN_POINT('Ctrl Pts',(31.3570445694482,-1.35453519623354E-14,
21.6874968809397));
#55343=CARTESIAN_POINT('Ctrl Pts',(31.0177834270861,0.587617535604927,21.7291635476064));
#55344=CARTESIAN_POINT('Ctrl Pts',(30.6785222847241,1.17523507120987,21.770830214273));
#55345=CARTESIAN_POINT('Ctrl Pts',(30.,1.17523507120987,21.8124968809397));
#55346=CARTESIAN_POINT('Ctrl Pts',(29.3214777152758,1.17523507120987,21.8541635476064));
#55347=CARTESIAN_POINT('Ctrl Pts',(28.9822165729138,0.587617535604928,21.895830214273));
#55348=CARTESIAN_POINT('Ctrl Pts',(28.6429554305518,-1.32141489532166E-14,
21.9374968809397));
#55349=CARTESIAN_POINT('Ctrl Pts',(28.9822165729138,-0.587617535604954,
21.9791635476064));
#55350=CARTESIAN_POINT('Ctrl Pts',(29.3214777152758,-1.17523507120989,22.020830214273));
#55351=CARTESIAN_POINT('Ctrl Pts',(30.,-1.17523507120989,22.0624968809397));
#55352=CARTESIAN_POINT('Ctrl Pts',(30.6785222847241,-1.17523507120989,22.1041635476064));
#55353=CARTESIAN_POINT('Ctrl Pts',(31.0177834270861,-0.587617535604955,
22.145830214273));
#55354=CARTESIAN_POINT('Ctrl Pts',(31.3570445694482,-1.35453519623354E-14,
22.1874968809397));
#55355=CARTESIAN_POINT('Ctrl Pts',(31.0177834270861,0.587617535604927,22.2291635476064));
#55356=CARTESIAN_POINT('Ctrl Pts',(30.6785222847241,1.17523507120987,22.270830214273));
#55357=CARTESIAN_POINT('Ctrl Pts',(30.,1.17523507120987,22.3124968809397));
#55358=CARTESIAN_POINT('Ctrl Pts',(29.3214777152758,1.17523507120987,22.3541635476064));
#55359=CARTESIAN_POINT('Ctrl Pts',(28.9822165729138,0.587617535604928,22.395830214273));
#55360=CARTESIAN_POINT('Ctrl Pts',(28.6429554305518,-1.32141489532166E-14,
22.4374968809397));
#55361=CARTESIAN_POINT('Ctrl Pts',(28.9822165729138,-0.587617535604954,
22.4791635476064));
#55362=CARTESIAN_POINT('Ctrl Pts',(29.3214777152758,-1.17523507120989,22.520830214273));
#55363=CARTESIAN_POINT('Ctrl Pts',(30.,-1.17523507120989,22.5624968809397));
#55364=CARTESIAN_POINT('Ctrl Pts',(30.6785222847241,-1.17523507120989,22.6041635476064));
#55365=CARTESIAN_POINT('Ctrl Pts',(31.0177834270861,-0.587617535604955,
22.645830214273));
#55366=CARTESIAN_POINT('Ctrl Pts',(31.3570445694482,-1.35453519623354E-14,
22.6874968809397));
#55367=CARTESIAN_POINT('Ctrl Pts',(31.0177834270861,0.587617535604927,22.7291635476064));
#55368=CARTESIAN_POINT('Ctrl Pts',(30.6785222847241,1.17523507120987,22.770830214273));
#55369=CARTESIAN_POINT('Ctrl Pts',(30.,1.17523507120987,22.8124968809397));
#55370=CARTESIAN_POINT('Ctrl Pts',(29.3214777152758,1.17523507120987,22.8541635476064));
#55371=CARTESIAN_POINT('Ctrl Pts',(28.9822165729138,0.587617535604928,22.895830214273));
#55372=CARTESIAN_POINT('Ctrl Pts',(28.6429554305518,-1.32141489532166E-14,
22.9374968809397));
#55373=CARTESIAN_POINT('Ctrl Pts',(28.9822165729138,-0.587617535604954,
22.9791635476064));
#55374=CARTESIAN_POINT('Ctrl Pts',(29.3214777152758,-1.17523507120989,23.020830214273));
#55375=CARTESIAN_POINT('Ctrl Pts',(30.,-1.17523507120989,23.0624968809397));
#55376=CARTESIAN_POINT('Ctrl Pts',(30.6785222847241,-1.17523507120989,23.1041635476064));
#55377=CARTESIAN_POINT('Ctrl Pts',(31.0177834270861,-0.587617535604955,
23.145830214273));
#55378=CARTESIAN_POINT('Ctrl Pts',(31.3570445694482,-1.35453519623354E-14,
23.1874968809397));
#55379=CARTESIAN_POINT('Ctrl Pts',(31.0177834270861,0.587617535604927,23.2291635476064));
#55380=CARTESIAN_POINT('Ctrl Pts',(30.6785222847241,1.17523507120987,23.270830214273));
#55381=CARTESIAN_POINT('Ctrl Pts',(30.,1.17523507120987,23.3124968809397));
#55382=CARTESIAN_POINT('Ctrl Pts',(29.3214777152758,1.17523507120987,23.3541635476064));
#55383=CARTESIAN_POINT('Ctrl Pts',(28.9822165729138,0.587617535604928,23.395830214273));
#55384=CARTESIAN_POINT('Ctrl Pts',(28.6429554305518,-1.32141489532166E-14,
23.4374968809397));
#55385=CARTESIAN_POINT('Ctrl Pts',(28.9822165729138,-0.587617535604954,
23.4791635476064));
#55386=CARTESIAN_POINT('Ctrl Pts',(29.3214777152758,-1.17523507120989,23.520830214273));
#55387=CARTESIAN_POINT('Ctrl Pts',(30.,-1.17523507120989,23.5624968809397));
#55388=CARTESIAN_POINT('Ctrl Pts',(30.6785222847241,-1.17523507120989,23.6041635476064));
#55389=CARTESIAN_POINT('Ctrl Pts',(31.0177834270861,-0.587617535604955,
23.645830214273));
#55390=CARTESIAN_POINT('Ctrl Pts',(31.3570445694482,-1.35453519623354E-14,
23.6874968809397));
#55391=CARTESIAN_POINT('Ctrl Pts',(31.0177834270861,0.587617535604927,23.7291635476064));
#55392=CARTESIAN_POINT('Ctrl Pts',(30.6785222847241,1.17523507120987,23.770830214273));
#55393=CARTESIAN_POINT('Ctrl Pts',(30.,1.17523507120987,23.8124968809397));
#55394=CARTESIAN_POINT('Ctrl Pts',(29.3214777152758,1.17523507120987,23.8541635476064));
#55395=CARTESIAN_POINT('Ctrl Pts',(28.9822165729138,0.587617535604928,23.895830214273));
#55396=CARTESIAN_POINT('Ctrl Pts',(28.6429554305518,-1.32141489532166E-14,
23.9374968809397));
#55397=CARTESIAN_POINT('Ctrl Pts',(28.9822165729138,-0.587617535604954,
23.9791635476064));
#55398=CARTESIAN_POINT('Ctrl Pts',(29.3214777152758,-1.17523507120989,24.020830214273));
#55399=CARTESIAN_POINT('Ctrl Pts',(30.,-1.17523507120989,24.0624968809397));
#55400=CARTESIAN_POINT('Ctrl Pts',(30.6785222847241,-1.17523507120989,24.1041635476064));
#55401=CARTESIAN_POINT('Ctrl Pts',(31.0177834270861,-0.587617535604955,
24.145830214273));
#55402=CARTESIAN_POINT('Ctrl Pts',(31.3570445694482,-1.35453519623354E-14,
24.1874968809397));
#55403=CARTESIAN_POINT('Ctrl Pts',(31.0177834270861,0.587617535604927,24.2291635476064));
#55404=CARTESIAN_POINT('Ctrl Pts',(30.6785222847241,1.17523507120987,24.270830214273));
#55405=CARTESIAN_POINT('Ctrl Pts',(30.,1.17523507120987,24.3124968809397));
#55406=CARTESIAN_POINT('Ctrl Pts',(29.3214777152758,1.17523507120987,24.3541635476064));
#55407=CARTESIAN_POINT('Ctrl Pts',(28.9822165729138,0.587617535604928,24.395830214273));
#55408=CARTESIAN_POINT('Ctrl Pts',(28.6429554305518,-1.32141489532166E-14,
24.4374968809397));
#55409=CARTESIAN_POINT('Ctrl Pts',(28.9822165729138,-0.587617535604954,
24.4791635476064));
#55410=CARTESIAN_POINT('Ctrl Pts',(29.3214777152758,-1.17523507120989,24.520830214273));
#55411=CARTESIAN_POINT('Ctrl Pts',(30.,-1.17523507120989,24.5624968809397));
#55412=CARTESIAN_POINT('Ctrl Pts',(30.6785222847241,-1.17523507120989,24.6041635476064));
#55413=CARTESIAN_POINT('Ctrl Pts',(31.0177834270861,-0.587617535604955,
24.645830214273));
#55414=CARTESIAN_POINT('Ctrl Pts',(31.3570445694482,-1.35453519623354E-14,
24.6874968809397));
#55415=CARTESIAN_POINT('Ctrl Pts',(31.0177834270861,0.587617535604927,24.7291635476064));
#55416=CARTESIAN_POINT('Ctrl Pts',(30.6785222847241,1.17523507120987,24.770830214273));
#55417=CARTESIAN_POINT('Ctrl Pts',(30.,1.17523507120987,24.8124968809397));
#55418=CARTESIAN_POINT('Ctrl Pts',(29.3214777152758,1.17523507120987,24.8541635476064));
#55419=CARTESIAN_POINT('Ctrl Pts',(28.9822165729138,0.587617535604928,24.895830214273));
#55420=CARTESIAN_POINT('Ctrl Pts',(28.6429554305518,-1.32141489532166E-14,
24.9374968809397));
#55421=CARTESIAN_POINT('Ctrl Pts',(28.9822165729138,-0.587617535604954,
24.9791635476064));
#55422=CARTESIAN_POINT('Ctrl Pts',(29.3214777152758,-1.17523507120989,25.020830214273));
#55423=CARTESIAN_POINT('Ctrl Pts',(30.,-1.17523507120989,25.0624968809397));
#55424=CARTESIAN_POINT('Ctrl Pts',(30.6785222847241,-1.17523507120989,25.1041635476064));
#55425=CARTESIAN_POINT('Ctrl Pts',(31.0177834270861,-0.587617535604955,
25.145830214273));
#55426=CARTESIAN_POINT('Ctrl Pts',(31.3570445694482,-1.35453519623354E-14,
25.1874968809397));
#55427=CARTESIAN_POINT('Ctrl Pts',(31.0177834270861,0.587617535604927,25.2291635476064));
#55428=CARTESIAN_POINT('Ctrl Pts',(30.6785222847241,1.17523507120987,25.270830214273));
#55429=CARTESIAN_POINT('Ctrl Pts',(30.,1.17523507120987,25.3124968809397));
#55430=CARTESIAN_POINT('Ctrl Pts',(29.3214777152758,1.17523507120987,25.3541635476064));
#55431=CARTESIAN_POINT('Ctrl Pts',(28.9822165729138,0.587617535604928,25.395830214273));
#55432=CARTESIAN_POINT('Ctrl Pts',(28.6429554305518,-1.32141489532166E-14,
25.4374968809397));
#55433=CARTESIAN_POINT('Ctrl Pts',(28.9822165729138,-0.587617535604954,
25.4791635476064));
#55434=CARTESIAN_POINT('Ctrl Pts',(29.3214777152758,-1.17523507120989,25.520830214273));
#55435=CARTESIAN_POINT('Ctrl Pts',(30.,-1.17523507120989,25.5624968809397));
#55436=CARTESIAN_POINT('Ctrl Pts',(30.6785222847241,-1.17523507120989,25.6041635476064));
#55437=CARTESIAN_POINT('Ctrl Pts',(31.0177834270861,-0.587617535604955,
25.645830214273));
#55438=CARTESIAN_POINT('Ctrl Pts',(31.3570445694482,-1.35453519623354E-14,
25.6874968809397));
#55439=CARTESIAN_POINT('Ctrl Pts',(31.0177834270861,0.587617535604927,25.7291635476064));
#55440=CARTESIAN_POINT('Ctrl Pts',(30.6785222847241,1.17523507120987,25.770830214273));
#55441=CARTESIAN_POINT('Ctrl Pts',(30.,1.17523507120987,25.8124968809397));
#55442=CARTESIAN_POINT('Ctrl Pts',(29.3214777152758,1.17523507120987,25.8541635476064));
#55443=CARTESIAN_POINT('Ctrl Pts',(28.9822165729138,0.587617535604928,25.895830214273));
#55444=CARTESIAN_POINT('Ctrl Pts',(28.6429554305518,-1.32141489532166E-14,
25.9374968809397));
#55445=CARTESIAN_POINT('Ctrl Pts',(28.9822165729138,-0.587617535604954,
25.9791635476064));
#55446=CARTESIAN_POINT('Ctrl Pts',(29.3214777152758,-1.17523507120989,26.020830214273));
#55447=CARTESIAN_POINT('Ctrl Pts',(30.,-1.17523507120989,26.0624968809397));
#55448=CARTESIAN_POINT('Ctrl Pts',(30.6785222847241,-1.17523507120989,26.1041635476064));
#55449=CARTESIAN_POINT('Ctrl Pts',(31.0177834270861,-0.587617535604955,
26.145830214273));
#55450=CARTESIAN_POINT('Ctrl Pts',(31.3570445694482,-1.35453519623354E-14,
26.1874968809397));
#55451=CARTESIAN_POINT('Ctrl Pts',(31.0177834270861,0.587617535604927,26.2291635476064));
#55452=CARTESIAN_POINT('Ctrl Pts',(30.6785222847241,1.17523507120987,26.270830214273));
#55453=CARTESIAN_POINT('Ctrl Pts',(30.,1.17523507120987,26.3124968809397));
#55454=CARTESIAN_POINT('Ctrl Pts',(29.3214777152758,1.17523507120987,26.3541635476064));
#55455=CARTESIAN_POINT('Ctrl Pts',(28.9822165729138,0.587617535604928,26.395830214273));
#55456=CARTESIAN_POINT('Ctrl Pts',(28.6429554305518,-1.32141489532166E-14,
26.4374968809397));
#55457=CARTESIAN_POINT('Ctrl Pts',(28.9822165729138,-0.587617535604954,
26.4791635476064));
#55458=CARTESIAN_POINT('Ctrl Pts',(29.3214777152758,-1.17523507120989,26.520830214273));
#55459=CARTESIAN_POINT('Ctrl Pts',(30.,-1.17523507120989,26.5624968809397));
#55460=CARTESIAN_POINT('Ctrl Pts',(30.6785222847241,-1.17523507120989,26.6041635476064));
#55461=CARTESIAN_POINT('Ctrl Pts',(31.0177834270861,-0.587617535604955,
26.645830214273));
#55462=CARTESIAN_POINT('Ctrl Pts',(31.3570445694482,-1.35453519623354E-14,
26.6874968809397));
#55463=CARTESIAN_POINT('Ctrl Pts',(31.0177834270861,0.587617535604927,26.7291635476064));
#55464=CARTESIAN_POINT('Ctrl Pts',(30.6785222847241,1.17523507120987,26.770830214273));
#55465=CARTESIAN_POINT('Ctrl Pts',(30.,1.17523507120987,26.8124968809397));
#55466=CARTESIAN_POINT('Ctrl Pts',(29.3214777152758,1.17523507120987,26.8541635476064));
#55467=CARTESIAN_POINT('Ctrl Pts',(28.9822165729138,0.587617535604928,26.895830214273));
#55468=CARTESIAN_POINT('Ctrl Pts',(28.6429554305518,-1.32141489532166E-14,
26.9374968809397));
#55469=CARTESIAN_POINT('Ctrl Pts',(28.9822165729138,-0.587617535604954,
26.9791635476064));
#55470=CARTESIAN_POINT('Ctrl Pts',(29.3214777152758,-1.17523507120989,27.020830214273));
#55471=CARTESIAN_POINT('Ctrl Pts',(30.,-1.17523507120989,27.0624968809397));
#55472=CARTESIAN_POINT('Ctrl Pts',(30.6785222847241,-1.17523507120989,27.1041635476064));
#55473=CARTESIAN_POINT('Ctrl Pts',(31.0177834270861,-0.587617535604955,
27.145830214273));
#55474=CARTESIAN_POINT('Ctrl Pts',(31.3570445694482,-1.35453519623354E-14,
27.1874968809397));
#55475=CARTESIAN_POINT('Ctrl Pts',(31.0177834270861,0.587617535604927,27.2291635476064));
#55476=CARTESIAN_POINT('Ctrl Pts',(30.6785222847241,1.17523507120987,27.270830214273));
#55477=CARTESIAN_POINT('Ctrl Pts',(30.,1.17523507120987,27.3124968809397));
#55478=CARTESIAN_POINT('Ctrl Pts',(29.3214777152758,1.17523507120987,27.3541635476064));
#55479=CARTESIAN_POINT('Ctrl Pts',(28.9822165729138,0.587617535604928,27.395830214273));
#55480=CARTESIAN_POINT('Ctrl Pts',(28.6429554305518,-1.32141489532166E-14,
27.4374968809397));
#55481=CARTESIAN_POINT('Ctrl Pts',(28.9822165729138,-0.587617535604954,
27.4791635476064));
#55482=CARTESIAN_POINT('Ctrl Pts',(29.3214777152758,-1.17523507120989,27.520830214273));
#55483=CARTESIAN_POINT('Ctrl Pts',(30.,-1.17523507120989,27.5624968809397));
#55484=CARTESIAN_POINT('Ctrl Pts',(30.6785222847241,-1.17523507120989,27.6041635476064));
#55485=CARTESIAN_POINT('Ctrl Pts',(31.0177834270861,-0.587617535604955,
27.645830214273));
#55486=CARTESIAN_POINT('Ctrl Pts',(31.3570445694482,-1.35453519623354E-14,
27.6874968809397));
#55487=CARTESIAN_POINT('Ctrl Pts',(31.0177834270861,0.587617535604927,27.7291635476064));
#55488=CARTESIAN_POINT('Ctrl Pts',(30.6785222847241,1.17523507120987,27.770830214273));
#55489=CARTESIAN_POINT('Ctrl Pts',(30.,1.17523507120987,27.8124968809397));
#55490=CARTESIAN_POINT('Ctrl Pts',(29.3214777152758,1.17523507120987,27.8541635476064));
#55491=CARTESIAN_POINT('Ctrl Pts',(28.9822165729138,0.587617535604928,27.895830214273));
#55492=CARTESIAN_POINT('Ctrl Pts',(28.6429554305518,-1.32141489532166E-14,
27.9374968809397));
#55493=CARTESIAN_POINT('Ctrl Pts',(28.9822165729138,-0.587617535604954,
27.9791635476064));
#55494=CARTESIAN_POINT('Ctrl Pts',(29.3214777152758,-1.17523507120989,28.020830214273));
#55495=CARTESIAN_POINT('Ctrl Pts',(30.,-1.17523507120989,28.0624968809397));
#55496=CARTESIAN_POINT('Ctrl Pts',(30.6785222847241,-1.17523507120989,28.1041635476064));
#55497=CARTESIAN_POINT('Ctrl Pts',(31.0177834270861,-0.587617535604955,
28.145830214273));
#55498=CARTESIAN_POINT('Ctrl Pts',(31.3570445694482,-1.35453519623354E-14,
28.1874968809397));
#55499=CARTESIAN_POINT('Ctrl Pts',(31.0177834270861,0.587617535604927,28.2291635476064));
#55500=CARTESIAN_POINT('Ctrl Pts',(30.6785222847241,1.17523507120987,28.270830214273));
#55501=CARTESIAN_POINT('Ctrl Pts',(30.,1.17523507120987,28.3124968809397));
#55502=CARTESIAN_POINT('Ctrl Pts',(29.3214777152758,1.17523507120987,28.3541635476064));
#55503=CARTESIAN_POINT('Ctrl Pts',(28.9822165729138,0.587617535604928,28.395830214273));
#55504=CARTESIAN_POINT('Ctrl Pts',(28.6429554305518,-1.32141489532166E-14,
28.4374968809397));
#55505=CARTESIAN_POINT('Ctrl Pts',(28.9822165729138,-0.587617535604954,
28.4791635476064));
#55506=CARTESIAN_POINT('Ctrl Pts',(29.3214777152758,-1.17523507120989,28.520830214273));
#55507=CARTESIAN_POINT('Ctrl Pts',(30.,-1.17523507120989,28.5624968809397));
#55508=CARTESIAN_POINT('Ctrl Pts',(30.6785222847241,-1.17523507120989,28.6041635476064));
#55509=CARTESIAN_POINT('Ctrl Pts',(31.0177834270861,-0.587617535604955,
28.645830214273));
#55510=CARTESIAN_POINT('Ctrl Pts',(31.3570445694482,-1.35453519623354E-14,
28.6874968809397));
#55511=CARTESIAN_POINT('Ctrl Pts',(31.0177834270861,0.587617535604927,28.7291635476064));
#55512=CARTESIAN_POINT('Ctrl Pts',(30.6785222847241,1.17523507120987,28.770830214273));
#55513=CARTESIAN_POINT('Ctrl Pts',(30.,1.17523507120987,28.8124968809397));
#55514=CARTESIAN_POINT('Ctrl Pts',(29.3214777152758,1.17523507120987,28.8541635476064));
#55515=CARTESIAN_POINT('Ctrl Pts',(28.9822165729138,0.587617535604928,28.895830214273));
#55516=CARTESIAN_POINT('Ctrl Pts',(28.6429554305518,-1.32141489532166E-14,
28.9374968809397));
#55517=CARTESIAN_POINT('Ctrl Pts',(28.9822165729138,-0.587617535604954,
28.9791635476064));
#55518=CARTESIAN_POINT('Ctrl Pts',(29.3214777152758,-1.17523507120989,29.020830214273));
#55519=CARTESIAN_POINT('Ctrl Pts',(30.,-1.17523507120989,29.0624968809397));
#55520=CARTESIAN_POINT('Ctrl Pts',(30.6785222847241,-1.17523507120989,29.1041635476064));
#55521=CARTESIAN_POINT('Ctrl Pts',(31.0177834270861,-0.587617535604955,
29.145830214273));
#55522=CARTESIAN_POINT('Ctrl Pts',(31.3570445694482,-1.35453519623354E-14,
29.1874968809397));
#55523=CARTESIAN_POINT('Ctrl Pts',(31.0177834270861,0.587617535604927,29.2291635476064));
#55524=CARTESIAN_POINT('Ctrl Pts',(30.6785222847241,1.17523507120987,29.270830214273));
#55525=CARTESIAN_POINT('Ctrl Pts',(30.,1.17523507120987,29.3124968809397));
#55526=CARTESIAN_POINT('Ctrl Pts',(29.3214777152758,1.17523507120987,29.3541635476064));
#55527=CARTESIAN_POINT('Ctrl Pts',(28.9822165729138,0.587617535604928,29.395830214273));
#55528=CARTESIAN_POINT('Ctrl Pts',(28.6429554305518,-1.32141489532166E-14,
29.4374968809397));
#55529=CARTESIAN_POINT('Ctrl Pts',(28.9822165729138,-0.587617535604954,
29.4791635476064));
#55530=CARTESIAN_POINT('Ctrl Pts',(29.3214777152758,-1.17523507120989,29.520830214273));
#55531=CARTESIAN_POINT('Ctrl Pts',(30.,-1.17523507120989,29.5624968809397));
#55532=CARTESIAN_POINT('Ctrl Pts',(30.6785222847241,-1.17523507120989,29.6041635476064));
#55533=CARTESIAN_POINT('Ctrl Pts',(31.0177834270861,-0.587617535604955,
29.645830214273));
#55534=CARTESIAN_POINT('Ctrl Pts',(31.3570445694482,-1.35453519623354E-14,
29.6874968809397));
#55535=CARTESIAN_POINT('Ctrl Pts',(31.0177834270861,0.587617535604927,29.7291635476064));
#55536=CARTESIAN_POINT('Ctrl Pts',(30.6785222847241,1.17523507120987,29.770830214273));
#55537=CARTESIAN_POINT('Ctrl Pts',(30.,1.17523507120987,29.8124968809397));
#55538=CARTESIAN_POINT('Ctrl Pts',(29.3214777152758,1.17523507120987,29.8541635476064));
#55539=CARTESIAN_POINT('Ctrl Pts',(28.9822165729138,0.587617535604928,29.895830214273));
#55540=CARTESIAN_POINT('Ctrl Pts',(28.6429554305518,-1.32141489532166E-14,
29.9374968809397));
#55541=CARTESIAN_POINT('Ctrl Pts',(28.9822165729138,-0.587617535604954,
29.9791635476064));
#55542=CARTESIAN_POINT('Ctrl Pts',(29.3214777152758,-1.17523507120989,30.020830214273));
#55543=CARTESIAN_POINT('Ctrl Pts',(30.,-1.17523507120989,30.0624968809397));
#55544=CARTESIAN_POINT('Ctrl Pts',(30.6785222847241,-1.17523507120989,30.1041635476064));
#55545=CARTESIAN_POINT('Ctrl Pts',(31.0177834270861,-0.587617535604955,
30.145830214273));
#55546=CARTESIAN_POINT('Ctrl Pts',(31.3570445694482,-1.35453519623354E-14,
30.1874968809397));
#55547=CARTESIAN_POINT('Ctrl Pts',(31.0177834270861,0.587617535604927,30.2291635476064));
#55548=CARTESIAN_POINT('Ctrl Pts',(30.6785222847241,1.17523507120987,30.270830214273));
#55549=CARTESIAN_POINT('Ctrl Pts',(30.,1.17523507120987,30.3124968809397));
#55550=CARTESIAN_POINT('Ctrl Pts',(29.3214777152758,1.17523507120987,30.3541635476064));
#55551=CARTESIAN_POINT('Ctrl Pts',(28.9822165729138,0.587617535604928,30.395830214273));
#55552=CARTESIAN_POINT('Ctrl Pts',(28.6429554305518,-1.32141489532166E-14,
30.4374968809397));
#55553=CARTESIAN_POINT('Ctrl Pts',(28.9822165729138,-0.587617535604954,
30.4791635476064));
#55554=CARTESIAN_POINT('Ctrl Pts',(29.3214777152758,-1.17523507120989,30.520830214273));
#55555=CARTESIAN_POINT('Ctrl Pts',(30.,-1.17523507120989,30.5624968809397));
#55556=CARTESIAN_POINT('Ctrl Pts',(30.6785222847241,-1.17523507120989,30.6041635476064));
#55557=CARTESIAN_POINT('Ctrl Pts',(31.0177834270861,-0.587617535604955,
30.645830214273));
#55558=CARTESIAN_POINT('Ctrl Pts',(31.3570445694482,-1.35453519623354E-14,
30.6874968809397));
#55559=CARTESIAN_POINT('Ctrl Pts',(31.0177834270861,0.587617535604927,30.7291635476064));
#55560=CARTESIAN_POINT('Ctrl Pts',(30.6785222847241,1.17523507120987,30.770830214273));
#55561=CARTESIAN_POINT('Ctrl Pts',(30.,1.17523507120987,30.8124968809397));
#55562=CARTESIAN_POINT('Ctrl Pts',(29.3214777152758,1.17523507120987,30.8541635476064));
#55563=CARTESIAN_POINT('Ctrl Pts',(28.9822165729138,0.587617535604928,30.895830214273));
#55564=CARTESIAN_POINT('Ctrl Pts',(28.6429554305518,-1.32141489532166E-14,
30.9374968809397));
#55565=CARTESIAN_POINT('Ctrl Pts',(28.9822165729138,-0.587617535604954,
30.9791635476064));
#55566=CARTESIAN_POINT('Ctrl Pts',(29.3214777152758,-1.17523507120989,31.020830214273));
#55567=CARTESIAN_POINT('Ctrl Pts',(30.,-1.17523507120989,31.0624968809397));
#55568=CARTESIAN_POINT('Ctrl Pts',(30.6785222847241,-1.17523507120989,31.1041635476064));
#55569=CARTESIAN_POINT('Ctrl Pts',(31.0177834270861,-0.587617535604955,
31.145830214273));
#55570=CARTESIAN_POINT('Ctrl Pts',(31.3570445694482,-1.35453519623354E-14,
31.1874968809397));
#55571=CARTESIAN_POINT('Ctrl Pts',(31.0177834270861,0.587617535604927,31.2291635476064));
#55572=CARTESIAN_POINT('Ctrl Pts',(30.6785222847241,1.17523507120987,31.270830214273));
#55573=CARTESIAN_POINT('Ctrl Pts',(30.,1.17523507120987,31.3124968809397));
#55574=CARTESIAN_POINT('',(30.,-1.50000000000002,30.75));
#55575=CARTESIAN_POINT('Origin',(30.,-1.24258096838242E-13,1029.88397459622));
#55576=CARTESIAN_POINT('Origin',(30.06875,2.82851012598683,15.7235432561772));
#55577=CARTESIAN_POINT('',(30.012548982272,2.70302030326666,15.7235432561772));
#55578=CARTESIAN_POINT('Origin',(30.,2.70864040503946,15.7235432561772));
#55579=CARTESIAN_POINT('',(29.987451017728,2.70302030326666,15.7235432561772));
#55580=CARTESIAN_POINT('Origin',(29.987451017728,2.70302030326666,15.7235432561772));
#55581=CARTESIAN_POINT('Origin',(30.2904604134361,2.81439671040465,15.7235432561772));
#55582=CARTESIAN_POINT('',(30.224586826676,2.69370321195774,15.7235432561772));
#55583=CARTESIAN_POINT('Origin',(30.2125174768313,2.70029057063376,15.7235432561772));
#55584=CARTESIAN_POINT('',(30.1995662307806,2.69567237556048,15.7235432561772));
#55585=CARTESIAN_POINT('Origin',(30.1995662307806,2.69567237556048,15.7235432561772));
#55586=CARTESIAN_POINT('Origin',(29.8466157199522,2.82518483606723,15.7235432561772));
#55587=CARTESIAN_POINT('',(29.8004337692194,2.69567237556048,15.7235432561772));
#55588=CARTESIAN_POINT('Origin',(29.7874825231687,2.70029057063376,15.7235432561772));
#55589=CARTESIAN_POINT('',(29.775413173324,2.69370321195775,15.7235432561772));
#55590=CARTESIAN_POINT('Origin',(29.775413173324,2.69370321195775,15.7235432561772));
#55591=CARTESIAN_POINT('Origin',(29.6254271049963,2.804441342164,15.7235432561772));
#55592=CARTESIAN_POINT('',(29.589548948342,2.67170473125694,15.7235432561772));
#55593=CARTESIAN_POINT('Origin',(29.5762752872513,2.67529254692237,15.7235432561772));
#55594=CARTESIAN_POINT('',(29.5647599813892,2.6677785445999,15.7235432561772));
#55595=CARTESIAN_POINT('Origin',(29.5647599813892,2.6677785445999,15.7235432561772));
#55596=CARTESIAN_POINT('Origin',(29.4065478564962,2.76640753481494,15.7235432561772));
#55597=CARTESIAN_POINT('',(29.3811946946869,2.63126513885323,15.7235432561772));
#55598=CARTESIAN_POINT('Origin',(29.3676804550908,2.63380045503416,15.7235432561772));
#55599=CARTESIAN_POINT('',(29.3567901889011,2.6254061353882,15.7235432561772));
#55600=CARTESIAN_POINT('Origin',(29.3567901889011,2.6254061353882,15.7235432561772));
#55601=CARTESIAN_POINT('Origin',(29.1913274378037,2.71131790508989,15.7235432561772));
#55602=CARTESIAN_POINT('',(29.1766555815128,2.57460292188403,15.7235432561772));
#55603=CARTESIAN_POINT('Origin',(29.1629840831922,2.57607010751313,15.7235432561772));
#55604=CARTESIAN_POINT('',(29.1527859987874,2.56684722431571,15.7235432561772));
#55605=CARTESIAN_POINT('Origin',(29.1527859987874,2.56684722431571,15.7235432561772));
#55606=CARTESIAN_POINT('Origin',(28.9810927543681,2.63951209887526,15.7235432561772));
#55607=CARTESIAN_POINT('',(28.9771926604684,2.50206742175908,15.7235432561772));
#55608=CARTESIAN_POINT('Origin',(28.9634481927567,2.50245743114905,15.7235432561772));
#55609=CARTESIAN_POINT('',(28.9540051647184,2.49246284654199,15.7235432561772));
#55610=CARTESIAN_POINT('Origin',(28.9540051647184,2.49246284654199,15.7235432561772));
#55611=CARTESIAN_POINT('Origin',(28.7771399729228,2.55143282284423,15.7235432561772));
#55612=CARTESIAN_POINT('Origin',(28.7616732366375,2.40271160649133,15.7235432561772));
#55613=CARTESIAN_POINT('Origin',(28.5807265301867,2.44762311502286,15.7235432561772));
#55614=CARTESIAN_POINT('Origin',(28.5769760048382,2.29814685040398,15.7235432561772));
#55615=CARTESIAN_POINT('Origin',(28.3930633803483,2.32872299678009,15.7235432561772));
#55616=CARTESIAN_POINT('Origin',(28.4010521891726,2.1794132547725,15.7235432561772));
#55617=CARTESIAN_POINT('Origin',(28.2153075291307,2.1954655268832,15.7235432561772));
#55618=CARTESIAN_POINT('Origin',(28.2349864184648,2.0472428516969,15.7235432561772));
#55619=CARTESIAN_POINT('Origin',(28.0485549004665,2.0486722819467,15.7235432561772));
#55620=CARTESIAN_POINT('Origin',(28.0798025434137,1.90245051566326,15.7235432561772));
#55621=CARTESIAN_POINT('Origin',(27.8938335797622,1.88924829113933,15.7235432561772));
#55622=CARTESIAN_POINT('Origin',(27.9364573242129,1.74592893957157,15.7235432561772));
#55623=CARTESIAN_POINT('Origin',(27.7520974754101,1.71817645637828,15.7235432561772));
#55624=CARTESIAN_POINT('Origin',(27.805834531806,1.57864313098712,15.7235432561772));
#55625=CARTESIAN_POINT('Origin',(27.6242204376256,1.53651149241201,15.7235432561772));
#55626=CARTESIAN_POINT('Origin',(27.6887394991445,1.40162446254803,15.7235432561772));
#55627=CARTESIAN_POINT('Origin',(27.5109908708699,1.3453734241531,15.7235432561772));
#55628=CARTESIAN_POINT('Origin',(27.5858941560429,1.2159643132099,15.7235432561772));
#55629=CARTESIAN_POINT('Origin',(30.5103800418355,2.78293160322096,15.7235432561772));
#55630=CARTESIAN_POINT('',(30.4352400186108,2.66777854459989,15.7235432561772));
#55631=CARTESIAN_POINT('Origin',(30.4237247127487,2.67529254692237,15.7235432561772));
#55632=CARTESIAN_POINT('',(30.410451051658,2.67170473125694,15.7235432561772));
#55633=CARTESIAN_POINT('Origin',(30.410451051658,2.67170473125694,15.7235432561772));
#55634=CARTESIAN_POINT('Origin',(30.7271530075584,2.73430879728474,15.7235432561772));
#55635=CARTESIAN_POINT('',(30.6432098110989,2.62540613538819,15.7235432561772));
#55636=CARTESIAN_POINT('Origin',(30.6323195449092,2.63380045503415,15.7235432561772));
#55637=CARTESIAN_POINT('',(30.6188053053131,2.63126513885322,15.7235432561772));
#55638=CARTESIAN_POINT('Origin',(30.6188053053131,2.63126513885322,15.7235432561772));
#55639=CARTESIAN_POINT('Origin',(30.9394428331868,2.66882806836332,15.7235432561772));
#55640=CARTESIAN_POINT('',(30.8472140012126,2.5668472243157,15.7235432561772));
#55641=CARTESIAN_POINT('Origin',(30.8370159168078,2.57607010751312,15.7235432561772));
#55642=CARTESIAN_POINT('',(30.8233444184872,2.57460292188402,15.7235432561772));
#55643=CARTESIAN_POINT('Origin',(30.8233444184872,2.57460292188402,15.7235432561772));
#55644=CARTESIAN_POINT('Origin',(31.1459406813522,2.58689312692505,15.7235432561772));
#55645=CARTESIAN_POINT('',(31.0459948352816,2.49246284654197,15.7235432561772));
#55646=CARTESIAN_POINT('Origin',(31.0365518072432,2.50245743114904,15.7235432561772));
#55647=CARTESIAN_POINT('',(31.0228073395316,2.50206742175906,15.7235432561772));
#55648=CARTESIAN_POINT('Origin',(31.0228073395316,2.50206742175906,15.7235432561772));
#55649=CARTESIAN_POINT('Origin',(31.3453734241531,2.48900912913003,15.7235432561772));
#55650=CARTESIAN_POINT('',(31.2383267633625,2.40271160649132,15.7235432561772));
#55651=CARTESIAN_POINT('Origin',(31.2296970110986,2.41341627257038,15.7235432561772));
#55652=CARTESIAN_POINT('',(31.2159643132099,2.41410584395711,15.7235432561772));
#55653=CARTESIAN_POINT('Origin',(31.2159643132099,2.41410584395711,15.7235432561772));
#55654=CARTESIAN_POINT('Origin',(31.536511492412,2.3757795623744,15.7235432561772));
#55655=CARTESIAN_POINT('',(31.4230239951618,2.29814685040396,15.7235432561772));
#55656=CARTESIAN_POINT('Origin',(31.4152607239647,2.30949560012898,15.7235432561772));
#55657=CARTESIAN_POINT('',(31.401624462548,2.3112605008555,15.7235432561772));
#55658=CARTESIAN_POINT('Origin',(31.401624462548,2.3112605008555,15.7235432561772));
#55659=CARTESIAN_POINT('Origin',(31.7181764563782,2.24790252458986,15.7235432561772));
#55660=CARTESIAN_POINT('',(31.5989478108274,2.17941325477248,15.7235432561772));
#55661=CARTESIAN_POINT('Origin',(31.5920988838457,2.19133611932756,15.7235432561772));
#55662=CARTESIAN_POINT('',(31.5786431309871,2.19416546819402,15.7235432561772));
#55663=CARTESIAN_POINT('Origin',(31.5786431309871,2.19416546819402,15.7235432561772));
#55664=CARTESIAN_POINT('Origin',(31.8892482911393,2.10616642023777,15.7235432561772));
#55665=CARTESIAN_POINT('',(31.7650135815352,2.04724285169688,15.7235432561772));
#55666=CARTESIAN_POINT('Origin',(31.7591212246811,2.05966632265728,15.7235432561772));
#55667=CARTESIAN_POINT('',(31.7459289395715,2.06354267578706,15.7235432561772));
#55668=CARTESIAN_POINT('Origin',(31.7459289395715,2.06354267578706,15.7235432561772));
#55669=CARTESIAN_POINT('Origin',(32.0486722819467,1.95144509953352,15.7235432561772));
#55670=CARTESIAN_POINT('',(31.9201974565863,1.90245051566323,15.7235432561772));
#55671=CARTESIAN_POINT('Origin',(31.9152979981993,1.91529799819927,15.7235432561772));
#55672=CARTESIAN_POINT('',(31.9024505156632,1.9201974565863,15.7235432561772));
#55673=CARTESIAN_POINT('Origin',(31.9024505156632,1.9201974565863,15.7235432561772));
#55674=CARTESIAN_POINT('Origin',(32.1954655268832,1.7846924708693,15.7235432561772));
#55675=CARTESIAN_POINT('',(32.0635426757871,1.74592893957153,15.7235432561772));
#55676=CARTESIAN_POINT('Origin',(32.0596663226573,1.75912122468115,15.7235432561772));
#55677=CARTESIAN_POINT('',(32.0472428516969,1.76501358153524,15.7235432561772));
#55678=CARTESIAN_POINT('Origin',(32.0472428516969,1.76501358153524,15.7235432561772));
#55679=CARTESIAN_POINT('Origin',(32.3287229967801,1.6069366196517,15.7235432561772));
#55680=CARTESIAN_POINT('',(32.194165468194,1.57864313098709,15.7235432561772));
#55681=CARTESIAN_POINT('Origin',(32.1913361193276,1.59209888384569,15.7235432561772));
#55682=CARTESIAN_POINT('',(32.1794132547725,1.59894781082743,15.7235432561772));
#55683=CARTESIAN_POINT('Origin',(32.1794132547725,1.59894781082743,15.7235432561772));
#55684=CARTESIAN_POINT('Origin',(32.4476231150228,1.41927346981329,15.7235432561772));
#55685=CARTESIAN_POINT('',(32.3112605008555,1.401624462548,15.7235432561772));
#55686=CARTESIAN_POINT('Origin',(32.309495600129,1.41526072396473,15.7235432561772));
#55687=CARTESIAN_POINT('',(32.298146850404,1.42302399516178,15.7235432561772));
#55688=CARTESIAN_POINT('Origin',(32.298146850404,1.42302399516178,15.7235432561772));
#55689=CARTESIAN_POINT('Origin',(32.5514328228442,1.22286002707717,15.7235432561772));
#55690=CARTESIAN_POINT('',(32.4141058439571,1.21596431320987,15.7235432561772));
#55691=CARTESIAN_POINT('Origin',(32.4134162725704,1.22969701109858,15.7235432561772));
#55692=CARTESIAN_POINT('',(32.4027116064913,1.23832676336245,15.7235432561772));
#55693=CARTESIAN_POINT('Origin',(32.4027116064913,1.23832676336245,15.7235432561772));
#55694=CARTESIAN_POINT('Origin',(32.6395120988752,1.01890724563189,15.7235432561772));
#55695=CARTESIAN_POINT('',(32.5020674217591,1.02280733953163,15.7235432561772));
#55696=CARTESIAN_POINT('Origin',(32.502457431149,1.03655180724325,15.7235432561772));
#55697=CARTESIAN_POINT('',(32.492462846542,1.04599483528156,15.7235432561772));
#55698=CARTESIAN_POINT('Origin',(32.492462846542,1.04599483528156,15.7235432561772));
#55699=CARTESIAN_POINT('Origin',(32.7113179050899,0.808672562196245,15.7235432561772));
#55700=CARTESIAN_POINT('',(32.574602921884,0.823344418487232,15.7235432561772));
#55701=CARTESIAN_POINT('Origin',(32.5760701075131,0.837015916807817,15.7235432561772));
#55702=CARTESIAN_POINT('',(32.5668472243157,0.84721400121258,15.7235432561772));
#55703=CARTESIAN_POINT('Origin',(32.5668472243157,0.84721400121258,15.7235432561772));
#55704=CARTESIAN_POINT('Origin',(32.7664075348149,0.593452143503749,15.7235432561772));
#55705=CARTESIAN_POINT('',(32.6312651388532,0.618805305313054,15.7235432561772));
#55706=CARTESIAN_POINT('Origin',(32.6338004550341,0.632319544909225,15.7235432561772));
#55707=CARTESIAN_POINT('',(32.6254061353882,0.64320981109888,15.7235432561772));
#55708=CARTESIAN_POINT('Origin',(32.6254061353882,0.64320981109888,15.7235432561772));
#55709=CARTESIAN_POINT('Origin',(32.804441342164,0.37457289500369,15.7235432561772));
#55710=CARTESIAN_POINT('',(32.6717047312569,0.410451051657977,15.7235432561772));
#55711=CARTESIAN_POINT('Origin',(32.6752925469224,0.423724712748682,15.7235432561772));
#55712=CARTESIAN_POINT('',(32.6677785445999,0.435240018610789,15.7235432561772));
#55713=CARTESIAN_POINT('Origin',(32.6677785445999,0.435240018610789,15.7235432561772));
#55714=CARTESIAN_POINT('Origin',(32.8251848360672,0.153384280047806,15.7235432561772));
#55715=CARTESIAN_POINT('',(32.6956723755605,0.199566230780603,15.7235432561772));
#55716=CARTESIAN_POINT('Origin',(32.7002905706337,0.212517476831278,15.7235432561772));
#55717=CARTESIAN_POINT('',(32.6937032119577,0.224586826675969,15.7235432561772));
#55718=CARTESIAN_POINT('Origin',(32.6937032119577,0.224586826675969,15.7235432561772));
#55719=CARTESIAN_POINT('Origin',(32.8285101259868,-0.0687500000000229,15.7235432561772));
#55720=CARTESIAN_POINT('',(32.7030203032667,-0.0125489822720396,15.7235432561772));
#55721=CARTESIAN_POINT('Origin',(32.7086404050395,-2.31188656783185E-14,
15.7235432561772));
#55722=CARTESIAN_POINT('',(32.7030203032667,0.0125489822719939,15.7235432561772));
#55723=CARTESIAN_POINT('Origin',(32.7030203032667,0.0125489822719939,15.7235432561772));
#55724=CARTESIAN_POINT('Origin',(32.8143967104046,-0.290460413436156,15.7235432561772));
#55725=CARTESIAN_POINT('',(32.6937032119577,-0.224586826676015,15.7235432561772));
#55726=CARTESIAN_POINT('Origin',(32.7002905706337,-0.212517476831324,15.7235432561772));
#55727=CARTESIAN_POINT('',(32.6956723755605,-0.199566230780649,15.7235432561772));
#55728=CARTESIAN_POINT('Origin',(32.6956723755605,-0.199566230780649,15.7235432561772));
#55729=CARTESIAN_POINT('Origin',(32.7829316032209,-0.510380041835567,15.7235432561772));
#55730=CARTESIAN_POINT('',(32.6677785445999,-0.435240018610835,15.7235432561772));
#55731=CARTESIAN_POINT('Origin',(32.6752925469224,-0.423724712748728,15.7235432561772));
#55732=CARTESIAN_POINT('',(32.6717047312569,-0.410451051658023,15.7235432561772));
#55733=CARTESIAN_POINT('Origin',(32.6717047312569,-0.410451051658023,15.7235432561772));
#55734=CARTESIAN_POINT('Origin',(32.7343087972847,-0.727153007558476,15.7235432561772));
#55735=CARTESIAN_POINT('',(32.6254061353882,-0.643209811098926,15.7235432561772));
#55736=CARTESIAN_POINT('Origin',(32.6338004550341,-0.632319544909271,15.7235432561772));
#55737=CARTESIAN_POINT('',(32.6312651388532,-0.6188053053131,15.7235432561772));
#55738=CARTESIAN_POINT('Origin',(32.6312651388532,-0.6188053053131,15.7235432561772));
#55739=CARTESIAN_POINT('Origin',(32.6688280683633,-0.939442833186874,15.7235432561772));
#55740=CARTESIAN_POINT('',(32.5668472243157,-0.847214001212625,15.7235432561772));
#55741=CARTESIAN_POINT('Origin',(32.5760701075131,-0.837015916807863,15.7235432561772));
#55742=CARTESIAN_POINT('',(32.574602921884,-0.823344418487278,15.7235432561772));
#55743=CARTESIAN_POINT('Origin',(32.574602921884,-0.823344418487278,15.7235432561772));
#55744=CARTESIAN_POINT('Origin',(32.586893126925,-1.14594068135223,15.7235432561772));
#55745=CARTESIAN_POINT('',(32.492462846542,-1.0459948352816,15.7235432561772));
#55746=CARTESIAN_POINT('Origin',(32.502457431149,-1.0365518072433,15.7235432561772));
#55747=CARTESIAN_POINT('',(32.5020674217591,-1.02280733953168,15.7235432561772));
#55748=CARTESIAN_POINT('Origin',(32.5020674217591,-1.02280733953168,15.7235432561772));
#55749=CARTESIAN_POINT('Origin',(32.48900912913,-1.34537342415311,15.7235432561772));
#55750=CARTESIAN_POINT('',(32.4027116064913,-1.2383267633625,15.7235432561772));
#55751=CARTESIAN_POINT('Origin',(32.4134162725704,-1.22969701109862,15.7235432561772));
#55752=CARTESIAN_POINT('',(32.4141058439571,-1.21596431320991,15.7235432561772));
#55753=CARTESIAN_POINT('Origin',(32.4141058439571,-1.21596431320991,15.7235432561772));
#55754=CARTESIAN_POINT('Origin',(32.3757795623744,-1.53651149241202,15.7235432561772));
#55755=CARTESIAN_POINT('',(32.2981468504039,-1.42302399516182,15.7235432561772));
#55756=CARTESIAN_POINT('Origin',(32.309495600129,-1.41526072396478,15.7235432561772));
#55757=CARTESIAN_POINT('',(32.3112605008555,-1.40162446254804,15.7235432561772));
#55758=CARTESIAN_POINT('Origin',(32.3112605008555,-1.40162446254804,15.7235432561772));
#55759=CARTESIAN_POINT('Origin',(32.2479025245898,-1.71817645637829,15.7235432561772));
#55760=CARTESIAN_POINT('',(32.1794132547725,-1.59894781082747,15.7235432561772));
#55761=CARTESIAN_POINT('Origin',(32.1913361193275,-1.59209888384574,15.7235432561772));
#55762=CARTESIAN_POINT('',(32.194165468194,-1.57864313098713,15.7235432561772));
#55763=CARTESIAN_POINT('Origin',(32.194165468194,-1.57864313098713,15.7235432561772));
#55764=CARTESIAN_POINT('Origin',(32.1061664202378,-1.88924829113934,15.7235432561772));
#55765=CARTESIAN_POINT('',(32.0472428516969,-1.76501358153528,15.7235432561772));
#55766=CARTESIAN_POINT('Origin',(32.0596663226573,-1.75912122468119,15.7235432561772));
#55767=CARTESIAN_POINT('',(32.063542675787,-1.74592893957158,15.7235432561772));
#55768=CARTESIAN_POINT('Origin',(32.063542675787,-1.74592893957158,15.7235432561772));
#55769=CARTESIAN_POINT('Origin',(31.9514450995335,-2.04867228194671,15.7235432561772));
#55770=CARTESIAN_POINT('',(31.9024505156632,-1.92019745658634,15.7235432561772));
#55771=CARTESIAN_POINT('Origin',(31.9152979981993,-1.91529799819931,15.7235432561772));
#55772=CARTESIAN_POINT('',(31.9201974565863,-1.90245051566327,15.7235432561772));
#55773=CARTESIAN_POINT('Origin',(31.9201974565863,-1.90245051566327,15.7235432561772));
#55774=CARTESIAN_POINT('Origin',(31.7846924708693,-2.19546552688321,15.7235432561772));
#55775=CARTESIAN_POINT('',(31.7459289395715,-2.0635426757871,15.7235432561772));
#55776=CARTESIAN_POINT('Origin',(31.7591212246811,-2.05966632265732,15.7235432561772));
#55777=CARTESIAN_POINT('',(31.7650135815352,-2.04724285169692,15.7235432561772));
#55778=CARTESIAN_POINT('Origin',(31.7650135815352,-2.04724285169692,15.7235432561772));
#55779=CARTESIAN_POINT('Origin',(31.6069366196517,-2.32872299678011,15.7235432561772));
#55780=CARTESIAN_POINT('',(31.5786431309871,-2.19416546819406,15.7235432561772));
#55781=CARTESIAN_POINT('Origin',(31.5920988838457,-2.1913361193276,15.7235432561772));
#55782=CARTESIAN_POINT('',(31.5989478108274,-2.17941325477251,15.7235432561772));
#55783=CARTESIAN_POINT('Origin',(31.5989478108274,-2.17941325477251,15.7235432561772));
#55784=CARTESIAN_POINT('Origin',(31.4192734698133,-2.44762311502288,15.7235432561772));
#55785=CARTESIAN_POINT('',(31.401624462548,-2.31126050085554,15.7235432561772));
#55786=CARTESIAN_POINT('Origin',(31.4152607239647,-2.30949560012901,15.7235432561772));
#55787=CARTESIAN_POINT('',(31.4230239951618,-2.29814685040399,15.7235432561772));
#55788=CARTESIAN_POINT('Origin',(31.4230239951618,-2.29814685040399,15.7235432561772));
#55789=CARTESIAN_POINT('Origin',(31.2228600270771,-2.55143282284425,15.7235432561772));
#55790=CARTESIAN_POINT('',(31.2159643132098,-2.41410584395714,15.7235432561772));
#55791=CARTESIAN_POINT('Origin',(31.2296970110986,-2.41341627257041,15.7235432561772));
#55792=CARTESIAN_POINT('',(31.2383267633624,-2.40271160649135,15.7235432561772));
#55793=CARTESIAN_POINT('Origin',(31.2383267633624,-2.40271160649135,15.7235432561772));
#55794=CARTESIAN_POINT('Origin',(31.0189072456319,-2.63951209887528,15.7235432561772));
#55795=CARTESIAN_POINT('',(31.0228073395316,-2.5020674217591,15.7235432561772));
#55796=CARTESIAN_POINT('Origin',(31.0365518072432,-2.50245743114907,15.7235432561772));
#55797=CARTESIAN_POINT('',(31.0459948352815,-2.49246284654201,15.7235432561772));
#55798=CARTESIAN_POINT('Origin',(31.0459948352815,-2.49246284654201,15.7235432561772));
#55799=CARTESIAN_POINT('Origin',(30.8086725621962,-2.71131790508991,15.7235432561772));
#55800=CARTESIAN_POINT('',(30.8233444184872,-2.57460292188405,15.7235432561772));
#55801=CARTESIAN_POINT('Origin',(30.8370159168078,-2.57607010751315,15.7235432561772));
#55802=CARTESIAN_POINT('',(30.8472140012126,-2.56684722431573,15.7235432561772));
#55803=CARTESIAN_POINT('Origin',(30.8472140012126,-2.56684722431573,15.7235432561772));
#55804=CARTESIAN_POINT('Origin',(30.5934521435037,-2.76640753481496,15.7235432561772));
#55805=CARTESIAN_POINT('',(30.618805305313,-2.63126513885325,15.7235432561772));
#55806=CARTESIAN_POINT('Origin',(30.6323195449092,-2.63380045503418,15.7235432561772));
#55807=CARTESIAN_POINT('',(30.6432098110989,-2.62540613538822,15.7235432561772));
#55808=CARTESIAN_POINT('Origin',(30.6432098110989,-2.62540613538822,15.7235432561772));
#55809=CARTESIAN_POINT('Origin',(30.3745728950037,-2.80444134216402,15.7235432561772));
#55810=CARTESIAN_POINT('',(30.410451051658,-2.67170473125697,15.7235432561772));
#55811=CARTESIAN_POINT('Origin',(30.4237247127487,-2.67529254692239,15.7235432561772));
#55812=CARTESIAN_POINT('',(30.4352400186108,-2.66777854459992,15.7235432561772));
#55813=CARTESIAN_POINT('Origin',(30.4352400186108,-2.66777854459992,15.7235432561772));
#55814=CARTESIAN_POINT('Origin',(30.1533842800478,-2.82518483606726,15.7235432561772));
#55815=CARTESIAN_POINT('',(30.1995662307806,-2.69567237556051,15.7235432561772));
#55816=CARTESIAN_POINT('Origin',(30.2125174768313,-2.70029057063379,15.7235432561772));
#55817=CARTESIAN_POINT('',(30.224586826676,-2.69370321195777,15.7235432561772));
#55818=CARTESIAN_POINT('Origin',(30.224586826676,-2.69370321195777,15.7235432561772));
#55819=CARTESIAN_POINT('Origin',(29.93125,-2.82851012598686,15.7235432561772));
#55820=CARTESIAN_POINT('',(29.987451017728,-2.70302030326669,15.7235432561772));
#55821=CARTESIAN_POINT('Origin',(30.,-2.70864040503949,15.7235432561772));
#55822=CARTESIAN_POINT('',(30.012548982272,-2.70302030326669,15.7235432561772));
#55823=CARTESIAN_POINT('Origin',(30.012548982272,-2.70302030326669,15.7235432561772));
#55824=CARTESIAN_POINT('Origin',(29.7095395865638,-2.81439671040468,15.7235432561772));
#55825=CARTESIAN_POINT('',(29.775413173324,-2.69370321195777,15.7235432561772));
#55826=CARTESIAN_POINT('Origin',(29.7874825231687,-2.70029057063378,15.7235432561772));
#55827=CARTESIAN_POINT('',(29.8004337692193,-2.6956723755605,15.7235432561772));
#55828=CARTESIAN_POINT('Origin',(29.8004337692193,-2.6956723755605,15.7235432561772));
#55829=CARTESIAN_POINT('Origin',(29.4896199581644,-2.78293160322098,15.7235432561772));
#55830=CARTESIAN_POINT('',(29.5647599813891,-2.66777854459992,15.7235432561772));
#55831=CARTESIAN_POINT('Origin',(29.5762752872513,-2.67529254692239,15.7235432561772));
#55832=CARTESIAN_POINT('',(29.589548948342,-2.67170473125696,15.7235432561772));
#55833=CARTESIAN_POINT('Origin',(29.589548948342,-2.67170473125696,15.7235432561772));
#55834=CARTESIAN_POINT('Origin',(29.2728469924415,-2.73430879728476,15.7235432561772));
#55835=CARTESIAN_POINT('',(29.3567901889011,-2.62540613538822,15.7235432561772));
#55836=CARTESIAN_POINT('Origin',(29.3676804550907,-2.63380045503417,15.7235432561772));
#55837=CARTESIAN_POINT('',(29.3811946946869,-2.63126513885324,15.7235432561772));
#55838=CARTESIAN_POINT('Origin',(29.3811946946869,-2.63126513885324,15.7235432561772));
#55839=CARTESIAN_POINT('Origin',(29.0605571668131,-2.66882806836334,15.7235432561772));
#55840=CARTESIAN_POINT('',(29.1527859987874,-2.56684722431572,15.7235432561772));
#55841=CARTESIAN_POINT('Origin',(29.1629840831921,-2.57607010751314,15.7235432561772));
#55842=CARTESIAN_POINT('',(29.1766555815127,-2.57460292188404,15.7235432561772));
#55843=CARTESIAN_POINT('Origin',(29.1766555815127,-2.57460292188404,15.7235432561772));
#55844=CARTESIAN_POINT('Origin',(28.8540593186477,-2.58689312692507,15.7235432561772));
#55845=CARTESIAN_POINT('',(28.9540051647184,-2.49246284654199,15.7235432561772));
#55846=CARTESIAN_POINT('Origin',(28.9634481927567,-2.50245743114906,15.7235432561772));
#55847=CARTESIAN_POINT('',(28.9771926604683,-2.50206742175908,15.7235432561772));
#55848=CARTESIAN_POINT('Origin',(28.9771926604683,-2.50206742175908,15.7235432561772));
#55849=CARTESIAN_POINT('Origin',(28.6546265758469,-2.48900912913005,15.7235432561772));
#55850=CARTESIAN_POINT('',(28.7616732366375,-2.40271160649133,15.7235432561772));
#55851=CARTESIAN_POINT('Origin',(28.7703029889014,-2.4134162725704,15.7235432561772));
#55852=CARTESIAN_POINT('',(28.7840356867901,-2.41410584395713,15.7235432561772));
#55853=CARTESIAN_POINT('Origin',(28.7840356867901,-2.41410584395713,15.7235432561772));
#55854=CARTESIAN_POINT('Origin',(28.463488507588,-2.37577956237441,15.7235432561772));
#55855=CARTESIAN_POINT('',(28.5769760048382,-2.29814685040397,15.7235432561772));
#55856=CARTESIAN_POINT('Origin',(28.5847392760352,-2.30949560012899,15.7235432561772));
#55857=CARTESIAN_POINT('',(28.5983755374519,-2.31126050085552,15.7235432561772));
#55858=CARTESIAN_POINT('Origin',(28.5983755374519,-2.31126050085552,15.7235432561772));
#55859=CARTESIAN_POINT('Origin',(28.2818235436217,-2.24790252458987,15.7235432561772));
#55860=CARTESIAN_POINT('',(28.4010521891725,-2.17941325477249,15.7235432561772));
#55861=CARTESIAN_POINT('Origin',(28.4079011161542,-2.19133611932757,15.7235432561772));
#55862=CARTESIAN_POINT('',(28.4213568690129,-2.19416546819403,15.7235432561772));
#55863=CARTESIAN_POINT('Origin',(28.4213568690129,-2.19416546819403,15.7235432561772));
#55864=CARTESIAN_POINT('Origin',(28.1107517088606,-2.10616642023779,15.7235432561772));
#55865=CARTESIAN_POINT('',(28.2349864184647,-2.04724285169689,15.7235432561772));
#55866=CARTESIAN_POINT('Origin',(28.2408787753188,-2.0596663226573,15.7235432561772));
#55867=CARTESIAN_POINT('',(28.2540710604284,-2.06354267578707,15.7235432561772));
#55868=CARTESIAN_POINT('Origin',(28.2540710604284,-2.06354267578707,15.7235432561772));
#55869=CARTESIAN_POINT('Origin',(27.9513277180533,-1.95144509953353,15.7235432561772));
#55870=CARTESIAN_POINT('',(28.0798025434136,-1.90245051566325,15.7235432561772));
#55871=CARTESIAN_POINT('Origin',(28.0847020018007,-1.91529799819928,15.7235432561772));
#55872=CARTESIAN_POINT('',(28.0975494843367,-1.92019745658631,15.7235432561772));
#55873=CARTESIAN_POINT('Origin',(28.0975494843367,-1.92019745658631,15.7235432561772));
#55874=CARTESIAN_POINT('Origin',(27.8045344731168,-1.78469247086931,15.7235432561772));
#55875=CARTESIAN_POINT('',(27.9364573242129,-1.74592893957155,15.7235432561772));
#55876=CARTESIAN_POINT('Origin',(27.9403336773427,-1.75912122468116,15.7235432561772));
#55877=CARTESIAN_POINT('',(27.9527571483031,-1.76501358153525,15.7235432561772));
#55878=CARTESIAN_POINT('Origin',(27.9527571483031,-1.76501358153525,15.7235432561772));
#55879=CARTESIAN_POINT('Origin',(27.6712770032199,-1.6069366196517,15.7235432561772));
#55880=CARTESIAN_POINT('',(27.8058345318059,-1.5786431309871,15.7235432561772));
#55881=CARTESIAN_POINT('Origin',(27.8086638806724,-1.59209888384571,15.7235432561772));
#55882=CARTESIAN_POINT('',(27.8205867452275,-1.59894781082744,15.7235432561772));
#55883=CARTESIAN_POINT('Origin',(27.8205867452275,-1.59894781082744,15.7235432561772));
#55884=CARTESIAN_POINT('Origin',(27.5523768849771,-1.4192734698133,15.7235432561772));
#55885=CARTESIAN_POINT('',(27.6887394991444,-1.40162446254801,15.7235432561772));
#55886=CARTESIAN_POINT('Origin',(27.690504399871,-1.41526072396474,15.7235432561772));
#55887=CARTESIAN_POINT('',(27.701853149596,-1.42302399516179,15.7235432561772));
#55888=CARTESIAN_POINT('Origin',(27.701853149596,-1.42302399516179,15.7235432561772));
#55889=CARTESIAN_POINT('Origin',(27.4485671771557,-1.22286002707717,15.7235432561772));
#55890=CARTESIAN_POINT('',(27.5858941560428,-1.21596431320988,15.7235432561772));
#55891=CARTESIAN_POINT('Origin',(27.5865837274296,-1.22969701109859,15.7235432561772));
#55892=CARTESIAN_POINT('',(27.5972883935086,-1.23832676336246,15.7235432561772));
#55893=CARTESIAN_POINT('Origin',(27.5972883935086,-1.23832676336246,15.7235432561772));
#55894=CARTESIAN_POINT('Origin',(27.3604879011247,-1.01890724563189,15.7235432561772));
#55895=CARTESIAN_POINT('',(27.4979325782409,-1.02280733953164,15.7235432561772));
#55896=CARTESIAN_POINT('Origin',(27.4975425688509,-1.03655180724326,15.7235432561772));
#55897=CARTESIAN_POINT('',(27.507537153458,-1.04599483528157,15.7235432561772));
#55898=CARTESIAN_POINT('Origin',(27.507537153458,-1.04599483528157,15.7235432561772));
#55899=CARTESIAN_POINT('Origin',(27.2886820949101,-0.808672562196254,15.7235432561772));
#55900=CARTESIAN_POINT('',(27.4253970781159,-0.823344418487241,15.7235432561772));
#55901=CARTESIAN_POINT('Origin',(27.4239298924868,-0.837015916807826,15.7235432561772));
#55902=CARTESIAN_POINT('',(27.4331527756843,-0.847214001212589,15.7235432561772));
#55903=CARTESIAN_POINT('Origin',(27.4331527756843,-0.847214001212589,15.7235432561772));
#55904=CARTESIAN_POINT('Origin',(27.233592465185,-0.593452143503757,15.7235432561772));
#55905=CARTESIAN_POINT('',(27.3687348611467,-0.618805305313063,15.7235432561772));
#55906=CARTESIAN_POINT('Origin',(27.3661995449658,-0.632319544909233,15.7235432561772));
#55907=CARTESIAN_POINT('',(27.3745938646118,-0.643209811098888,15.7235432561772));
#55908=CARTESIAN_POINT('Origin',(27.3745938646118,-0.643209811098888,15.7235432561772));
#55909=CARTESIAN_POINT('Origin',(27.195558657836,-0.374572895003696,15.7235432561772));
#55910=CARTESIAN_POINT('',(27.328295268743,-0.410451051657984,15.7235432561772));
#55911=CARTESIAN_POINT('Origin',(27.3247074530776,-0.423724712748689,15.7235432561772));
#55912=CARTESIAN_POINT('',(27.3322214554001,-0.435240018610796,15.7235432561772));
#55913=CARTESIAN_POINT('Origin',(27.3322214554001,-0.435240018610796,15.7235432561772));
#55914=CARTESIAN_POINT('Origin',(27.1748151639327,-0.153384280047813,15.7235432561772));
#55915=CARTESIAN_POINT('',(27.3043276244395,-0.199566230780611,15.7235432561772));
#55916=CARTESIAN_POINT('Origin',(27.2997094293662,-0.212517476831286,15.7235432561772));
#55917=CARTESIAN_POINT('',(27.3062967880422,-0.224586826675978,15.7235432561772));
#55918=CARTESIAN_POINT('Origin',(27.3062967880422,-0.224586826675978,15.7235432561772));
#55919=CARTESIAN_POINT('Origin',(27.1714898740131,0.068750000000016,15.7235432561772));
#55920=CARTESIAN_POINT('Origin',(27.2969796967333,-0.0125489822720016,15.7235432561772));
#55921=CARTESIAN_POINT('Origin',(27.1856032895953,0.29046041343615,15.7235432561772));
#55922=CARTESIAN_POINT('Origin',(27.3043276244395,0.199566230780642,15.7235432561772));
#55923=CARTESIAN_POINT('Origin',(27.217068396779,0.510380041835561,15.7235432561772));
#55924=CARTESIAN_POINT('Origin',(27.328295268743,0.410451051658016,15.7235432561772));
#55925=CARTESIAN_POINT('Origin',(27.2656912027152,0.727153007558468,15.7235432561772));
#55926=CARTESIAN_POINT('Origin',(27.3687348611468,0.618805305313091,15.7235432561772));
#55927=CARTESIAN_POINT('Origin',(27.3311719316367,0.939442833186866,15.7235432561772));
#55928=CARTESIAN_POINT('Origin',(27.4253970781159,0.823344418487269,15.7235432561772));
#55929=CARTESIAN_POINT('Origin',(27.4131068730749,1.14594068135223,15.7235432561772));
#55930=CARTESIAN_POINT('Origin',(27.4979325782409,1.02280733953167,15.7235432561772));
#75323=UNCERTAINTY_MEASURE_WITH_UNIT(LENGTH_MEASURE(0.01),#75337,
'DISTANCE_ACCURACY_VALUE',
'Maximum model space distance between geometric entities at asserted c
onnectivities');
#75326=UNCERTAINTY_MEASURE_WITH_UNIT(LENGTH_MEASURE(0.01),#75337,
'DISTANCE_ACCURACY_VALUE',
'Maximum model space distance between geometric entities at asserted c
onnectivities');
#75333=(
GEOMETRIC_REPRESENTATION_CONTEXT(3)
GLOBAL_UNCERTAINTY_ASSIGNED_CONTEXT((#75323))
GLOBAL_UNIT_ASSIGNED_CONTEXT((#75337,#75339,#75340))
REPRESENTATION_CONTEXT('','3D')
);
#75336=(
GEOMETRIC_REPRESENTATION_CONTEXT(3)
GLOBAL_UNCERTAINTY_ASSIGNED_CONTEXT((#75326))
GLOBAL_UNIT_ASSIGNED_CONTEXT((#75337,#75339,#75340))
REPRESENTATION_CONTEXT('','3D')
);
#75337=(
LENGTH_UNIT()
NAMED_UNIT(*)
SI_UNIT(.MILLI.,.METRE.)
);
#75339=(
NAMED_UNIT(*)
PLANE_ANGLE_UNIT()
SI_UNIT($,.RADIAN.)
);
#75340=(
NAMED_UNIT(*)
SI_UNIT($,.STERADIAN.)
SOLID_ANGLE_UNIT()
);
#75347=SHAPE_DEFINITION_REPRESENTATION(#75356,#75373);
#75356=PRODUCT_DEFINITION_SHAPE('',$,#75383);
#75373=SHAPE_REPRESENTATION('',(#32197),#75333);
#75376=PRODUCT_DEFINITION_CONTEXT('part definition',#75405,'design');
#75383=PRODUCT_DEFINITION('Screw_01','Screw_01',#75392,#75376);
#75392=PRODUCT_DEFINITION_FORMATION('',$,#75413);
#75405=APPLICATION_CONTEXT(
'Core Data for Automotive Mechanical Design Process');
#75406=PRODUCT_CONTEXT('part definition',#75405,'mechanical');
#75413=PRODUCT('Screw_01','Screw_01',$,(#75406));
#75419=PRESENTATION_STYLE_ASSIGNMENT((#75423));
#75423=SURFACE_STYLE_USAGE(.BOTH.,#75427);
#75427=SURFACE_SIDE_STYLE('',(#75431));
#75431=SURFACE_STYLE_FILL_AREA(#75435);
#75435=FILL_AREA_STYLE('Opaque(86,86,86)',(#75439));
#75439=FILL_AREA_STYLE_COLOUR('Opaque(86,86,86)',#75443);
#75443=COLOUR_RGB('Opaque(86,86,86)', 0.08235294, 0.09019608, 0.10196078);
ENDSEC;
END-ISO-10303-21;
